ISO-10303-21;
HEADER;
FILE_DESCRIPTION (('STEP AP214'),
    '1' );
FILE_NAME ('Injection Molded Chain Links 7.step',
    '2026-10-08T22:59:04',
    ( '' ),
    ( '' ),
    'SwSTEP 2.0',
    'SolidWorks 2020',
    '' );
FILE_SCHEMA (( 'AUTOMOTIVE_DESIGN' ));
ENDSEC;

DATA;
#10=DIRECTION ( 'NONE',  ( 0.000000000000000000, 0.3427706569149662763, -0.9394191166662954062 ) ) ;
#32=ORIENTED_EDGE ( 'NONE', *, *, #162707, .T. ) ;
#34=AXIS2_PLACEMENT_3D ( 'NONE', #189135, #91325, #191735 ) ;
#88=ORIENTED_EDGE ( 'NONE', *, *, #100506, .F. ) ;
#91=EDGE_LOOP ( 'NONE', ( #74556, #125437, #66569, #237966 ) ) ;
#102=ORIENTED_EDGE ( 'NONE', *, *, #34870, .F. ) ;
#117=CARTESIAN_POINT ( 'NONE',  ( -20.94999999999999929, 14.80545736607782814, -235.9842437978701639 ) ) ;
#136=DIRECTION ( 'NONE',  ( 0.000000000000000000, -0.2128009952263678062, 0.9770955615653298398 ) ) ;
#151=ORIENTED_EDGE ( 'NONE', *, *, #31189, .T. ) ;
#157=CARTESIAN_POINT ( 'NONE',  ( -21.05000000000000071, 0.4879293624014888198, -209.1697915983179428 ) ) ;
#163=CARTESIAN_POINT ( 'NONE',  ( 21.07928932188134397, 1.148907358139439339E-11, -201.0000000000015064 ) ) ;
#171=CIRCLE ( 'NONE', #95836, 0.9750000000000036415 ) ;
#189=CIRCLE ( 'NONE', #183374, 0.1000000000000015044 ) ;
#201=DIRECTION ( 'NONE',  ( 1.000000000000000000, 1.832422279913646096E-16, 3.990820347355631841E-17 ) ) ;
#225=ORIENTED_EDGE ( 'NONE', *, *, #31957, .F. ) ;
#243=DIRECTION ( 'NONE',  ( 0.000000000000000000, -0.9770955615653290627, -0.2128009952263723858 ) ) ;
#286=VERTEX_POINT ( 'NONE', #33766 ) ;
#324=DIRECTION ( 'NONE',  ( 0.000000000000000000, 0.2128009952263601456, -0.9770955615653316162 ) ) ;
#325=CARTESIAN_POINT ( 'NONE',  ( -18.50000000000000000, -7.631834139421013852, -210.1304494778855769 ) ) ;
#340=ORIENTED_EDGE ( 'NONE', *, *, #133488, .F. ) ;
#365=VERTEX_POINT ( 'NONE', #103924 ) ;
#369=CARTESIAN_POINT ( 'NONE',  ( -20.54999999999999361, 15.92646454033039305, -219.3818586450342707 ) ) ;
#387=DIRECTION ( 'NONE',  ( 0.000000000000000000, 0.9770955615653551529, 0.2128009952262517601 ) ) ;
#397=ORIENTED_EDGE ( 'NONE', *, *, #191069, .F. ) ;
#401=VERTEX_POINT ( 'NONE', #80504 ) ;
#427=EDGE_LOOP ( 'NONE', ( #38646, #216992, #230740, #125875 ) ) ;
#483=CYLINDRICAL_SURFACE ( 'NONE', #100617, 0.1000000000000055844 ) ;
#524=EDGE_CURVE ( 'NONE', #89812, #126094, #5508, .T. ) ;
#540=ORIENTED_EDGE ( 'NONE', *, *, #177845, .T. ) ;
#548=ORIENTED_EDGE ( 'NONE', *, *, #24283, .F. ) ;
#555=CARTESIAN_POINT ( 'NONE',  ( -18.33682934331559267, -0.6949736787240441416, -242.5041756961801980 ) ) ;
#564=DIRECTION ( 'NONE',  ( 0.000000000000000000, 0.9550021345545507412, -0.2965989261549202838 ) ) ;
#596=CARTESIAN_POINT ( 'NONE',  ( -21.14999999999999858, -1.427715776309795404, -194.9144328397408401 ) ) ;
#632=EDGE_CURVE ( 'NONE', #13934, #143709, #236723, .T. ) ;
#633=VERTEX_POINT ( 'NONE', #171670 ) ;
#648=DIRECTION ( 'NONE',  ( 0.000000000000000000, 0.2128009952263604232, -0.9770955615653316162 ) ) ;
#657=DIRECTION ( 'NONE',  ( 1.000000000000000000, 0.000000000000000000, 0.000000000000000000 ) ) ;
#720=ORIENTED_EDGE ( 'NONE', *, *, #92942, .T. ) ;
#723=ADVANCED_FACE ( 'NONE', ( #191226 ), #255273, .F. ) ;
#727=DIRECTION ( 'NONE',  ( 0.000000000000000000, 0.9770955615653316162, 0.2128009952263604232 ) ) ;
#748=DIRECTION ( 'NONE',  ( 1.000000000000000000, 0.000000000000000000, 0.000000000000000000 ) ) ;
#769=ORIENTED_EDGE ( 'NONE', *, *, #44737, .T. ) ;
#801=ORIENTED_EDGE ( 'NONE', *, *, #154892, .F. ) ;
#809=DIRECTION ( 'NONE',  ( -1.000000000000000000, -2.885090398161910739E-16, -6.283419270304611573E-17 ) ) ;
#831=ORIENTED_EDGE ( 'NONE', *, *, #64309, .T. ) ;
#833=EDGE_LOOP ( 'NONE', ( #155225, #94012, #29102, #142462, #244770 ) ) ;
#843=CIRCLE ( 'NONE', #192410, 2.000000000000003109 ) ;
#857=CARTESIAN_POINT ( 'NONE',  ( 18.59999999999999076, 10.99842653345846699, -220.2504445088529792 ) ) ;
#889=FACE_OUTER_BOUND ( 'NONE', #237114, .T. ) ;
#914=B_SPLINE_CURVE_WITH_KNOTS ( 'NONE', 3,
 ( #31194, #50679, #228074, #166844 ),
 .UNSPECIFIED., .F., .F.,
 ( 4, 4 ),
 ( 0.000000000000000000, 0.0001048066582182268164 ),
 .UNSPECIFIED. ) ;
#920=EDGE_CURVE ( 'NONE', #170466, #191384, #225694, .T. ) ;
#931=ADVANCED_FACE ( 'NONE', ( #208858 ), #144935, .T. ) ;
#951=ORIENTED_EDGE ( 'NONE', *, *, #5769, .F. ) ;
#954=DIRECTION ( 'NONE',  ( -1.000000000000000000, 0.000000000000000000, 0.000000000000000000 ) ) ;
#1005=EDGE_CURVE ( 'NONE', #205753, #123238, #843, .T. ) ;
#1045=TOROIDAL_SURFACE ( 'NONE', #30150, 11.65000000000000036, 0.1000000000000000056 ) ;
#1055=ORIENTED_EDGE ( 'NONE', *, *, #23889, .F. ) ;
#1060=EDGE_CURVE ( 'NONE', #31696, #10002, #250840, .T. ) ;
#1062=CARTESIAN_POINT ( 'NONE',  ( 23.14999999999998437, 0.8618440306782493288, -204.9572370243411115 ) ) ;
#1078=EDGE_LOOP ( 'NONE', ( #153899, #117454, #241349, #25597 ) ) ;
#1104=VERTEX_POINT ( 'NONE', #27388 ) ;
#1129=FACE_OUTER_BOUND ( 'NONE', #213578, .T. ) ;
#1137=ORIENTED_EDGE ( 'NONE', *, *, #13931, .T. ) ;
#1162=DIRECTION ( 'NONE',  ( 0.000000000000000000, 0.2128009952264768301, -0.9770955615653060811 ) ) ;
#1184=CARTESIAN_POINT ( 'NONE',  ( -21.05000000000000071, 6.350981563072554792, -199.7191680003453769 ) ) ;
#1202=ORIENTED_EDGE ( 'NONE', *, *, #70596, .F. ) ;
#1216=CIRCLE ( 'NONE', #126111, 0.09999999999999939493 ) ;
#1218=AXIS2_PLACEMENT_3D ( 'NONE', #140597, #156355, #178481 ) ;
#1274=CARTESIAN_POINT ( 'NONE',  ( -23.15000000000000213, 7.128833340094563376, -233.7327013124401276 ) ) ;
#1312=EDGE_CURVE ( 'NONE', #167415, #254024, #125760, .T. ) ;
#1319=CIRCLE ( 'NONE', #118039, 0.1000000000000055844 ) ;
#1344=EDGE_CURVE ( 'NONE', #95913, #198456, #59265, .T. ) ;
#1383=CIRCLE ( 'NONE', #155572, 0.1000000000000050987 ) ;
#1394=EDGE_LOOP ( 'NONE', ( #63811, #237664, #26093, #226339 ) ) ;
#1398=CARTESIAN_POINT ( 'NONE',  ( 18.49999999999999645, 1.148907358139439339E-11, -201.0000000000015064 ) ) ;
#1402=ORIENTED_EDGE ( 'NONE', *, *, #146572, .F. ) ;
#1433=VECTOR ( 'NONE', #43701, 1000.000000000000114 ) ;
#1436=CARTESIAN_POINT ( 'NONE',  ( -21.14999999999999858, 12.92448621296781930, -205.1280733356431938 ) ) ;
#1446=DIRECTION ( 'NONE',  ( 1.000000000000000000, 0.000000000000000000, 0.000000000000000000 ) ) ;
#1456=AXIS2_PLACEMENT_3D ( 'NONE', #81465, #648, #179341 ) ;
#1486=CARTESIAN_POINT ( 'NONE',  ( -20.94999999999999929, 7.675662554762638479, -241.7139905447625381 ) ) ;
#1498=DIRECTION ( 'NONE',  ( 1.000000000000000000, 0.000000000000000000, 0.000000000000000000 ) ) ;
#1506=CARTESIAN_POINT ( 'NONE',  ( 20.94999999999999929, 14.61354176542825201, -235.9279552357344016 ) ) ;
#1537=DIRECTION ( 'NONE',  ( 0.000000000000000000, -0.9770955615653315052, -0.2128009952263603954 ) ) ;
#1546=CARTESIAN_POINT ( 'NONE',  ( 21.10642757222115407, 13.08238103144605979, -210.6784328906550172 ) ) ;
#1547=DIRECTION ( 'NONE',  ( -1.000000000000000000, 0.000000000000000000, 0.000000000000000000 ) ) ;
#1572=ADVANCED_FACE ( 'NONE', ( #45310 ), #171968, .T. ) ;
#1602=ORIENTED_EDGE ( 'NONE', *, *, #31508, .T. ) ;
#1603=VECTOR ( 'NONE', #33822, 1000.000000000000227 ) ;
#1613=AXIS2_PLACEMENT_3D ( 'NONE', #48354, #105731, #87466 ) ;
#1631=CIRCLE ( 'NONE', #143297, 11.74999999999999289 ) ;
#1642=DIRECTION ( 'NONE',  ( 0.000000000000000000, -0.2128009952263982818, 0.9770955615653232895 ) ) ;
#1669=CYLINDRICAL_SURFACE ( 'NONE', #106167, 0.5000000000000007772 ) ;
#1672=CARTESIAN_POINT ( 'NONE',  ( 23.24999999999999289, 11.40444339177024524, -198.6185779617709670 ) ) ;
#1675=EDGE_LOOP ( 'NONE', ( #32442, #157357, #48251, #91290 ) ) ;
#1676=DIRECTION ( 'NONE',  ( 0.000000000000000000, 0.9770955615653550419, 0.2128009952262526761 ) ) ;
#1691=CARTESIAN_POINT ( 'NONE',  ( 18.59999999999999076, 14.51805813080544638, -219.6885945441820809 ) ) ;
#1713=CIRCLE ( 'NONE', #93299, 0.09999999999999781286 ) ;
#1725=DIRECTION ( 'NONE',  ( 0.7071359030027705161, -0.6908824414807910319, -0.1504668293611502450 ) ) ;
#1730=ADVANCED_FACE ( 'NONE', ( #97219 ), #221967, .F. ) ;
#1731=VERTEX_POINT ( 'NONE', #253758 ) ;
#1748=DIRECTION ( 'NONE',  ( 0.000000000000000000, 0.2128009952263588966, -0.9770955615653318382 ) ) ;
#1776=CARTESIAN_POINT ( 'NONE',  ( -23.15000000000000213, 6.300962096140152013, -220.8843452229073705 ) ) ;
#1814=CARTESIAN_POINT ( 'NONE',  ( -21.05000000000000071, 10.71906255309368383, -222.4921384173655383 ) ) ;
#1842=AXIS2_PLACEMENT_3D ( 'NONE', #100695, #94617, #171631 ) ;
#1859=DIRECTION ( 'NONE',  ( 0.000000000000000000, -0.2128009952263403282, 0.9770955615653358350 ) ) ;
#1860=ORIENTED_EDGE ( 'NONE', *, *, #103698, .T. ) ;
#1876=CARTESIAN_POINT ( 'NONE',  ( -18.50000000000000000, -4.375386779258390924, -188.8379487402709742 ) ) ;
#1882=AXIS2_PLACEMENT_3D ( 'NONE', #230618, #135336, #213596 ) ;
#1883=CARTESIAN_POINT ( 'NONE',  ( 20.51284917709620359, 11.70743148473744988, -206.3025725608655421 ) ) ;
#1889=ORIENTED_EDGE ( 'NONE', *, *, #90325, .F. ) ;
#1928=EDGE_CURVE ( 'NONE', #155405, #122855, #1216, .T. ) ;
#1953=CARTESIAN_POINT ( 'NONE',  ( 21.05000000000000071, 7.128833340094563376, -233.7327013124401276 ) ) ;
#1962=CARTESIAN_POINT ( 'NONE',  ( 20.95429402530587737, 10.48661124036732240, -207.4390072342162910 ) ) ;
#2025=ORIENTED_EDGE ( 'NONE', *, *, #124889, .F. ) ;
#2037=DIRECTION ( 'NONE',  ( 1.000000000000000000, -0.000000000000000000, -0.000000000000000000 ) ) ;
#2067=ORIENTED_EDGE ( 'NONE', *, *, #86124, .F. ) ;
#2088=ORIENTED_EDGE ( 'NONE', *, *, #219268, .F. ) ;
#2134=DIRECTION ( 'NONE',  ( 0.7071067811865474617, 0.6909108974501236844, 0.1504730267678057731 ) ) ;
#2187=CARTESIAN_POINT ( 'NONE',  ( 20.96428641294528106, 17.15731666422714241, -224.5635080354869046 ) ) ;
#2232=CARTESIAN_POINT ( 'NONE',  ( 23.14999999999999503, 19.71413185295147485, -225.2601813404592406 ) ) ;
#2243=DIRECTION ( 'NONE',  ( 0.000000000000000000, 0.9770955615653255100, 0.2128009952263878735 ) ) ;
#2244=VECTOR ( 'NONE', #91441, 1000.000000000000227 ) ;
#2260=DIRECTION ( 'NONE',  ( 0.000000000000000000, 0.2128009952263604232, -0.9770955615653316162 ) ) ;
#2264=EDGE_CURVE ( 'NONE', #74308, #96338, #84766, .T. ) ;
#2375=CARTESIAN_POINT ( 'NONE',  ( -18.59999999999999787, 7.476371755685454090, -241.7308184205399471 ) ) ;
#2425=AXIS2_PLACEMENT_3D ( 'NONE', #153513, #135160, #16531 ) ;
#2436=DIRECTION ( 'NONE',  ( 0.000000000000000000, -0.6728388485993177515, 0.7397890806274072251 ) ) ;
#2440=FACE_BOUND ( 'NONE', #136830, .T. ) ;
#2459=EDGE_LOOP ( 'NONE', ( #84036, #123017, #84651, #33522 ) ) ;
#2460=DIRECTION ( 'NONE',  ( 1.000000000000000000, 0.000000000000000000, 0.000000000000000000 ) ) ;
#2467=FACE_OUTER_BOUND ( 'NONE', #246611, .T. ) ;
#2472=LINE ( 'NONE', #198121, #128010 ) ;
#2535=CIRCLE ( 'NONE', #81614, 0.09999999999999534261 ) ;
#2541=DIRECTION ( 'NONE',  ( 1.000000000000000000, 0.000000000000000000, 0.000000000000000000 ) ) ;
#2617=VERTEX_POINT ( 'NONE', #67513 ) ;
#2619=VERTEX_POINT ( 'NONE', #204448 ) ;
#2629=CIRCLE ( 'NONE', #44168, 0.1000000000000133560 ) ;
#2637=CARTESIAN_POINT ( 'NONE',  ( 22.60000000000000142, -2.401771312552908544, -189.4980873520049727 ) ) ;
#2653=VECTOR ( 'NONE', #183279, 1000.000000000000227 ) ;
#2657=ORIENTED_EDGE ( 'NONE', *, *, #53200, .F. ) ;
#2659=EDGE_CURVE ( 'NONE', #97694, #95409, #97427, .T. ) ;
#2704=CARTESIAN_POINT ( 'NONE',  ( 18.59999999999999076, 16.64998792410002793, -222.7039835543563981 ) ) ;
#2712=AXIS2_PLACEMENT_3D ( 'NONE', #235282, #39692, #98306 ) ;
#2742=ADVANCED_FACE ( 'NONE', ( #55617 ), #76610, .T. ) ;
#2780=AXIS2_PLACEMENT_3D ( 'NONE', #255033, #59429, #56866 ) ;
#2792=CIRCLE ( 'NONE', #210918, 11.70000000000000284 ) ;
#2847=DIRECTION ( 'NONE',  ( -1.000000000000000000, -3.190570557967288949E-16, -6.948722487160392945E-17 ) ) ;
#2861=LINE ( 'NONE', #82383, #110139 ) ;
#2899=DIRECTION ( 'NONE',  ( -6.938893903907220489E-15, 0.9770955615653313941, 0.2128009952263603677 ) ) ;
#2905=EDGE_CURVE ( 'NONE', #9452, #52291, #137738, .T. ) ;
#2942=ORIENTED_EDGE ( 'NONE', *, *, #81627, .F. ) ;
#2948=CARTESIAN_POINT ( 'NONE',  ( -20.85000000000000142, 7.128833340094563376, -233.7327013124401276 ) ) ;
#2952=ORIENTED_EDGE ( 'NONE', *, *, #40598, .F. ) ;
#2968=EDGE_LOOP ( 'NONE', ( #53161, #30718, #250507, #106077 ) ) ;
#2973=VERTEX_POINT ( 'NONE', #204134 ) ;
#2974=ORIENTED_EDGE ( 'NONE', *, *, #137648, .T. ) ;
#2997=VECTOR ( 'NONE', #114422, 1000.000000000000000 ) ;
#3009=ADVANCED_FACE ( 'NONE', ( #29405 ), #144154, .T. ) ;
#3036=CARTESIAN_POINT ( 'NONE',  ( 21.05000000000000071, -4.259020970815407203, -226.0869574510824123 ) ) ;
#3054=DIRECTION ( 'NONE',  ( -4.408576920032447355E-17, -0.07893460099012301889, 0.9968797965484755830 ) ) ;
#3068=LINE ( 'NONE', #63050, #182868 ) ;
#3069=CARTESIAN_POINT ( 'NONE',  ( 23.25000000000000000, -6.388372595096674544, -212.0629706944429813 ) ) ;
#3103=DIRECTION ( 'NONE',  ( -1.000000000000000000, -2.885090398161910246E-16, -6.283419270304610340E-17 ) ) ;
#3128=VECTOR ( 'NONE', #167945, 1000.000000000000000 ) ;
#3150=CARTESIAN_POINT ( 'NONE',  ( -20.54999999999999716, 9.593045456726526865, -211.4478935133083439 ) ) ;
#3171=CARTESIAN_POINT ( 'NONE',  ( 21.04116576186338250, 13.00484560748014928, -210.7852636494204148 ) ) ;
#3189=VECTOR ( 'NONE', #148385, 1000.000000000000227 ) ;
#3205=EDGE_CURVE ( 'NONE', #165685, #140605, #97793, .T. ) ;
#3246=CARTESIAN_POINT ( 'NONE',  ( 20.94999999999999929, 10.52493806863738790, -207.3780514093641330 ) ) ;
#3257=VERTEX_POINT ( 'NONE', #1776 ) ;
#3265=CARTESIAN_POINT ( 'NONE',  ( -22.50000000000000000, -0.02128009951114784304, -200.9022904438449757 ) ) ;
#3308=DIRECTION ( 'NONE',  ( -1.000000000000000000, 0.000000000000000000, 0.000000000000000000 ) ) ;
#3329=CARTESIAN_POINT ( 'NONE',  ( -21.05000000000000071, 11.40444339177023458, -198.6185779617709670 ) ) ;
#3335=CIRCLE ( 'NONE', #128446, 0.1000000000000054040 ) ;
#3336=AXIS2_PLACEMENT_3D ( 'NONE', #15491, #131566, #112020 ) ;
#3341=VECTOR ( 'NONE', #152131, 1000.000000000000227 ) ;
#3385=DIRECTION ( 'NONE',  ( 1.000000000000000000, -0.000000000000000000, -0.000000000000000000 ) ) ;
#3388=ORIENTED_EDGE ( 'NONE', *, *, #110340, .T. ) ;
#3409=DIRECTION ( 'NONE',  ( 0.000000000000000000, -0.9770955615653312831, -0.2128009952263621163 ) ) ;
#3417=EDGE_CURVE ( 'NONE', #164555, #164130, #10368, .T. ) ;
#3466=AXIS2_PLACEMENT_3D ( 'NONE', #55087, #130799, #193365 ) ;
#3471=LINE ( 'NONE', #122154, #188091 ) ;
#3485=CIRCLE ( 'NONE', #28683, 0.1000000000000009354 ) ;
#3493=AXIS2_PLACEMENT_3D ( 'NONE', #198496, #2847, #155560 ) ;
#3494=DIRECTION ( 'NONE',  ( 1.000000000000000000, 0.000000000000000000, 0.000000000000000000 ) ) ;
#3508=AXIS2_PLACEMENT_3D ( 'NONE', #91775, #253408, #94328 ) ;
#3546=VERTEX_POINT ( 'NONE', #229830 ) ;
#3555=AXIS2_PLACEMENT_3D ( 'NONE', #127927, #67945, #88768 ) ;
#3562=EDGE_CURVE ( 'NONE', #89391, #17786, #52208, .T. ) ;
#3563=AXIS2_PLACEMENT_3D ( 'NONE', #112483, #207733, #130743 ) ;
#3610=CARTESIAN_POINT ( 'NONE',  ( -21.45000000000000284, 10.13883017033223943, -211.3290274220034632 ) ) ;
#3623=AXIS2_PLACEMENT_3D ( 'NONE', #139481, #83340, #242436 ) ;
#3643=VECTOR ( 'NONE', #113953, 1000.000000000000000 ) ;
#3662=ADVANCED_FACE ( 'NONE', ( #2440, #200665 ), #63707, .T. ) ;
#3669=DIRECTION ( 'NONE',  ( -0.000000000000000000, 0.08413937888704209334, -0.9964539953858898569 ) ) ;
#3701=DIRECTION ( 'NONE',  ( 0.000000000000000000, 0.9770955615653316162, 0.2128009952263604232 ) ) ;
#3713=CIRCLE ( 'NONE', #161968, 0.1000000000000054040 ) ;
#3730=CARTESIAN_POINT ( 'NONE',  ( -18.50000000000000355, -7.661125819576635188, -210.0861952081431241 ) ) ;
#3740=ORIENTED_EDGE ( 'NONE', *, *, #54654, .T. ) ;
#3753=DIRECTION ( 'NONE',  ( -1.000000000000000000, 0.000000000000000000, 0.000000000000000000 ) ) ;
#3766=CYLINDRICAL_SURFACE ( 'NONE', #129363, 0.5000000000000007772 ) ;
#3859=CARTESIAN_POINT ( 'NONE',  ( -18.58222699835055280, 18.41441690808118636, -236.9991004306322964 ) ) ;
#3865=CARTESIAN_POINT ( 'NONE',  ( -21.45000000000000284, 12.05403912736948158, -220.1228874760914209 ) ) ;
#3867=DIRECTION ( 'NONE',  ( 1.000000000000000000, -0.000000000000000000, -0.000000000000000000 ) ) ;
#3912=DIRECTION ( 'NONE',  ( 0.000000000000000000, 0.2128009952263605897, -0.9770955615653313941 ) ) ;
#3994=DIRECTION ( 'NONE',  ( 0.000000000000000000, -0.3042567129660006531, -0.9525900758537875213 ) ) ;
#4038=PLANE ( 'NONE',  #36375 ) ;
#4087=PLANE ( 'NONE',  #187789 ) ;
#4101=EDGE_LOOP ( 'NONE', ( #159843, #251637, #155073, #209880 ) ) ;
#4123=FACE_OUTER_BOUND ( 'NONE', #96548, .T. ) ;
#4136=DIRECTION ( 'NONE',  ( 0.000000000000000000, -0.9770955615653543758, -0.2128009952262553683 ) ) ;
#4137=EDGE_CURVE ( 'NONE', #102962, #83472, #88070, .T. ) ;
#4164=CARTESIAN_POINT ( 'NONE',  ( -20.54999999999999716, 13.65786464920749843, -219.7735913778983559 ) ) ;
#4190=CARTESIAN_POINT ( 'NONE',  ( -21.55000000000000426, 12.09451175070297069, -220.1140729702605370 ) ) ;
#4192=DIRECTION ( 'NONE',  ( 1.000000000000000000, 0.000000000000000000, 0.000000000000000000 ) ) ;
#4254=ORIENTED_EDGE ( 'NONE', *, *, #248219, .T. ) ;
#4317=EDGE_CURVE ( 'NONE', #121941, #54351, #253580, .T. ) ;
#4318=DIRECTION ( 'NONE',  ( -1.000000000000000000, -0.000000000000000000, -0.000000000000000000 ) ) ;
#4331=EDGE_CURVE ( 'NONE', #236679, #115361, #92459, .T. ) ;
#4334=CIRCLE ( 'NONE', #191650, 0.1000000000000054040 ) ;
#4357=AXIS2_PLACEMENT_3D ( 'NONE', #8233, #146422, #108602 ) ;
#4368=FACE_OUTER_BOUND ( 'NONE', #235275, .T. ) ;
#4369=AXIS2_PLACEMENT_3D ( 'NONE', #234059, #89413, #172863 ) ;
#4400=ORIENTED_EDGE ( 'NONE', *, *, #98880, .F. ) ;
#4413=CARTESIAN_POINT ( 'NONE',  ( -18.39999999999999858, -0.9152171842607119689, -242.2974985173726452 ) ) ;
#4420=DIRECTION ( 'NONE',  ( 1.000000000000000000, 0.000000000000000000, 0.000000000000000000 ) ) ;
#4435=DIRECTION ( 'NONE',  ( -1.000000000000000000, 0.000000000000000000, 0.000000000000000000 ) ) ;
#4457=CYLINDRICAL_SURFACE ( 'NONE', #84992, 0.8750000000000007772 ) ;
#4465=CARTESIAN_POINT ( 'NONE',  ( 21.05000000000000071, 12.97080753594469371, -210.6099088122175260 ) ) ;
#4471=ORIENTED_EDGE ( 'NONE', *, *, #199536, .T. ) ;
#4493=VECTOR ( 'NONE', #152257, 999.9999999999998863 ) ;
#4536=EDGE_CURVE ( 'NONE', #162009, #47690, #142343, .T. ) ;
#4581=ORIENTED_EDGE ( 'NONE', *, *, #81512, .T. ) ;
#4643=ORIENTED_EDGE ( 'NONE', *, *, #147244, .T. ) ;
#4648=CARTESIAN_POINT ( 'NONE',  ( 20.94999999999999929, 7.128833340094563376, -233.7327013124401276 ) ) ;
#4684=LINE ( 'NONE', #226296, #32672 ) ;
#4747=ORIENTED_EDGE ( 'NONE', *, *, #148032, .F. ) ;
#4748=SPHERICAL_SURFACE ( 'NONE', #55724, 0.1000000000000000056 ) ;
#4758=ORIENTED_EDGE ( 'NONE', *, *, #125966, .T. ) ;
#4839=ORIENTED_EDGE ( 'NONE', *, *, #225038, .T. ) ;
#4843=LINE ( 'NONE', #143086, #181226 ) ;
#4855=ORIENTED_EDGE ( 'NONE', *, *, #232881, .F. ) ;
#4887=AXIS2_PLACEMENT_3D ( 'NONE', #223235, #103280, #105847 ) ;
#4912=CARTESIAN_POINT ( 'NONE',  ( 20.94999999999999929, 9.374458193048763377, -220.5475659691911119 ) ) ;
#4923=CYLINDRICAL_SURFACE ( 'NONE', #204373, 0.09999999999999156786 ) ;
#4947=ORIENTED_EDGE ( 'NONE', *, *, #77275, .T. ) ;
#4970=EDGE_LOOP ( 'NONE', ( #100228, #145811, #149572, #10042 ) ) ;
#4986=ORIENTED_EDGE ( 'NONE', *, *, #180218, .F. ) ;
#5025=CARTESIAN_POINT ( 'NONE',  ( -21.11825140030068582, 6.296246187023214702, -199.6213722296933213 ) ) ;
#5038=CARTESIAN_POINT ( 'NONE',  ( -20.85000000000000142, 7.783179459866052419, -245.3643104511423303 ) ) ;
#5058=ORIENTED_EDGE ( 'NONE', *, *, #177675, .F. ) ;
#5069=DIRECTION ( 'NONE',  ( 0.000000000000000000, 0.2128009952263403282, -0.9770955615653358350 ) ) ;
#5070=AXIS2_PLACEMENT_3D ( 'NONE', #190245, #88544, #226786 ) ;
#5073=CARTESIAN_POINT ( 'NONE',  ( -18.59999999999999787, -7.631834139420953456, -210.1304494778855769 ) ) ;
#5074=AXIS2_PLACEMENT_3D ( 'NONE', #178977, #39462, #199804 ) ;
#5095=CARTESIAN_POINT ( 'NONE',  ( -21.05000000000000071, 0.6713328740235187109, -212.7808875799876205 ) ) ;
#5101=CARTESIAN_POINT ( 'NONE',  ( -18.54148534481894828, 18.40294846151842378, -236.9778203247716419 ) ) ;
#5144=ORIENTED_EDGE ( 'NONE', *, *, #202970, .F. ) ;
#5146=VERTEX_POINT ( 'NONE', #155204 ) ;
#5170=AXIS2_PLACEMENT_3D ( 'NONE', #62143, #118263, #37456 ) ;
#5187=DIRECTION ( 'NONE',  ( 0.000000000000000000, 0.2128009952263568982, -0.9770955615653323934 ) ) ;
#5221=CIRCLE ( 'NONE', #213335, 0.09999999999999895084 ) ;
#5259=VECTOR ( 'NONE', #162666, 1000.000000000000000 ) ;
#5285=EDGE_CURVE ( 'NONE', #50999, #149564, #9442, .T. ) ;
#5316=CARTESIAN_POINT ( 'NONE',  ( -20.64999999999999858, 1.148907358139439339E-11, -201.0000000000015064 ) ) ;
#5323=CARTESIAN_POINT ( 'NONE',  ( 21.05000000000000071, 12.10919762232931518, -206.2073353557311748 ) ) ;
#5352=DIRECTION ( 'NONE',  ( 0.000000000000000000, -0.2128009952263605342, 0.9770955615653315052 ) ) ;
#5373=CARTESIAN_POINT ( 'NONE',  ( 23.14999999999999503, 13.98997548377052524, -210.4902890347897255 ) ) ;
#5384=CARTESIAN_POINT ( 'NONE',  ( -18.59999999999999787, 14.06640494040441602, -210.3712993791105532 ) ) ;
#5395=CARTESIAN_POINT ( 'NONE',  ( -18.59999999999999787, 18.41524492703432614, -237.0006385043383546 ) ) ;
#5430=CARTESIAN_POINT ( 'NONE',  ( 21.05995757104869526, 11.16948182890036456, -211.0481761046111444 ) ) ;
#5462=DIRECTION ( 'NONE',  ( -1.000000000000000000, -2.885090398161910739E-16, -6.283419270304611573E-17 ) ) ;
#5464=CARTESIAN_POINT ( 'NONE',  ( -21.53752568617696284, 6.610297987518923613, -199.4590530230520073 ) ) ;
#5477=ADVANCED_FACE ( 'NONE', ( #18868 ), #102222, .T. ) ;
#5485=CARTESIAN_POINT ( 'NONE',  ( -20.85000000000000142, 14.78417726655519715, -235.8865342417136333 ) ) ;
#5500=ORIENTED_EDGE ( 'NONE', *, *, #154025, .F. ) ;
#5508=CIRCLE ( 'NONE', #238770, 0.09999999999999939493 ) ;
#5515=AXIS2_PLACEMENT_3D ( 'NONE', #225739, #168413, #165816 ) ;
#5522=DIRECTION ( 'NONE',  ( 0.000000000000000000, -0.2128009952263568982, 0.9770955615653323934 ) ) ;
#5525=ORIENTED_EDGE ( 'NONE', *, *, #232673, .F. ) ;
#5593=VERTEX_POINT ( 'NONE', #70879 ) ;
#5603=AXIS2_PLACEMENT_3D ( 'NONE', #192623, #71408, #150925 ) ;
#5608=ORIENTED_EDGE ( 'NONE', *, *, #160778, .F. ) ;
#5638=ADVANCED_FACE ( 'NONE', ( #167403 ), #152586, .T. ) ;
#5642=EDGE_CURVE ( 'NONE', #3546, #29211, #145229, .T. ) ;
#5654=DIRECTION ( 'NONE',  ( 0.000000000000000000, 0.9770955615653260651, 0.2128009952263853755 ) ) ;
#5666=CIRCLE ( 'NONE', #97222, 7.900000000000004796 ) ;
#5714=DIRECTION ( 'NONE',  ( -1.000000000000000000, 0.000000000000000000, 0.000000000000000000 ) ) ;
#5736=VERTEX_POINT ( 'NONE', #235065 ) ;
#5751=FACE_OUTER_BOUND ( 'NONE', #251156, .T. ) ;
#5769=EDGE_CURVE ( 'NONE', #165685, #235545, #23767, .T. ) ;
#5775=AXIS2_PLACEMENT_3D ( 'NONE', #53628, #14526, #213987 ) ;
#5802=DIRECTION ( 'NONE',  ( 1.000000000000000000, 0.000000000000000000, 0.000000000000000000 ) ) ;
#5856=ORIENTED_EDGE ( 'NONE', *, *, #86765, .F. ) ;
#5896=DIRECTION ( 'NONE',  ( 0.000000000000000000, -0.07893460099012303277, 0.9968797965484756940 ) ) ;
#5928=CYLINDRICAL_SURFACE ( 'NONE', #160450, 0.1000000000000055844 ) ;
#5941=CARTESIAN_POINT ( 'NONE',  ( -20.94999999999999929, 0.5663372425336981042, -209.0641885820623997 ) ) ;
#5951=ORIENTED_EDGE ( 'NONE', *, *, #74570, .F. ) ;
#5975=DIRECTION ( 'NONE',  ( 0.000000000000000000, 0.2128009952263568982, -0.9770955615653323934 ) ) ;
#6027=DIRECTION ( 'NONE',  ( -1.000000000000000000, 0.000000000000000000, 0.000000000000000000 ) ) ;
#6041=CIRCLE ( 'NONE', #31038, 0.1000000000000055844 ) ;
#6042=CARTESIAN_POINT ( 'NONE',  ( 20.99551997958289107, 17.15237243733800554, -224.5408061578818888 ) ) ;
#6054=CARTESIAN_POINT ( 'NONE',  ( -20.96428641294375339, 17.15731666422713531, -224.5635080354877857 ) ) ;
#6061=CYLINDRICAL_SURFACE ( 'NONE', #220171, 11.80000000000000959 ) ;
#6081=ADVANCED_FACE ( 'NONE', ( #19418 ), #215276, .F. ) ;
#6094=ORIENTED_EDGE ( 'NONE', *, *, #145945, .F. ) ;
#6113=ORIENTED_EDGE ( 'NONE', *, *, #148023, .T. ) ;
#6140=ORIENTED_EDGE ( 'NONE', *, *, #45433, .F. ) ;
#6154=ADVANCED_FACE ( 'NONE', ( #21993 ), #220184, .T. ) ;
#6173=DIRECTION ( 'NONE',  ( 0.000000000000000000, 0.2128009952263607285, -0.9770955615653316162 ) ) ;
#6180=DIRECTION ( 'NONE',  ( 4.239556034732056743E-17, 0.08413937888704771384, -0.9964539953858891908 ) ) ;
#6181=CIRCLE ( 'NONE', #231075, 0.3999999999999952482 ) ;
#6200=FACE_OUTER_BOUND ( 'NONE', #214151, .T. ) ;
#6210=DIRECTION ( 'NONE',  ( 0.000000000000000000, 0.2128009952263403282, -0.9770955615653358350 ) ) ;
#6212=CARTESIAN_POINT ( 'NONE',  ( -18.50000000000000000, 11.66622623553636018, -211.0987209794895421 ) ) ;
#6259=CIRCLE ( 'NONE', #101927, 0.09999999999999939493 ) ;
#6280=ORIENTED_EDGE ( 'NONE', *, *, #5769, .T. ) ;
#6386=DIRECTION ( 'NONE',  ( 0.000000000000000000, 0.9770955615653310611, 0.2128009952263620608 ) ) ;
#6416=CARTESIAN_POINT ( 'NONE',  ( -18.50000000000000000, 18.34743685832668447, -236.8753540304231535 ) ) ;
#6424=DIRECTION ( 'NONE',  ( -0.000000000000000000, 0.9770955615653313941, 0.2128009952263603954 ) ) ;
#6429=CARTESIAN_POINT ( 'NONE',  ( 18.44208962362797166, -0.7486949262819061479, -242.4509058008785303 ) ) ;
#6438=FACE_OUTER_BOUND ( 'NONE', #168608, .T. ) ;
#6445=EDGE_CURVE ( 'NONE', #165216, #98224, #155126, .T. ) ;
#6449=ADVANCED_FACE ( 'NONE', ( #84482 ), #194061, .F. ) ;
#6501=LINE ( 'NONE', #22244, #168340 ) ;
#6515=ORIENTED_EDGE ( 'NONE', *, *, #105356, .T. ) ;
#6545=DIRECTION ( 'NONE',  ( 0.7071359030027289938, -0.1504668293610967600, 0.6908824414808452108 ) ) ;
#6547=CIRCLE ( 'NONE', #77276, 0.09999999999999895084 ) ;
#6564=CARTESIAN_POINT ( 'NONE',  ( 20.85000000000000142, 14.61354176542825201, -235.9279552357344016 ) ) ;
#6584=CARTESIAN_POINT ( 'NONE',  ( 23.24999999999999645, 5.076932660807368158, -234.1795834024155170 ) ) ;
#6615=AXIS2_PLACEMENT_3D ( 'NONE', #27885, #109942, #10861 ) ;
#6625=EDGE_CURVE ( 'NONE', #163980, #63679, #110833, .T. ) ;
#6640=CIRCLE ( 'NONE', #123172, 0.09999999999999061029 ) ;
#6655=EDGE_CURVE ( 'NONE', #239248, #236182, #177510, .T. ) ;
#6661=VERTEX_POINT ( 'NONE', #47965 ) ;
#6670=DIRECTION ( 'NONE',  ( 0.000000000000000000, 0.2128009952264976468, -0.9770955615653015291 ) ) ;
#6672=CARTESIAN_POINT ( 'NONE',  ( 20.94999999999999929, 1.148907358139439339E-11, -201.0000000000015064 ) ) ;
#6684=EDGE_CURVE ( 'NONE', #256235, #45345, #77478, .T. ) ;
#6694=( NAMED_UNIT ( * ) SI_UNIT ( $, .STERADIAN. ) SOLID_ANGLE_UNIT ( ) );
#6700=AXIS2_PLACEMENT_3D ( 'NONE', #204237, #28213, #26924 ) ;
#6719=EDGE_CURVE ( 'NONE', #122837, #142228, #56925, .T. ) ;
#6729=AXIS2_PLACEMENT_3D ( 'NONE', #15769, #191838, #53582 ) ;
#6740=CARTESIAN_POINT ( 'NONE',  ( 21.05000000000000071, 11.16079915604378492, -211.0041093385139561 ) ) ;
#6758=CARTESIAN_POINT ( 'NONE',  ( -21.14999999999999858, -2.576749817950531707, -189.6385361693310756 ) ) ;
#6760=ORIENTED_EDGE ( 'NONE', *, *, #134384, .T. ) ;
#6768=( BOUNDED_SURFACE ( )  B_SPLINE_SURFACE ( 3, 2, ( 
 ( #132982, #71725, #11760 ),
 ( #252905, #215066, #134232 ),
 ( #52127, #232086, #55970 ),
 ( #50832, #151261, #230804 ),
 ( #110825, #213785, #114686 ),
 ( #96384, #194253, #191694 ) ),
 .UNSPECIFIED., .F., .F., .F. ) 
 B_SPLINE_SURFACE_WITH_KNOTS ( ( 4, 2, 4 ),
 ( 3, 3 ),
 ( 0.0001792624049599585438, 0.0003686986002124638092, 0.0005581347954649691287 ),
 ( 0.000000000000000000, 1.000000000000000000 ),
 .UNSPECIFIED. ) 
 GEOMETRIC_REPRESENTATION_ITEM ( )  RATIONAL_B_SPLINE_SURFACE ( (
 ( 1.000000000000000000, 0.9238795325113041690, 1.000000000000000000),
 ( 1.000000000000000000, 0.9229318695237117565, 1.000000000000000000),
 ( 1.000000000000000000, 0.8926288119232198559, 1.000000000000000000),
 ( 1.000000000000000000, 0.8123777807270403661, 1.000000000000000000),
 ( 1.000000000000000000, 0.7629087100932245846, 1.000000000000000000),
 ( 1.000000000000000000, 0.7071067811865475727, 1.000000000000000000) ) ) 
 REPRESENTATION_ITEM ( '' )  SURFACE ( )  );
#6806=DIRECTION ( 'NONE',  ( 0.000000000000000000, 0.2128009952263601179, -0.9770955615653315052 ) ) ;
#6808=DIRECTION ( 'NONE',  ( 1.000000000000000000, 0.000000000000000000, 0.000000000000000000 ) ) ;
#6810=VECTOR ( 'NONE', #190001, 1000.000000000000000 ) ;
#6876=ORIENTED_EDGE ( 'NONE', *, *, #197856, .F. ) ;
#6963=DIRECTION ( 'NONE',  ( -0.000000000000000000, -0.2128009952263603677, 0.9770955615653313941 ) ) ;
#6973=ORIENTED_EDGE ( 'NONE', *, *, #40381, .F. ) ;
#7020=CARTESIAN_POINT ( 'NONE',  ( 18.51565452909213505, -7.607553483789936344, -210.0204117391616023 ) ) ;
#7027=CARTESIAN_POINT ( 'NONE',  ( 18.39999999999999858, -7.883686024897172295, -209.9138933503092233 ) ) ;
#7039=CARTESIAN_POINT ( 'NONE',  ( 21.08804281139591907, 13.00663943612646456, -210.8067932428972426 ) ) ;
#7044=ORIENTED_EDGE ( 'NONE', *, *, #158296, .F. ) ;
#7088=CARTESIAN_POINT ( 'NONE',  ( 18.59999999999999432, 2.899901325892992876, -187.5321506284477096 ) ) ;
#7125=CIRCLE ( 'NONE', #102797, 0.09999999999999724387 ) ;
#7157=VERTEX_POINT ( 'NONE', #128171 ) ;
#7177=ORIENTED_EDGE ( 'NONE', *, *, #192145, .F. ) ;
#7182=CARTESIAN_POINT ( 'NONE',  ( 23.24999999999999289, 3.801854678198143933, -188.1465607323988252 ) ) ;
#7190=DIRECTION ( 'NONE',  ( -1.000000000000000000, 0.000000000000000000, 0.000000000000000000 ) ) ;
#7206=DIRECTION ( 'NONE',  ( 0.000000000000000000, 0.9770955615653259541, 0.2128009952263860971 ) ) ;
#7209=CARTESIAN_POINT ( 'NONE',  ( -20.54999999999999716, -7.079251802663311111, -212.6676826711374417 ) ) ;
#7253=VECTOR ( 'NONE', #109318, 1000.000000000000000 ) ;
#7260=CARTESIAN_POINT ( 'NONE',  ( 20.94999999999999929, 4.252251777740766236, -211.8999245327126744 ) ) ;
#7318=EDGE_CURVE ( 'NONE', #149564, #18045, #245255, .T. ) ;
#7322=DIRECTION ( 'NONE',  ( 0.000000000000000000, 0.06835365183351375939, -0.9976611540402997580 ) ) ;
#7341=CARTESIAN_POINT ( 'NONE',  ( 18.49999999999999289, 18.34711819382569686, -236.8747682978092541 ) ) ;
#7347=LINE ( 'NONE', #167735, #42360 ) ;
#7366=AXIS2_PLACEMENT_3D ( 'NONE', #88416, #148434, #227959 ) ;
#7375=CARTESIAN_POINT ( 'NONE',  ( 21.04105312098486635, 11.29556661886501523, -211.1574496082819792 ) ) ;
#7404=TOROIDAL_SURFACE ( 'NONE', #7800, 1.900000000000002576, 0.1000000000000000056 ) ;
#7412=CARTESIAN_POINT ( 'NONE',  ( -20.54999999999999716, 11.58468387039766512, -220.1227639117171861 ) ) ;
#7418=AXIS2_PLACEMENT_3D ( 'NONE', #105013, #85457, #102456 ) ;
#7430=ORIENTED_EDGE ( 'NONE', *, *, #10859, .F. ) ;
#7439=ORIENTED_EDGE ( 'NONE', *, *, #26708, .F. ) ;
#7454=VECTOR ( 'NONE', #213670, 1000.000000000000000 ) ;
#7468=VERTEX_POINT ( 'NONE', #92575 ) ;
#7475=DIRECTION ( 'NONE',  ( 0.000000000000000000, -0.2128009952263603677, 0.9770955615653313941 ) ) ;
#7493=DIRECTION ( 'NONE',  ( -1.000000000000000000, 2.775557561562908012E-13, 0.000000000000000000 ) ) ;
#7523=EDGE_CURVE ( 'NONE', #175634, #184179, #74919, .T. ) ;
#7556=CIRCLE ( 'NONE', #186637, 0.1000000000000034472 ) ;
#7577=ORIENTED_EDGE ( 'NONE', *, *, #63158, .T. ) ;
#7608=VERTEX_POINT ( 'NONE', #76866 ) ;
#7612=ORIENTED_EDGE ( 'NONE', *, *, #22453, .F. ) ;
#7613=FACE_OUTER_BOUND ( 'NONE', #205747, .T. ) ;
#7616=CIRCLE ( 'NONE', #3493, 11.65000000000000568 ) ;
#7669=CYLINDRICAL_SURFACE ( 'NONE', #230566, 0.09999999999999939493 ) ;
#7683=DIRECTION ( 'NONE',  ( 1.000000000000000000, 0.000000000000000000, 0.000000000000000000 ) ) ;
#7688=DIRECTION ( 'NONE',  ( 0.000000000000000000, -0.9770955615653307280, -0.2128009952263642535 ) ) ;
#7702=CARTESIAN_POINT ( 'NONE',  ( 18.49999999999999289, 11.04098673250373785, -220.4458636211660689 ) ) ;
#7721=PLANE ( 'NONE',  #139446 ) ;
#7761=CARTESIAN_POINT ( 'NONE',  ( -22.49510344025093644, -2.413535076292374182, -189.6025810811986219 ) ) ;
#7764=CARTESIAN_POINT ( 'NONE',  ( -21.14999999999999858, -2.576749817950531707, -189.6385361693310756 ) ) ;
#7779=ORIENTED_EDGE ( 'NONE', *, *, #27414, .F. ) ;
#7799=CARTESIAN_POINT ( 'NONE',  ( 20.85000000000000142, 7.128833340094563376, -233.7327013124401276 ) ) ;
#7800=AXIS2_PLACEMENT_3D ( 'NONE', #193210, #15873, #254422 ) ;
#7841=ORIENTED_EDGE ( 'NONE', *, *, #200893, .F. ) ;
#7842=TOROIDAL_SURFACE ( 'NONE', #203651, 0.4000000000000012990, 0.1000000000000000056 ) ;
#7844=DIRECTION ( 'NONE',  ( -3.469446951953738513E-14, 0.9770955615653543758, 0.2128009952262553683 ) ) ;
#7846=ORIENTED_EDGE ( 'NONE', *, *, #75513, .T. ) ;
#7927=EDGE_LOOP ( 'NONE', ( #165363, #39452, #248370, #167477, #89151 ) ) ;
#7943=CIRCLE ( 'NONE', #12232, 0.1000000000000054040 ) ;
#7955=AXIS2_PLACEMENT_3D ( 'NONE', #129170, #48337, #204831 ) ;
#7989=VERTEX_POINT ( 'NONE', #118269 ) ;
#8008=AXIS2_PLACEMENT_3D ( 'NONE', #61583, #79833, #198522 ) ;
#8059=CIRCLE ( 'NONE', #70621, 0.9750000000000036415 ) ;
#8076=ADVANCED_FACE ( 'NONE', ( #34912 ), #75315, .F. ) ;
#8089=SPHERICAL_SURFACE ( 'NONE', #206107, 0.1000000000000000056 ) ;
#8097=CYLINDRICAL_SURFACE ( 'NONE', #167345, 0.09999999999999939493 ) ;
#8103=DIRECTION ( 'NONE',  ( 0.000000000000000000, 0.9968797965484670343, 0.07893460099023182075 ) ) ;
#8117=DIRECTION ( 'NONE',  ( 1.000000000000000000, 0.000000000000000000, 0.000000000000000000 ) ) ;
#8140=VECTOR ( 'NONE', #57598, 1000.000000000000000 ) ;
#8143=ORIENTED_EDGE ( 'NONE', *, *, #72129, .F. ) ;
#8157=EDGE_CURVE ( 'NONE', #69101, #143844, #83067, .T. ) ;
#8233=CARTESIAN_POINT ( 'NONE',  ( -23.25000000000000000, -13.98128454229089357, -192.0195388455185821 ) ) ;
#8265=CYLINDRICAL_SURFACE ( 'NONE', #38213, 0.1000000000000054040 ) ;
#8291=FACE_OUTER_BOUND ( 'NONE', #143303, .T. ) ;
#8292=( BOUNDED_SURFACE ( )  B_SPLINE_SURFACE ( 3, 2, ( 
 ( #113888, #70943, #189586 ),
 ( #13515, #10950, #53916 ),
 ( #252106, #190889, #227407 ),
 ( #232582, #108750, #153063 ) ),
 .UNSPECIFIED., .F., .F., .F. ) 
 B_SPLINE_SURFACE_WITH_KNOTS ( ( 4, 4 ),
 ( 3, 3 ),
 ( 3.388131789017201356E-19, 0.0003124336117481281557 ),
 ( 0.000000000000000000, 1.000000000000000000 ),
 .UNSPECIFIED. ) 
 GEOMETRIC_REPRESENTATION_ITEM ( )  RATIONAL_B_SPLINE_SURFACE ( (
 ( 1.000000000000000000, 0.7040654476014488461, 1.000000000000000000),
 ( 1.000000000000000000, 0.7039193538784696003, 1.000000000000000000),
 ( 1.000000000000000000, 0.7089171279144220739, 1.000000000000000000),
 ( 1.000000000000000000, 0.7071067811864741870, 1.000000000000000000) ) ) 
 REPRESENTATION_ITEM ( '' )  SURFACE ( )  );
#8295=ORIENTED_EDGE ( 'NONE', *, *, #197951, .F. ) ;
#8347=DIRECTION ( 'NONE',  ( 1.000000000000000000, 0.000000000000000000, 0.000000000000000000 ) ) ;
#8348=DIRECTION ( 'NONE',  ( 0.000000000000000000, -0.2128009952263608118, 0.9770955615653313941 ) ) ;
#8367=DIRECTION ( 'NONE',  ( -0.7071067811865430208, 0.6909108974500454137, 0.1504730267681856082 ) ) ;
#8414=AXIS2_PLACEMENT_3D ( 'NONE', #2948, #162056, #198589 ) ;
#8430=EDGE_CURVE ( 'NONE', #51404, #22582, #120170, .T. ) ;
#8433=ORIENTED_EDGE ( 'NONE', *, *, #69677, .T. ) ;
#8435=DIRECTION ( 'NONE',  ( -0.000000000000000000, 0.2128009952263603677, -0.9770955615653313941 ) ) ;
#8452=DIRECTION ( 'NONE',  ( 0.000000000000000000, -0.9770955615653316162, -0.2128009952263604232 ) ) ;
#8453=ORIENTED_EDGE ( 'NONE', *, *, #230162, .F. ) ;
#8500=CARTESIAN_POINT ( 'NONE',  ( 23.15000000000000213, -3.281532336344783030, -226.3283167004136942 ) ) ;
#8510=ORIENTED_EDGE ( 'NONE', *, *, #32436, .T. ) ;
#8521=DIRECTION ( 'NONE',  ( 0.000000000000000000, -0.2128009952263603677, 0.9770955615653313941 ) ) ;
#8548=ORIENTED_EDGE ( 'NONE', *, *, #144022, .F. ) ;
#8577=ORIENTED_EDGE ( 'NONE', *, *, #62025, .T. ) ;
#8580=CARTESIAN_POINT ( 'NONE',  ( -23.15000000000000213, 6.681951250119205987, -231.6808006331528986 ) ) ;
#8590=CARTESIAN_POINT ( 'NONE',  ( -20.85000000000000142, 14.80545736607782814, -235.9842437978701639 ) ) ;
#8600=FACE_OUTER_BOUND ( 'NONE', #58788, .T. ) ;
#8622=CARTESIAN_POINT ( 'NONE',  ( -23.25000000000000000, 6.683038871553167226, -212.1840060551439819 ) ) ;
#8629=ORIENTED_EDGE ( 'NONE', *, *, #174392, .F. ) ;
#8674=ADVANCED_FACE ( 'NONE', ( #8291 ), #166141, .T. ) ;
#8691=VECTOR ( 'NONE', #79131, 1000.000000000000000 ) ;
#8706=EDGE_CURVE ( 'NONE', #68947, #64432, #68256, .T. ) ;
#8711=CARTESIAN_POINT ( 'NONE',  ( 23.14999999999999858, 8.111588099649802430, -211.9294447938511325 ) ) ;
#8733=CARTESIAN_POINT ( 'NONE',  ( 21.97500000000000497, 14.04870287383362992, -219.6884709798078177 ) ) ;
#8744=VECTOR ( 'NONE', #154057, 1000.000000000000227 ) ;
#8745=AXIS2_PLACEMENT_3D ( 'NONE', #6672, #125351, #206170 ) ;
#8773=AXIS2_PLACEMENT_3D ( 'NONE', #107860, #183562, #64881 ) ;
#8776=ORIENTED_EDGE ( 'NONE', *, *, #146384, .T. ) ;
#8781=CIRCLE ( 'NONE', #154383, 0.5000000000000007772 ) ;
#8788=ORIENTED_EDGE ( 'NONE', *, *, #183323, .T. ) ;
#8804=CIRCLE ( 'NONE', #154584, 4.099999999999988098 ) ;
#8808=ORIENTED_EDGE ( 'NONE', *, *, #234202, .F. ) ;
#8823=VERTEX_POINT ( 'NONE', #215147 ) ;
#8830=CARTESIAN_POINT ( 'NONE',  ( -20.64999999999999858, 7.128833340094563376, -233.7327013124401276 ) ) ;
#8854=EDGE_CURVE ( 'NONE', #135145, #112587, #91087, .T. ) ;
#8874=DIRECTION ( 'NONE',  ( 0.000000000000000000, 0.2128009952263630322, -0.9770955615653309501 ) ) ;
#8914=CIRCLE ( 'NONE', #175519, 0.5000000000000084377 ) ;
#8938=DIRECTION ( 'NONE',  ( -0.000000000000000000, 0.9770955615653316162, 0.2128009952263604232 ) ) ;
#8941=CARTESIAN_POINT ( 'NONE',  ( -2.995603634470829482E-16, 11.01970663298110154, -220.3481540650095098 ) ) ;
#8959=CARTESIAN_POINT ( 'NONE',  ( -21.05000000000000071, -10.51247937907010233, -206.3598299697285654 ) ) ;
#8960=CARTESIAN_POINT ( 'NONE',  ( -23.15000000000000213, 15.92646454033039660, -219.3818586450342707 ) ) ;
#8964=LINE ( 'NONE', #185030, #72973 ) ;
#8983=CARTESIAN_POINT ( 'NONE',  ( 18.49999999999998934, 16.64998792410002793, -222.7039835543563981 ) ) ;
#9022=CARTESIAN_POINT ( 'NONE',  ( 20.94999999999999929, 11.16079915604378492, -211.0041093385139561 ) ) ;
#9027=ORIENTED_EDGE ( 'NONE', *, *, #91163, .F. ) ;
#9038=CARTESIAN_POINT ( 'NONE',  ( 18.59999999999997655, 7.128833340094563376, -233.7327013124401276 ) ) ;
#9040=AXIS2_PLACEMENT_3D ( 'NONE', #160031, #242098, #201694 ) ;
#9049=CARTESIAN_POINT ( 'NONE',  ( -21.05000000000000071, 19.65328051035826817, -225.4506993556300074 ) ) ;
#9059=DIRECTION ( 'NONE',  ( 1.000000000000000000, 0.000000000000000000, 0.000000000000000000 ) ) ;
#9061=DIRECTION ( 'NONE',  ( 1.000000000000000000, -0.000000000000000000, -0.000000000000000000 ) ) ;
#9086=AXIS2_PLACEMENT_3D ( 'NONE', #102636, #222588, #124808 ) ;
#9101=EDGE_CURVE ( 'NONE', #89222, #247713, #110599, .T. ) ;
#9108=DIRECTION ( 'NONE',  ( 1.000000000000000000, 0.000000000000000000, 0.000000000000000000 ) ) ;
#9128=DIRECTION ( 'NONE',  ( -0.7070776581709311559, -0.1504792239192758452, 0.6909393522474779337 ) ) ;
#9130=VERTEX_POINT ( 'NONE', #76605 ) ;
#9164=VERTEX_POINT ( 'NONE', #154898 ) ;
#9194=ORIENTED_EDGE ( 'NONE', *, *, #113879, .T. ) ;
#9195=ORIENTED_EDGE ( 'NONE', *, *, #159099, .T. ) ;
#9202=EDGE_LOOP ( 'NONE', ( #123997, #81062, #37336, #1602 ) ) ;
#9203=DIRECTION ( 'NONE',  ( 1.000000000000000000, 0.000000000000000000, 0.000000000000000000 ) ) ;
#9237=CARTESIAN_POINT ( 'NONE',  ( -21.45000000000000284, 12.03275902784684703, -220.0251779199349187 ) ) ;
#9248=AXIS2_PLACEMENT_3D ( 'NONE', #251866, #151523, #150232 ) ;
#9262=DIRECTION ( 'NONE',  ( 0.000000000000000000, 0.2128009952263268945, -0.9770955615653388326 ) ) ;
#9265=CARTESIAN_POINT ( 'NONE',  ( 22.44352723754029810, -2.470007687997479717, -189.6151348049303635 ) ) ;
#9268=DIRECTION ( 'NONE',  ( -0.9880948137434723000, 0.1503223940869687358, 0.03273861465020812961 ) ) ;
#9275=CARTESIAN_POINT ( 'NONE',  ( -21.08134388332232589, -1.273944004185077805, -194.7942773797408336 ) ) ;
#9325=ORIENTED_EDGE ( 'NONE', *, *, #232881, .T. ) ;
#9345=CARTESIAN_POINT ( 'NONE',  ( -20.54999999999999716, 10.55064993524514705, -215.8448235403523370 ) ) ;
#9356=CARTESIAN_POINT ( 'NONE',  ( 18.49999999999999289, 15.47141130571843881, -222.9781839875250284 ) ) ;
#9359=ADVANCED_FACE ( 'NONE', ( #142973 ), #227979, .T. ) ;
#9363=DIRECTION ( 'NONE',  ( 1.000000000000000000, 0.000000000000000000, 0.000000000000000000 ) ) ;
#9364=DIRECTION ( 'NONE',  ( 1.000000000000000000, 0.000000000000000000, 0.000000000000000000 ) ) ;
#9381=CARTESIAN_POINT ( 'NONE',  ( 20.94999999999999929, 7.244009986534929446, -211.6437749090809177 ) ) ;
#9392=DIRECTION ( 'NONE',  ( 0.000000000000000000, 0.05689261644169250898, -0.9983803033886528011 ) ) ;
#9423=VERTEX_POINT ( 'NONE', #88126 ) ;
#9438=ADVANCED_FACE ( 'NONE', ( #128578 ), #125997, .F. ) ;
#9442=CIRCLE ( 'NONE', #155230, 0.1000000000000054040 ) ;
#9443=ORIENTED_EDGE ( 'NONE', *, *, #72576, .T. ) ;
#9452=VERTEX_POINT ( 'NONE', #7341 ) ;
#9490=DIRECTION ( 'NONE',  ( -0.000000000000000000, -0.2128009952263603677, 0.9770955615653313941 ) ) ;
#9559=EDGE_CURVE ( 'NONE', #111950, #205893, #145595, .T. ) ;
#9562=CARTESIAN_POINT ( 'NONE',  ( 23.14999999999999147, 1.148907358139439339E-11, -201.0000000000015064 ) ) ;
#9577=DIRECTION ( 'NONE',  ( 0.000000000000000000, 0.2128009952263604232, -0.9770955615653315052 ) ) ;
#9607=AXIS2_PLACEMENT_3D ( 'NONE', #221425, #19412, #24560 ) ;
#9608=FACE_OUTER_BOUND ( 'NONE', #138982, .T. ) ;
#9649=LINE ( 'NONE', #187030, #117444 ) ;
#9653=EDGE_LOOP ( 'NONE', ( #183980, #91049, #165239, #27522, #210826, #235871, #71280, #170038, #172026, #238677, #31658, #148322 ) ) ;
#9675=CARTESIAN_POINT ( 'NONE',  ( 20.85000000000000142, 18.51199663233068193, -231.2535697180530292 ) ) ;
#9733=AXIS2_PLACEMENT_3D ( 'NONE', #11114, #94484, #253554 ) ;
#9759=DIRECTION ( 'NONE',  ( 0.000000000000000000, 0.07893460099012014619, -0.9968797965484758050 ) ) ;
#9760=DIRECTION ( 'NONE',  ( 0.000000000000000000, 0.2128009952263485993, -0.9770955615653341697 ) ) ;
#9770=AXIS2_PLACEMENT_3D ( 'NONE', #17027, #195677, #41729 ) ;
#9790=DIRECTION ( 'NONE',  ( -0.000000000000000000, 0.9770955615653313941, 0.2128009952263603954 ) ) ;
#9820=CYLINDRICAL_SURFACE ( 'NONE', #9733, 0.09999999999999641120 ) ;
#9824=ORIENTED_EDGE ( 'NONE', *, *, #106138, .T. ) ;
#9865=ADVANCED_FACE ( 'NONE', ( #226047 ), #210387, .F. ) ;
#9874=DIRECTION ( 'NONE',  ( -1.000000000000000000, 0.000000000000000000, 0.000000000000000000 ) ) ;
#9893=DIRECTION ( 'NONE',  ( 1.000000000000000000, 0.000000000000000000, 0.000000000000000000 ) ) ;
#9905=CARTESIAN_POINT ( 'NONE',  ( -20.94999999999999929, -4.756823075239758225, -233.1486023682345490 ) ) ;
#9909=AXIS2_PLACEMENT_3D ( 'NONE', #230148, #256068, #236556 ) ;
#9911=CARTESIAN_POINT ( 'NONE',  ( -20.64999999999999858, 11.58468387039766512, -220.1227639117171861 ) ) ;
#9913=FACE_OUTER_BOUND ( 'NONE', #111900, .T. ) ;
#9948=LINE ( 'NONE', #68649, #151445 ) ;
#9988=DIRECTION ( 'NONE',  ( -0.000000000000000000, -0.9770955615653316162, -0.2128009952263604232 ) ) ;
#10002=VERTEX_POINT ( 'NONE', #138415 ) ;
#10011=CARTESIAN_POINT ( 'NONE',  ( -20.64999999999999858, -4.259020970815408091, -226.0869574510824123 ) ) ;
#10033=ORIENTED_EDGE ( 'NONE', *, *, #100506, .T. ) ;
#10042=ORIENTED_EDGE ( 'NONE', *, *, #174392, .T. ) ;
#10046=SPHERICAL_SURFACE ( 'NONE', #152878, 0.1000000000000000056 ) ;
#10055=CARTESIAN_POINT ( 'NONE',  ( 18.49999999999999645, 4.252251777740764460, -211.8999245327126744 ) ) ;
#10062=AXIS2_PLACEMENT_3D ( 'NONE', #145771, #3701, #87073 ) ;
#10089=DIRECTION ( 'NONE',  ( 0.000000000000000000, 0.2128009952263601179, -0.9770955615653315052 ) ) ;
#10116=CARTESIAN_POINT ( 'NONE',  ( 21.04999999999999716, 12.04127962393059548, -206.0806704050589246 ) ) ;
#10135=ORIENTED_EDGE ( 'NONE', *, *, #219774, .T. ) ;
#10175=ORIENTED_EDGE ( 'NONE', *, *, #185522, .F. ) ;
#10194=ORIENTED_EDGE ( 'NONE', *, *, #160872, .T. ) ;
#10221=VERTEX_POINT ( 'NONE', #207426 ) ;
#10222=EDGE_CURVE ( 'NONE', #74028, #30038, #204681, .T. ) ;
#10228=CARTESIAN_POINT ( 'NONE',  ( 18.59999999999999787, 7.567413955921498570, -241.6205176796878504 ) ) ;
#10245=ADVANCED_FACE ( 'NONE', ( #228267 ), #187867, .T. ) ;
#10248=VERTEX_POINT ( 'NONE', #70503 ) ;
#10254=DIRECTION ( 'NONE',  ( 0.000000000000000000, 0.2128009952263601456, -0.9770955615653316162 ) ) ;
#10261=CIRCLE ( 'NONE', #231029, 11.65000000000001457 ) ;
#10301=DIRECTION ( 'NONE',  ( 1.000000000000000000, 0.000000000000000000, 0.000000000000000000 ) ) ;
#10303=DIRECTION ( 'NONE',  ( -0.000000000000000000, -0.9770955615653316162, -0.2128009952263604232 ) ) ;
#10316=DIRECTION ( 'NONE',  ( 0.000000000000000000, -0.2128009952263604232, 0.9770955615653316162 ) ) ;
#10320=CARTESIAN_POINT ( 'NONE',  ( 23.15000000000000213, -4.756823075239758225, -233.1486023682345490 ) ) ;
#10331=ORIENTED_EDGE ( 'NONE', *, *, #149458, .F. ) ;
#10336=CARTESIAN_POINT ( 'NONE',  ( -22.39999999999999858, -2.479040261793999722, -189.6172560698084624 ) ) ;
#10338=CARTESIAN_POINT ( 'NONE',  ( -23.15000000000000213, -4.356730526971941408, -226.1082375506050539 ) ) ;
#10357=AXIS2_PLACEMENT_3D ( 'NONE', #110072, #113923, #53950 ) ;
#10360=CIRCLE ( 'NONE', #39593, 0.09999999999999939493 ) ;
#10368=CIRCLE ( 'NONE', #156128, 0.09999999999999939493 ) ;
#10460=CARTESIAN_POINT ( 'NONE',  ( 21.05000000000000071, 7.128833340094563376, -233.7327013124401276 ) ) ;
#10461=CARTESIAN_POINT ( 'NONE',  ( -23.25000000000000000, 8.882751598337867094, -187.0399955572217721 ) ) ;
#10467=ORIENTED_EDGE ( 'NONE', *, *, #101947, .F. ) ;
#10476=CARTESIAN_POINT ( 'NONE',  ( -20.85000000000000142, 7.128833340094563376, -233.7327013124401276 ) ) ;
#10493=ORIENTED_EDGE ( 'NONE', *, *, #117634, .F. ) ;
#10507=CARTESIAN_POINT ( 'NONE',  ( -20.64999999999999858, -4.161311414658873886, -226.0656773515597706 ) ) ;
#10521=CIRCLE ( 'NONE', #131299, 4.099999999999986322 ) ;
#10527=FACE_OUTER_BOUND ( 'NONE', #60589, .T. ) ;
#10559=CARTESIAN_POINT ( 'NONE',  ( -23.15000000000000213, 5.354661166737471056, -213.3684367965233832 ) ) ;
#10573=AXIS2_PLACEMENT_3D ( 'NONE', #124463, #149175, #170049 ) ;
#10583=CARTESIAN_POINT ( 'NONE',  ( 20.94999999999999929, 1.148907358139439339E-11, -201.0000000000015064 ) ) ;
#10600=CARTESIAN_POINT ( 'NONE',  ( 21.05000000000000071, -3.770473190032740174, -225.9805569534692324 ) ) ;
#10644=AXIS2_PLACEMENT_3D ( 'NONE', #107855, #44040, #205663 ) ;
#10663=CIRCLE ( 'NONE', #52326, 0.09999999999999942268 ) ;
#10678=EDGE_LOOP ( 'NONE', ( #225231, #146612, #68127, #21308 ) ) ;
#10682=CARTESIAN_POINT ( 'NONE',  ( 21.07933241753356768, 6.163820597116702160, -199.5620170604115344 ) ) ;
#10691=EDGE_LOOP ( 'NONE', ( #194173, #209080, #62755, #235627 ) ) ;
#10698=DIRECTION ( 'NONE',  ( 0.000000000000000000, 0.2128009952263609783, -0.9770955615653315052 ) ) ;
#10716=DIRECTION ( 'NONE',  ( 2.952720810173289605E-16, -0.9770955615653318382, -0.2128009952263588411 ) ) ;
#10778=ADVANCED_FACE ( 'NONE', ( #156145 ), #131406, .F. ) ;
#10827=CARTESIAN_POINT ( 'NONE',  ( -22.50000000000000000, 11.38316329224760359, -198.5208684056144079 ) ) ;
#10859=EDGE_CURVE ( 'NONE', #93645, #145277, #62152, .T. ) ;
#10861=DIRECTION ( 'NONE',  ( 0.000000000000000000, -0.07893460099012301889, 0.9968797965484754720 ) ) ;
#10867=DIRECTION ( 'NONE',  ( 0.000000000000000000, 0.2128009952263601456, -0.9770955615653316162 ) ) ;
#10877=ADVANCED_FACE ( 'NONE', ( #182102 ), #46817, .T. ) ;
#10890=CARTESIAN_POINT ( 'NONE',  ( 18.52165635395192211, -7.769097849577835113, -209.8815359301855494 ) ) ;
#10900=ORIENTED_EDGE ( 'NONE', *, *, #197435, .F. ) ;
#10907=VECTOR ( 'NONE', #76189, 1000.000000000000000 ) ;
#10917=FACE_OUTER_BOUND ( 'NONE', #55184, .T. ) ;
#10946=CARTESIAN_POINT ( 'NONE',  ( -20.94788355080264353, 18.36312997293286031, -236.9042258689303821 ) ) ;
#10950=CARTESIAN_POINT ( 'NONE',  ( -22.45354308602712123, -2.500503598582757281, -189.5187041294708479 ) ) ;
#10980=DIRECTION ( 'NONE',  ( 0.000000000000000000, -0.2128009952263604510, 0.9770955615653315052 ) ) ;
#11000=AXIS2_PLACEMENT_3D ( 'NONE', #206616, #164923, #145348 ) ;
#11024=CARTESIAN_POINT ( 'NONE',  ( -18.54159361262937722, -7.746324184985851069, -209.9014299668642138 ) ) ;
#11043=CIRCLE ( 'NONE', #98470, 0.1000000000000016293 ) ;
#11063=CIRCLE ( 'NONE', #215073, 0.1000000000000055844 ) ;
#11114=CARTESIAN_POINT ( 'NONE',  ( -1.739115166359751170E-14, 15.92646454033038594, -219.3818586450342707 ) ) ;
#11163=AXIS2_PLACEMENT_3D ( 'NONE', #236012, #57360, #237311 ) ;
#11214=AXIS2_PLACEMENT_3D ( 'NONE', #54172, #155880, #134975 ) ;
#11229=CIRCLE ( 'NONE', #23730, 0.1000000000000076938 ) ;
#11239=CARTESIAN_POINT ( 'NONE',  ( 21.05000000000000071, 6.256349259666485807, -229.7266095100222572 ) ) ;
#11248=AXIS2_PLACEMENT_3D ( 'NONE', #122677, #182646, #153826 ) ;
#11260=AXIS2_PLACEMENT_3D ( 'NONE', #192098, #211660, #33056 ) ;
#11263=CIRCLE ( 'NONE', #148651, 12.97500000000000320 ) ;
#11298=CARTESIAN_POINT ( 'NONE',  ( -23.25000000000000000, -13.88357498613435936, -191.9982587459959689 ) ) ;
#11309=ORIENTED_EDGE ( 'NONE', *, *, #60034, .T. ) ;
#11313=AXIS2_PLACEMENT_3D ( 'NONE', #55480, #97162, #213298 ) ;
#11436=DIRECTION ( 'NONE',  ( 0.000000000000000000, 0.2128009952263485993, -0.9770955615653341697 ) ) ;
#11472=CARTESIAN_POINT ( 'NONE',  ( 20.94403535211772294, 18.37039103902859694, -236.9176190769588857 ) ) ;
#11478=CARTESIAN_POINT ( 'NONE',  ( 20.94999999999999929, 9.374458193048763377, -220.5475659691911119 ) ) ;
#11523=DIRECTION ( 'NONE',  ( 0.000000000000000000, 0.2128009952263403282, -0.9770955615653358350 ) ) ;
#11527=CARTESIAN_POINT ( 'NONE',  ( 18.59999999999999076, 15.53922597307775000, -223.0482397989536025 ) ) ;
#11532=ORIENTED_EDGE ( 'NONE', *, *, #21790, .F. ) ;
#11542=CARTESIAN_POINT ( 'NONE',  ( -21.05000000000000071, -10.74476030654554393, -206.4104182790846096 ) ) ;
#11550=DIRECTION ( 'NONE',  ( 1.000000000000000000, -0.000000000000000000, -0.000000000000000000 ) ) ;
#11585=CARTESIAN_POINT ( 'NONE',  ( -20.54999999999999716, 11.48697431424113446, -220.1440440112397994 ) ) ;
#11589=CARTESIAN_POINT ( 'NONE',  ( 18.36493879433278309, -0.6805351584761402117, -242.5179116711672407 ) ) ;
#11595=VECTOR ( 'NONE', #22016, 1000.000000000000000 ) ;
#11634=DIRECTION ( 'NONE',  ( -1.000000000000000000, 0.000000000000000000, -0.000000000000000000 ) ) ;
#11675=AXIS2_PLACEMENT_3D ( 'NONE', #226330, #88098, #163827 ) ;
#11694=CARTESIAN_POINT ( 'NONE',  ( -18.59999999999999787, 1.148907358139439339E-11, -201.0000000000015064 ) ) ;
#11716=EDGE_CURVE ( 'NONE', #63679, #222677, #5666, .T. ) ;
#11754=DIRECTION ( 'NONE',  ( 1.000000000000000000, 1.832422279913646096E-16, 3.990820347355631841E-17 ) ) ;
#11758=DIRECTION ( 'NONE',  ( -0.000000000000000000, 0.2128009952263603677, -0.9770955615653313941 ) ) ;
#11759=FACE_OUTER_BOUND ( 'NONE', #147428, .T. ) ;
#11760=CARTESIAN_POINT ( 'NONE',  ( -21.05000000000000071, -1.236118717437888259, -194.8647072476926212 ) ) ;
#11782=ADVANCED_FACE ( 'NONE', ( #209712 ), #7669, .T. ) ;
#11835=EDGE_LOOP ( 'NONE', ( #100292, #96571, #66921, #137758, #190948 ) ) ;
#11851=CARTESIAN_POINT ( 'NONE',  ( -20.54999999999999716, 9.614325556249161409, -211.5456030694648746 ) ) ;
#11855=EDGE_CURVE ( 'NONE', #24047, #241077, #63962, .T. ) ;
#11885=AXIS2_PLACEMENT_3D ( 'NONE', #109948, #13437, #12169 ) ;
#11889=VERTEX_POINT ( 'NONE', #171903 ) ;
#11938=CIRCLE ( 'NONE', #57692, 0.1000000000000055844 ) ;
#11954=AXIS2_PLACEMENT_3D ( 'NONE', #255715, #38030, #60115 ) ;
#11963=CARTESIAN_POINT ( 'NONE',  ( 21.56666275994539816, -1.480534921131848591, -194.2019862094512064 ) ) ;
#11964=CARTESIAN_POINT ( 'NONE',  ( -20.64999999999999858, 7.128833340094563376, -233.7327013124401276 ) ) ;
#11969=AXIS2_PLACEMENT_3D ( 'NONE', #11851, #232177, #151358 ) ;
#11974=EDGE_CURVE ( 'NONE', #16838, #54351, #180489, .T. ) ;
#12026=CARTESIAN_POINT ( 'NONE',  ( -23.15000000000000213, 6.268811756569107274, -220.3853799378769622 ) ) ;
#12037=CARTESIAN_POINT ( 'NONE',  ( -23.25000000000000000, 7.128833340094563376, -233.7327013124401276 ) ) ;
#12038=CARTESIAN_POINT ( 'NONE',  ( -23.25000000000000000, 7.128833340094563376, -233.7327013124401276 ) ) ;
#12042=LINE ( 'NONE', #91557, #13207 ) ;
#12095=CARTESIAN_POINT ( 'NONE',  ( 20.94999999999999929, 7.128833340094563376, -233.7327013124401276 ) ) ;
#12101=PLANE ( 'NONE',  #4357 ) ;
#12125=AXIS2_PLACEMENT_3D ( 'NONE', #246292, #67644, #10254 ) ;
#12127=EDGE_CURVE ( 'NONE', #146487, #130685, #182140, .T. ) ;
#12167=ADVANCED_FACE ( 'NONE', ( #225081 ), #4748, .F. ) ;
#12169=DIRECTION ( 'NONE',  ( 0.000000000000000000, 0.2128009952263603122, -0.9770955615653315052 ) ) ;
#12189=ADVANCED_FACE ( 'NONE', ( #29513 ), #49034, .T. ) ;
#12225=LINE ( 'NONE', #130860, #239602 ) ;
#12232=AXIS2_PLACEMENT_3D ( 'NONE', #47761, #28257, #107752 ) ;
#12241=CARTESIAN_POINT ( 'NONE',  ( -20.92356734117541706, 18.39335631088232503, -236.9600537807593241 ) ) ;
#12247=AXIS2_PLACEMENT_3D ( 'NONE', #206994, #49194, #230404 ) ;
#12270=EDGE_LOOP ( 'NONE', ( #166422, #21867, #81165, #114694 ) ) ;
#12320=LINE ( 'NONE', #33187, #37003 ) ;
#12332=EDGE_LOOP ( 'NONE', ( #75777, #98915, #15644, #228792 ) ) ;
#12333=CARTESIAN_POINT ( 'NONE',  ( -18.52186455168988388, -7.768930579343111376, -209.8816825891055373 ) ) ;
#12350=CIRCLE ( 'NONE', #95523, 11.80000000000001670 ) ;
#12351=ORIENTED_EDGE ( 'NONE', *, *, #13041, .F. ) ;
#12366=LINE ( 'NONE', #7182, #31856 ) ;
#12370=DIRECTION ( 'NONE',  ( 0.000000000000000000, 0.2128009952263611726, -0.9770955615653312831 ) ) ;
#12376=EDGE_CURVE ( 'NONE', #126912, #231604, #141407, .T. ) ;
#12402=B_SPLINE_CURVE_WITH_KNOTS ( 'NONE', 3,
 ( #129198, #148767, #104460, #164473, #49648, #105740, #206160, #208744 ),
 .UNSPECIFIED., .F., .F.,
 ( 4, 2, 2, 4 ),
 ( 0.000000000000000000, 0.0001306511400391696253, 0.0001959767100587203668, 0.0002613022800782711084 ),
 .UNSPECIFIED. ) ;
#12407=CARTESIAN_POINT ( 'NONE',  ( 21.05000000000000071, 10.47809638650343622, -198.7179823275938020 ) ) ;
#12419=EDGE_CURVE ( 'NONE', #131400, #75618, #68243, .T. ) ;
#12444=DIRECTION ( 'NONE',  ( 0.000000000000000000, 0.9770955615653559301, 0.2128009952262481796 ) ) ;
#12456=CIRCLE ( 'NONE', #208265, 0.1999999999999884925 ) ;
#12478=DIRECTION ( 'NONE',  ( 1.000000000000000000, 1.794895427898102820E-16, 3.909090864890033875E-17 ) ) ;
#12510=EDGE_CURVE ( 'NONE', #365, #19404, #164299, .T. ) ;
#12541=DIRECTION ( 'NONE',  ( 0.000000000000000000, -0.2128009952263485993, 0.9770955615653341697 ) ) ;
#12567=CARTESIAN_POINT ( 'NONE',  ( 20.04142135623730070, 15.90518444080776383, -219.2841490888777116 ) ) ;
#12570=AXIS2_PLACEMENT_3D ( 'NONE', #152218, #231737, #153523 ) ;
#12577=CARTESIAN_POINT ( 'NONE',  ( -20.64999999999999858, 9.690755012883057518, -211.4266134137857023 ) ) ;
#12583=CARTESIAN_POINT ( 'NONE',  ( -21.44999999999999929, 11.68239342655420110, -220.1014838121945161 ) ) ;
#12614=DIRECTION ( 'NONE',  ( -0.000000000000000000, 0.08413937888703756918, -0.9964539953858901900 ) ) ;
#12638=CARTESIAN_POINT ( 'NONE',  ( 18.49999999999999289, 8.433899723187009201, -209.4150263691077782 ) ) ;
#12641=ORIENTED_EDGE ( 'NONE', *, *, #60307, .T. ) ;
#12670=FACE_OUTER_BOUND ( 'NONE', #169729, .T. ) ;
#12712=EDGE_LOOP ( 'NONE', ( #54838, #188745, #160254, #179121 ) ) ;
#12721=CARTESIAN_POINT ( 'NONE',  ( 18.49999999999996803, 14.83511725869332132, -235.8887435844146978 ) ) ;
#12730=AXIS2_PLACEMENT_3D ( 'NONE', #214761, #210920, #36150 ) ;
#12733=DIRECTION ( 'NONE',  ( 0.000000000000000000, -0.2128009952263604232, 0.9770955615653316162 ) ) ;
#12790=DIRECTION ( 'NONE',  ( -1.000000000000000000, -2.885090398161910739E-16, -6.283419270304611573E-17 ) ) ;
#12834=CARTESIAN_POINT ( 'NONE',  ( 20.94999999999999929, -4.254329952141541860, -236.2118329068272260 ) ) ;
#12853=AXIS2_PLACEMENT_3D ( 'NONE', #139184, #222573, #177083 ) ;
#12887=LINE ( 'NONE', #115812, #106862 ) ;
#12901=ADVANCED_FACE ( 'NONE', ( #160708 ), #216785, .T. ) ;
#12907=ADVANCED_FACE ( 'NONE', ( #197229 ), #36917, .F. ) ;
#12914=EDGE_CURVE ( 'NONE', #48943, #73041, #172140, .T. ) ;
#12959=EDGE_CURVE ( 'NONE', #142529, #16905, #27618, .T. ) ;
#13026=SPHERICAL_SURFACE ( 'NONE', #251690, 0.1000000000000000056 ) ;
#13041=EDGE_CURVE ( 'NONE', #246033, #1104, #43100, .T. ) ;
#13066=EDGE_LOOP ( 'NONE', ( #3740, #247955, #119586, #220087 ) ) ;
#13094=CARTESIAN_POINT ( 'NONE',  ( 21.00000000000000000, 14.02742277431099538, -219.5907614236512870 ) ) ;
#13114=CARTESIAN_POINT ( 'NONE',  ( 22.48660254037843842, 11.37252324248628632, -198.4720136275361710 ) ) ;
#13133=CARTESIAN_POINT ( 'NONE',  ( 22.49066049874202022, -2.424081457535128159, -189.6048348505414083 ) ) ;
#13135=CARTESIAN_POINT ( 'NONE',  ( -23.15000000000000213, 7.128833340094563376, -233.7327013124401276 ) ) ;
#13137=DIRECTION ( 'NONE',  ( 1.000000000000000000, 0.000000000000000000, 0.000000000000000000 ) ) ;
#13139=DIRECTION ( 'NONE',  ( 0.000000000000000000, -0.9770955615653316162, -0.2128009952263604232 ) ) ;
#13151=VECTOR ( 'NONE', #45502, 1000.000000000000000 ) ;
#13155=ORIENTED_EDGE ( 'NONE', *, *, #223882, .F. ) ;
#13169=CARTESIAN_POINT ( 'NONE',  ( 23.24999999999999289, 10.99842653345846699, -220.2504445088529792 ) ) ;
#13175=DIRECTION ( 'NONE',  ( -2.840903330521632269E-16, 0.9550021345545507412, -0.2965989261549202838 ) ) ;
#13177=ORIENTED_EDGE ( 'NONE', *, *, #235593, .F. ) ;
#13207=VECTOR ( 'NONE', #248058, 1000.000000000000000 ) ;
#13234=CARTESIAN_POINT ( 'NONE',  ( 20.94999999999999574, 14.83422855357708414, -203.3235740904736417 ) ) ;
#13255=CARTESIAN_POINT ( 'NONE',  ( 21.07971444708685738, 6.166122833947518700, -199.5672020556278028 ) ) ;
#13270=DIRECTION ( 'NONE',  ( 0.000000000000000000, -0.2128009952263485993, 0.9770955615653341697 ) ) ;
#13287=DIRECTION ( 'NONE',  ( 0.000000000000000000, -0.9550021345545530727, 0.2965989261549131228 ) ) ;
#13288=CARTESIAN_POINT ( 'NONE',  ( 18.57399277249656322, 18.41291479239798790, -236.9963116028434058 ) ) ;
#13314=EDGE_CURVE ( 'NONE', #136330, #46709, #9948, .T. ) ;
#13336=ORIENTED_EDGE ( 'NONE', *, *, #126090, .T. ) ;
#13347=VERTEX_POINT ( 'NONE', #107760 ) ;
#13366=CARTESIAN_POINT ( 'NONE',  ( -18.59999999999999787, 14.83511725869332132, -235.8887435844146978 ) ) ;
#13402=CARTESIAN_POINT ( 'NONE',  ( 18.60000000000000142, -7.567701079425715349, -210.0537230116848946 ) ) ;
#13409=CARTESIAN_POINT ( 'NONE',  ( 21.09096482362019387, 6.209396322289256531, -199.6072866877750300 ) ) ;
#13437=DIRECTION ( 'NONE',  ( 1.000000000000000000, 0.000000000000000000, 0.000000000000000000 ) ) ;
#13448=CARTESIAN_POINT ( 'NONE',  ( -18.58735405345342784, -0.7666499927750894949, -242.4349016823527734 ) ) ;
#13466=AXIS2_PLACEMENT_3D ( 'NONE', #246637, #27642, #83679 ) ;
#13470=ADVANCED_FACE ( 'NONE', ( #210718 ), #59819, .T. ) ;
#13493=DIRECTION ( 'NONE',  ( 1.000000000000000000, 0.000000000000000000, 0.000000000000000000 ) ) ;
#13515=CARTESIAN_POINT ( 'NONE',  ( -22.45437739390954590, -2.479040262656531546, -189.6172560658480677 ) ) ;
#13564=CARTESIAN_POINT ( 'NONE',  ( 20.94999999999999929, 7.128833340094563376, -233.7327013124401276 ) ) ;
#13598=EDGE_LOOP ( 'NONE', ( #125478, #242850, #227325, #52218 ) ) ;
#13601=CARTESIAN_POINT ( 'NONE',  ( -18.47079683080344026, -7.741948359812542257, -209.9616156304373931 ) ) ;
#13613=ORIENTED_EDGE ( 'NONE', *, *, #39357, .T. ) ;
#13618=EDGE_CURVE ( 'NONE', #125420, #132220, #15963, .T. ) ;
#13646=FACE_OUTER_BOUND ( 'NONE', #243621, .T. ) ;
#13675=LINE ( 'NONE', #227586, #248432 ) ;
#13764=CARTESIAN_POINT ( 'NONE',  ( 18.42636655943170609, -0.7441698762049262506, -242.2113638065491728 ) ) ;
#13768=DIRECTION ( 'NONE',  ( 0.000000000000000000, 0.2128009952264354188, -0.9770955615653151849 ) ) ;
#13780=CARTESIAN_POINT ( 'NONE',  ( 20.99999999999997868, 1.148907358139439339E-11, -201.0000000000015064 ) ) ;
#13812=CIRCLE ( 'NONE', #242941, 0.1000000000000027534 ) ;
#13851=VECTOR ( 'NONE', #65101, 1000.000000000000000 ) ;
#13894=ORIENTED_EDGE ( 'NONE', *, *, #25148, .F. ) ;
#13903=ORIENTED_EDGE ( 'NONE', *, *, #44385, .F. ) ;
#13904=CARTESIAN_POINT ( 'NONE',  ( 23.15000000000000213, -4.735542975717121905, -233.2463119243910796 ) ) ;
#13931=EDGE_CURVE ( 'NONE', #168616, #129923, #101685, .T. ) ;
#13934=VERTEX_POINT ( 'NONE', #80818 ) ;
#13937=DIRECTION ( 'NONE',  ( -1.000000000000000000, 0.000000000000000000, 0.000000000000000000 ) ) ;
#13941=DIRECTION ( 'NONE',  ( -2.915501640297154283E-16, 0.9770955615653317272, 0.2128009952263596460 ) ) ;
#14021=EDGE_CURVE ( 'NONE', #98769, #89222, #87239, .T. ) ;
#14036=AXIS2_PLACEMENT_3D ( 'NONE', #160201, #98879, #251884 ) ;
#14040=CARTESIAN_POINT ( 'NONE',  ( 20.89878130938411616, 18.40663661316795441, -236.9846611508999388 ) ) ;
#14114=DIRECTION ( 'NONE',  ( 1.000000000000000000, 0.000000000000000000, 0.000000000000000000 ) ) ;
#14134=EDGE_CURVE ( 'NONE', #37415, #232829, #85303, .T. ) ;
#14143=CARTESIAN_POINT ( 'NONE',  ( 21.05000000000000426, 6.285166956194035315, -199.7189084715529361 ) ) ;
#14184=FACE_OUTER_BOUND ( 'NONE', #240436, .T. ) ;
#14192=CARTESIAN_POINT ( 'NONE',  ( -18.59999999999999787, 6.266619843005246437, -211.3861694115776402 ) ) ;
#14234=CARTESIAN_POINT ( 'NONE',  ( -23.15000000000000213, -4.756823075239758225, -233.1486023682345490 ) ) ;
#14236=DIRECTION ( 'NONE',  ( 1.000000000000000000, 0.000000000000000000, 0.000000000000000000 ) ) ;
#14259=AXIS2_PLACEMENT_3D ( 'NONE', #1953, #5802, #222272 ) ;
#14280=DIRECTION ( 'NONE',  ( 0.000000000000000000, 0.2128009952263587856, -0.9770955615653318382 ) ) ;
#14295=VERTEX_POINT ( 'NONE', #15443 ) ;
#14314=ORIENTED_EDGE ( 'NONE', *, *, #225104, .T. ) ;
#14331=CARTESIAN_POINT ( 'NONE',  ( 19.97071067811864609, 15.99555563007541004, -219.3668113423574653 ) ) ;
#14338=CIRCLE ( 'NONE', #222563, 0.1000000000000001305 ) ;
#14349=EDGE_CURVE ( 'NONE', #217380, #167762, #72712, .T. ) ;
#14408=DIRECTION ( 'NONE',  ( 0.000000000000000000, 0.2128009952263650861, -0.9770955615653305060 ) ) ;
#14413=SHAPE_DEFINITION_REPRESENTATION ( #109742, #53611 ) ;
#14417=CARTESIAN_POINT ( 'NONE',  ( 22.59999954896768770, -2.509145966787972526, -189.5205087850422956 ) ) ;
#14445=ADVANCED_FACE ( 'NONE', ( #221301 ), #85623, .F. ) ;
#14452=ORIENTED_EDGE ( 'NONE', *, *, #201907, .T. ) ;
#14461=AXIS2_PLACEMENT_3D ( 'NONE', #84041, #87921, #26715 ) ;
#14479=EDGE_LOOP ( 'NONE', ( #254199, #155879, #118725, #222268 ) ) ;
#14516=VERTEX_POINT ( 'NONE', #187350 ) ;
#14526=DIRECTION ( 'NONE',  ( -0.000000000000000000, 0.9770955615653313941, 0.2128009952263603954 ) ) ;
#14529=VECTOR ( 'NONE', #148793, 1000.000000000000227 ) ;
#14532=EDGE_LOOP ( 'NONE', ( #14452, #55263, #55021, #5058 ) ) ;
#14539=VECTOR ( 'NONE', #189980, 1000.000000000000000 ) ;
#14552=AXIS2_PLACEMENT_3D ( 'NONE', #4190, #81151, #2899 ) ;
#14591=CARTESIAN_POINT ( 'NONE',  ( 18.50016250449482413, 18.35558276679035572, -236.8903279188155864 ) ) ;
#14652=ORIENTED_EDGE ( 'NONE', *, *, #248556, .F. ) ;
#14654=AXIS2_PLACEMENT_3D ( 'NONE', #122623, #242540, #5187 ) ;
#14699=FILL_AREA_STYLE_COLOUR ( '', #15089 ) ;
#14726=CARTESIAN_POINT ( 'NONE',  ( -21.05000000000000071, 2.953700692300310848, -208.6327728934509764 ) ) ;
#14730=EDGE_LOOP ( 'NONE', ( #769, #143049, #150264 ) ) ;
#14758=DIRECTION ( 'NONE',  ( 1.000000000000000000, 0.000000000000000000, 0.000000000000000000 ) ) ;
#14778=CIRCLE ( 'NONE', #110410, 0.8750000000000007772 ) ;
#14815=ORIENTED_EDGE ( 'NONE', *, *, #39161, .T. ) ;
#14852=CYLINDRICAL_SURFACE ( 'NONE', #160291, 0.1000000000000013656 ) ;
#14860=DIRECTION ( 'NONE',  ( 0.000000000000000000, -0.2128009952263403282, 0.9770955615653358350 ) ) ;
#14866=VERTEX_POINT ( 'NONE', #230991 ) ;
#14885=EDGE_LOOP ( 'NONE', ( #240958, #256390, #132223, #26538 ) ) ;
#14902=CARTESIAN_POINT ( 'NONE',  ( -22.50000000000000000, 11.36146383068193444, -198.4232501820394816 ) ) ;
#14943=DIRECTION ( 'NONE',  ( 0.000000000000000000, 0.2128009952263604232, -0.9770955615653316162 ) ) ;
#14944=SPHERICAL_SURFACE ( 'NONE', #220378, 0.1000000000000000056 ) ;
#14956=AXIS2_PLACEMENT_3D ( 'NONE', #173550, #52243, #17006 ) ;
#14960=LINE ( 'NONE', #174061, #91767 ) ;
#14998=DIRECTION ( 'NONE',  ( 1.000000000000000000, -7.136802563874200093E-16, -1.554319503706925554E-16 ) ) ;
#15021=CARTESIAN_POINT ( 'NONE',  ( -18.59999994787167310, -0.7120786659332111190, -242.4841517841200869 ) ) ;
#15089=COLOUR_RGB ( '', 0.09019608, 0.27058824, 0.51372549) ;
#15097=CARTESIAN_POINT ( 'NONE',  ( 20.95512820512820440, 11.25838014693915845, -210.9828572391343755 ) ) ;
#15116=CARTESIAN_POINT ( 'NONE',  ( -23.25000000000000000, 1.148907358139439339E-11, -201.0000000000015064 ) ) ;
#15129=LINE ( 'NONE', #196315, #188778 ) ;
#15151=CARTESIAN_POINT ( 'NONE',  ( 23.14999999999999503, 17.01923898301590654, -224.3994341343041867 ) ) ;
#15153=LINE ( 'NONE', #10011, #29772 ) ;
#15166=EDGE_LOOP ( 'NONE', ( #157242, #105619, #201458, #169047 ) ) ;
#15191=CARTESIAN_POINT ( 'NONE',  ( 22.00356870143462373, 7.088088014901702927, -199.4562900056679382 ) ) ;
#15194=EDGE_LOOP ( 'NONE', ( #229468, #95873, #98961, #151637 ) ) ;
#15204=ADVANCED_FACE ( 'NONE', ( #71611 ), #35830, .T. ) ;
#15215=AXIS2_PLACEMENT_3D ( 'NONE', #37426, #40012, #214754 ) ;
#15234=CARTESIAN_POINT ( 'NONE',  ( -23.25000000000000000, -4.914013037343267776, -233.1828366659746905 ) ) ;
#15254=ORIENTED_EDGE ( 'NONE', *, *, #208907, .F. ) ;
#15260=FACE_OUTER_BOUND ( 'NONE', #88619, .T. ) ;
#15264=DIRECTION ( 'NONE',  ( 0.000000000000000000, 0.2211802418851293583, -0.9752329468386697897 ) ) ;
#15279=CARTESIAN_POINT ( 'NONE',  ( -18.59999999999999787, 14.80545736607782814, -235.9842437978701639 ) ) ;
#15320=AXIS2_PLACEMENT_3D ( 'NONE', #21366, #138679, #180421 ) ;
#15342=CARTESIAN_POINT ( 'NONE',  ( -21.05000000000000071, 6.093673009692400555, -199.5727803633481301 ) ) ;
#15345=DIRECTION ( 'NONE',  ( 1.000000000000000000, 0.000000000000000000, 0.000000000000000000 ) ) ;
#15368=AXIS2_PLACEMENT_3D ( 'NONE', #69119, #30002, #112098 ) ;
#15379=DIRECTION ( 'NONE',  ( 0.7070776581708964059, -0.1504792239192832004, 0.6909393522475117955 ) ) ;
#15413=EDGE_CURVE ( 'NONE', #3257, #118478, #23379, .T. ) ;
#15427=CARTESIAN_POINT ( 'NONE',  ( -18.59999999999999787, 0.5663372425336981042, -209.0641885820623997 ) ) ;
#15443=CARTESIAN_POINT ( 'NONE',  ( -20.00857864376270001, 13.53887499352833146, -219.6971619212644669 ) ) ;
#15456=CARTESIAN_POINT ( 'NONE',  ( -23.15000000000000213, -6.688413578037177842, -212.5825622730469036 ) ) ;
#15489=AXIS2_PLACEMENT_3D ( 'NONE', #177360, #193048, #96477 ) ;
#15491=CARTESIAN_POINT ( 'NONE',  ( -23.15000000000000213, 8.793666940903476004, -220.9353059101866847 ) ) ;
#15500=SPHERICAL_SURFACE ( 'NONE', #217921, 0.1000000000000000056 ) ;
#15538=DIRECTION ( 'NONE',  ( 0.7071067811865475727, 0.6909108974501237954, 0.1504730267678056066 ) ) ;
#15568=AXIS2_PLACEMENT_3D ( 'NONE', #98911, #218875, #162788 ) ;
#15573=CYLINDRICAL_SURFACE ( 'NONE', #15368, 0.1000000000000055844 ) ;
#15588=FACE_OUTER_BOUND ( 'NONE', #256301, .T. ) ;
#15589=DIRECTION ( 'NONE',  ( 0.000000000000000000, 0.2128009952263604232, -0.9770955615653316162 ) ) ;
#15610=EDGE_LOOP ( 'NONE', ( #226684, #234267, #208657, #16189 ) ) ;
#15612=DIRECTION ( 'NONE',  ( 0.000000000000000000, -0.9964539953858893018, -0.08413937888704772772 ) ) ;
#15642=CARTESIAN_POINT ( 'NONE',  ( -20.85000000000000142, 7.654382455240002159, -241.6162809886059790 ) ) ;
#15644=ORIENTED_EDGE ( 'NONE', *, *, #141080, .F. ) ;
#15677=ORIENTED_EDGE ( 'NONE', *, *, #92021, .F. ) ;
#15692=AXIS2_PLACEMENT_3D ( 'NONE', #212704, #56166, #34095 ) ;
#15720=CARTESIAN_POINT ( 'NONE',  ( 21.05000000000000071, -1.476250985535760840, -194.6915786084529145 ) ) ;
#15733=CIRCLE ( 'NONE', #32486, 0.09999999999999939493 ) ;
#15742=AXIS2_PLACEMENT_3D ( 'NONE', #125632, #47358, #64381 ) ;
#15753=VERTEX_POINT ( 'NONE', #55520 ) ;
#15761=FACE_OUTER_BOUND ( 'NONE', #199988, .T. ) ;
#15769=CARTESIAN_POINT ( 'NONE',  ( 23.24999999999999645, 7.128833340094563376, -233.7327013124401276 ) ) ;
#15792=ORIENTED_EDGE ( 'NONE', *, *, #220093, .T. ) ;
#15808=CARTESIAN_POINT ( 'NONE',  ( -20.54999999999999716, 9.690755012883057518, -211.4266134137857023 ) ) ;
#15813=CIRCLE ( 'NONE', #53370, 0.09999999999999939493 ) ;
#15833=CARTESIAN_POINT ( 'NONE',  ( 20.95462737510932882, 11.92587769522588559, -206.1500708958423047 ) ) ;
#15839=AXIS2_PLACEMENT_3D ( 'NONE', #136226, #152004, #33352 ) ;
#15864=ORIENTED_EDGE ( 'NONE', *, *, #89846, .F. ) ;
#15867=DIRECTION ( 'NONE',  ( 0.000000000000000000, 0.2128009952263568427, -0.9770955615653322823 ) ) ;
#15873=DIRECTION ( 'NONE',  ( 1.000000000000000000, 0.000000000000000000, 0.000000000000000000 ) ) ;
#15876=ORIENTED_EDGE ( 'NONE', *, *, #222511, .T. ) ;
#15880=CARTESIAN_POINT ( 'NONE',  ( 18.51697539158856998, 18.38637412622488299, -236.9471295141160283 ) ) ;
#15901=ORIENTED_EDGE ( 'NONE', *, *, #130987, .F. ) ;
#15917=DIRECTION ( 'NONE',  ( -1.000000000000000000, 0.000000000000000000, 0.000000000000000000 ) ) ;
#15946=FACE_OUTER_BOUND ( 'NONE', #94023, .T. ) ;
#15963=LINE ( 'NONE', #32973, #126668 ) ;
#15980=EDGE_CURVE ( 'NONE', #234078, #192351, #48832, .T. ) ;
#15982=ORIENTED_EDGE ( 'NONE', *, *, #81253, .T. ) ;
#15994=CARTESIAN_POINT ( 'NONE',  ( 21.14999999999999858, 6.390846877240202950, -199.6081416912452653 ) ) ;
#16015=DIRECTION ( 'NONE',  ( 1.000000000000000000, 0.000000000000000000, 0.000000000000000000 ) ) ;
#16022=AXIS2_PLACEMENT_3D ( 'NONE', #141028, #81020, #220557 ) ;
#16030=ORIENTED_EDGE ( 'NONE', *, *, #51186, .T. ) ;
#16045=CARTESIAN_POINT ( 'NONE',  ( 23.24999999999999645, 7.128833340094563376, -233.7327013124401276 ) ) ;
#16056=( GEOMETRIC_REPRESENTATION_CONTEXT ( 3 ) GLOBAL_UNCERTAINTY_ASSIGNED_CONTEXT ( ( #80551 ) ) GLOBAL_UNIT_ASSIGNED_CONTEXT ( ( #66681, #142349, #6694 ) ) REPRESENTATION_CONTEXT ( 'NONE', 'WORKASPACE' ) );
#16059=CIRCLE ( 'NONE', #182633, 4.050000000000000711 ) ;
#16065=CARTESIAN_POINT ( 'NONE',  ( -22.37643362114956602, -1.525963729632202837, -193.5277898285476397 ) ) ;
#16067=FACE_OUTER_BOUND ( 'NONE', #36833, .T. ) ;
#16082=CARTESIAN_POINT ( 'NONE',  ( 20.94999999999999929, 9.374458193048763377, -220.5475659691911119 ) ) ;
#16118=CARTESIAN_POINT ( 'NONE',  ( -23.25000000000000000, 15.90518444080776028, -219.2841490888777116 ) ) ;
#16128=ADVANCED_FACE ( 'NONE', ( #93091 ), #165370, .T. ) ;
#16150=CARTESIAN_POINT ( 'NONE',  ( -23.15000000000000213, -4.914013037343267776, -233.1828366659746905 ) ) ;
#16168=VECTOR ( 'NONE', #8521, 1000.000000000000227 ) ;
#16178=DIRECTION ( 'NONE',  ( 1.000000000000000000, 0.000000000000000000, 0.000000000000000000 ) ) ;
#16187=AXIS2_PLACEMENT_3D ( 'NONE', #22474, #101953, #94589 ) ;
#16189=ORIENTED_EDGE ( 'NONE', *, *, #54521, .F. ) ;
#16199=EDGE_CURVE ( 'NONE', #210485, #195345, #111375, .T. ) ;
#16205=AXIS2_PLACEMENT_3D ( 'NONE', #5073, #101599, #126336 ) ;
#16260=LINE ( 'NONE', #71088, #10907 ) ;
#16262=DIRECTION ( 'NONE',  ( 0.000000000000000000, -0.2128009952263403282, 0.9770955615653358350 ) ) ;
#16321=DIRECTION ( 'NONE',  ( -1.000000000000000000, -0.000000000000000000, -0.000000000000000000 ) ) ;
#16334=DIRECTION ( 'NONE',  ( 0.000000000000000000, 0.2128009952263605342, -0.9770955615653315052 ) ) ;
#16340=EDGE_CURVE ( 'NONE', #135756, #76729, #148938, .T. ) ;
#16341=VECTOR ( 'NONE', #97586, 999.9999999999998863 ) ;
#16349=ORIENTED_EDGE ( 'NONE', *, *, #155894, .T. ) ;
#16356=CARTESIAN_POINT ( 'NONE',  ( 21.05000000000000071, 2.859758780633683273, -208.6670499591424459 ) ) ;
#16372=LINE ( 'NONE', #215809, #94830 ) ;
#16392=EDGE_CURVE ( 'NONE', #123238, #85747, #244640, .T. ) ;
#16420=DIRECTION ( 'NONE',  ( -1.000000000000000000, 0.000000000000000000, 0.000000000000000000 ) ) ;
#16434=DIRECTION ( 'NONE',  ( 1.000000000000000000, 0.000000000000000000, 0.000000000000000000 ) ) ;
#16447=CARTESIAN_POINT ( 'NONE',  ( -22.47007471830798764, -1.642974910573230973, -193.4561278898739545 ) ) ;
#16456=DIRECTION ( 'NONE',  ( 1.000000000000000000, 0.000000000000000000, 0.000000000000000000 ) ) ;
#16457=ADVANCED_FACE ( 'NONE', ( #19360 ), #61035, .F. ) ;
#16478=FACE_OUTER_BOUND ( 'NONE', #41857, .T. ) ;
#16496=LINE ( 'NONE', #76438, #239223 ) ;
#16531=DIRECTION ( 'NONE',  ( 1.000000000000000000, 0.000000000000000000, 0.000000000000000000 ) ) ;
#16532=DIRECTION ( 'NONE',  ( 1.000000000000000000, 0.000000000000000000, 0.000000000000000000 ) ) ;
#16542=ORIENTED_EDGE ( 'NONE', *, *, #77576, .F. ) ;
#16592=CARTESIAN_POINT ( 'NONE',  ( 21.05000000000000071, 7.872214528623318053, -209.6555322433423783 ) ) ;
#16614=CARTESIAN_POINT ( 'NONE',  ( -18.50000000000000000, 13.56015509305096778, -219.7948714774209691 ) ) ;
#16627=TOROIDAL_SURFACE ( 'NONE', #199967, 0.6000000000000009770, 0.1000000000000000056 ) ;
#16644=CARTESIAN_POINT ( 'NONE',  ( -18.50000000000000000, 13.98997548377051459, -210.4902890347897255 ) ) ;
#16646=AXIS2_PLACEMENT_3D ( 'NONE', #138683, #14943, #34515 ) ;
#16667=CARTESIAN_POINT ( 'NONE',  ( 21.05000000000000071, 11.16079915604378492, -211.0041093385139561 ) ) ;
#16683=VECTOR ( 'NONE', #142575, 1000.000000000000227 ) ;
#16731=EDGE_CURVE ( 'NONE', #183349, #227433, #240561, .T. ) ;
#16735=AXIS2_PLACEMENT_3D ( 'NONE', #198099, #254203, #156448 ) ;
#16739=DIRECTION ( 'NONE',  ( 1.000000000000000000, 0.000000000000000000, 0.000000000000000000 ) ) ;
#16749=EDGE_CURVE ( 'NONE', #123238, #75618, #58149, .T. ) ;
#16779=AXIS2_PLACEMENT_3D ( 'NONE', #60182, #177608, #200993 ) ;
#16808=CARTESIAN_POINT ( 'NONE',  ( 22.39999999999999503, 11.45959274888149970, -198.4018787499352641 ) ) ;
#16824=FACE_OUTER_BOUND ( 'NONE', #112413, .T. ) ;
#16838=VERTEX_POINT ( 'NONE', #176859 ) ;
#16847=ORIENTED_EDGE ( 'NONE', *, *, #90244, .T. ) ;
#16905=VERTEX_POINT ( 'NONE', #240660 ) ;
#16906=VERTEX_POINT ( 'NONE', #145403 ) ;
#16910=DIRECTION ( 'NONE',  ( 0.000000000000000000, 0.9770955615653548199, 0.2128009952262535920 ) ) ;
#16934=ORIENTED_EDGE ( 'NONE', *, *, #180729, .T. ) ;
#16936=EDGE_CURVE ( 'NONE', #71912, #176927, #257248, .T. ) ;
#16951=AXIS2_PLACEMENT_3D ( 'NONE', #40468, #118700, #199522 ) ;
#16984=CYLINDRICAL_SURFACE ( 'NONE', #167496, 0.1000000000000054040 ) ;
#16988=CARTESIAN_POINT ( 'NONE',  ( 21.05000000000000071, -1.387796589506715250, -194.7104960456530023 ) ) ;
#16998=CARTESIAN_POINT ( 'NONE',  ( 20.94999999999999574, 2.953700692300310848, -208.6327728934509764 ) ) ;
#17006=DIRECTION ( 'NONE',  ( 0.000000000000000000, -0.3042567129659849434, -0.9525900758537926283 ) ) ;
#17019=VERTEX_POINT ( 'NONE', #147986 ) ;
#17027=CARTESIAN_POINT ( 'NONE',  ( 21.05000000000000071, -4.161311414658873886, -226.0656773515597706 ) ) ;
#17097=DIRECTION ( 'NONE',  ( 1.000000000000000000, 0.000000000000000000, 0.000000000000000000 ) ) ;
#17120=CIRCLE ( 'NONE', #125253, 0.1000000000000054040 ) ;
#17129=ORIENTED_EDGE ( 'NONE', *, *, #54259, .T. ) ;
#17145=AXIS2_PLACEMENT_3D ( 'NONE', #25451, #8452, #87949 ) ;
#17150=ORIENTED_EDGE ( 'NONE', *, *, #237480, .T. ) ;
#17155=LINE ( 'NONE', #216609, #27653 ) ;
#17166=ORIENTED_EDGE ( 'NONE', *, *, #81735, .F. ) ;
#17197=DIRECTION ( 'NONE',  ( -3.265361837132812600E-16, 0.9770955615653313941, 0.2128009952263603677 ) ) ;
#17225=CARTESIAN_POINT ( 'NONE',  ( 18.60000000000000142, -7.631834139420945462, -210.1304494778855769 ) ) ;
#17245=VERTEX_POINT ( 'NONE', #224666 ) ;
#17250=CARTESIAN_POINT ( 'NONE',  ( -23.25000000000000000, -7.274670914976377745, -212.7102428701827250 ) ) ;
#17280=CIRCLE ( 'NONE', #21381, 7.720710678118662074 ) ;
#17321=AXIS2_PLACEMENT_3D ( 'NONE', #176102, #118686, #80798 ) ;
#17408=ORIENTED_EDGE ( 'NONE', *, *, #151110, .F. ) ;
#17409=CIRCLE ( 'NONE', #250630, 0.1999999999999866329 ) ;
#17457=ORIENTED_EDGE ( 'NONE', *, *, #150697, .T. ) ;
#17482=ADVANCED_FACE ( 'NONE', ( #232408 ), #113717, .F. ) ;
#17497=EDGE_LOOP ( 'NONE', ( #170548, #233066, #176917 ) ) ;
#17516=DIRECTION ( 'NONE',  ( 0.000000000000000000, -0.2128009952263501814, 0.9770955615653337256 ) ) ;
#17541=DIRECTION ( 'NONE',  ( 1.000000000000000000, 2.885090398161910739E-16, 6.283419270304611573E-17 ) ) ;
#17552=ADVANCED_FACE ( 'NONE', ( #39347 ), #4038, .F. ) ;
#17553=CARTESIAN_POINT ( 'NONE',  ( -18.49999999999999645, -0.6245386572416675719, -242.4051462500093237 ) ) ;
#17573=DIRECTION ( 'NONE',  ( -1.000000000000000000, -0.000000000000000000, -0.000000000000000000 ) ) ;
#17602=AXIS2_PLACEMENT_3D ( 'NONE', #36716, #35436, #15867 ) ;
#17634=DIRECTION ( 'NONE',  ( 1.000000000000000000, 0.000000000000000000, 0.000000000000000000 ) ) ;
#17654=DIRECTION ( 'NONE',  ( -1.000000000000000000, 0.000000000000000000, 0.000000000000000000 ) ) ;
#17676=LINE ( 'NONE', #241867, #156793 ) ;
#17696=ORIENTED_EDGE ( 'NONE', *, *, #65637, .T. ) ;
#17697=DIRECTION ( 'NONE',  ( 0.000000000000000000, -0.9770955615653315052, -0.2128009952263603954 ) ) ;
#17717=DIRECTION ( 'NONE',  ( 0.000000000000000000, 0.2128009952263605065, -0.9770955615653315052 ) ) ;
#17725=CARTESIAN_POINT ( 'NONE',  ( 21.05000000000000071, -3.685352791942196227, -226.3713951780953550 ) ) ;
#17761=AXIS2_PLACEMENT_3D ( 'NONE', #23303, #61111, #20727 ) ;
#17771=CARTESIAN_POINT ( 'NONE',  ( 21.05000000000000071, -6.488386256076840830, -212.2361678873109554 ) ) ;
#17777=CIRCLE ( 'NONE', #1218, 11.80000000000000959 ) ;
#17786=VERTEX_POINT ( 'NONE', #54720 ) ;
#17789=DIRECTION ( 'NONE',  ( 0.000000000000000000, -0.2128009952263403282, 0.9770955615653358350 ) ) ;
#17802=ORIENTED_EDGE ( 'NONE', *, *, #192481, .T. ) ;
#17810=DIRECTION ( 'NONE',  ( -0.000000000000000000, 0.9525900758537790836, -0.3042567129660269099 ) ) ;
#17819=CARTESIAN_POINT ( 'NONE',  ( 21.05000000000000071, 6.277629359189123903, -229.8243190661787878 ) ) ;
#17833=VERTEX_POINT ( 'NONE', #135525 ) ;
#17839=EDGE_CURVE ( 'NONE', #64432, #169963, #28191, .T. ) ;
#17857=VERTEX_POINT ( 'NONE', #119859 ) ;
#17880=EDGE_CURVE ( 'NONE', #248008, #206865, #225401, .T. ) ;
#17900=FACE_OUTER_BOUND ( 'NONE', #39410, .T. ) ;
#17913=AXIS2_PLACEMENT_3D ( 'NONE', #59802, #242311, #121124 ) ;
#17921=B_SPLINE_CURVE_WITH_KNOTS ( 'NONE', 3,
 ( #208500, #225447, #3859, #148510, #65109, #104221, #46811, #5101, #67676, #203346, #106795, #222892, #88496, #44281, #185055, #123812, #144637, #6416, #224176 ),
 .UNSPECIFIED., .F., .F.,
 ( 4, 3, 3, 3, 3, 3, 4 ),
 ( 0.000000000000000000, 2.646747978908523070E-05, 5.271166642128864737E-05, 9.008788829882664645E-05, 0.0001426648776560804626, 0.0001897378458659709517, 0.0001917382627806279321 ),
 .UNSPECIFIED. ) ;
#17922=CIRCLE ( 'NONE', #213749, 11.74999999999999289 ) ;
#17935=AXIS2_PLACEMENT_3D ( 'NONE', #253613, #17573, #193666 ) ;
#17941=EDGE_CURVE ( 'NONE', #192518, #120023, #144508, .T. ) ;
#17954=VERTEX_POINT ( 'NONE', #46697 ) ;
#17956=DIRECTION ( 'NONE',  ( 0.000000000000000000, 0.2128009952263601456, -0.9770955615653316162 ) ) ;
#17987=CYLINDRICAL_SURFACE ( 'NONE', #133979, 4.000000000000006217 ) ;
#18005=AXIS2_PLACEMENT_3D ( 'NONE', #56857, #53037, #33529 ) ;
#18011=CARTESIAN_POINT ( 'NONE',  ( -23.25000000000000000, 8.555687629545136730, -220.7824469969188783 ) ) ;
#18016=ORIENTED_EDGE ( 'NONE', *, *, #46548, .T. ) ;
#18019=CARTESIAN_POINT ( 'NONE',  ( -20.94999999999999929, 7.128833340094563376, -233.7327013124401276 ) ) ;
#18045=VERTEX_POINT ( 'NONE', #24613 ) ;
#18053=AXIS2_PLACEMENT_3D ( 'NONE', #147873, #30500, #48749 ) ;
#18055=CARTESIAN_POINT ( 'NONE',  ( 22.59080734064467322, 11.47432927991815887, -198.4695429027906926 ) ) ;
#18062=DIRECTION ( 'NONE',  ( 0.000000000000000000, 0.2128009952263590909, -0.9770955615653318382 ) ) ;
#18085=CARTESIAN_POINT ( 'NONE',  ( -18.50000000000000000, 18.34711819382569686, -236.8747682978092541 ) ) ;
#18102=ADVANCED_FACE ( 'NONE', ( #213480 ), #34884, .F. ) ;
#18107=DIRECTION ( 'NONE',  ( -1.000000000000000000, -2.885090398161910739E-16, -6.283419270304611573E-17 ) ) ;
#18136=VERTEX_POINT ( 'NONE', #153566 ) ;
#18169=DIRECTION ( 'NONE',  ( 1.000000000000000000, 0.000000000000000000, 0.000000000000000000 ) ) ;
#18188=( BOUNDED_SURFACE ( )  B_SPLINE_SURFACE ( 3, 2, ( 
 ( #59865, #162871, #164142 ),
 ( #102842, #122443, #1184 ),
 ( #5025, #201978, #63743 ),
 ( #19495, #143274, #119897 ),
 ( #98983, #62470, #42905 ),
 ( #80718, #84542, #161585 ) ),
 .UNSPECIFIED., .F., .F., .F. ) 
 B_SPLINE_SURFACE_WITH_KNOTS ( ( 4, 2, 4 ),
 ( 3, 3 ),
 ( 0.0001300404313046668353, 0.0003183318589266786276, 0.0005066232865486904741 ),
 ( 0.000000000000000000, 1.000000000000000000 ),
 .UNSPECIFIED. ) 
 GEOMETRIC_REPRESENTATION_ITEM ( )  RATIONAL_B_SPLINE_SURFACE ( (
 ( 1.000000000000000000, 0.7071067811865475727, 1.000000000000000000),
 ( 1.000000000000000000, 0.7625113560559803050, 1.000000000000000000),
 ( 1.000000000000000000, 0.8126073484662428292, 1.000000000000000000),
 ( 1.000000000000000000, 0.8923049332758562491, 1.000000000000000000),
 ( 1.000000000000000000, 0.9231914937750119732, 1.000000000000000000),
 ( 1.000000000000000000, 0.9238795325112866275, 1.000000000000000000) ) ) 
 REPRESENTATION_ITEM ( '' )  SURFACE ( )  );
#18207=EDGE_CURVE ( 'NONE', #74110, #190072, #194950, .T. ) ;
#18231=DIRECTION ( 'NONE',  ( -1.000000000000000000, -0.000000000000000000, -0.000000000000000000 ) ) ;
#18250=CARTESIAN_POINT ( 'NONE',  ( -23.25000000000000000, -4.756823075239758225, -233.1486023682345490 ) ) ;
#18297=CARTESIAN_POINT ( 'NONE',  ( -20.85000000000000142, 14.76289716703255728, -235.7888246855571026 ) ) ;
#18355=EDGE_CURVE ( 'NONE', #131461, #51901, #4684, .T. ) ;
#18373=AXIS2_PLACEMENT_3D ( 'NONE', #244327, #22749, #63116 ) ;
#18393=ADVANCED_FACE ( 'NONE', ( #103777 ), #132576, .F. ) ;
#18409=ADVANCED_FACE ( 'NONE', ( #185907 ), #163794, .F. ) ;
#18412=DIRECTION ( 'NONE',  ( -0.000000000000000000, -0.7397890806274223241, -0.6728388485993012091 ) ) ;
#18418=EDGE_CURVE ( 'NONE', #98837, #9423, #103329, .T. ) ;
#18440=CIRCLE ( 'NONE', #164205, 0.09999999999999895084 ) ;
#18457=CARTESIAN_POINT ( 'NONE',  ( -20.54999999999999716, 7.128833340094563376, -233.7327013124401276 ) ) ;
#18478=ORIENTED_EDGE ( 'NONE', *, *, #187578, .F. ) ;
#18504=ORIENTED_EDGE ( 'NONE', *, *, #121536, .T. ) ;
#18506=DIRECTION ( 'NONE',  ( -1.000000000000000000, 7.136802563874199107E-16, 1.554319503706931963E-16 ) ) ;
#18520=CARTESIAN_POINT ( 'NONE',  ( 23.25000000000000000, -4.756823075239758225, -233.1486023682345490 ) ) ;
#18522=FACE_OUTER_BOUND ( 'NONE', #155759, .T. ) ;
#18537=CARTESIAN_POINT ( 'NONE',  ( 23.14999999999999858, 7.128833340094563376, -233.7327013124401276 ) ) ;
#18573=DIRECTION ( 'NONE',  ( 1.000000000000000000, 0.000000000000000000, 0.000000000000000000 ) ) ;
#18669=CARTESIAN_POINT ( 'NONE',  ( -23.15000000000000213, -4.914013037343267776, -233.1828366659746905 ) ) ;
#18675=AXIS2_PLACEMENT_3D ( 'NONE', #95367, #237443, #133211 ) ;
#18676=AXIS2_PLACEMENT_3D ( 'NONE', #209476, #206911, #28309 ) ;
#18677=EDGE_LOOP ( 'NONE', ( #178131, #233185, #2657, #145285 ) ) ;
#18682=DIRECTION ( 'NONE',  ( 1.000000000000000000, 0.000000000000000000, 0.000000000000000000 ) ) ;
#18683=DIRECTION ( 'NONE',  ( 1.000000000000000000, 7.136802563874199107E-16, 1.554319503706925307E-16 ) ) ;
#18685=ORIENTED_EDGE ( 'NONE', *, *, #252515, .T. ) ;
#18728=DIRECTION ( 'NONE',  ( -1.000000000000000000, -0.000000000000000000, -0.000000000000000000 ) ) ;
#18730=EDGE_LOOP ( 'NONE', ( #29690, #166679, #113832, #180043, #132593 ) ) ;
#18745=EDGE_CURVE ( 'NONE', #253449, #185405, #20347, .T. ) ;
#18785=DIRECTION ( 'NONE',  ( -0.000000000000000000, 0.2128009952263597848, -0.9770955615653316162 ) ) ;
#18814=EDGE_CURVE ( 'NONE', #22873, #7608, #149527, .T. ) ;
#18820=CARTESIAN_POINT ( 'NONE',  ( -18.59999999999999787, 13.53887499352833146, -219.6971619212644669 ) ) ;
#18822=DIRECTION ( 'NONE',  ( 0.000000000000000000, -0.9525900758537790836, 0.3042567129660269099 ) ) ;
#18843=CARTESIAN_POINT ( 'NONE',  ( 19.92426406871192412, 16.76897757977919667, -222.7804130109902871 ) ) ;
#18865=CARTESIAN_POINT ( 'NONE',  ( -20.94999999999999929, 1.148907358139439339E-11, -201.0000000000015064 ) ) ;
#18867=CARTESIAN_POINT ( 'NONE',  ( 20.94999999999999929, 2.739812813550879245, -213.5801053551551547 ) ) ;
#18868=FACE_OUTER_BOUND ( 'NONE', #133814, .T. ) ;
#18873=ORIENTED_EDGE ( 'NONE', *, *, #166916, .T. ) ;
#18884=ORIENTED_EDGE ( 'NONE', *, *, #223352, .F. ) ;
#18886=CARTESIAN_POINT ( 'NONE',  ( 22.39999999999999503, -1.657885652111590336, -193.3876638332971538 ) ) ;
#18891=DIRECTION ( 'NONE',  ( 0.000000000000000000, 0.3042567129660006531, 0.9525900758537875213 ) ) ;
#18896=CARTESIAN_POINT ( 'NONE',  ( 20.12481660106788084, 11.05867956686307352, -207.0105110312538272 ) ) ;
#18916=ORIENTED_EDGE ( 'NONE', *, *, #107374, .T. ) ;
#18933=AXIS2_PLACEMENT_3D ( 'NONE', #4648, #142867, #26832 ) ;
#18962=DIRECTION ( 'NONE',  ( 0.000000000000000000, 0.2128009952263485993, -0.9770955615653341697 ) ) ;
#18965=EDGE_CURVE ( 'NONE', #30421, #81280, #140717, .T. ) ;
#19000=VERTEX_POINT ( 'NONE', #70201 ) ;
#19001=AXIS2_PLACEMENT_3D ( 'NONE', #177717, #44601, #61590 ) ;
#19007=CARTESIAN_POINT ( 'NONE',  ( 18.49999999999999645, 7.128833340094563376, -233.7327013124401276 ) ) ;
#19009=TOROIDAL_SURFACE ( 'NONE', #118996, 11.65000000000000036, 0.1000000000000000056 ) ;
#19033=VERTEX_POINT ( 'NONE', #108023 ) ;
#19062=DIRECTION ( 'NONE',  ( 0.000000000000000000, 0.9979305700607959961, 0.06430067914209769420 ) ) ;
#19070=DIRECTION ( 'NONE',  ( 0.000000000000000000, 0.8659859643398412077, -0.5000683049008356473 ) ) ;
#19076=CIRCLE ( 'NONE', #177350, 0.2000000000000003997 ) ;
#19090=LINE ( 'NONE', #152225, #179210 ) ;
#19105=AXIS2_PLACEMENT_3D ( 'NONE', #128512, #106352, #65968 ) ;
#19115=EDGE_CURVE ( 'NONE', #170560, #56802, #82825, .T. ) ;
#19126=AXIS2_PLACEMENT_3D ( 'NONE', #87735, #150313, #27818 ) ;
#19182=DIRECTION ( 'NONE',  ( 0.000000000000000000, -0.9394191166662618775, -0.3427706569150580362 ) ) ;
#19186=CARTESIAN_POINT ( 'NONE',  ( -23.25000000000000000, 5.354661166737471056, -213.3684367965233832 ) ) ;
#19225=DIRECTION ( 'NONE',  ( 0.000000000000000000, 0.2128009952263603677, -0.9770955615653313941 ) ) ;
#19229=DIRECTION ( 'NONE',  ( -0.000000000000000000, -0.2128009952263603677, 0.9770955615653313941 ) ) ;
#19247=DIRECTION ( 'NONE',  ( 0.000000000000000000, -0.2044060691543873876, 0.9788861828082220384 ) ) ;
#19272=ORIENTED_EDGE ( 'NONE', *, *, #12914, .F. ) ;
#19277=ORIENTED_EDGE ( 'NONE', *, *, #208760, .T. ) ;
#19310=CARTESIAN_POINT ( 'NONE',  ( -22.57320508075687115, 11.48087284840413425, -198.4995883060917663 ) ) ;
#19311=CIRCLE ( 'NONE', #239905, 0.6000000000000064171 ) ;
#19330=EDGE_CURVE ( 'NONE', #185124, #61748, #178283, .T. ) ;
#19335=ORIENTED_EDGE ( 'NONE', *, *, #70913, .F. ) ;
#19341=EDGE_LOOP ( 'NONE', ( #142626, #43780, #208666, #82593 ) ) ;
#19360=FACE_OUTER_BOUND ( 'NONE', #32273, .T. ) ;
#19371=ADVANCED_FACE ( 'NONE', ( #24336, #245938, #88102 ), #183397, .F. ) ;
#19404=VERTEX_POINT ( 'NONE', #124705 ) ;
#19412=DIRECTION ( 'NONE',  ( 1.000000000000000000, -0.000000000000000000, -0.000000000000000000 ) ) ;
#19418=FACE_OUTER_BOUND ( 'NONE', #48718, .T. ) ;
#19422=FACE_OUTER_BOUND ( 'NONE', #101648, .T. ) ;
#19429=EDGE_CURVE ( 'NONE', #195237, #234608, #71067, .T. ) ;
#19462=CYLINDRICAL_SURFACE ( 'NONE', #148898, 0.1000000000000055844 ) ;
#19473=LINE ( 'NONE', #178569, #195847 ) ;
#19495=CARTESIAN_POINT ( 'NONE',  ( -21.09107601085580086, 6.209752320307551976, -199.6073535771626553 ) ) ;
#19553=DIRECTION ( 'NONE',  ( 0.000000000000000000, 0.2128009952263590909, -0.9770955615653318382 ) ) ;
#19619=DIRECTION ( 'NONE',  ( 1.000000000000000000, 0.000000000000000000, 0.000000000000000000 ) ) ;
#19671=ORIENTED_EDGE ( 'NONE', *, *, #160936, .F. ) ;
#19701=CIRCLE ( 'NONE', #52803, 0.1000000000000055844 ) ;
#19725=VERTEX_POINT ( 'NONE', #26595 ) ;
#19734=EDGE_LOOP ( 'NONE', ( #159888, #42005, #149791, #254449 ) ) ;
#19737=DIRECTION ( 'NONE',  ( 0.000000000000000000, -0.2128009952263578697, 0.9770955615653320603 ) ) ;
#19750=CARTESIAN_POINT ( 'NONE',  ( 23.15000000000000213, -3.363022478626109368, -226.2703567425896267 ) ) ;
#19764=CARTESIAN_POINT ( 'NONE',  ( -20.94999999999999929, 7.128833340094563376, -233.7327013124401276 ) ) ;
#19783=PLANE ( 'NONE',  #91642 ) ;
#19865=CIRCLE ( 'NONE', #49059, 4.000000000000006217 ) ;
#19874=CYLINDRICAL_SURFACE ( 'NONE', #75335, 0.1000000000000054040 ) ;
#19899=EDGE_CURVE ( 'NONE', #114396, #176555, #117212, .T. ) ;
#19903=DIRECTION ( 'NONE',  ( 0.000000000000000000, -0.9770955615653316162, -0.2128009952263604232 ) ) ;
#19940=VECTOR ( 'NONE', #222142, 1000.000000000000000 ) ;
#19946=AXIS2_PLACEMENT_3D ( 'NONE', #95689, #175278, #254728 ) ;
#19950=ORIENTED_EDGE ( 'NONE', *, *, #224634, .T. ) ;
#19973=EDGE_CURVE ( 'NONE', #237270, #195703, #72140, .T. ) ;
#19984=EDGE_LOOP ( 'NONE', ( #133292, #201580, #7841, #122249 ) ) ;
#19989=LINE ( 'NONE', #215587, #105442 ) ;
#19991=CARTESIAN_POINT ( 'NONE',  ( 18.59999999999999787, 0.6656436123793491033, -212.6810495496487476 ) ) ;
#20011=ORIENTED_EDGE ( 'NONE', *, *, #180829, .F. ) ;
#20015=CARTESIAN_POINT ( 'NONE',  ( -22.39999999999999858, 0.09770955616802273758, -200.9787199004788931 ) ) ;
#20016=CARTESIAN_POINT ( 'NONE',  ( 23.15000000000000213, -7.274670914976375080, -212.7102428701827250 ) ) ;
#20027=DIRECTION ( 'NONE',  ( 0.000000000000000000, 0.2128009952263601456, -0.9770955615653316162 ) ) ;
#20068=AXIS2_PLACEMENT_3D ( 'NONE', #100196, #196753, #156388 ) ;
#20104=TOROIDAL_SURFACE ( 'NONE', #49318, 0.2000000000000000111, 0.1000000000000000056 ) ;
#20118=ORIENTED_EDGE ( 'NONE', *, *, #118057, .F. ) ;
#20151=CARTESIAN_POINT ( 'NONE',  ( -18.46919391072059824, -0.9001965033011636308, -242.3115848965057353 ) ) ;
#20245=VERTEX_POINT ( 'NONE', #187923 ) ;
#20246=EDGE_LOOP ( 'NONE', ( #253256, #150628, #104101, #106708 ) ) ;
#20250=EDGE_LOOP ( 'NONE', ( #177095, #83444, #220090, #105906 ) ) ;
#20275=CARTESIAN_POINT ( 'NONE',  ( -18.50000000000000000, 7.633102355717365839, -241.5185714324494484 ) ) ;
#20280=EDGE_CURVE ( 'NONE', #219487, #31299, #148967, .T. ) ;
#20328=B_SPLINE_CURVE_WITH_KNOTS ( 'NONE', 3,
 ( #215463, #95520, #235045, #176372, #132085, #56377, #171264, #195929, #112529, #254566 ),
 .UNSPECIFIED., .F., .F.,
 ( 4, 3, 3, 4 ),
 ( 0.000000000000000000, 3.394313611811828588E-05, 6.779740500700482298E-05, 0.0001049857339142853951 ),
 .UNSPECIFIED. ) ;
#20334=CIRCLE ( 'NONE', #253363, 0.09999999999999942268 ) ;
#20347=CIRCLE ( 'NONE', #128473, 7.791421356237313134 ) ;
#20394=CARTESIAN_POINT ( 'NONE',  ( 18.39999999999999858, -0.8467571797981052750, -242.2246066262668194 ) ) ;
#20437=VERTEX_POINT ( 'NONE', #188737 ) ;
#20481=ORIENTED_EDGE ( 'NONE', *, *, #245197, .T. ) ;
#20508=FACE_OUTER_BOUND ( 'NONE', #104315, .T. ) ;
#20515=ADVANCED_FACE ( 'NONE', ( #152216 ), #170522, .T. ) ;
#20556=ORIENTED_EDGE ( 'NONE', *, *, #188861, .F. ) ;
#20648=CIRCLE ( 'NONE', #257899, 0.1999999999999881317 ) ;
#20649=VERTEX_POINT ( 'NONE', #142466 ) ;
#20666=ORIENTED_EDGE ( 'NONE', *, *, #212530, .F. ) ;
#20672=ORIENTED_EDGE ( 'NONE', *, *, #52577, .F. ) ;
#20707=CARTESIAN_POINT ( 'NONE',  ( 18.59999999999999432, 2.838478681111047841, -208.5693404029859437 ) ) ;
#20716=TOROIDAL_SURFACE ( 'NONE', #208154, 0.2000000000000000111, 0.1000000000000000056 ) ;
#20727=DIRECTION ( 'NONE',  ( 0.000000000000000000, -0.05616704890742720696, 0.9984213852963240710 ) ) ;
#20743=EDGE_LOOP ( 'NONE', ( #65157, #109101, #81618, #202039, #77739 ) ) ;
#20751=CARTESIAN_POINT ( 'NONE',  ( -18.39999999999999858, -7.785976468740645196, -209.8926132507865816 ) ) ;
#20794=DIRECTION ( 'NONE',  ( 1.000000000000000000, 0.000000000000000000, 0.000000000000000000 ) ) ;
#20911=CIRCLE ( 'NONE', #141674, 0.1000000000000054040 ) ;
#20944=EDGE_CURVE ( 'NONE', #118817, #26573, #99217, .T. ) ;
#20952=ORIENTED_EDGE ( 'NONE', *, *, #173549, .F. ) ;
#20954=DIRECTION ( 'NONE',  ( -2.602085213965226419E-14, -0.2128009952263604232, 0.9770955615653316162 ) ) ;
#20957=DIRECTION ( 'NONE',  ( 1.000000000000000000, 0.000000000000000000, 0.000000000000000000 ) ) ;
#20979=AXIS2_PLACEMENT_3D ( 'NONE', #36159, #214772, #115683 ) ;
#20985=ORIENTED_EDGE ( 'NONE', *, *, #239331, .F. ) ;
#21003=CARTESIAN_POINT ( 'NONE',  ( -20.85000000000000142, 18.51199663233067483, -231.2535697180530292 ) ) ;
#21015=CIRCLE ( 'NONE', #179401, 0.09999999999999939493 ) ;
#21053=DIRECTION ( 'NONE',  ( 0.000000000000000000, 0.6728388485993012091, -0.7397890806274222131 ) ) ;
#21067=CIRCLE ( 'NONE', #166816, 0.09999999999999939493 ) ;
#21111=DIRECTION ( 'NONE',  ( 0.000000000000000000, -0.2128009952263604232, 0.9770955615653316162 ) ) ;
#21134=ORIENTED_EDGE ( 'NONE', *, *, #234211, .T. ) ;
#21169=ORIENTED_EDGE ( 'NONE', *, *, #60614, .T. ) ;
#21215=DIRECTION ( 'NONE',  ( 1.000000000000000000, 0.000000000000000000, 0.000000000000000000 ) ) ;
#21230=CYLINDRICAL_SURFACE ( 'NONE', #1842, 0.09999999999999939493 ) ;
#21255=CARTESIAN_POINT ( 'NONE',  ( -23.15000000000000213, 6.855069093508305400, -220.2576993407411692 ) ) ;
#21258=LINE ( 'NONE', #176471, #68684 ) ;
#21264=CIRCLE ( 'NONE', #233624, 12.87499999999998934 ) ;
#21269=ORIENTED_EDGE ( 'NONE', *, *, #22955, .F. ) ;
#21275=CARTESIAN_POINT ( 'NONE',  ( 23.14999999999999503, 11.04098673250373785, -220.4458636211660689 ) ) ;
#21292=ORIENTED_EDGE ( 'NONE', *, *, #223882, .T. ) ;
#21300=EDGE_LOOP ( 'NONE', ( #188833, #147205, #49727, #110491 ) ) ;
#21308=ORIENTED_EDGE ( 'NONE', *, *, #103234, .F. ) ;
#21309=DIRECTION ( 'NONE',  ( 0.000000000000000000, 0.9770955615653316162, 0.2128009952263597848 ) ) ;
#21326=ORIENTED_EDGE ( 'NONE', *, *, #237406, .T. ) ;
#21347=EDGE_CURVE ( 'NONE', #155405, #38095, #47553, .T. ) ;
#21366=CARTESIAN_POINT ( 'NONE',  ( -20.85000000000000142, -4.254329952141549853, -236.2118329068272260 ) ) ;
#21373=TOROIDAL_SURFACE ( 'NONE', #238003, 0.4000000000000017431, 0.1000000000000000056 ) ;
#21377=DIRECTION ( 'NONE',  ( 0.000000000000000000, 0.2128009952263485993, -0.9770955615653341697 ) ) ;
#21381=AXIS2_PLACEMENT_3D ( 'NONE', #182444, #32379, #89733 ) ;
#21395=DIRECTION ( 'NONE',  ( 1.000000000000000000, 0.000000000000000000, 0.000000000000000000 ) ) ;
#21401=CYLINDRICAL_SURFACE ( 'NONE', #122619, 0.09999999999999939493 ) ;
#21418=FACE_OUTER_BOUND ( 'NONE', #134242, .T. ) ;
#21433=CARTESIAN_POINT ( 'NONE',  ( -21.05000000000000071, 0.6171228861679354250, -203.8335771285409521 ) ) ;
#21456=CARTESIAN_POINT ( 'NONE',  ( -18.50000000000000000, -21.97324378644421117, -224.3523082604776562 ) ) ;
#21459=CIRCLE ( 'NONE', #183937, 0.09999999999999671652 ) ;
#21461=ORIENTED_EDGE ( 'NONE', *, *, #40094, .F. ) ;
#21491=DIRECTION ( 'NONE',  ( 0.000000000000000000, -0.2128009952263604232, 0.9770955615653316162 ) ) ;
#21511=DIRECTION ( 'NONE',  ( 1.734723475976817507E-14, 0.2128009952263604232, -0.9770955615653316162 ) ) ;
#21586=VERTEX_POINT ( 'NONE', #139932 ) ;
#21650=VERTEX_POINT ( 'NONE', #186802 ) ;
#21673=EDGE_LOOP ( 'NONE', ( #133428, #79857, #111775, #59943 ) ) ;
#21678=EDGE_LOOP ( 'NONE', ( #181864, #181571, #105753, #140725 ) ) ;
#21701=CARTESIAN_POINT ( 'NONE',  ( -18.60000000000001208, -7.621793812739404039, -210.0085087240642565 ) ) ;
#21707=AXIS2_PLACEMENT_3D ( 'NONE', #120154, #118846, #82231 ) ;
#21725=ORIENTED_EDGE ( 'NONE', *, *, #39908, .T. ) ;
#21739=ORIENTED_EDGE ( 'NONE', *, *, #95128, .T. ) ;
#21756=DIRECTION ( 'NONE',  ( 0.000000000000000000, 0.2128009952263601456, -0.9770955615653316162 ) ) ;
#21767=VECTOR ( 'NONE', #107825, 1000.000000000000000 ) ;
#21785=DIRECTION ( 'NONE',  ( 1.000000000000000000, 0.000000000000000000, 0.000000000000000000 ) ) ;
#21790=EDGE_CURVE ( 'NONE', #18045, #135942, #3335, .T. ) ;
#21809=EDGE_CURVE ( 'NONE', #9452, #218469, #146546, .T. ) ;
#21833=EDGE_LOOP ( 'NONE', ( #18504, #21461, #159516, #7430 ) ) ;
#21867=ORIENTED_EDGE ( 'NONE', *, *, #219268, .T. ) ;
#21881=DIRECTION ( 'NONE',  ( -0.000000000000000000, 0.9550021345545507412, -0.2965989261549202838 ) ) ;
#21918=ORIENTED_EDGE ( 'NONE', *, *, #221157, .F. ) ;
#21923=EDGE_LOOP ( 'NONE', ( #249870, #137457, #123945, #97521, #220991 ) ) ;
#21951=CYLINDRICAL_SURFACE ( 'NONE', #179432, 0.09999999999999724387 ) ;
#21979=VERTEX_POINT ( 'NONE', #150499 ) ;
#21984=ORIENTED_EDGE ( 'NONE', *, *, #128327, .F. ) ;
#21993=FACE_OUTER_BOUND ( 'NONE', #233261, .T. ) ;
#22016=DIRECTION ( 'NONE',  ( -0.7071067811865474617, -0.6909108974501236844, -0.1504730267678057731 ) ) ;
#22022=VECTOR ( 'NONE', #57985, 1000.000000000000000 ) ;
#22078=ORIENTED_EDGE ( 'NONE', *, *, #22089, .F. ) ;
#22089=EDGE_CURVE ( 'NONE', #5736, #242867, #180217, .T. ) ;
#22099=AXIS2_PLACEMENT_3D ( 'NONE', #172433, #229789, #233659 ) ;
#22116=ORIENTED_EDGE ( 'NONE', *, *, #55774, .F. ) ;
#22120=CARTESIAN_POINT ( 'NONE',  ( -20.54999999999999716, 8.751106741858205140, -220.7398867978735950 ) ) ;
#22121=CIRCLE ( 'NONE', #251031, 11.65000000000001457 ) ;
#22127=CARTESIAN_POINT ( 'NONE',  ( 21.05000000000000071, -1.236118717438610792, -194.8647072476872495 ) ) ;
#22154=CIRCLE ( 'NONE', #142726, 0.1000000000000055844 ) ;
#22164=CARTESIAN_POINT ( 'NONE',  ( -21.55000000000000426, 12.07323165118033614, -220.0163634141040063 ) ) ;
#22193=VECTOR ( 'NONE', #106197, 1000.000000000000000 ) ;
#22232=CIRCLE ( 'NONE', #180606, 0.09999999999999130418 ) ;
#22244=CARTESIAN_POINT ( 'NONE',  ( 20.94999999999999574, 4.193200906077805712, -212.0298262072164164 ) ) ;
#22252=MANIFOLD_SOLID_BREP ( 'Stock-MAS-200-1', #70238 ) ;
#22265=AXIS2_PLACEMENT_3D ( 'NONE', #245355, #66713, #71861 ) ;
#22268=DIRECTION ( 'NONE',  ( 0.000000000000000000, 0.2128009952263605897, -0.9770955615653315052 ) ) ;
#22306=CYLINDRICAL_SURFACE ( 'NONE', #126716, 0.1000000000000055844 ) ;
#22321=AXIS2_PLACEMENT_3D ( 'NONE', #124232, #242878, #201183 ) ;
#22342=VECTOR ( 'NONE', #189636, 1000.000000000000000 ) ;
#22410=VERTEX_POINT ( 'NONE', #233475 ) ;
#22427=EDGE_CURVE ( 'NONE', #17857, #136449, #111897, .T. ) ;
#22453=EDGE_CURVE ( 'NONE', #30421, #19000, #143317, .T. ) ;
#22456=DIRECTION ( 'NONE',  ( 0.000000000000000000, -0.2128009952263603677, 0.9770955615653313941 ) ) ;
#22471=DIRECTION ( 'NONE',  ( -7.304098846218135653E-16, -0.9770955615653315052, -0.2128009952263603954 ) ) ;
#22474=CARTESIAN_POINT ( 'NONE',  ( 23.14999999999999503, 17.01923898301590654, -224.3994341343041867 ) ) ;
#22486=FACE_OUTER_BOUND ( 'NONE', #176396, .T. ) ;
#22493=DIRECTION ( 'NONE',  ( 1.000000000000000000, 2.885090398161910739E-16, 6.283419270304611573E-17 ) ) ;
#22497=AXIS2_PLACEMENT_3D ( 'NONE', #238547, #59889, #42923 ) ;
#22577=DIRECTION ( 'NONE',  ( -1.000000000000000000, 0.000000000000000000, 0.000000000000000000 ) ) ;
#22582=VERTEX_POINT ( 'NONE', #155235 ) ;
#22587=VERTEX_POINT ( 'NONE', #76937 ) ;
#22600=EDGE_CURVE ( 'NONE', #232353, #179165, #181988, .T. ) ;
#22610=B_SPLINE_CURVE_WITH_KNOTS ( 'NONE', 3,
 ( #232301, #114898, #37952, #134434, #191898, #116204, #173648, #36680, #113612, #95336, #15833, #174930, #236127, #255642, #57470, #154074, #53643, #74535, #75780, #137029, #112343, #32837 ),
 .UNSPECIFIED., .F., .F.,
 ( 4, 3, 3, 3, 3, 3, 3, 4 ),
 ( 0.000000000000000000, 7.307836821071800646E-06, 4.161455748548169948E-05, 7.576591810647022036E-05, 0.0001098090429817492279, 0.0001438003617351094759, 0.0001777914035423671713, 0.0002117966137402901058 ),
 .UNSPECIFIED. ) ;
#22625=CARTESIAN_POINT ( 'NONE',  ( 21.03670563405601968, 13.00435671336279064, -210.7822641011882183 ) ) ;
#22664=DIRECTION ( 'NONE',  ( 1.000000000000000000, 0.000000000000000000, 0.000000000000000000 ) ) ;
#22683=DIRECTION ( 'NONE',  ( 1.000000000000000000, 0.000000000000000000, 0.000000000000000000 ) ) ;
#22687=AXIS2_PLACEMENT_3D ( 'NONE', #105907, #129350, #90201 ) ;
#22688=ORIENTED_EDGE ( 'NONE', *, *, #117429, .F. ) ;
#22689=DIRECTION ( 'NONE',  ( 0.000000000000000000, 0.2128009952263618110, -0.9770955615653312831 ) ) ;
#22692=VERTEX_POINT ( 'NONE', #144601 ) ;
#22741=DIRECTION ( 'NONE',  ( 1.000000000000000000, 0.000000000000000000, 0.000000000000000000 ) ) ;
#22749=DIRECTION ( 'NONE',  ( -1.000000000000000000, -2.885090398161910739E-16, -6.283419270304611573E-17 ) ) ;
#22774=B_SPLINE_CURVE_WITH_KNOTS ( 'NONE', 3,
 ( #79295, #18055, #256611, #158880 ),
 .UNSPECIFIED., .F., .F.,
 ( 4, 4 ),
 ( 3.878959614448864246E-18, 0.0001058379652594393101 ),
 .UNSPECIFIED. ) ;
#22787=VECTOR ( 'NONE', #226688, 1000.000000000000227 ) ;
#22841=DIRECTION ( 'NONE',  ( -1.000000000000000000, -3.190570557967288949E-16, -6.948722487160392945E-17 ) ) ;
#22853=CARTESIAN_POINT ( 'NONE',  ( -23.15000000000000213, 0.8831241302008846494, -205.0549465804976421 ) ) ;
#22873=VERTEX_POINT ( 'NONE', #119628 ) ;
#22887=AXIS2_PLACEMENT_3D ( 'NONE', #229610, #249178, #49679 ) ;
#22896=DIRECTION ( 'NONE',  ( -1.000000000000000000, 0.000000000000000000, 0.000000000000000000 ) ) ;
#22900=CARTESIAN_POINT ( 'NONE',  ( -23.15000000000000213, 17.01923898301589944, -224.3994341343041867 ) ) ;
#22902=CARTESIAN_POINT ( 'NONE',  ( -18.59999999999999787, 11.76393579169289083, -211.0774408799668720 ) ) ;
#22911=LINE ( 'NONE', #141537, #235037 ) ;
#22921=ORIENTED_EDGE ( 'NONE', *, *, #71831, .F. ) ;
#22955=EDGE_CURVE ( 'NONE', #227928, #187942, #162326, .T. ) ;
#22958=CIRCLE ( 'NONE', #98099, 0.09999999999999810429 ) ;
#22959=VECTOR ( 'NONE', #221286, 1000.000000000000114 ) ;
#22966=CARTESIAN_POINT ( 'NONE',  ( -21.13614978966381841, 6.350246358321663287, -199.6169840513710483 ) ) ;
#22983=AXIS2_PLACEMENT_3D ( 'NONE', #252751, #212375, #255274 ) ;
#22991=FACE_OUTER_BOUND ( 'NONE', #21300, .T. ) ;
#23002=CARTESIAN_POINT ( 'NONE',  ( 20.94999999999999574, 0.6656436123793491033, -212.6810495496487476 ) ) ;
#23034=ORIENTED_EDGE ( 'NONE', *, *, #136536, .T. ) ;
#23036=CYLINDRICAL_SURFACE ( 'NONE', #173307, 0.09999999999999724387 ) ;
#23081=DIRECTION ( 'NONE',  ( 1.000000000000000000, 0.000000000000000000, 0.000000000000000000 ) ) ;
#23082=CARTESIAN_POINT ( 'NONE',  ( 20.99780126800945368, 16.99738886486927569, -224.5087459288183993 ) ) ;
#23119=CARTESIAN_POINT ( 'NONE',  ( 20.97462148592293119, 11.27926720595585230, -211.0854055964561553 ) ) ;
#23148=VERTEX_POINT ( 'NONE', #226389 ) ;
#23157=AXIS2_PLACEMENT_3D ( 'NONE', #108521, #88942, #248025 ) ;
#23170=ORIENTED_EDGE ( 'NONE', *, *, #49973, .T. ) ;
#23187=CARTESIAN_POINT ( 'NONE',  ( 18.50000000000000000, -7.631834139421004970, -210.1304494778856053 ) ) ;
#23188=CARTESIAN_POINT ( 'NONE',  ( 23.14999999999999503, 13.96869538424789070, -210.3925794786331949 ) ) ;
#23207=VECTOR ( 'NONE', #25575, 1000.000000000000227 ) ;
#23209=DIRECTION ( 'NONE',  ( -1.000000000000000000, -0.000000000000000000, -0.000000000000000000 ) ) ;
#23229=DIRECTION ( 'NONE',  ( 0.000000000000000000, -0.5000683049008606273, -0.8659859643398268858 ) ) ;
#23230=EDGE_LOOP ( 'NONE', ( #123035, #162328, #157062, #15254 ) ) ;
#23255=ADVANCED_FACE ( 'NONE', ( #133724 ), #112889, .T. ) ;
#23303=CARTESIAN_POINT ( 'NONE',  ( 18.59999999999999076, 7.783179459866048866, -245.3643104511423019 ) ) ;
#23347=LINE ( 'NONE', #44175, #56016 ) ;
#23379=CIRCLE ( 'NONE', #56617, 12.87499999999999467 ) ;
#23386=CARTESIAN_POINT ( 'NONE',  ( 18.59999999999999787, 1.148907358139439339E-11, -201.0000000000015064 ) ) ;
#23392=AXIS2_PLACEMENT_3D ( 'NONE', #10055, #148287, #111730 ) ;
#23446=CIRCLE ( 'NONE', #65102, 0.09999999999999810429 ) ;
#23457=ORIENTED_EDGE ( 'NONE', *, *, #90332, .F. ) ;
#23461=EDGE_CURVE ( 'NONE', #59785, #83634, #42342, .T. ) ;
#23506=DIRECTION ( 'NONE',  ( -1.000000000000000000, 0.000000000000000000, 0.000000000000000000 ) ) ;
#23510=FACE_OUTER_BOUND ( 'NONE', #108039, .T. ) ;
#23519=CARTESIAN_POINT ( 'NONE',  ( -18.59999999999999787, 13.96869538424787649, -210.3925794786331949 ) ) ;
#23527=CARTESIAN_POINT ( 'NONE',  ( 19.97071067811865674, 16.69779891432240859, -222.5912266955230621 ) ) ;
#23585=LINE ( 'NONE', #103055, #120519 ) ;
#23599=ORIENTED_EDGE ( 'NONE', *, *, #36171, .T. ) ;
#23616=EDGE_LOOP ( 'NONE', ( #169857, #250289, #180348, #74402 ) ) ;
#23620=CIRCLE ( 'NONE', #15215, 0.6000000000000064171 ) ;
#23680=ORIENTED_EDGE ( 'NONE', *, *, #45774, .T. ) ;
#23686=CARTESIAN_POINT ( 'NONE',  ( -20.54999999999999716, 1.148907358139439339E-11, -201.0000000000015064 ) ) ;
#23691=CIRCLE ( 'NONE', #102736, 2.000000000000002220 ) ;
#23694=ADVANCED_FACE ( 'NONE', ( #179949 ), #156559, .F. ) ;
#23730=AXIS2_PLACEMENT_3D ( 'NONE', #8500, #87998, #247082 ) ;
#23742=CARTESIAN_POINT ( 'NONE',  ( 23.24999999999997513, 17.01923898301590654, -224.3994341343041867 ) ) ;
#23744=EDGE_LOOP ( 'NONE', ( #250062, #175573, #167220, #201461 ) ) ;
#23767=CIRCLE ( 'NONE', #11260, 0.5000000000000007772 ) ;
#23818=CARTESIAN_POINT ( 'NONE',  ( -20.94999999999999929, 2.859758780633683273, -208.6670499591424459 ) ) ;
#23841=DIRECTION ( 'NONE',  ( 0.000000000000000000, -0.9770955615653316162, -0.2128009952263604232 ) ) ;
#23848=CARTESIAN_POINT ( 'NONE',  ( 21.08621493067296271, 6.191908953220322864, -199.5939561276201459 ) ) ;
#23878=DIRECTION ( 'NONE',  ( 0.000000000000000000, 0.2128009952263604232, -0.9770955615653316162 ) ) ;
#23889=EDGE_CURVE ( 'NONE', #122770, #203779, #50228, .T. ) ;
#23914=ORIENTED_EDGE ( 'NONE', *, *, #143237, .F. ) ;
#23916=EDGE_CURVE ( 'NONE', #91428, #80096, #249981, .T. ) ;
#23949=ORIENTED_EDGE ( 'NONE', *, *, #101799, .T. ) ;
#23995=ORIENTED_EDGE ( 'NONE', *, *, #60824, .T. ) ;
#24016=EDGE_CURVE ( 'NONE', #10221, #168616, #200100, .T. ) ;
#24024=CARTESIAN_POINT ( 'NONE',  ( -21.14999999999999858, 11.38316329224760004, -198.5208684056144079 ) ) ;
#24047=VERTEX_POINT ( 'NONE', #185428 ) ;
#24052=FACE_OUTER_BOUND ( 'NONE', #73482, .T. ) ;
#24061=ADVANCED_FACE ( 'NONE', ( #112323 ), #71306, .T. ) ;
#24064=CARTESIAN_POINT ( 'NONE',  ( 21.09551895715215153, 12.98223157744519618, -210.6965877634172841 ) ) ;
#24067=EDGE_CURVE ( 'NONE', #86393, #50999, #188002, .T. ) ;
#24068=VECTOR ( 'NONE', #97660, 1000.000000000000000 ) ;
#24083=CARTESIAN_POINT ( 'NONE',  ( 23.15000000000000213, -4.259020970815407203, -226.0869574510824123 ) ) ;
#24111=VECTOR ( 'NONE', #248281, 1000.000000000000000 ) ;
#24136=CARTESIAN_POINT ( 'NONE',  ( 21.05000000000000071, 10.38143492858865891, -207.4255871593388463 ) ) ;
#24139=CARTESIAN_POINT ( 'NONE',  ( 23.25000000000000000, -13.88357498613435048, -191.9982587459959689 ) ) ;
#24146=EDGE_CURVE ( 'NONE', #63679, #203031, #169755, .T. ) ;
#24170=FACE_OUTER_BOUND ( 'NONE', #187347, .T. ) ;
#24182=CARTESIAN_POINT ( 'NONE',  ( -18.39999999999999858, -7.792936614629570435, -209.8606550935952271 ) ) ;
#24184=ORIENTED_EDGE ( 'NONE', *, *, #148106, .F. ) ;
#24199=CARTESIAN_POINT ( 'NONE',  ( 20.94999999999999574, 4.252251777740764460, -211.8999245327126744 ) ) ;
#24230=ORIENTED_EDGE ( 'NONE', *, *, #51420, .F. ) ;
#24231=EDGE_CURVE ( 'NONE', #30937, #17857, #117453, .T. ) ;
#24238=DIRECTION ( 'NONE',  ( 0.000000000000000000, 0.2128009952263605065, -0.9770955615653315052 ) ) ;
#24246=CARTESIAN_POINT ( 'NONE',  ( -21.14999999999999858, -2.598867842139046314, -189.5410128746472083 ) ) ;
#24283=EDGE_CURVE ( 'NONE', #107106, #245608, #37991, .T. ) ;
#24310=CYLINDRICAL_SURFACE ( 'NONE', #139412, 0.1000000000000035305 ) ;
#24318=ADVANCED_FACE ( 'NONE', ( #256903 ), #46154, .F. ) ;
#24319=ORIENTED_EDGE ( 'NONE', *, *, #87929, .T. ) ;
#24330=CIRCLE ( 'NONE', #203379, 11.75000000000000355 ) ;
#24336=FACE_BOUND ( 'NONE', #30311, .T. ) ;
#24345=EDGE_CURVE ( 'NONE', #92979, #243059, #83710, .T. ) ;
#24359=EDGE_CURVE ( 'NONE', #151535, #148073, #161735, .T. ) ;
#24391=EDGE_CURVE ( 'NONE', #234881, #232370, #121394, .T. ) ;
#24405=EDGE_CURVE ( 'NONE', #147767, #32779, #242140, .T. ) ;
#24477=DIRECTION ( 'NONE',  ( 1.000000000000000000, 0.000000000000000000, 0.000000000000000000 ) ) ;
#24481=ORIENTED_EDGE ( 'NONE', *, *, #49121, .T. ) ;
#24500=CARTESIAN_POINT ( 'NONE',  ( 18.60000000000000142, -7.567701079425715349, -210.0537230116848946 ) ) ;
#24535=CYLINDRICAL_SURFACE ( 'NONE', #63986, 0.1000000000000055844 ) ;
#24549=EDGE_LOOP ( 'NONE', ( #127219, #183059, #94665, #146334 ) ) ;
#24560=DIRECTION ( 'NONE',  ( 0.000000000000000000, -0.2128009952263982818, 0.9770955615653232895 ) ) ;
#24585=ORIENTED_EDGE ( 'NONE', *, *, #126410, .T. ) ;
#24613=CARTESIAN_POINT ( 'NONE',  ( -21.44999999999999929, 11.50825441376376901, -220.2417535673963300 ) ) ;
#24617=EDGE_CURVE ( 'NONE', #74571, #18045, #212944, .T. ) ;
#24619=CARTESIAN_POINT ( 'NONE',  ( 21.97500000000000497, 12.13349391679638778, -210.8946109257198032 ) ) ;
#24673=DIRECTION ( 'NONE',  ( 1.000000000000000000, -7.136802563874199107E-16, -1.554319503706929991E-16 ) ) ;
#24697=DIRECTION ( 'NONE',  ( 1.000000000000000000, 2.885090398161910739E-16, 6.283419270304611573E-17 ) ) ;
#24729=LINE ( 'NONE', #5095, #13851 ) ;
#24731=ORIENTED_EDGE ( 'NONE', *, *, #86765, .T. ) ;
#24744=DIRECTION ( 'NONE',  ( 0.000000000000000000, 0.2128009952263582305, -0.9770955615653319493 ) ) ;
#24767=CARTESIAN_POINT ( 'NONE',  ( -20.94999999999999929, 4.288595810029049993, -211.9930862808554934 ) ) ;
#24772=DIRECTION ( 'NONE',  ( 2.710505431213777355E-16, -0.9770955615653316162, -0.2128009952263604232 ) ) ;
#24775=ORIENTED_EDGE ( 'NONE', *, *, #149438, .T. ) ;
#24784=VERTEX_POINT ( 'NONE', #201795 ) ;
#24797=CARTESIAN_POINT ( 'NONE',  ( -20.94999999999999929, 7.128833340094563376, -233.7327013124401276 ) ) ;
#24806=PLANE ( 'NONE',  #133364 ) ;
#24822=VERTEX_POINT ( 'NONE', #158854 ) ;
#24829=AXIS2_PLACEMENT_3D ( 'NONE', #47312, #51157, #75601 ) ;
#24874=ORIENTED_EDGE ( 'NONE', *, *, #120389, .T. ) ;
#24877=DIRECTION ( 'NONE',  ( 0.000000000000000000, 0.2128009952263485993, -0.9770955615653341697 ) ) ;
#24892=AXIS2_PLACEMENT_3D ( 'NONE', #237281, #18231, #235977 ) ;
#24947=FACE_OUTER_BOUND ( 'NONE', #217778, .T. ) ;
#24959=EDGE_CURVE ( 'NONE', #206404, #183689, #180354, .T. ) ;
#24964=CYLINDRICAL_SURFACE ( 'NONE', #71358, 12.87499999999999467 ) ;
#24965=FACE_OUTER_BOUND ( 'NONE', #169317, .T. ) ;
#24996=ORIENTED_EDGE ( 'NONE', *, *, #152647, .F. ) ;
#25029=ORIENTED_EDGE ( 'NONE', *, *, #4331, .F. ) ;
#25081=ORIENTED_EDGE ( 'NONE', *, *, #163516, .T. ) ;
#25083=CARTESIAN_POINT ( 'NONE',  ( -20.94999999999999929, 0.6656436123793473270, -212.6810495496487476 ) ) ;
#25088=CARTESIAN_POINT ( 'NONE',  ( 18.49999999999998934, 8.433899723187009201, -209.4150263691077782 ) ) ;
#25115=ORIENTED_EDGE ( 'NONE', *, *, #234676, .F. ) ;
#25148=EDGE_CURVE ( 'NONE', #117008, #246109, #88934, .T. ) ;
#25161=ORIENTED_EDGE ( 'NONE', *, *, #38107, .T. ) ;
#25218=EDGE_CURVE ( 'NONE', #35875, #121315, #176458, .T. ) ;
#25252=ORIENTED_EDGE ( 'NONE', *, *, #29094, .T. ) ;
#25296=VERTEX_POINT ( 'NONE', #231349 ) ;
#25326=CYLINDRICAL_SURFACE ( 'NONE', #178135, 0.09999999999999181766 ) ;
#25391=DIRECTION ( 'NONE',  ( 0.000000000000000000, 0.2128009952263604510, -0.9770955615653315052 ) ) ;
#25431=ADVANCED_FACE ( 'NONE', ( #25697 ), #51685, .T. ) ;
#25439=DIRECTION ( 'NONE',  ( 0.000000000000000000, 0.9770955615653316162, 0.2128009952263604232 ) ) ;
#25451=CARTESIAN_POINT ( 'NONE',  ( 23.14999999999999503, 9.083217576421224848, -211.4565844547649931 ) ) ;
#25500=CARTESIAN_POINT ( 'NONE',  ( -20.54999999999999716, 6.724511449164476851, -231.8762197454659884 ) ) ;
#25517=CARTESIAN_POINT ( 'NONE',  ( -21.09610168723072121, 6.225701436283752166, -199.6097317171979171 ) ) ;
#25565=ORIENTED_EDGE ( 'NONE', *, *, #89279, .F. ) ;
#25575=DIRECTION ( 'NONE',  ( 0.000000000000000000, 0.9770955615653310611, 0.2128009952263620608 ) ) ;
#25585=AXIS2_PLACEMENT_3D ( 'NONE', #185470, #68089, #94058 ) ;
#25597=ORIENTED_EDGE ( 'NONE', *, *, #145722, .F. ) ;
#25633=CARTESIAN_POINT ( 'NONE',  ( -20.85000000000000142, 17.16609282392353464, -224.6038045889790453 ) ) ;
#25654=FACE_OUTER_BOUND ( 'NONE', #169502, .T. ) ;
#25685=CARTESIAN_POINT ( 'NONE',  ( -20.94999999999999929, 2.817198581588411077, -208.4716308468294130 ) ) ;
#25689=DIRECTION ( 'NONE',  ( 0.000000000000000000, 0.8149014228131981064, -0.5795995782408966956 ) ) ;
#25697=FACE_OUTER_BOUND ( 'NONE', #27746, .T. ) ;
#25809=EDGE_LOOP ( 'NONE', ( #51057, #44422, #253029, #255023, #102770, #152214, #85431, #234827, #186789, #164004 ) ) ;
#25843=FACE_OUTER_BOUND ( 'NONE', #233355, .T. ) ;
#25852=EDGE_CURVE ( 'NONE', #156652, #203538, #109594, .T. ) ;
#25854=LINE ( 'NONE', #105335, #205883 ) ;
#25861=CARTESIAN_POINT ( 'NONE',  ( 21.05000000000000071, -4.557064143889601127, -233.1584191572127622 ) ) ;
#25870=DIRECTION ( 'NONE',  ( 0.000000000000000000, -0.2128009952263602567, 0.9770955615653315052 ) ) ;
#25880=ORIENTED_EDGE ( 'NONE', *, *, #110373, .T. ) ;
#25883=CARTESIAN_POINT ( 'NONE',  ( -18.59999999999999787, 12.85464084203975155, -205.2772944332067766 ) ) ;
#25886=EDGE_CURVE ( 'NONE', #219487, #226256, #142888, .T. ) ;
#25904=CARTESIAN_POINT ( 'NONE',  ( 20.94999999999999929, -4.892732937820623462, -233.2805462221312496 ) ) ;
#25907=CARTESIAN_POINT ( 'NONE',  ( 21.07928932188134397, -1.250084634896337255, -194.7953894783290423 ) ) ;
#25960=CARTESIAN_POINT ( 'NONE',  ( -18.59999999999999787, 14.80545736607782814, -235.9842437978701639 ) ) ;
#25968=EDGE_CURVE ( 'NONE', #168616, #38453, #235038, .T. ) ;
#25975=ORIENTED_EDGE ( 'NONE', *, *, #9101, .F. ) ;
#26012=CARTESIAN_POINT ( 'NONE',  ( 18.31325810956367661, -0.7275186016206726114, -242.4731767114571142 ) ) ;
#26019=EDGE_LOOP ( 'NONE', ( #254521, #234828, #73886, #90759 ) ) ;
#26027=ORIENTED_EDGE ( 'NONE', *, *, #117857, .F. ) ;
#26093=ORIENTED_EDGE ( 'NONE', *, *, #155266, .F. ) ;
#26106=ORIENTED_EDGE ( 'NONE', *, *, #62238, .F. ) ;
#26132=CIRCLE ( 'NONE', #171908, 0.1000000000000054040 ) ;
#26174=DIRECTION ( 'NONE',  ( -0.000000000000000000, -0.2814428106787469908, -0.9595780032479106492 ) ) ;
#26184=ORIENTED_EDGE ( 'NONE', *, *, #116472, .T. ) ;
#26189=DIRECTION ( 'NONE',  ( 0.000000000000000000, 0.9770955615653548199, 0.2128009952262535920 ) ) ;
#26215=B_SPLINE_CURVE_WITH_KNOTS ( 'NONE', 3,
 ( #185126, #245100, #225505, #46879 ),
 .UNSPECIFIED., .F., .F.,
 ( 4, 4 ),
 ( 0.000000000000000000, 0.0002118541922231706302 ),
 .UNSPECIFIED. ) ;
#26221=CARTESIAN_POINT ( 'NONE',  ( 21.04999999999999716, 12.01637667977029267, -206.2275507673361403 ) ) ;
#26223=CARTESIAN_POINT ( 'NONE',  ( 23.14999999999999503, 8.980461154494404852, -187.0187154576991304 ) ) ;
#26233=VECTOR ( 'NONE', #109966, 1000.000000000000227 ) ;
#26237=DIRECTION ( 'NONE',  ( -1.000000000000000000, 0.000000000000000000, 0.000000000000000000 ) ) ;
#26238=ADVANCED_FACE ( 'NONE', ( #20508 ), #36225, .T. ) ;
#26250=ORIENTED_EDGE ( 'NONE', *, *, #143541, .F. ) ;
#26319=CARTESIAN_POINT ( 'NONE',  ( 21.05281448260627641, 11.16554581325007334, -211.0271857082375391 ) ) ;
#26324=CARTESIAN_POINT ( 'NONE',  ( -20.64999999999999858, -3.770473190032741062, -225.9805569534692324 ) ) ;
#26339=AXIS2_PLACEMENT_3D ( 'NONE', #18865, #235339, #56677 ) ;
#26345=DIRECTION ( 'NONE',  ( 1.000000000000000000, 0.000000000000000000, 0.000000000000000000 ) ) ;
#26349=CYLINDRICAL_SURFACE ( 'NONE', #247389, 0.1000000000000054040 ) ;
#26350=EDGE_CURVE ( 'NONE', #156593, #234500, #51485, .T. ) ;
#26362=DIRECTION ( 'NONE',  ( 0.000000000000000000, -0.2128009952263604232, 0.9770955615653316162 ) ) ;
#26364=CARTESIAN_POINT ( 'NONE',  ( -20.85000000000000142, 7.576017155224048061, -241.7224044826512284 ) ) ;
#26375=ADVANCED_FACE ( 'NONE', ( #223807 ), #85551, .T. ) ;
#26409=CYLINDRICAL_SURFACE ( 'NONE', #256829, 0.1000000000000054040 ) ;
#26415=DIRECTION ( 'NONE',  ( 1.000000000000000000, 0.000000000000000000, 0.000000000000000000 ) ) ;
#26422=VERTEX_POINT ( 'NONE', #102550 ) ;
#26464=AXIS2_PLACEMENT_3D ( 'NONE', #75885, #38068, #215390 ) ;
#26491=ORIENTED_EDGE ( 'NONE', *, *, #75077, .T. ) ;
#26531=DIRECTION ( 'NONE',  ( 1.000000000000000000, 0.000000000000000000, 0.000000000000000000 ) ) ;
#26538=ORIENTED_EDGE ( 'NONE', *, *, #142306, .F. ) ;
#26547=DIRECTION ( 'NONE',  ( 0.000000000000000000, 0.8879235499942239596, 0.4599910535713220838 ) ) ;
#26573=VERTEX_POINT ( 'NONE', #39775 ) ;
#26578=CARTESIAN_POINT ( 'NONE',  ( -18.40904629823846506, -0.7490475871975608158, -242.2033266940802889 ) ) ;
#26595=CARTESIAN_POINT ( 'NONE',  ( -20.64999999999999858, 4.389020526555173163, -221.1525959572864792 ) ) ;
#26615=CARTESIAN_POINT ( 'NONE',  ( 23.25000000000000000, -3.770473190032740174, -225.9805569534692324 ) ) ;
#26630=EDGE_CURVE ( 'NONE', #61748, #54081, #75053, .T. ) ;
#26633=CARTESIAN_POINT ( 'NONE',  ( -21.05000000000000071, 7.872214528623318053, -209.6555322433423498 ) ) ;
#26634=DIRECTION ( 'NONE',  ( 0.000000000000000000, -0.9770955615653316162, -0.2128009952263604232 ) ) ;
#26656=DIRECTION ( 'NONE',  ( 0.000000000000000000, 0.9770955615653548199, 0.2128009952262535920 ) ) ;
#26673=ADVANCED_FACE ( 'NONE', ( #38456 ), #30450, .F. ) ;
#26708=EDGE_CURVE ( 'NONE', #87352, #35875, #44883, .T. ) ;
#26715=DIRECTION ( 'NONE',  ( 0.000000000000000000, -0.9550021345545507412, 0.2965989261549202283 ) ) ;
#26733=ORIENTED_EDGE ( 'NONE', *, *, #43193, .F. ) ;
#26734=AXIS2_PLACEMENT_3D ( 'NONE', #15116, #114203, #195048 ) ;
#26735=CARTESIAN_POINT ( 'NONE',  ( -20.64999999999999858, 8.751106741858205140, -220.7398867978736234 ) ) ;
#26738=AXIS2_PLACEMENT_3D ( 'NONE', #53105, #72706, #94799 ) ;
#26755=CARTESIAN_POINT ( 'NONE',  ( -20.54999999999999716, 6.268811756569107274, -220.3853799378769622 ) ) ;
#26779=ADVANCED_FACE ( 'NONE', ( #24052 ), #4457, .T. ) ;
#26780=CARTESIAN_POINT ( 'NONE',  ( -20.85000000000000142, 7.633102355717365839, -241.5185714324494484 ) ) ;
#26789=CARTESIAN_POINT ( 'NONE',  ( 18.49999999999999289, 15.22030141505243961, -222.9130098973476777 ) ) ;
#26825=ORIENTED_EDGE ( 'NONE', *, *, #2905, .T. ) ;
#26832=DIRECTION ( 'NONE',  ( 0.000000000000000000, 0.2128009952263601456, -0.9770955615653316162 ) ) ;
#26871=CYLINDRICAL_SURFACE ( 'NONE', #19105, 0.1000000000000055844 ) ;
#26908=FACE_OUTER_BOUND ( 'NONE', #109476, .T. ) ;
#26920=CARTESIAN_POINT ( 'NONE',  ( -21.37071067811865532, 12.38659663131667976, -219.9481158626206252 ) ) ;
#26924=DIRECTION ( 'NONE',  ( 0.000000000000000000, -0.6728388485993177515, 0.7397890806274072251 ) ) ;
#26928=DIRECTION ( 'NONE',  ( -0.000000000000000000, 0.7397890806274223241, 0.6728388485993012091 ) ) ;
#26936=DIRECTION ( 'NONE',  ( 0.000000000000000000, 0.2128009952263601456, -0.9770955615653316162 ) ) ;
#26947=CARTESIAN_POINT ( 'NONE',  ( -21.05315837326133632, 17.15379753644537075, -224.5473496284387522 ) ) ;
#26966=VECTOR ( 'NONE', #134202, 1000.000000000000000 ) ;
#26969=AXIS2_PLACEMENT_3D ( 'NONE', #17771, #19070, #98566 ) ;
#27082=CIRCLE ( 'NONE', #172851, 0.1000000000000068751 ) ;
#27087=ORIENTED_EDGE ( 'NONE', *, *, #117469, .F. ) ;
#27110=DIRECTION ( 'NONE',  ( 0.000000000000000000, -0.2128009952263485993, 0.9770955615653341697 ) ) ;
#27115=EDGE_CURVE ( 'NONE', #185405, #19000, #2861, .T. ) ;
#27199=ORIENTED_EDGE ( 'NONE', *, *, #87112, .T. ) ;
#27234=LINE ( 'NONE', #246251, #243761 ) ;
#27245=CIRCLE ( 'NONE', #10644, 0.09999999999999061029 ) ;
#27273=DIRECTION ( 'NONE',  ( 2.940209281316622002E-16, -0.9770955615653309501, -0.2128009952263629490 ) ) ;
#27278=SPHERICAL_SURFACE ( 'NONE', #55730, 0.1000000000000000056 ) ;
#27281=CARTESIAN_POINT ( 'NONE',  ( 19.58285714285715073, 11.77074044182232448, -206.2449930062242629 ) ) ;
#27282=CARTESIAN_POINT ( 'NONE',  ( 21.05000000000000426, -1.267579133596468122, -194.8710457894447927 ) ) ;
#27288=CARTESIAN_POINT ( 'NONE',  ( -18.50000000000000000, 12.87592094156238609, -205.3750039893633073 ) ) ;
#27299=AXIS2_PLACEMENT_3D ( 'NONE', #248323, #230048, #170123 ) ;
#27311=DIRECTION ( 'NONE',  ( 1.000000000000000000, 0.000000000000000000, 0.000000000000000000 ) ) ;
#27316=CIRCLE ( 'NONE', #177150, 0.1000000000000116629 ) ;
#27328=CARTESIAN_POINT ( 'NONE',  ( 18.33996824403354609, -0.7705153381573188742, -242.4320089669257356 ) ) ;
#27330=CARTESIAN_POINT ( 'NONE',  ( -18.50000000000000000, -11.78281952876890060, -191.5407366062592871 ) ) ;
#27346=DIRECTION ( 'NONE',  ( 0.000000000000000000, -0.2965989261549489275, -0.9550021345545417484 ) ) ;
#27356=AXIS2_PLACEMENT_3D ( 'NONE', #119318, #58027, #94599 ) ;
#27357=CARTESIAN_POINT ( 'NONE',  ( 20.04142135623730070, 15.92646454033040015, -219.3818586450342423 ) ) ;
#27368=CARTESIAN_POINT ( 'NONE',  ( -23.25000000000000000, 1.148907358139439339E-11, -201.0000000000015064 ) ) ;
#27376=FACE_OUTER_BOUND ( 'NONE', #19341, .T. ) ;
#27382=CARTESIAN_POINT ( 'NONE',  ( -20.54999999999999716, 6.759468328187065111, -212.0650163994647812 ) ) ;
#27388=CARTESIAN_POINT ( 'NONE',  ( 18.49999999999999645, 8.006782298343173565, -209.8034900594678618 ) ) ;
#27393=CARTESIAN_POINT ( 'NONE',  ( 22.60000000000000142, -2.453693327374942612, -189.5089294449251724 ) ) ;
#27411=ORIENTED_EDGE ( 'NONE', *, *, #24067, .F. ) ;
#27414=EDGE_CURVE ( 'NONE', #146352, #247780, #6259, .T. ) ;
#27420=VERTEX_POINT ( 'NONE', #195661 ) ;
#27458=VERTEX_POINT ( 'NONE', #95250 ) ;
#27522=ORIENTED_EDGE ( 'NONE', *, *, #48838, .T. ) ;
#27531=CARTESIAN_POINT ( 'NONE',  ( 23.24999999999999645, 1.148907358139439339E-11, -201.0000000000015064 ) ) ;
#27557=AXIS2_PLACEMENT_3D ( 'NONE', #125727, #245683, #26656 ) ;
#27566=VERTEX_POINT ( 'NONE', #52907 ) ;
#27593=CARTESIAN_POINT ( 'NONE',  ( -21.05000000000000071, 1.681127862299736098, -208.7190549363676269 ) ) ;
#27608=EDGE_CURVE ( 'NONE', #80096, #157474, #222929, .T. ) ;
#27618=LINE ( 'NONE', #204918, #30642 ) ;
#27620=ORIENTED_EDGE ( 'NONE', *, *, #17880, .T. ) ;
#27630=CARTESIAN_POINT ( 'NONE',  ( 21.04999999999908411, 11.16248219967772215, -211.0118371899025078 ) ) ;
#27635=DIRECTION ( 'NONE',  ( 0.000000000000000000, 0.2128009952263604232, -0.9770955615653316162 ) ) ;
#27641=EDGE_CURVE ( 'NONE', #198456, #168941, #135441, .T. ) ;
#27642=DIRECTION ( 'NONE',  ( 1.000000000000000000, -0.000000000000000000, -0.000000000000000000 ) ) ;
#27653=VECTOR ( 'NONE', #18412, 999.9999999999998863 ) ;
#27655=PLANE ( 'NONE',  #14552 ) ;
#27661=CARTESIAN_POINT ( 'NONE',  ( 18.59999999999999076, 7.788796164756791818, -245.4641525896719543 ) ) ;
#27711=LINE ( 'NONE', #9381, #239474 ) ;
#27719=CYLINDRICAL_SURFACE ( 'NONE', #217079, 0.1000000000000057648 ) ;
#27720=ORIENTED_EDGE ( 'NONE', *, *, #46548, .F. ) ;
#27746=EDGE_LOOP ( 'NONE', ( #107474, #52917, #82773, #107776 ) ) ;
#27788=ORIENTED_EDGE ( 'NONE', *, *, #72898, .T. ) ;
#27795=CIRCLE ( 'NONE', #98434, 0.1000000000000054040 ) ;
#27801=TOROIDAL_SURFACE ( 'NONE', #123448, 0.2000000000000000111, 0.1000000000000000056 ) ;
#27807=ORIENTED_EDGE ( 'NONE', *, *, #119560, .F. ) ;
#27818=DIRECTION ( 'NONE',  ( 0.000000000000000000, -0.2965989261549410450, -0.9550021345545443019 ) ) ;
#27844=EDGE_CURVE ( 'NONE', #136330, #116019, #197983, .T. ) ;
#27885=CARTESIAN_POINT ( 'NONE',  ( -21.05000000000000071, 0.4810385098657082859, -209.0827657365571213 ) ) ;
#27901=DIRECTION ( 'NONE',  ( -1.000000000000000000, -2.885090398161910739E-16, -6.283419270304611573E-17 ) ) ;
#27907=CARTESIAN_POINT ( 'NONE',  ( 18.49351773456763226, -7.697694071498478507, -210.0302349457594175 ) ) ;
#27936=EDGE_CURVE ( 'NONE', #201031, #229898, #235580, .T. ) ;
#27971=EDGE_CURVE ( 'NONE', #54334, #258000, #193915, .T. ) ;
#27995=AXIS2_PLACEMENT_3D ( 'NONE', #202233, #26174, #204779 ) ;
#28007=CIRCLE ( 'NONE', #90502, 0.1000000000000055844 ) ;
#28062=DIRECTION ( 'NONE',  ( 0.000000000000000000, -0.2128009952263601734, 0.9770955615653316162 ) ) ;
#28069=ORIENTED_EDGE ( 'NONE', *, *, #130369, .F. ) ;
#28084=DIRECTION ( 'NONE',  ( -1.000000000000000000, 8.034189347746079853E-16, -2.566115377699053192E-16 ) ) ;
#28085=CIRCLE ( 'NONE', #173865, 0.1000000000000072498 ) ;
#28101=DIRECTION ( 'NONE',  ( 0.000000000000000000, -0.2128009952263264781, 0.9770955615653388326 ) ) ;
#28109=LINE ( 'NONE', #85447, #70514 ) ;
#28118=AXIS2_PLACEMENT_3D ( 'NONE', #189553, #8347, #249526 ) ;
#28124=DIRECTION ( 'NONE',  ( 1.000000000000000000, 0.000000000000000000, 0.000000000000000000 ) ) ;
#28132=DIRECTION ( 'NONE',  ( -0.000000000000000000, 0.3427706569149635007, -0.9394191166662961834 ) ) ;
#28135=CARTESIAN_POINT ( 'NONE',  ( 18.52928932188133970, 15.28939250479744949, -222.8979625946709007 ) ) ;
#28155=AXIS2_PLACEMENT_3D ( 'NONE', #15808, #152753, #95312 ) ;
#28162=ORIENTED_EDGE ( 'NONE', *, *, #53819, .T. ) ;
#28177=AXIS2_PLACEMENT_3D ( 'NONE', #110942, #13139, #50940 ) ;
#28191=CIRCLE ( 'NONE', #157366, 0.09999999999999939493 ) ;
#28213=DIRECTION ( 'NONE',  ( 0.000000000000000000, 0.7397890806274222131, 0.6728388485993012091 ) ) ;
#28227=DIRECTION ( 'NONE',  ( -0.000000000000000000, 0.9770955615653313941, 0.2128009952263603954 ) ) ;
#28229=AXIS2_PLACEMENT_3D ( 'NONE', #60597, #176725, #140129 ) ;
#28232=CARTESIAN_POINT ( 'NONE',  ( -21.05000000000000071, 17.11694853917243364, -224.3781540347815735 ) ) ;
#28257=DIRECTION ( 'NONE',  ( 0.000000000000000000, -0.9770955615653316162, -0.2128009952263604232 ) ) ;
#28274=ORIENTED_EDGE ( 'NONE', *, *, #191069, .T. ) ;
#28298=ORIENTED_EDGE ( 'NONE', *, *, #139158, .F. ) ;
#28309=DIRECTION ( 'NONE',  ( 0.000000000000000000, -0.2128009952263403282, 0.9770955615653358350 ) ) ;
#28311=EDGE_CURVE ( 'NONE', #232107, #181313, #152616, .T. ) ;
#28313=ORIENTED_EDGE ( 'NONE', *, *, #185110, .F. ) ;
#28320=AXIS2_PLACEMENT_3D ( 'NONE', #146883, #46508, #246014 ) ;
#28327=FACE_OUTER_BOUND ( 'NONE', #252103, .T. ) ;
#28435=DIRECTION ( 'NONE',  ( -1.000000000000000000, 0.000000000000000000, 0.000000000000000000 ) ) ;
#28443=CARTESIAN_POINT ( 'NONE',  ( 18.49999999999999289, 8.980461154494401299, -187.0187154576991304 ) ) ;
#28455=VERTEX_POINT ( 'NONE', #24767 ) ;
#28491=DIRECTION ( 'NONE',  ( 0.000000000000000000, 0.9984213852963246261, 0.05616704890741601452 ) ) ;
#28547=ORIENTED_EDGE ( 'NONE', *, *, #54054, .T. ) ;
#28560=EDGE_LOOP ( 'NONE', ( #54850, #6094, #221918, #30572 ) ) ;
#28563=ADVANCED_FACE ( 'NONE', ( #138241 ), #217776, .T. ) ;
#28568=ADVANCED_FACE ( 'NONE', ( #187681 ), #164260, .T. ) ;
#28574=DIRECTION ( 'NONE',  ( 0.000000000000000000, 0.2128009952263605897, -0.9770955615653315052 ) ) ;
#28583=ADVANCED_FACE ( 'NONE', ( #247633 ), #87253, .T. ) ;
#28609=EDGE_CURVE ( 'NONE', #120023, #84780, #52613, .T. ) ;
#28616=CONICAL_SURFACE ( 'NONE', #211743, 4.299999999999966960, 0.7853981633974466137 ) ;
#28627=DIRECTION ( 'NONE',  ( 0.000000000000000000, -0.2128009952263603677, 0.9770955615653313941 ) ) ;
#28635=DIRECTION ( 'NONE',  ( 1.000000000000000000, 1.794895427898103559E-16, 3.909090864890002444E-17 ) ) ;
#28640=DIRECTION ( 'NONE',  ( 0.000000000000000000, -0.9964539953858966292, -0.08413937888696132461 ) ) ;
#28650=FACE_OUTER_BOUND ( 'NONE', #172609, .T. ) ;
#28656=EDGE_CURVE ( 'NONE', #187924, #150841, #110888, .T. ) ;
#28663=DIRECTION ( 'NONE',  ( 0.000000000000000000, 0.2128009952263605897, -0.9770955615653315052 ) ) ;
#28683=AXIS2_PLACEMENT_3D ( 'NONE', #243311, #242034, #63387 ) ;
#28718=CARTESIAN_POINT ( 'NONE',  ( -21.05000000000000071, -1.236118717437885595, -194.8647072476926496 ) ) ;
#28737=EDGE_CURVE ( 'NONE', #124170, #246109, #118059, .T. ) ;
#28749=ADVANCED_FACE ( 'NONE', ( #178058, #250200 ), #135033, .F. ) ;
#28754=EDGE_LOOP ( 'NONE', ( #6515, #77287, #186256, #150754 ) ) ;
#28765=FACE_OUTER_BOUND ( 'NONE', #72607, .T. ) ;
#28807=VERTEX_POINT ( 'NONE', #136309 ) ;
#28825=LINE ( 'NONE', #26223, #149473 ) ;
#28884=DIRECTION ( 'NONE',  ( -0.000000000000000000, 0.2128009952263604232, -0.9770955615653316162 ) ) ;
#28906=ORIENTED_EDGE ( 'NONE', *, *, #117634, .T. ) ;
#28909=DIRECTION ( 'NONE',  ( 0.000000000000000000, 0.2128009952263485993, -0.9770955615653341697 ) ) ;
#28972=CARTESIAN_POINT ( 'NONE',  ( 20.85000000000000142, 7.128833340094563376, -233.7327013124401276 ) ) ;
#28982=CARTESIAN_POINT ( 'NONE',  ( 18.53691006697109600, 15.32283903239712330, -222.9441006232443669 ) ) ;
#28985=VECTOR ( 'NONE', #3867, 1000.000000000000000 ) ;
#29000=CARTESIAN_POINT ( 'NONE',  ( 21.14999999999999858, 6.390846877240206503, -199.6081416912452653 ) ) ;
#29014=AXIS2_PLACEMENT_3D ( 'NONE', #99843, #159876, #60731 ) ;
#29026=ORIENTED_EDGE ( 'NONE', *, *, #225704, .F. ) ;
#29035=FACE_OUTER_BOUND ( 'NONE', #7927, .T. ) ;
#29088=ORIENTED_EDGE ( 'NONE', *, *, #80755, .F. ) ;
#29094=EDGE_CURVE ( 'NONE', #97897, #17019, #253416, .T. ) ;
#29102=ORIENTED_EDGE ( 'NONE', *, *, #51478, .T. ) ;
#29103=EDGE_CURVE ( 'NONE', #216057, #2617, #140452, .T. ) ;
#29108=DIRECTION ( 'NONE',  ( -1.000000000000000000, 0.000000000000000000, 0.000000000000000000 ) ) ;
#29114=CARTESIAN_POINT ( 'NONE',  ( 23.24999999999999289, 4.054946580507614584, -200.1168758698121053 ) ) ;
#29124=DIRECTION ( 'NONE',  ( 1.000000000000000000, 0.000000000000000000, 0.000000000000000000 ) ) ;
#29134=ORIENTED_EDGE ( 'NONE', *, *, #221941, .T. ) ;
#29179=CARTESIAN_POINT ( 'NONE',  ( -20.00857864376270001, 11.56851667937982775, -211.1200010790121553 ) ) ;
#29211=VERTEX_POINT ( 'NONE', #100725 ) ;
#29245=DIRECTION ( 'NONE',  ( 1.000000000000000000, 0.000000000000000000, 0.000000000000000000 ) ) ;
#29256=CARTESIAN_POINT ( 'NONE',  ( -18.59999999999999787, 7.783179459866048866, -245.3643104511423303 ) ) ;
#29261=FACE_OUTER_BOUND ( 'NONE', #86386, .T. ) ;
#29264=VECTOR ( 'NONE', #10301, 1000.000000000000000 ) ;
#29274=VERTEX_POINT ( 'NONE', #219411 ) ;
#29280=CARTESIAN_POINT ( 'NONE',  ( -22.39999999999999858, 11.38316329224760359, -198.5208684056144079 ) ) ;
#29296=DIRECTION ( 'NONE',  ( -1.000000000000000000, 0.000000000000000000, -0.000000000000000000 ) ) ;
#29344=CARTESIAN_POINT ( 'NONE',  ( -18.49346865148328334, -7.697768582032982643, -210.0301188723689449 ) ) ;
#29354=DIRECTION ( 'NONE',  ( 0.000000000000000000, -0.2128009952263320570, 0.9770955615653377224 ) ) ;
#29396=VERTEX_POINT ( 'NONE', #130592 ) ;
#29405=FACE_OUTER_BOUND ( 'NONE', #253061, .T. ) ;
#29423=EDGE_LOOP ( 'NONE', ( #127578, #97029, #158222, #82014 ) ) ;
#29437=CARTESIAN_POINT ( 'NONE',  ( -18.50000000000000000, 7.128833340094563376, -233.7327013124401276 ) ) ;
#29439=AXIS2_PLACEMENT_3D ( 'NONE', #72778, #248825, #152308 ) ;
#29503=CYLINDRICAL_SURFACE ( 'NONE', #46782, 0.1000000000000055844 ) ;
#29513=FACE_OUTER_BOUND ( 'NONE', #198370, .T. ) ;
#29533=CIRCLE ( 'NONE', #208589, 0.1000000000000001305 ) ;
#29544=EDGE_LOOP ( 'NONE', ( #45075, #157520, #195825, #99268 ) ) ;
#29584=DIRECTION ( 'NONE',  ( 0.000000000000000000, -0.2128009952263403282, 0.9770955615653358350 ) ) ;
#29589=DIRECTION ( 'NONE',  ( 1.000000000000000000, -0.000000000000000000, -0.000000000000000000 ) ) ;
#29591=EDGE_LOOP ( 'NONE', ( #36885, #84732, #187892, #249763 ) ) ;
#29596=ORIENTED_EDGE ( 'NONE', *, *, #122142, .T. ) ;
#29617=ORIENTED_EDGE ( 'NONE', *, *, #74160, .F. ) ;
#29668=CARTESIAN_POINT ( 'NONE',  ( 20.84999999999999432, 14.80545736607782814, -235.9842437978701639 ) ) ;
#29690=ORIENTED_EDGE ( 'NONE', *, *, #207197, .T. ) ;
#29694=ADVANCED_FACE ( 'NONE', ( #203423 ), #193291, .T. ) ;
#29699=ORIENTED_EDGE ( 'NONE', *, *, #24016, .T. ) ;
#29700=ORIENTED_EDGE ( 'NONE', *, *, #77195, .F. ) ;
#29705=DIRECTION ( 'NONE',  ( 0.000000000000000000, 0.2128009952263601456, -0.9770955615653316162 ) ) ;
#29746=EDGE_CURVE ( 'NONE', #184568, #91428, #122371, .T. ) ;
#29761=VERTEX_POINT ( 'NONE', #170763 ) ;
#29772=VECTOR ( 'NONE', #89532, 1000.000000000000227 ) ;
#29841=CARTESIAN_POINT ( 'NONE',  ( 21.05000000000000071, -1.476031472317220317, -194.6925868278244991 ) ) ;
#29859=DIRECTION ( 'NONE',  ( 0.000000000000000000, 0.2128009952263403282, -0.9770955615653358350 ) ) ;
#29876=DIRECTION ( 'NONE',  ( 0.000000000000000000, 0.2128009952263588411, -0.9770955615653318382 ) ) ;
#29947=CARTESIAN_POINT ( 'NONE',  ( 22.59999999999999787, 11.36146383068193444, -198.4232501820394816 ) ) ;
#29958=AXIS2_PLACEMENT_3D ( 'NONE', #85186, #228606, #207767 ) ;
#29982=CARTESIAN_POINT ( 'NONE',  ( -21.05000000000000071, -1.489567864901279792, -194.6304332222954372 ) ) ;
#30002=DIRECTION ( 'NONE',  ( 0.000000000000000000, -0.9770955615653316162, -0.2128009952263604232 ) ) ;
#30022=ORIENTED_EDGE ( 'NONE', *, *, #93786, .T. ) ;
#30038=VERTEX_POINT ( 'NONE', #137971 ) ;
#30075=ORIENTED_EDGE ( 'NONE', *, *, #146764, .F. ) ;
#30090=CARTESIAN_POINT ( 'NONE',  ( 20.94999999999999929, -4.871452838297987142, -233.3782557782877518 ) ) ;
#30108=DIRECTION ( 'NONE',  ( 0.000000000000000000, 0.2128009952263403282, -0.9770955615653358350 ) ) ;
#30119=DIRECTION ( 'NONE',  ( 0.000000000000000000, 0.7397890806274315390, 0.6728388485992909951 ) ) ;
#30150=AXIS2_PLACEMENT_3D ( 'NONE', #56683, #235344, #16334 ) ;
#30173=ORIENTED_EDGE ( 'NONE', *, *, #205150, .T. ) ;
#30186=PLANE ( 'NONE',  #89742 ) ;
#30195=CARTESIAN_POINT ( 'NONE',  ( -20.85000000000000142, 7.675662554762638479, -241.7139905447625381 ) ) ;
#30203=ORIENTED_EDGE ( 'NONE', *, *, #71757, .F. ) ;
#30223=FACE_OUTER_BOUND ( 'NONE', #145252, .T. ) ;
#30255=CIRCLE ( 'NONE', #101094, 0.09999999999999939493 ) ;
#30270=CARTESIAN_POINT ( 'NONE',  ( 20.94999999999999929, 7.916168987336737572, -211.9720049928963874 ) ) ;
#30290=CARTESIAN_POINT ( 'NONE',  ( -21.44999999999999929, 11.48697431424113446, -220.1440440112397994 ) ) ;
#30298=AXIS2_PLACEMENT_3D ( 'NONE', #38882, #220069, #158837 ) ;
#30301=EDGE_LOOP ( 'NONE', ( #178910, #77394, #52090, #40940 ) ) ;
#30311=EDGE_LOOP ( 'NONE', ( #24319, #242860, #142210, #40788, #23680, #249184, #193562, #237266, #45732, #200686, #99771 ) ) ;
#30327=CARTESIAN_POINT ( 'NONE',  ( 18.49999999999999289, 16.67126802362266247, -222.8016931105129004 ) ) ;
#30353=EDGE_CURVE ( 'NONE', #131951, #218226, #230898, .T. ) ;
#30377=CARTESIAN_POINT ( 'NONE',  ( -18.59999999999999787, 13.63658454968486389, -219.6758818217417968 ) ) ;
#30401=CARTESIAN_POINT ( 'NONE',  ( -23.15000000000000213, 7.575715430069919876, -235.7846019917273281 ) ) ;
#30421=VERTEX_POINT ( 'NONE', #39892 ) ;
#30441=CARTESIAN_POINT ( 'NONE',  ( 18.50000000000000000, -0.7490476236415681832, -242.2033265267442061 ) ) ;
#30447=CARTESIAN_POINT ( 'NONE',  ( 20.99142135623731065, 16.98881331171930498, -224.4946931418895701 ) ) ;
#30450=( BOUNDED_SURFACE ( )  B_SPLINE_SURFACE ( 3, 2, ( 
 ( #18886, #254871, #76287 ),
 ( #98382, #155863, #177984 ),
 ( #235362, #56698, #103547 ),
 ( #86540, #220929, #43600 ) ),
 .UNSPECIFIED., .F., .F., .T. ) 
 B_SPLINE_SURFACE_WITH_KNOTS ( ( 4, 4 ),
 ( 3, 3 ),
 ( -8.673617379884035472E-18, 0.001979672783031532438 ),
 ( 0.000000000000000000, 1.000000000000000000 ),
 .UNSPECIFIED. ) 
 GEOMETRIC_REPRESENTATION_ITEM ( )  RATIONAL_B_SPLINE_SURFACE ( (
 ( 1.000000000000000000, 0.7103081912007066512, 1.000000000000000000),
 ( 1.000000000000000000, 0.7104998333558129042, 1.000000000000000000),
 ( 1.000000000000000000, 0.7107238315756106983, 1.000000000000000000),
 ( 1.000000000000000000, 0.7110073749539022048, 1.000000000000000000) ) ) 
 REPRESENTATION_ITEM ( '' )  SURFACE ( )  );
#30469=ORIENTED_EDGE ( 'NONE', *, *, #101630, .F. ) ;
#30484=CARTESIAN_POINT ( 'NONE',  ( 21.95218792049437795, 7.015487724139642722, -199.3707517748408122 ) ) ;
#30493=VERTEX_POINT ( 'NONE', #49815 ) ;
#30500=DIRECTION ( 'NONE',  ( -1.000000000000000000, -2.885090398161910739E-16, -6.283419270304611573E-17 ) ) ;
#30513=CIRCLE ( 'NONE', #5515, 0.09999999999999939493 ) ;
#30548=ADVANCED_FACE ( 'NONE', ( #191931 ), #210234, .F. ) ;
#30566=CYLINDRICAL_SURFACE ( 'NONE', #10357, 7.900000000000007461 ) ;
#30572=ORIENTED_EDGE ( 'NONE', *, *, #221556, .F. ) ;
#30582=ORIENTED_EDGE ( 'NONE', *, *, #89279, .T. ) ;
#30590=VECTOR ( 'NONE', #216251, 1000.000000000000000 ) ;
#30595=ORIENTED_EDGE ( 'NONE', *, *, #40751, .T. ) ;
#30614=VECTOR ( 'NONE', #28132, 1000.000000000000227 ) ;
#30631=ORIENTED_EDGE ( 'NONE', *, *, #79395, .F. ) ;
#30635=EDGE_CURVE ( 'NONE', #159106, #163761, #106141, .T. ) ;
#30642=VECTOR ( 'NONE', #83658, 1000.000000000000000 ) ;
#30643=DIRECTION ( 'NONE',  ( 0.000000000000000000, -0.9770955615653316162, -0.2128009952263604232 ) ) ;
#30672=CIRCLE ( 'NONE', #63970, 0.5000000000000005551 ) ;
#30673=CARTESIAN_POINT ( 'NONE',  ( 18.59999999999999076, 14.49677803128281184, -219.5908849880255502 ) ) ;
#30677=CARTESIAN_POINT ( 'NONE',  ( -23.15000000000000213, -3.642792592896924919, -226.5668142904084164 ) ) ;
#30697=CIRCLE ( 'NONE', #22321, 11.80000000000000249 ) ;
#30707=EDGE_CURVE ( 'NONE', #154129, #29761, #131100, .T. ) ;
#30718=ORIENTED_EDGE ( 'NONE', *, *, #145545, .F. ) ;
#30751=DIRECTION ( 'NONE',  ( -1.000000000000000000, 0.000000000000000000, 0.000000000000000000 ) ) ;
#30801=CARTESIAN_POINT ( 'NONE',  ( -21.59142135623730852, 10.29829244934489552, -211.3966423728064115 ) ) ;
#30802=DIRECTION ( 'NONE',  ( 1.000000000000000000, 0.000000000000000000, 0.000000000000000000 ) ) ;
#30858=CIRCLE ( 'NONE', #122425, 0.1000000000000054040 ) ;
#30873=LINE ( 'NONE', #7412, #93690 ) ;
#30905=AXIS2_PLACEMENT_3D ( 'NONE', #78619, #181604, #102017 ) ;
#30907=VECTOR ( 'NONE', #171449, 1000.000000000000227 ) ;
#30921=CARTESIAN_POINT ( 'NONE',  ( 21.14999999999999858, -2.576749817950531707, -189.6385361693310756 ) ) ;
#30925=VERTEX_POINT ( 'NONE', #80447 ) ;
#30931=CARTESIAN_POINT ( 'NONE',  ( -20.94999999999999929, 0.6656436123793473270, -212.6810495496487476 ) ) ;
#30937=VERTEX_POINT ( 'NONE', #160053 ) ;
#30977=VECTOR ( 'NONE', #151629, 1000.000000000000000 ) ;
#30981=CARTESIAN_POINT ( 'NONE',  ( 21.14999999999999858, 13.96869538424788715, -210.3925794786331949 ) ) ;
#31015=EDGE_LOOP ( 'NONE', ( #186683, #148550, #155008, #251521 ) ) ;
#31033=ORIENTED_EDGE ( 'NONE', *, *, #175307, .F. ) ;
#31038=AXIS2_PLACEMENT_3D ( 'NONE', #114373, #190062, #11436 ) ;
#31057=AXIS2_PLACEMENT_3D ( 'NONE', #57712, #19903, #99399 ) ;
#31067=DIRECTION ( 'NONE',  ( -1.000000000000000000, 0.000000000000000000, 0.000000000000000000 ) ) ;
#31094=DIRECTION ( 'NONE',  ( 1.000000000000000000, 0.000000000000000000, 0.000000000000000000 ) ) ;
#31112=DIRECTION ( 'NONE',  ( 0.000000000000000000, 0.2128009952263604232, -0.9770955615653316162 ) ) ;
#31116=ORIENTED_EDGE ( 'NONE', *, *, #128327, .T. ) ;
#31174=CARTESIAN_POINT ( 'NONE',  ( 20.95512820512820440, 10.49413282287806481, -207.4737445703522383 ) ) ;
#31179=ORIENTED_EDGE ( 'NONE', *, *, #62238, .T. ) ;
#31189=EDGE_CURVE ( 'NONE', #209650, #102873, #80997, .T. ) ;
#31191=EDGE_CURVE ( 'NONE', #85747, #157859, #147654, .T. ) ;
#31194=CARTESIAN_POINT ( 'NONE',  ( -22.59999999999999787, 11.45898712536580177, -198.4011321578509808 ) ) ;
#31210=( BOUNDED_SURFACE ( )  B_SPLINE_SURFACE ( 3, 2, ( 
 ( #103288, #168475, #164582 ),
 ( #124176, #146280, #223241 ),
 ( #44629, #108450, #5464 ),
 ( #207564, #105852, #185419 ) ),
 .UNSPECIFIED., .F., .F., .F. ) 
 B_SPLINE_SURFACE_WITH_KNOTS ( ( 4, 4 ),
 ( 3, 3 ),
 ( 0.04058434257139457990, 0.04256401539001584966 ),
 ( 0.000000000000000000, 1.000000000000000000 ),
 .UNSPECIFIED. ) 
 GEOMETRIC_REPRESENTATION_ITEM ( )  RATIONAL_B_SPLINE_SURFACE ( (
 ( 1.000000000000000000, 0.7103081912008579746, 1.000000000000000000),
 ( 1.000000000000000000, 0.7104998333553130818, 1.000000000000000000),
 ( 1.000000000000000000, 0.7107238315756889691, 1.000000000000000000),
 ( 1.000000000000000000, 0.7110073749539658206, 1.000000000000000000) ) ) 
 REPRESENTATION_ITEM ( '' )  SURFACE ( )  );
#31212=CARTESIAN_POINT ( 'NONE',  ( -22.47886152344871036, -2.442487176688612482, -189.6088675674811839 ) ) ;
#31235=ADVANCED_FACE ( 'NONE', ( #54813 ), #230924, .F. ) ;
#31271=VERTEX_POINT ( 'NONE', #131798 ) ;
#31272=CARTESIAN_POINT ( 'NONE',  ( -20.64999999999999858, 9.614325556249161409, -211.5456030694648746 ) ) ;
#31273=ORIENTED_EDGE ( 'NONE', *, *, #3562, .F. ) ;
#31276=ORIENTED_EDGE ( 'NONE', *, *, #197415, .F. ) ;
#31282=DIRECTION ( 'NONE',  ( -1.000000000000000000, 0.000000000000000000, 0.000000000000000000 ) ) ;
#31299=VERTEX_POINT ( 'NONE', #136932 ) ;
#31305=DIRECTION ( 'NONE',  ( -0.000000000000000000, 0.9525900758537790836, -0.3042567129660269099 ) ) ;
#31332=ORIENTED_EDGE ( 'NONE', *, *, #206914, .T. ) ;
#31348=EDGE_LOOP ( 'NONE', ( #214771, #182410, #101520, #256633 ) ) ;
#31352=CARTESIAN_POINT ( 'NONE',  ( -20.64999999999999858, 6.268811756569107274, -220.3853799378769622 ) ) ;
#31407=DIRECTION ( 'NONE',  ( 0.000000000000000000, 0.2128009952263604510, -0.9770955615653315052 ) ) ;
#31437=CARTESIAN_POINT ( 'NONE',  ( 22.49999999999999645, -2.392305309346458575, -189.5981695081429450 ) ) ;
#31482=ORIENTED_EDGE ( 'NONE', *, *, #148751, .F. ) ;
#31508=EDGE_CURVE ( 'NONE', #174819, #151535, #50758, .T. ) ;
#31523=CARTESIAN_POINT ( 'NONE',  ( -23.25000000000000000, 8.809961202382810441, -241.4517562488062481 ) ) ;
#31547=TOROIDAL_SURFACE ( 'NONE', #243878, 4.149999999999999467, 0.1000000000000000056 ) ;
#31550=FACE_OUTER_BOUND ( 'NONE', #68171, .T. ) ;
#31555=CARTESIAN_POINT ( 'NONE',  ( 22.50000000000000000, 7.551210502620180343, -199.2530827308407027 ) ) ;
#31556=AXIS2_PLACEMENT_3D ( 'NONE', #186657, #228343, #210068 ) ;
#31563=VERTEX_POINT ( 'NONE', #71545 ) ;
#31571=ORIENTED_EDGE ( 'NONE', *, *, #195381, .T. ) ;
#31653=ORIENTED_EDGE ( 'NONE', *, *, #74838, .T. ) ;
#31658=ORIENTED_EDGE ( 'NONE', *, *, #132024, .T. ) ;
#31664=DIRECTION ( 'NONE',  ( 0.000000000000000000, 0.2128009952263602012, -0.9770955615653315052 ) ) ;
#31686=ORIENTED_EDGE ( 'NONE', *, *, #16340, .F. ) ;
#31696=VERTEX_POINT ( 'NONE', #46180 ) ;
#31743=FACE_OUTER_BOUND ( 'NONE', #59184, .T. ) ;
#31763=DIRECTION ( 'NONE',  ( -1.000000000000000000, 0.000000000000000000, 0.000000000000000000 ) ) ;
#31769=DIRECTION ( 'NONE',  ( 1.000000000000000000, 0.000000000000000000, 0.000000000000000000 ) ) ;
#31784=CARTESIAN_POINT ( 'NONE',  ( -21.17356465864818560, 6.254644016943381679, -199.5365753680107161 ) ) ;
#31785=CARTESIAN_POINT ( 'NONE',  ( 22.37643362114956247, 7.430040941609745708, -199.2804123294420720 ) ) ;
#31788=DIRECTION ( 'NONE',  ( -1.000000000000000000, 0.000000000000000000, -0.000000000000000000 ) ) ;
#31811=CARTESIAN_POINT ( 'NONE',  ( -20.54999999999999716, 7.533155231024652565, -235.5891828794142384 ) ) ;
#31855=CIRCLE ( 'NONE', #177616, 11.79999999999999005 ) ;
#31856=VECTOR ( 'NONE', #91872, 1000.000000000000227 ) ;
#31865=ORIENTED_EDGE ( 'NONE', *, *, #85173, .F. ) ;
#31891=ORIENTED_EDGE ( 'NONE', *, *, #239331, .T. ) ;
#31896=ORIENTED_EDGE ( 'NONE', *, *, #108187, .T. ) ;
#31908=DIRECTION ( 'NONE',  ( 0.000000000000000000, 0.9770955615653262871, 0.2128009952263842652 ) ) ;
#31919=EDGE_CURVE ( 'NONE', #148888, #59550, #12225, .T. ) ;
#31926=DIRECTION ( 'NONE',  ( 1.000000000000000000, 0.000000000000000000, 0.000000000000000000 ) ) ;
#31952=ORIENTED_EDGE ( 'NONE', *, *, #65647, .F. ) ;
#31957=EDGE_CURVE ( 'NONE', #204482, #96897, #14778, .T. ) ;
#31964=ORIENTED_EDGE ( 'NONE', *, *, #63763, .F. ) ;
#31969=CARTESIAN_POINT ( 'NONE',  ( 21.07928932188134397, 6.162520550847347955, -199.5566553493351307 ) ) ;
#31979=ORIENTED_EDGE ( 'NONE', *, *, #249299, .F. ) ;
#31982=CARTESIAN_POINT ( 'NONE',  ( -20.00857864376270001, 13.44116543737180081, -219.7184420207870801 ) ) ;
#31999=LINE ( 'NONE', #1814, #74005 ) ;
#32018=ADVANCED_FACE ( 'NONE', ( #158179 ), #98122, .T. ) ;
#32029=ORIENTED_EDGE ( 'NONE', *, *, #219462, .F. ) ;
#32092=CARTESIAN_POINT ( 'NONE',  ( -23.15000000000000213, -1.109497582084245426, -218.6091262806550048 ) ) ;
#32102=ADVANCED_FACE ( 'NONE', ( #83685 ), #185398, .T. ) ;
#32108=ORIENTED_EDGE ( 'NONE', *, *, #62958, .F. ) ;
#32127=AXIS2_PLACEMENT_3D ( 'NONE', #62412, #139351, #218895 ) ;
#32135=ORIENTED_EDGE ( 'NONE', *, *, #185820, .T. ) ;
#32161=VERTEX_POINT ( 'NONE', #203679 ) ;
#32167=DIRECTION ( 'NONE',  ( -0.000000000000000000, -0.2128009952263603677, 0.9770955615653313941 ) ) ;
#32177=ORIENTED_EDGE ( 'NONE', *, *, #139169, .T. ) ;
#32184=EDGE_LOOP ( 'NONE', ( #151388, #243742, #29617, #134794 ) ) ;
#32205=ORIENTED_EDGE ( 'NONE', *, *, #202327, .F. ) ;
#32207=ORIENTED_EDGE ( 'NONE', *, *, #93935, .F. ) ;
#32208=AXIS2_PLACEMENT_3D ( 'NONE', #26920, #105102, #148126 ) ;
#32218=EDGE_LOOP ( 'NONE', ( #4839, #237343, #4471, #251299, #46869, #177459 ) ) ;
#32224=EDGE_CURVE ( 'NONE', #92979, #71034, #127999, .T. ) ;
#32254=DIRECTION ( 'NONE',  ( 0.000000000000000000, 0.2128009952263485993, -0.9770955615653341697 ) ) ;
#32273=EDGE_LOOP ( 'NONE', ( #57288, #21739, #78278, #189043, #67139 ) ) ;
#32276=CARTESIAN_POINT ( 'NONE',  ( -22.39999999999999858, -1.560176095955062348, -193.3663837337744837 ) ) ;
#32282=EDGE_CURVE ( 'NONE', #70740, #132220, #22958, .T. ) ;
#32295=CARTESIAN_POINT ( 'NONE',  ( -21.45000000000000284, 12.05403912736948158, -220.1228874760914209 ) ) ;
#32299=AXIS2_PLACEMENT_3D ( 'NONE', #1691, #102064, #81217 ) ;
#32379=DIRECTION ( 'NONE',  ( -1.000000000000000000, -0.000000000000000000, -0.000000000000000000 ) ) ;
#32398=ORIENTED_EDGE ( 'NONE', *, *, #86124, .T. ) ;
#32404=DIRECTION ( 'NONE',  ( 0.000000000000000000, -0.2128009952263603677, 0.9770955615653313941 ) ) ;
#32405=DIRECTION ( 'NONE',  ( 0.000000000000000000, 0.2128009952263601179, -0.9770955615653315052 ) ) ;
#32418=EDGE_LOOP ( 'NONE', ( #191249, #103411, #91368, #128069 ) ) ;
#32435=CARTESIAN_POINT ( 'NONE',  ( 18.49999999999999645, 2.859758780633683273, -208.6670499591424459 ) ) ;
#32436=EDGE_CURVE ( 'NONE', #75618, #131400, #148191, .T. ) ;
#32442=ORIENTED_EDGE ( 'NONE', *, *, #107189, .T. ) ;
#32450=DIRECTION ( 'NONE',  ( 1.000000000000000000, -0.000000000000000000, -0.000000000000000000 ) ) ;
#32486=AXIS2_PLACEMENT_3D ( 'NONE', #150575, #214389, #172748 ) ;
#32489=CARTESIAN_POINT ( 'NONE',  ( -22.50000000000000000, -2.381330705637465961, -189.5959759702857923 ) ) ;
#32494=AXIS2_PLACEMENT_3D ( 'NONE', #26780, #123289, #185822 ) ;
#32547=EDGE_LOOP ( 'NONE', ( #28162, #67262 ) ) ;
#32553=EDGE_CURVE ( 'NONE', #97608, #237457, #206467, .T. ) ;
#32582=AXIS2_PLACEMENT_3D ( 'NONE', #158686, #175664, #217319 ) ;
#32584=ORIENTED_EDGE ( 'NONE', *, *, #176332, .T. ) ;
#32605=DIRECTION ( 'NONE',  ( 1.000000000000000000, 0.000000000000000000, 0.000000000000000000 ) ) ;
#32627=AXIS2_PLACEMENT_3D ( 'NONE', #112578, #105129, #113846 ) ;
#32650=LINE ( 'NONE', #194279, #108575 ) ;
#32654=AXIS2_PLACEMENT_3D ( 'NONE', #30921, #186111, #227793 ) ;
#32668=DIRECTION ( 'NONE',  ( -0.7071067811865474617, -0.6909108974501236844, -0.1504730267678055788 ) ) ;
#32672=VECTOR ( 'NONE', #43840, 1000.000000000000000 ) ;
#32735=VERTEX_POINT ( 'NONE', #136648 ) ;
#32768=LINE ( 'NONE', #155279, #161725 ) ;
#32779=VERTEX_POINT ( 'NONE', #77957 ) ;
#32783=EDGE_LOOP ( 'NONE', ( #167539, #126184, #71852, #127015 ) ) ;
#32818=COLOUR_RGB ( '', 0.09019608, 0.27058824, 0.51372549) ;
#32824=ORIENTED_EDGE ( 'NONE', *, *, #85206, .F. ) ;
#32830=CARTESIAN_POINT ( 'NONE',  ( 18.58143601961950608, 15.46352952504945932, -222.9623815432983918 ) ) ;
#32837=CARTESIAN_POINT ( 'NONE',  ( 20.95512820512820440, 12.01161663143393632, -206.2285874551107554 ) ) ;
#32862=EDGE_CURVE ( 'NONE', #250321, #233023, #2629, .T. ) ;
#32870=EDGE_LOOP ( 'NONE', ( #234709, #193177, #113873, #14314 ) ) ;
#32881=DIRECTION ( 'NONE',  ( 0.000000000000000000, 0.2128009952263601456, -0.9770955615653316162 ) ) ;
#32890=CARTESIAN_POINT ( 'NONE',  ( 18.56579813702274961, 18.41141989892753372, -236.9935361838138022 ) ) ;
#32893=VERTEX_POINT ( 'NONE', #139202 ) ;
#32973=CARTESIAN_POINT ( 'NONE',  ( -23.25000000000000000, 14.06640494040441602, -210.3712993791105532 ) ) ;
#32997=ORIENTED_EDGE ( 'NONE', *, *, #32282, .F. ) ;
#33033=AXIS2_PLACEMENT_3D ( 'NONE', #93585, #12790, #235648 ) ;
#33036=DIRECTION ( 'NONE',  ( 0.000000000000000000, 0.2128009952263604232, -0.9770955615653315052 ) ) ;
#33042=DIRECTION ( 'NONE',  ( -1.000000000000000000, 0.000000000000000000, 0.000000000000000000 ) ) ;
#33056=DIRECTION ( 'NONE',  ( 0.000000000000000000, 0.2128009952263601456, -0.9770955615653316162 ) ) ;
#33063=CARTESIAN_POINT ( 'NONE',  ( 18.39999999999999858, -7.792936614629562442, -209.8606550935952271 ) ) ;
#33115=CARTESIAN_POINT ( 'NONE',  ( -18.59999999999999787, 11.66622623553636018, -211.0987209794895421 ) ) ;
#33118=CIRCLE ( 'NONE', #45542, 0.1000000000000054040 ) ;
#33122=VECTOR ( 'NONE', #232425, 1000.000000000000227 ) ;
#33135=LINE ( 'NONE', #16118, #58775 ) ;
#33140=ORIENTED_EDGE ( 'NONE', *, *, #40598, .T. ) ;
#33181=DIRECTION ( 'NONE',  ( 0.000000000000000000, 0.2128009952263601456, -0.9770955615653316162 ) ) ;
#33187=CARTESIAN_POINT ( 'NONE',  ( 19.97071067811864609, 16.71907901384503603, -222.6889362516795927 ) ) ;
#33206=ORIENTED_EDGE ( 'NONE', *, *, #204395, .F. ) ;
#33249=DIRECTION ( 'NONE',  ( 1.000000000000000000, 0.000000000000000000, 0.000000000000000000 ) ) ;
#33260=EDGE_CURVE ( 'NONE', #155898, #10002, #17676, .T. ) ;
#33272=FACE_OUTER_BOUND ( 'NONE', #62016, .T. ) ;
#33293=EDGE_CURVE ( 'NONE', #7989, #14516, #61077, .T. ) ;
#33315=EDGE_CURVE ( 'NONE', #2973, #9452, #206830, .T. ) ;
#33324=CIRCLE ( 'NONE', #16735, 0.1000000000000055844 ) ;
#33352=DIRECTION ( 'NONE',  ( 0.000000000000000000, 0.2128009952263485993, -0.9770955615653341697 ) ) ;
#33373=DIRECTION ( 'NONE',  ( -1.000000000000000000, -0.000000000000000000, -0.000000000000000000 ) ) ;
#33382=ORIENTED_EDGE ( 'NONE', *, *, #253642, .T. ) ;
#33390=CARTESIAN_POINT ( 'NONE',  ( 20.94999999999999574, 11.97453674493551645, -206.0596400812808611 ) ) ;
#33495=EDGE_LOOP ( 'NONE', ( #142533, #216917, #155545, #8295 ) ) ;
#33501=ORIENTED_EDGE ( 'NONE', *, *, #168610, .F. ) ;
#33522=ORIENTED_EDGE ( 'NONE', *, *, #234125, .F. ) ;
#33529=DIRECTION ( 'NONE',  ( 0.000000000000000000, -0.2128009952263612281, 0.9770955615653312831 ) ) ;
#33554=FACE_OUTER_BOUND ( 'NONE', #230728, .T. ) ;
#33573=CARTESIAN_POINT ( 'NONE',  ( -20.94999999999999929, 0.4879293624014888198, -209.1697915983179428 ) ) ;
#33592=AXIS2_PLACEMENT_3D ( 'NONE', #166729, #220267, #161584 ) ;
#33605=SPHERICAL_SURFACE ( 'NONE', #252323, 0.1000000000000000056 ) ;
#33661=B_SPLINE_CURVE_WITH_KNOTS ( 'NONE', 3,
 ( #174518, #38806, #118346, #214859, #157495, #196575, #175760, #36253, #197858, #57039 ),
 .UNSPECIFIED., .F., .F.,
 ( 4, 2, 2, 2, 4 ),
 ( 0.000000000000000000, 0.0001584437871624776975, 0.0002376656807437485031, 0.0002772766275343839060, 0.0003168875743250193088 ),
 .UNSPECIFIED. ) ;
#33670=DIRECTION ( 'NONE',  ( 0.000000000000000000, -0.3634403228828271271, 0.9316174814283092465 ) ) ;
#33677=CARTESIAN_POINT ( 'NONE',  ( -20.54999999999999716, -6.438379425586759908, -212.1495692908769684 ) ) ;
#33679=DIRECTION ( 'NONE',  ( 0.7071067811865302533, -0.6909108974501196876, -0.1504730267679053324 ) ) ;
#33697=DIRECTION ( 'NONE',  ( -1.000000000000000000, 0.000000000000000000, -0.000000000000000000 ) ) ;
#33726=VECTOR ( 'NONE', #35967, 1000.000000000000000 ) ;
#33728=EDGE_CURVE ( 'NONE', #92979, #125420, #61267, .T. ) ;
#33730=DIRECTION ( 'NONE',  ( 1.000000000000000000, 0.000000000000000000, 0.000000000000000000 ) ) ;
#33732=CARTESIAN_POINT ( 'NONE',  ( 21.04999999999999716, 6.164532172064068227, -199.6789591974932421 ) ) ;
#33744=FACE_OUTER_BOUND ( 'NONE', #90965, .T. ) ;
#33748=CARTESIAN_POINT ( 'NONE',  ( 20.12500000000000000, 10.82572568129133295, -207.2016591585088463 ) ) ;
#33756=CARTESIAN_POINT ( 'NONE',  ( 21.05000000000000071, -4.714262876194486473, -233.3440214805475819 ) ) ;
#33766=CARTESIAN_POINT ( 'NONE',  ( 23.14999999999999858, 9.290509600414956992, -221.0404682250134840 ) ) ;
#33787=CARTESIAN_POINT ( 'NONE',  ( -20.94999999999999929, 7.128833340094563376, -233.7327013124401276 ) ) ;
#33811=EDGE_CURVE ( 'NONE', #126073, #143815, #190283, .T. ) ;
#33822=DIRECTION ( 'NONE',  ( 0.000000000000000000, 0.3427706569149635007, -0.9394191166662961834 ) ) ;
#33858=ORIENTED_EDGE ( 'NONE', *, *, #102321, .T. ) ;
#33868=CARTESIAN_POINT ( 'NONE',  ( -18.49513951962167724, -0.6503453050635661370, -242.3638832198185469 ) ) ;
#33871=DIRECTION ( 'NONE',  ( 2.952720810173287633E-16, -0.9770955615653312831, -0.2128009952263610616 ) ) ;
#33912=ADVANCED_FACE ( 'NONE', ( #235798 ), #252789, .T. ) ;
#33924=EDGE_LOOP ( 'NONE', ( #228874, #149607, #141171, #49926 ) ) ;
#33925=VECTOR ( 'NONE', #225444, 1000.000000000000227 ) ;
#33950=ORIENTED_EDGE ( 'NONE', *, *, #66202, .F. ) ;
#33965=CARTESIAN_POINT ( 'NONE',  ( -20.12071067811865888, 11.73531732528137006, -211.0836736768127366 ) ) ;
#33973=DIRECTION ( 'NONE',  ( 0.000000000000000000, -0.2128009952263604232, 0.9770955615653316162 ) ) ;
#34060=DIRECTION ( 'NONE',  ( -1.000000000000000000, -1.794895427898103559E-16, -3.909090864890002444E-17 ) ) ;
#34069=DIRECTION ( 'NONE',  ( 0.000000000000000000, -0.8149014228131966631, 0.5795995782408988051 ) ) ;
#34094=EDGE_LOOP ( 'NONE', ( #189104, #45388, #173974, #184437 ) ) ;
#34095=DIRECTION ( 'NONE',  ( 0.000000000000000000, -0.9770955615653320603, -0.2128009952263585081 ) ) ;
#34111=CARTESIAN_POINT ( 'NONE',  ( 18.49999999999999289, 15.40600705476365029, -222.9910675435765199 ) ) ;
#34115=ORIENTED_EDGE ( 'NONE', *, *, #53062, .T. ) ;
#34127=DIRECTION ( 'NONE',  ( 2.342056488767300981E-15, 0.07893460099012014619, -0.9968797965484758050 ) ) ;
#34155=VERTEX_POINT ( 'NONE', #187397 ) ;
#34159=EDGE_LOOP ( 'NONE', ( #48577, #24874 ) ) ;
#34166=CARTESIAN_POINT ( 'NONE',  ( 18.49999999999999289, 18.34711819382569686, -236.8747682978092541 ) ) ;
#34173=VERTEX_POINT ( 'NONE', #189955 ) ;
#34233=CARTESIAN_POINT ( 'NONE',  ( -18.59999999999999787, 8.809961202382808665, -241.4517562488062481 ) ) ;
#34252=CARTESIAN_POINT ( 'NONE',  ( 18.39999999999999858, -0.9152171842607033092, -242.2974985173726452 ) ) ;
#34280=CARTESIAN_POINT ( 'NONE',  ( -20.85000000000000142, 7.783179459866048866, -245.3643104511423019 ) ) ;
#34311=CARTESIAN_POINT ( 'NONE',  ( 20.95512820512820440, 14.90253654416821760, -219.5025151102366578 ) ) ;
#34325=DIRECTION ( 'NONE',  ( 0.000000000000000000, 0.2128009952263403282, -0.9770955615653358350 ) ) ;
#34340=EDGE_CURVE ( 'NONE', #17833, #36199, #72589, .T. ) ;
#34346=CARTESIAN_POINT ( 'NONE',  ( 22.32929514600007792, 7.383979495903388646, -199.2904498502753938 ) ) ;
#34348=ORIENTED_EDGE ( 'NONE', *, *, #161821, .T. ) ;
#34355=DIRECTION ( 'NONE',  ( 0.000000000000000000, 0.2128009952263485993, -0.9770955615653341697 ) ) ;
#34358=AXIS2_PLACEMENT_3D ( 'NONE', #96554, #133143, #174892 ) ;
#34425=AXIS2_PLACEMENT_3D ( 'NONE', #115976, #15612, #112134 ) ;
#34440=CARTESIAN_POINT ( 'NONE',  ( -20.94999999999999929, -10.47749788991998088, -206.4278944321438587 ) ) ;
#34462=LINE ( 'NONE', #133525, #3643 ) ;
#34477=VERTEX_POINT ( 'NONE', #155561 ) ;
#34480=CARTESIAN_POINT ( 'NONE',  ( -23.25000000000000000, 7.882824859404637508, -245.3558965132535832 ) ) ;
#34487=EDGE_LOOP ( 'NONE', ( #101406, #141936, #4254, #50526 ) ) ;
#34492=CARTESIAN_POINT ( 'NONE',  ( 21.14999999999999503, -10.86374996222470379, -206.3339888224507206 ) ) ;
#34495=CARTESIAN_POINT ( 'NONE',  ( -22.59999999999999787, -2.381330705637465961, -189.5959759702857923 ) ) ;
#34500=B_SPLINE_CURVE_WITH_KNOTS ( 'NONE', 3,
 ( #67021, #146532, #31784, #69605, #129570, #153019, #214242, #212955, #149147, #210399 ),
 .UNSPECIFIED., .F., .F.,
 ( 4, 3, 3, 4 ),
 ( 0.000000000000000000, 0.0002000000000008569359, 0.001000000000082977483, 0.001967863649483338889 ),
 .UNSPECIFIED. ) ;
#34510=DIRECTION ( 'NONE',  ( 0.000000000000000000, 0.2128009952263603677, -0.9770955615653313941 ) ) ;
#34515=DIRECTION ( 'NONE',  ( -1.000000000000000000, 0.000000000000000000, 0.000000000000000000 ) ) ;
#34516=CARTESIAN_POINT ( 'NONE',  ( 21.05000000000000071, 0.6656436123793473270, -212.6810495496487476 ) ) ;
#34535=VECTOR ( 'NONE', #129825, 1000.000000000000114 ) ;
#34556=ORIENTED_EDGE ( 'NONE', *, *, #140979, .T. ) ;
#34568=ORIENTED_EDGE ( 'NONE', *, *, #84295, .F. ) ;
#34592=EDGE_CURVE ( 'NONE', #401, #203779, #221887, .T. ) ;
#34603=EDGE_CURVE ( 'NONE', #2617, #252276, #124116, .T. ) ;
#34611=CARTESIAN_POINT ( 'NONE',  ( -20.64999999999999858, 11.48697431424113446, -220.1440440112397994 ) ) ;
#34614=CARTESIAN_POINT ( 'NONE',  ( 23.15000000000000213, -11.38316329222462464, -203.4791315943886048 ) ) ;
#34635=CARTESIAN_POINT ( 'NONE',  ( 18.39999999999999858, -0.7490476236415681832, -242.2033265267442061 ) ) ;
#34642=LINE ( 'NONE', #213242, #256804 ) ;
#34693=EDGE_CURVE ( 'NONE', #193316, #14866, #45238, .T. ) ;
#34754=VECTOR ( 'NONE', #11754, 1000.000000000000000 ) ;
#34802=ORIENTED_EDGE ( 'NONE', *, *, #121067, .T. ) ;
#34812=TOROIDAL_SURFACE ( 'NONE', #242887, 0.6000000000000009770, 0.1000000000000000056 ) ;
#34824=ORIENTED_EDGE ( 'NONE', *, *, #69943, .F. ) ;
#34839=CARTESIAN_POINT ( 'NONE',  ( 21.05000000000000071, 11.77895973109482952, -206.1023438919106070 ) ) ;
#34870=EDGE_CURVE ( 'NONE', #147215, #170466, #148003, .T. ) ;
#34884=CYLINDRICAL_SURFACE ( 'NONE', #115823, 0.1000000000000055844 ) ;
#34907=CARTESIAN_POINT ( 'NONE',  ( 20.88420186297724612, 18.41141989892752662, -236.9935361838138022 ) ) ;
#34912=FACE_OUTER_BOUND ( 'NONE', #186959, .T. ) ;
#34920=LINE ( 'NONE', #113136, #2997 ) ;
#34923=AXIS2_PLACEMENT_3D ( 'NONE', #254280, #130492, #193059 ) ;
#34966=VECTOR ( 'NONE', #207173, 1000.000000000000227 ) ;
#34976=ORIENTED_EDGE ( 'NONE', *, *, #192204, .F. ) ;
#34984=LINE ( 'NONE', #98720, #247287 ) ;
#35011=CIRCLE ( 'NONE', #147399, 0.5000000000000007772 ) ;
#35039=DIRECTION ( 'NONE',  ( 3.469446951953728416E-14, -0.9525900758537746427, 0.3042567129660413983 ) ) ;
#35047=CARTESIAN_POINT ( 'NONE',  ( 21.70464131381650219, 6.932842828061961171, -199.4901007520778080 ) ) ;
#35065=CARTESIAN_POINT ( 'NONE',  ( 20.94999999999999929, 9.307299318941717914, -220.9418877738490039 ) ) ;
#35090=VECTOR ( 'NONE', #236068, 1000.000000000000000 ) ;
#35142=DIRECTION ( 'NONE',  ( -0.1538461538461493860, 0.9654630569144674324, 0.2102675597426261755 ) ) ;
#35223=DIRECTION ( 'NONE',  ( -0.000000000000000000, 0.08413937888707637147, -0.9964539953858869703 ) ) ;
#35234=DIRECTION ( 'NONE',  ( 0.000000000000000000, 0.2128009952263582305, -0.9770955615653319493 ) ) ;
#35245=AXIS2_PLACEMENT_3D ( 'NONE', #88550, #211089, #106838 ) ;
#35277=ORIENTED_EDGE ( 'NONE', *, *, #248054, .F. ) ;
#35280=VECTOR ( 'NONE', #9363, 1000.000000000000000 ) ;
#35294=DIRECTION ( 'NONE',  ( -1.000000000000000000, 0.000000000000000000, -0.000000000000000000 ) ) ;
#35320=DIRECTION ( 'NONE',  ( -0.000000000000000000, 0.2128009952263604232, -0.9770955615653316162 ) ) ;
#35380=CARTESIAN_POINT ( 'NONE',  ( -21.05000000000000071, 4.639061695946145925, -222.3006832421257286 ) ) ;
#35421=ORIENTED_EDGE ( 'NONE', *, *, #22453, .T. ) ;
#35427=ORIENTED_EDGE ( 'NONE', *, *, #63896, .F. ) ;
#35436=DIRECTION ( 'NONE',  ( 1.000000000000000000, 0.000000000000000000, 0.000000000000000000 ) ) ;
#35449=DIRECTION ( 'NONE',  ( 1.000000000000000000, 0.000000000000000000, 0.000000000000000000 ) ) ;
#35476=ORIENTED_EDGE ( 'NONE', *, *, #1312, .T. ) ;
#35513=CARTESIAN_POINT ( 'NONE',  ( 23.24999999999999289, 8.980461154494404852, -187.0187154576991304 ) ) ;
#35524=CARTESIAN_POINT ( 'NONE',  ( 23.15000000000000213, -8.874060656858233642, -215.4698323230865640 ) ) ;
#35565=EDGE_LOOP ( 'NONE', ( #2952, #50676, #220488, #252924 ) ) ;
#35574=DIRECTION ( 'NONE',  ( 1.000000000000000000, 0.000000000000000000, 0.000000000000000000 ) ) ;
#35578=EDGE_CURVE ( 'NONE', #160183, #175179, #145371, .T. ) ;
#35601=CARTESIAN_POINT ( 'NONE',  ( 22.49231231312463208, 11.37015642645466507, -198.4612171126308624 ) ) ;
#35602=DIRECTION ( 'NONE',  ( 1.000000000000000000, 0.000000000000000000, 0.000000000000000000 ) ) ;
#35614=ORIENTED_EDGE ( 'NONE', *, *, #49856, .T. ) ;
#35615=CARTESIAN_POINT ( 'NONE',  ( 18.39999999999999858, -7.817436562502981801, -209.8389866834999111 ) ) ;
#35652=ORIENTED_EDGE ( 'NONE', *, *, #19115, .F. ) ;
#35654=SPHERICAL_SURFACE ( 'NONE', #222220, 0.1000000000000000056 ) ;
#35666=CARTESIAN_POINT ( 'NONE',  ( -20.94999999999999929, 18.34743685832668803, -236.8753540304231535 ) ) ;
#35678=ORIENTED_EDGE ( 'NONE', *, *, #218113, .T. ) ;
#35691=DIRECTION ( 'NONE',  ( -1.000000000000000000, -0.000000000000000000, -0.000000000000000000 ) ) ;
#35707=ORIENTED_EDGE ( 'NONE', *, *, #35859, .T. ) ;
#35807=ORIENTED_EDGE ( 'NONE', *, *, #251507, .F. ) ;
#35809=EDGE_CURVE ( 'NONE', #27566, #19033, #200315, .T. ) ;
#35822=CARTESIAN_POINT ( 'NONE',  ( -23.25000000000000000, -0.9152171842607033092, -242.2974985173726452 ) ) ;
#35828=DIRECTION ( 'NONE',  ( 0.000000000000000000, 0.3042567129660269654, 0.9525900758537791946 ) ) ;
#35830=TOROIDAL_SURFACE ( 'NONE', #152565, 0.2000000000000000111, 0.1000000000000000056 ) ;
#35840=TOROIDAL_SURFACE ( 'NONE', #44219, 2.100000000000002309, 0.1000000000000000056 ) ;
#35859=EDGE_CURVE ( 'NONE', #37415, #208398, #255095, .T. ) ;
#35871=CARTESIAN_POINT ( 'NONE',  ( -18.44204374631835464, -0.7347539659637959408, -242.2268351530478867 ) ) ;
#35875=VERTEX_POINT ( 'NONE', #239449 ) ;
#35879=DIRECTION ( 'NONE',  ( -1.000000000000000000, -0.000000000000000000, -0.000000000000000000 ) ) ;
#35898=DIRECTION ( 'NONE',  ( 0.000000000000000000, 0.2128009952263693050, -0.9770955615653296178 ) ) ;
#35932=SPHERICAL_SURFACE ( 'NONE', #16187, 0.1000000000000000056 ) ;
#35957=CIRCLE ( 'NONE', #56574, 0.09999999999999939493 ) ;
#35961=DIRECTION ( 'NONE',  ( -1.000000000000000000, -0.000000000000000000, -0.000000000000000000 ) ) ;
#35967=DIRECTION ( 'NONE',  ( 1.000000000000000000, 0.000000000000000000, 0.000000000000000000 ) ) ;
#35968=AXIS2_PLACEMENT_3D ( 'NONE', #134204, #239417, #114656 ) ;
#35991=FACE_OUTER_BOUND ( 'NONE', #118152, .T. ) ;
#36023=ORIENTED_EDGE ( 'NONE', *, *, #212981, .F. ) ;
#36045=AXIS2_PLACEMENT_3D ( 'NONE', #171750, #13937, #132599 ) ;
#36047=ORIENTED_EDGE ( 'NONE', *, *, #209446, .F. ) ;
#36057=DIRECTION ( 'NONE',  ( 0.000000000000000000, 0.2128009952263604232, -0.9770955615653315052 ) ) ;
#36068=DIRECTION ( 'NONE',  ( 0.000000000000000000, -0.2128009952263604232, 0.9770955615653316162 ) ) ;
#36076=CARTESIAN_POINT ( 'NONE',  ( 20.94999999999999574, 0.5876173420563349792, -209.1618981382189588 ) ) ;
#36150=DIRECTION ( 'NONE',  ( 0.000000000000000000, 0.2128009952263603399, -0.9770955615653315052 ) ) ;
#36159=CARTESIAN_POINT ( 'NONE',  ( -20.94999999999999929, 1.148907358139439339E-11, -201.0000000000015064 ) ) ;
#36171=EDGE_CURVE ( 'NONE', #201031, #31563, #3713, .T. ) ;
#36180=ORIENTED_EDGE ( 'NONE', *, *, #65527, .F. ) ;
#36186=DIRECTION ( 'NONE',  ( 0.000000000000000000, 0.2128009952263485993, -0.9770955615653341697 ) ) ;
#36199=VERTEX_POINT ( 'NONE', #78754 ) ;
#36225=SPHERICAL_SURFACE ( 'NONE', #222176, 0.1000000000000000056 ) ;
#36237=CARTESIAN_POINT ( 'NONE',  ( 21.14261333020286671, 13.07706791821966696, -210.6891105688758046 ) ) ;
#36239=ORIENTED_EDGE ( 'NONE', *, *, #63547, .T. ) ;
#36247=PLANE ( 'NONE',  #57207 ) ;
#36251=DIRECTION ( 'NONE',  ( -1.000000000000000000, 0.000000000000000000, 0.000000000000000000 ) ) ;
#36253=CARTESIAN_POINT ( 'NONE',  ( 18.42555734704284731, -7.781548346777066527, -209.8995918847530788 ) ) ;
#36262=CARTESIAN_POINT ( 'NONE',  ( -21.05000000000000071, 6.277629359189121239, -229.8243190661787878 ) ) ;
#36269=CARTESIAN_POINT ( 'NONE',  ( -23.25000000000000000, 1.148907358139439339E-11, -201.0000000000015064 ) ) ;
#36303=DIRECTION ( 'NONE',  ( -1.000000000000000000, -0.000000000000000000, -0.000000000000000000 ) ) ;
#36319=ADVANCED_FACE ( 'NONE', ( #85154, #222106 ), #43509, .T. ) ;
#36334=CIRCLE ( 'NONE', #15489, 0.2000000000000119182 ) ;
#36364=CARTESIAN_POINT ( 'NONE',  ( -21.05000000000000071, -4.714262876194486473, -233.3440214805475819 ) ) ;
#36375=AXIS2_PLACEMENT_3D ( 'NONE', #58854, #241385, #139678 ) ;
#36399=VECTOR ( 'NONE', #83180, 1000.000000000000114 ) ;
#36402=CARTESIAN_POINT ( 'NONE',  ( -23.15000000000000213, -3.664072692419560795, -226.4691047342518857 ) ) ;
#36480=DIRECTION ( 'NONE',  ( 0.000000000000000000, 0.2128009952263485993, -0.9770955615653341697 ) ) ;
#36489=ADVANCED_FACE ( 'NONE', ( #149042 ), #224473, .T. ) ;
#36499=DIRECTION ( 'NONE',  ( -1.000000000000000000, 0.000000000000000000, 0.000000000000000000 ) ) ;
#36503=CARTESIAN_POINT ( 'NONE',  ( -22.59999999999999787, 11.45898712536580177, -198.4011321578509808 ) ) ;
#36509=DIRECTION ( 'NONE',  ( 0.000000000000000000, -0.2128009952263604232, 0.9770955615653316162 ) ) ;
#36547=DIRECTION ( 'NONE',  ( 0.000000000000000000, 0.2128009952263237581, -0.9770955615653394988 ) ) ;
#36554=CARTESIAN_POINT ( 'NONE',  ( 22.59066674512273920, 11.47438154053713077, -198.4697828622833242 ) ) ;
#36557=DIRECTION ( 'NONE',  ( -0.000000000000000000, 0.2128009952263604232, -0.9770955615653316162 ) ) ;
#36570=DIRECTION ( 'NONE',  ( 0.000000000000000000, 0.2128009952263621163, -0.9770955615653311721 ) ) ;
#36573=CARTESIAN_POINT ( 'NONE',  ( 21.11825140030103043, -1.364550518801973977, -194.7006879377100006 ) ) ;
#36580=CARTESIAN_POINT ( 'NONE',  ( 20.94999999999999929, 8.433899723187009201, -209.4150263691077782 ) ) ;
#36620=AXIS2_PLACEMENT_3D ( 'NONE', #191841, #133124, #36622 ) ;
#36622=DIRECTION ( 'NONE',  ( 0.000000000000000000, 0.9394191166662618775, 0.3427706569150580362 ) ) ;
#36624=CARTESIAN_POINT ( 'NONE',  ( -23.25000000000000000, 8.653397185701672711, -220.7611668973962367 ) ) ;
#36676=ORIENTED_EDGE ( 'NONE', *, *, #13931, .F. ) ;
#36680=CARTESIAN_POINT ( 'NONE',  ( 20.95325940946048249, 11.89208280016391583, -206.1518144919116651 ) ) ;
#36695=AXIS2_PLACEMENT_3D ( 'NONE', #226419, #49083, #115478 ) ;
#36716=CARTESIAN_POINT ( 'NONE',  ( -23.15000000000000213, -3.770473190032741062, -225.9805569534692324 ) ) ;
#36749=CARTESIAN_POINT ( 'NONE',  ( -22.50000000000000000, 11.38316329224757872, -198.5208684056144079 ) ) ;
#36777=PLANE ( 'NONE',  #152384 ) ;
#36823=AXIS2_PLACEMENT_3D ( 'NONE', #178158, #36068, #97266 ) ;
#36833=EDGE_LOOP ( 'NONE', ( #165947, #167010, #165513, #135955 ) ) ;
#36835=PRESENTATION_STYLE_ASSIGNMENT (( #155500 ) ) ;
#36878=EDGE_CURVE ( 'NONE', #225002, #401, #87272, .T. ) ;
#36885=ORIENTED_EDGE ( 'NONE', *, *, #102121, .F. ) ;
#36898=CARTESIAN_POINT ( 'NONE',  ( 20.95512820512820440, 12.96604748760834092, -210.6109454999921411 ) ) ;
#36903=DIRECTION ( 'NONE',  ( 0.000000000000000000, -0.9770955615653316162, -0.2128009952263604232 ) ) ;
#36917=PLANE ( 'NONE',  #143018 ) ;
#36920=CARTESIAN_POINT ( 'NONE',  ( -21.07928932188134041, -1.250084634896336366, -194.7953894783290423 ) ) ;
#36921=DIRECTION ( 'NONE',  ( 0.000000000000000000, 0.2128009952263603677, -0.9770955615653313941 ) ) ;
#36940=DIRECTION ( 'NONE',  ( 0.000000000000000000, -0.9770955615653301729, -0.2128009952263661964 ) ) ;
#36947=DIRECTION ( 'NONE',  ( 0.000000000000000000, 0.2128009952263403282, -0.9770955615653358350 ) ) ;
#37003=VECTOR ( 'NONE', #210501, 1000.000000000000227 ) ;
#37068=CARTESIAN_POINT ( 'NONE',  ( -20.94999999999999929, -10.58757034444203704, -206.3761839813444396 ) ) ;
#37120=ADVANCED_FACE ( 'NONE', ( #44194 ), #123723, .T. ) ;
#37134=CYLINDRICAL_SURFACE ( 'NONE', #156702, 0.09999999999999938105 ) ;
#37154=CARTESIAN_POINT ( 'NONE',  ( -18.50000000000000000, -0.6576273345615585297, -242.5323337003318898 ) ) ;
#37203=CARTESIAN_POINT ( 'NONE',  ( 20.96937028524354929, 11.97530479700835393, -206.0589415372148778 ) ) ;
#37209=ORIENTED_EDGE ( 'NONE', *, *, #112447, .T. ) ;
#37253=ORIENTED_EDGE ( 'NONE', *, *, #142306, .T. ) ;
#37280=AXIS2_PLACEMENT_3D ( 'NONE', #10338, #89844, #211092 ) ;
#37282=ORIENTED_EDGE ( 'NONE', *, *, #210109, .T. ) ;
#37284=DIRECTION ( 'NONE',  ( 0.7071067811865302533, -0.6909108974501196876, -0.1504730267679053324 ) ) ;
#37292=ORIENTED_EDGE ( 'NONE', *, *, #136050, .T. ) ;
#37320=CYLINDRICAL_SURFACE ( 'NONE', #152743, 11.74999999999999289 ) ;
#37336=ORIENTED_EDGE ( 'NONE', *, *, #42020, .T. ) ;
#37371=CARTESIAN_POINT ( 'NONE',  ( -20.64999999999999858, -6.438379425586759908, -212.1495692908769684 ) ) ;
#37414=AXIS2_PLACEMENT_3D ( 'NONE', #84959, #242773, #164546 ) ;
#37415=VERTEX_POINT ( 'NONE', #219599 ) ;
#37420=CIRCLE ( 'NONE', #70745, 0.1000000000000055844 ) ;
#37426=CARTESIAN_POINT ( 'NONE',  ( -23.25000000000000000, -3.770473190032741062, -225.9805569534692324 ) ) ;
#37446=DIRECTION ( 'NONE',  ( 1.000000000000000000, 0.000000000000000000, 0.000000000000000000 ) ) ;
#37456=DIRECTION ( 'NONE',  ( 0.000000000000000000, 0.2128009952263485993, -0.9770955615653341697 ) ) ;
#37474=EDGE_LOOP ( 'NONE', ( #75760, #16349, #90928, #250273 ) ) ;
#37500=DIRECTION ( 'NONE',  ( 0.000000000000000000, -0.9316174814283004757, -0.3634403228828503307 ) ) ;
#37513=CARTESIAN_POINT ( 'NONE',  ( -20.94999999999999929, 12.97363049771892207, -205.3537238898406940 ) ) ;
#37518=DIRECTION ( 'NONE',  ( 1.000000000000000000, 0.000000000000000000, 0.000000000000000000 ) ) ;
#37574=AXIS2_PLACEMENT_3D ( 'NONE', #188592, #210734, #169079 ) ;
#37590=CARTESIAN_POINT ( 'NONE',  ( 21.93642651522410603, 7.159341611308064124, -199.4407717320839879 ) ) ;
#37610=ADVANCED_FACE ( 'NONE', ( #232476 ), #209039, .F. ) ;
#37618=CARTESIAN_POINT ( 'NONE',  ( -21.44999999999999929, 11.70367352607683564, -220.1991933683510467 ) ) ;
#37682=CARTESIAN_POINT ( 'NONE',  ( -20.85000000000000497, 17.13730476842946615, -224.4716215546871467 ) ) ;
#37715=CARTESIAN_POINT ( 'NONE',  ( -23.15000000000000213, 7.128833340094563376, -233.7327013124401276 ) ) ;
#37740=CARTESIAN_POINT ( 'NONE',  ( -18.59999999999999787, 8.882751598337863541, -187.0399955572217721 ) ) ;
#37746=LINE ( 'NONE', #256717, #44259 ) ;
#37749=ORIENTED_EDGE ( 'NONE', *, *, #13618, .T. ) ;
#37762=ORIENTED_EDGE ( 'NONE', *, *, #58711, .T. ) ;
#37816=ORIENTED_EDGE ( 'NONE', *, *, #217683, .F. ) ;
#37817=CARTESIAN_POINT ( 'NONE',  ( 21.13461538461538325, 12.99955419111918253, -210.8083363671015604 ) ) ;
#37832=DIRECTION ( 'NONE',  ( 1.000000000000000000, 0.000000000000000000, 0.000000000000000000 ) ) ;
#37864=EDGE_LOOP ( 'NONE', ( #102482, #183876, #116941, #249431 ) ) ;
#37867=CIRCLE ( 'NONE', #183588, 0.09999999999998862577 ) ;
#37902=ORIENTED_EDGE ( 'NONE', *, *, #138928, .T. ) ;
#37908=CIRCLE ( 'NONE', #192030, 0.09999999999999248379 ) ;
#37909=VERTEX_POINT ( 'NONE', #199770 ) ;
#37914=CARTESIAN_POINT ( 'NONE',  ( 23.14999999999999858, 7.128833340094563376, -233.7327013124401276 ) ) ;
#37920=EDGE_CURVE ( 'NONE', #22410, #135145, #75202, .T. ) ;
#37939=( BOUNDED_SURFACE ( )  B_SPLINE_SURFACE ( 3, 2, ( 
 ( #116716, #217078, #159707 ),
 ( #239236, #201385, #118001 ),
 ( #155873, #102250, #60582 ),
 ( #254878, #235371, #176711 ),
 ( #98390, #197529, #18896 ),
 ( #177994, #76292, #257451 ),
 ( #158446, #157154, #61887 ),
 ( #1883, #138806, #196248 ),
 ( #56705, #237942, #59264 ),
 ( #179291, #120593, #80114 ),
 ( #141411, #215798, #81408 ),
 ( #140111, #37203, #220937 ) ),
 .UNSPECIFIED., .F., .F., .F. ) 
 B_SPLINE_SURFACE_WITH_KNOTS ( ( 4, 2, 2, 2, 2, 4 ),
 ( 3, 3 ),
 ( 3.174653483277204646, 3.943930578431714018, 4.713207673586222946, 5.482484768740731873, 5.867123316317986337, 6.251761863895240801 ),
 ( 0.000000000000000000, 1.000000000000000000 ),
 .UNSPECIFIED. ) 
 GEOMETRIC_REPRESENTATION_ITEM ( )  RATIONAL_B_SPLINE_SURFACE ( (
 ( 1.000000000000000000, 0.8659465255642173620, 1.000000000000000000),
 ( 1.000000000000000000, 0.8648614068495104057, 1.000000000000000000),
 ( 1.000000000000000000, 0.8489031841315631821, 1.000000000000000000),
 ( 1.000000000000000000, 0.7927507630169553510, 1.000000000000000000),
 ( 1.000000000000000000, 0.7523013859136092885, 1.000000000000000000),
 ( 1.000000000000000000, 0.6616226951069902329, 1.000000000000000000),
 ( 1.000000000000000000, 0.6112214368811986764, 1.000000000000000000),
 ( 1.000000000000000000, 0.5507684314454389662, 1.000000000000000000),
 ( 1.000000000000000000, 0.5333267243029248261, 1.000000000000000000),
 ( 1.000000000000000000, 0.5084565446606316153, 1.000000000000000000),
 ( 1.000000000000000000, 0.5010722703356487173, 1.000000000000000000),
 ( 1.000000000000000000, 0.5001234037138250210, 1.000000000000000000) ) ) 
 REPRESENTATION_ITEM ( '' )  SURFACE ( )  );
#37952=CARTESIAN_POINT ( 'NONE',  ( 20.95035502843362707, 11.84989802294387218, -206.1731169549366598 ) ) ;
#37978=ORIENTED_EDGE ( 'NONE', *, *, #249604, .T. ) ;
#37991=CIRCLE ( 'NONE', #50407, 0.1000000000000055844 ) ;
#38007=EDGE_CURVE ( 'NONE', #81634, #34173, #49655, .T. ) ;
#38009=VERTEX_POINT ( 'NONE', #130472 ) ;
#38014=ORIENTED_EDGE ( 'NONE', *, *, #257077, .F. ) ;
#38030=DIRECTION ( 'NONE',  ( 1.000000000000000000, 0.000000000000000000, 0.000000000000000000 ) ) ;
#38068=DIRECTION ( 'NONE',  ( 1.000000000000000000, 0.000000000000000000, 0.000000000000000000 ) ) ;
#38072=B_SPLINE_CURVE_WITH_KNOTS ( 'NONE', 3,
 ( #229616, #172251, #67966, #50944, #112249, #9275, #147505, #52235, #189207, #148800, #91391, #193065, #130498, #210062, #251740, #168406, #228335, #230916, #71840 ),
 .UNSPECIFIED., .F., .F.,
 ( 4, 3, 3, 3, 3, 3, 4 ),
 ( 0.000000000000000000, 1.655171619025965957E-05, 2.773500582848639000E-05, 5.941817267379636262E-05, 0.0001114174635873664597, 0.0001914169455916642400, 0.0002627181070751139673 ),
 .UNSPECIFIED. ) ;
#38095=VERTEX_POINT ( 'NONE', #147002 ) ;
#38096=ADVANCED_FACE ( 'NONE', ( #145720 ), #21951, .T. ) ;
#38107=EDGE_CURVE ( 'NONE', #237997, #121941, #183586, .T. ) ;
#38111=FACE_OUTER_BOUND ( 'NONE', #12332, .T. ) ;
#38120=AXIS2_PLACEMENT_3D ( 'NONE', #209988, #49616, #9203 ) ;
#38123=ORIENTED_EDGE ( 'NONE', *, *, #155894, .F. ) ;
#38147=ORIENTED_EDGE ( 'NONE', *, *, #232062, .F. ) ;
#38165=CARTESIAN_POINT ( 'NONE',  ( -20.85000000000000142, -4.871452838297996024, -233.3782557782877518 ) ) ;
#38166=EDGE_LOOP ( 'NONE', ( #46710, #32, #192899, #54703 ) ) ;
#38177=DIRECTION ( 'NONE',  ( 0.000000000000000000, -0.2128009952263605342, 0.9770955615653316162 ) ) ;
#38204=CARTESIAN_POINT ( 'NONE',  ( -18.50000000000000711, 12.87592094156238609, -205.3750039893633073 ) ) ;
#38213=AXIS2_PLACEMENT_3D ( 'NONE', #163475, #87767, #225975 ) ;
#38258=ADVANCED_FACE ( 'NONE', ( #12670 ), #183713, .T. ) ;
#38292=DIRECTION ( 'NONE',  ( 0.000000000000000000, -0.9770955615653316162, -0.2128009952263604232 ) ) ;
#38312=CARTESIAN_POINT ( 'NONE',  ( -20.64999999999999858, 6.375212254182287097, -220.8739277186596155 ) ) ;
#38342=CIRCLE ( 'NONE', #146634, 0.1000000000000038219 ) ;
#38348=ORIENTED_EDGE ( 'NONE', *, *, #186698, .T. ) ;
#38349=FACE_OUTER_BOUND ( 'NONE', #21833, .T. ) ;
#38352=DIRECTION ( 'NONE',  ( -0.000000000000000000, -0.9770955615653316162, -0.2128009952263604232 ) ) ;
#38388=ORIENTED_EDGE ( 'NONE', *, *, #250987, .T. ) ;
#38391=ORIENTED_EDGE ( 'NONE', *, *, #195541, .F. ) ;
#38408=ORIENTED_EDGE ( 'NONE', *, *, #173940, .T. ) ;
#38419=CARTESIAN_POINT ( 'NONE',  ( -18.33981767444511490, -0.7704322632317684993, -242.4320893355032638 ) ) ;
#38453=VERTEX_POINT ( 'NONE', #165110 ) ;
#38456=FACE_OUTER_BOUND ( 'NONE', #139628, .T. ) ;
#38458=EDGE_CURVE ( 'NONE', #227551, #248008, #88101, .T. ) ;
#38485=ORIENTED_EDGE ( 'NONE', *, *, #72129, .T. ) ;
#38495=ORIENTED_EDGE ( 'NONE', *, *, #158945, .F. ) ;
#38561=EDGE_CURVE ( 'NONE', #207244, #111449, #151045, .T. ) ;
#38575=TOROIDAL_SURFACE ( 'NONE', #59189, 4.149999999999999467, 0.1000000000000000056 ) ;
#38587=CIRCLE ( 'NONE', #225820, 0.1000000000000054040 ) ;
#38602=ORIENTED_EDGE ( 'NONE', *, *, #129172, .T. ) ;
#38629=DIRECTION ( 'NONE',  ( 1.000000000000000000, 0.000000000000000000, 0.000000000000000000 ) ) ;
#38639=LINE ( 'NONE', #44744, #99976 ) ;
#38646=ORIENTED_EDGE ( 'NONE', *, *, #177558, .T. ) ;
#38679=B_SPLINE_CURVE_WITH_KNOTS ( 'NONE', 3,
 ( #15342, #72761, #152287, #231815, #94844, #53159, #96118, #175696 ),
 .UNSPECIFIED., .F., .F.,
 ( 4, 2, 2, 4 ),
 ( 0.000000000000000000, 9.550056980125026785E-05, 0.0001910011396025005357, 0.0003820022792049986319 ),
 .UNSPECIFIED. ) ;
#38685=ORIENTED_EDGE ( 'NONE', *, *, #111895, .T. ) ;
#38694=CARTESIAN_POINT ( 'NONE',  ( -20.94999999999999929, -4.639171910822553535, -233.3276674689317076 ) ) ;
#38728=EDGE_LOOP ( 'NONE', ( #63992, #22078, #205238, #42054 ) ) ;
#38730=CARTESIAN_POINT ( 'NONE',  ( -20.94999999999999929, 12.80863705670245700, -205.3010250813005655 ) ) ;
#38743=DIRECTION ( 'NONE',  ( -0.000000000000000000, 0.2128009952263603677, -0.9770955615653313941 ) ) ;
#38768=CYLINDRICAL_SURFACE ( 'NONE', #124096, 12.87499999999999467 ) ;
#38788=ORIENTED_EDGE ( 'NONE', *, *, #25886, .F. ) ;
#38790=VECTOR ( 'NONE', #158660, 1000.000000000000227 ) ;
#38806=CARTESIAN_POINT ( 'NONE',  ( 18.50000000000000355, -7.661135498422202872, -210.0861805852114514 ) ) ;
#38850=ORIENTED_EDGE ( 'NONE', *, *, #118886, .F. ) ;
#38860=CARTESIAN_POINT ( 'NONE',  ( 20.94999999999999929, 7.128833340094563376, -233.7327013124401276 ) ) ;
#38869=EDGE_CURVE ( 'NONE', #130685, #227551, #184347, .T. ) ;
#38882=CARTESIAN_POINT ( 'NONE',  ( -18.59999999999999787, 2.859758780633683273, -208.6670499591424459 ) ) ;
#38890=CARTESIAN_POINT ( 'NONE',  ( -23.15000000000000213, -3.770473190032741062, -225.9805569534692324 ) ) ;
#38897=DIRECTION ( 'NONE',  ( 0.000000000000000000, 0.8659859643398412077, -0.5000683049008356473 ) ) ;
#38916=VERTEX_POINT ( 'NONE', #166121 ) ;
#39012=DIRECTION ( 'NONE',  ( -0.000000000000000000, 0.08413937888704771384, -0.9964539953858891908 ) ) ;
#39043=EDGE_LOOP ( 'NONE', ( #251823, #126220, #60794, #234875 ) ) ;
#39068=CARTESIAN_POINT ( 'NONE',  ( -23.15000000000000213, 6.268811756569107274, -220.3853799378769622 ) ) ;
#39091=AXIS2_PLACEMENT_3D ( 'NONE', #240618, #219758, #241893 ) ;
#39123=CARTESIAN_POINT ( 'NONE',  ( 23.14999999999998437, 1.148907358139439339E-11, -201.0000000000015064 ) ) ;
#39161=EDGE_CURVE ( 'NONE', #193316, #32161, #45828, .T. ) ;
#39210=DIRECTION ( 'NONE',  ( -1.000000000000000000, -0.000000000000000000, -0.000000000000000000 ) ) ;
#39219=CARTESIAN_POINT ( 'NONE',  ( 21.05000000000000071, -6.688413578037176066, -212.5825622730469036 ) ) ;
#39262=ADVANCED_FACE ( 'NONE', ( #112242 ), #97179, .F. ) ;
#39291=ORIENTED_EDGE ( 'NONE', *, *, #168603, .T. ) ;
#39339=VERTEX_POINT ( 'NONE', #210057 ) ;
#39347=FACE_OUTER_BOUND ( 'NONE', #57894, .T. ) ;
#39357=EDGE_CURVE ( 'NONE', #234608, #165014, #197178, .T. ) ;
#39394=EDGE_LOOP ( 'NONE', ( #98893, #19277, #71084, #146332 ) ) ;
#39410=EDGE_LOOP ( 'NONE', ( #235812, #65144, #34556, #57222 ) ) ;
#39427=DIRECTION ( 'NONE',  ( 1.000000000000000000, 0.000000000000000000, 0.000000000000000000 ) ) ;
#39452=ORIENTED_EDGE ( 'NONE', *, *, #255519, .F. ) ;
#39462=DIRECTION ( 'NONE',  ( 1.000000000000000000, 0.000000000000000000, 0.000000000000000000 ) ) ;
#39481=DIRECTION ( 'NONE',  ( 1.000000000000000000, 0.000000000000000000, 0.000000000000000000 ) ) ;
#39483=EDGE_CURVE ( 'NONE', #236905, #64897, #156524, .T. ) ;
#39538=ORIENTED_EDGE ( 'NONE', *, *, #45596, .F. ) ;
#39549=CARTESIAN_POINT ( 'NONE',  ( 21.14999999999999858, 13.96869538424789070, -210.3925794786331949 ) ) ;
#39554=AXIS2_PLACEMENT_3D ( 'NONE', #64865, #23209, #141835 ) ;
#39563=FACE_OUTER_BOUND ( 'NONE', #257678, .T. ) ;
#39593=AXIS2_PLACEMENT_3D ( 'NONE', #148059, #228879, #48942 ) ;
#39607=DIRECTION ( 'NONE',  ( 0.000000000000000000, 0.2128009952263603954, -0.9770955615653316162 ) ) ;
#39608=CARTESIAN_POINT ( 'NONE',  ( 23.15000000000000213, -6.388372595096674544, -212.0629706944429813 ) ) ;
#39676=DIRECTION ( 'NONE',  ( 0.000000000000000000, 0.2128009952264065807, -0.9770955615653215132 ) ) ;
#39692=DIRECTION ( 'NONE',  ( 1.000000000000000000, 0.000000000000000000, 0.000000000000000000 ) ) ;
#39693=CARTESIAN_POINT ( 'NONE',  ( 20.94999999999999929, 19.68370618165487329, -225.3554403480446240 ) ) ;
#39697=VERTEX_POINT ( 'NONE', #114484 ) ;
#39732=CARTESIAN_POINT ( 'NONE',  ( -18.31331870001017137, -0.7273975225635296304, -242.4732920726780208 ) ) ;
#39746=EDGE_CURVE ( 'NONE', #126149, #132220, #28085, .T. ) ;
#39760=ORIENTED_EDGE ( 'NONE', *, *, #14021, .T. ) ;
#39775=CARTESIAN_POINT ( 'NONE',  ( 21.05000000000000071, -2.576749817950531707, -189.6385361693310756 ) ) ;
#39784=DIRECTION ( 'NONE',  ( 0.000000000000000000, 0.06835365183351375939, -0.9976611540402997580 ) ) ;
#39809=ADVANCED_FACE ( 'NONE', ( #141417 ), #135312, .F. ) ;
#39826=ORIENTED_EDGE ( 'NONE', *, *, #167771, .T. ) ;
#39851=DIRECTION ( 'NONE',  ( -1.000000000000000000, 0.000000000000000000, 0.000000000000000000 ) ) ;
#39852=CARTESIAN_POINT ( 'NONE',  ( 21.05000000000000071, 10.45765418377745881, -207.3040725013013912 ) ) ;
#39860=CARTESIAN_POINT ( 'NONE',  ( 20.94999999999999929, 7.467768556382911704, -241.6289316175765407 ) ) ;
#39868=DIRECTION ( 'NONE',  ( 0.000000000000000000, -0.9770955615653320603, -0.2128009952263585081 ) ) ;
#39892=CARTESIAN_POINT ( 'NONE',  ( 22.39999999999999503, -2.479040261793999722, -189.6172560698084624 ) ) ;
#39903=CARTESIAN_POINT ( 'NONE',  ( 21.53752568617696639, 6.610297987518621632, -199.4590530230506999 ) ) ;
#39908=EDGE_CURVE ( 'NONE', #237997, #20437, #182379, .T. ) ;
#39929=( BOUNDED_SURFACE ( )  B_SPLINE_SURFACE ( 3, 2, ( 
 ( #39852, #257525, #3246 ),
 ( #180628, #144043, #63224 ),
 ( #24136, #82761, #1962 ),
 ( #81481, #183200, #78920 ) ),
 .UNSPECIFIED., .F., .F., .F. ) 
 B_SPLINE_SURFACE_WITH_KNOTS ( ( 4, 4 ),
 ( 3, 3 ),
 ( 0.0002700421466196776762, 0.0004789321604330829441 ),
 ( 0.000000000000000000, 1.000000000000000000 ),
 .UNSPECIFIED. ) 
 GEOMETRIC_REPRESENTATION_ITEM ( )  RATIONAL_B_SPLINE_SURFACE ( (
 ( 1.000000000000000000, 0.7071067811864790720, 1.000000000000000000),
 ( 1.000000000000000000, 0.7163411249512339207, 1.000000000000000000),
 ( 1.000000000000000000, 0.7221957104841457697, 1.000000000000000000),
 ( 1.000000000000000000, 0.7250110520819958992, 1.000000000000000000) ) ) 
 REPRESENTATION_ITEM ( '' )  SURFACE ( )  );
#39933=PLANE ( 'NONE',  #29014 ) ;
#39943=DIRECTION ( 'NONE',  ( -0.000000000000000000, 0.9770955615653313941, 0.2128009952263603954 ) ) ;
#39948=FACE_OUTER_BOUND ( 'NONE', #213682, .T. ) ;
#39949=ORIENTED_EDGE ( 'NONE', *, *, #204395, .T. ) ;
#39950=EDGE_LOOP ( 'NONE', ( #57841, #41766, #159056, #125239 ) ) ;
#39959=ADVANCED_FACE ( 'NONE', ( #10917 ), #94871, .T. ) ;
#40012=DIRECTION ( 'NONE',  ( 1.000000000000000000, 0.000000000000000000, 0.000000000000000000 ) ) ;
#40046=CARTESIAN_POINT ( 'NONE',  ( 21.05000000000000071, 9.374458193048763377, -220.5475659691911119 ) ) ;
#40051=EDGE_CURVE ( 'NONE', #147767, #3546, #228160, .T. ) ;
#40085=CARTESIAN_POINT ( 'NONE',  ( 21.05000000000000071, 17.15380675273574695, -224.5473919504296703 ) ) ;
#40094=EDGE_CURVE ( 'NONE', #128109, #129320, #214246, .T. ) ;
#40099=CARTESIAN_POINT ( 'NONE',  ( -20.95000000000000284, 12.93677228415563896, -205.1844859741924836 ) ) ;
#40100=ORIENTED_EDGE ( 'NONE', *, *, #109616, .F. ) ;
#40106=DIRECTION ( 'NONE',  ( 1.836970198721029934E-16, -0.9770955615653316162, -0.2128009952263604232 ) ) ;
#40172=ORIENTED_EDGE ( 'NONE', *, *, #183614, .F. ) ;
#40175=DIRECTION ( 'NONE',  ( 0.000000000000000000, -0.9770955615653201809, -0.2128009952264121873 ) ) ;
#40176=ORIENTED_EDGE ( 'NONE', *, *, #157575, .T. ) ;
#40188=CARTESIAN_POINT ( 'NONE',  ( 18.59999999999999076, 8.433899723187009201, -209.4150263691077782 ) ) ;
#40229=AXIS2_PLACEMENT_3D ( 'NONE', #213886, #230908, #130489 ) ;
#40284=AXIS2_PLACEMENT_3D ( 'NONE', #98307, #197441, #17516 ) ;
#40316=ORIENTED_EDGE ( 'NONE', *, *, #16749, .T. ) ;
#40326=DIRECTION ( 'NONE',  ( -1.000000000000000000, 0.000000000000000000, -0.000000000000000000 ) ) ;
#40354=DIRECTION ( 'NONE',  ( 0.000000000000000000, -0.9770955615653316162, -0.2128009952263604232 ) ) ;
#40356=DIRECTION ( 'NONE',  ( 1.000000000000000000, 0.000000000000000000, 0.000000000000000000 ) ) ;
#40364=CARTESIAN_POINT ( 'NONE',  ( 18.59999999999999787, 1.148907358139439339E-11, -201.0000000000015064 ) ) ;
#40368=CARTESIAN_POINT ( 'NONE',  ( -20.94999999999999929, -10.82118976317943826, -206.5294079347637819 ) ) ;
#40381=EDGE_CURVE ( 'NONE', #23148, #218469, #32768, .T. ) ;
#40407=DIRECTION ( 'NONE',  ( -1.000000000000000000, 0.000000000000000000, 0.000000000000000000 ) ) ;
#40429=AXIS2_PLACEMENT_3D ( 'NONE', #87380, #164376, #204764 ) ;
#40461=CARTESIAN_POINT ( 'NONE',  ( -20.94999999999999929, 4.252251777740766236, -211.8999245327126744 ) ) ;
#40466=DIRECTION ( 'NONE',  ( 0.000000000000000000, -0.2128009952263603954, 0.9770955615653315052 ) ) ;
#40468=CARTESIAN_POINT ( 'NONE',  ( -20.64999999999999858, 6.659649981195239654, -220.3002595397864241 ) ) ;
#40481=DIRECTION ( 'NONE',  ( -0.000000000000000000, -0.2814428106787469352, -0.9595780032479105381 ) ) ;
#40493=LINE ( 'NONE', #56142, #106074 ) ;
#40497=ORIENTED_EDGE ( 'NONE', *, *, #51216, .T. ) ;
#40559=ORIENTED_EDGE ( 'NONE', *, *, #23889, .T. ) ;
#40598=EDGE_CURVE ( 'NONE', #74110, #52138, #245086, .T. ) ;
#40623=DIRECTION ( 'NONE',  ( 1.000000000000000000, 0.000000000000000000, 0.000000000000000000 ) ) ;
#40633=CARTESIAN_POINT ( 'NONE',  ( -21.05000000000000071, 14.90151243843701856, -203.3975529985363551 ) ) ;
#40645=ORIENTED_EDGE ( 'NONE', *, *, #1344, .T. ) ;
#40722=EDGE_LOOP ( 'NONE', ( #220328, #19671, #183887, #7439 ) ) ;
#40751=EDGE_CURVE ( 'NONE', #68824, #98041, #153748, .T. ) ;
#40774=CIRCLE ( 'NONE', #49101, 0.1000000000000055844 ) ;
#40788=ORIENTED_EDGE ( 'NONE', *, *, #45036, .T. ) ;
#40796=ADVANCED_FACE ( 'NONE', ( #207222 ), #242469, .F. ) ;
#40866=EDGE_CURVE ( 'NONE', #98041, #185124, #248912, .T. ) ;
#40891=CIRCLE ( 'NONE', #244848, 0.09999999999999939493 ) ;
#40900=ORIENTED_EDGE ( 'NONE', *, *, #25852, .F. ) ;
#40910=ORIENTED_EDGE ( 'NONE', *, *, #197142, .F. ) ;
#40940=ORIENTED_EDGE ( 'NONE', *, *, #132202, .F. ) ;
#41041=CARTESIAN_POINT ( 'NONE',  ( -21.05000000000000071, 4.252251777740766236, -211.8999245327126744 ) ) ;
#41049=CARTESIAN_POINT ( 'NONE',  ( 21.05000000000000071, 13.06362847850371622, -210.5896934006125889 ) ) ;
#41051=ORIENTED_EDGE ( 'NONE', *, *, #71482, .T. ) ;
#41099=CARTESIAN_POINT ( 'NONE',  ( 18.57071067811864040, 14.46815956487128574, -219.5971177848713864 ) ) ;
#41102=AXIS2_PLACEMENT_3D ( 'NONE', #18297, #140819, #181247 ) ;
#41156=AXIS2_PLACEMENT_3D ( 'NONE', #200013, #21395, #201285 ) ;
#41160=ORIENTED_EDGE ( 'NONE', *, *, #255231, .T. ) ;
#41202=EDGE_LOOP ( 'NONE', ( #240517, #26106, #123627, #90400 ) ) ;
#41241=CIRCLE ( 'NONE', #178040, 0.09999999999999939493 ) ;
#41262=DIRECTION ( 'NONE',  ( 0.000000000000000000, -0.2128009952263485993, 0.9770955615653341697 ) ) ;
#41311=ORIENTED_EDGE ( 'NONE', *, *, #236764, .T. ) ;
#41321=CARTESIAN_POINT ( 'NONE',  ( -22.39999999999999858, -1.657885652111596109, -193.3876638332971254 ) ) ;
#41341=DIRECTION ( 'NONE',  ( -0.000000000000000000, -0.2128009952263603677, 0.9770955615653313941 ) ) ;
#41365=ADVANCED_FACE ( 'NONE', ( #137604 ), #78909, .T. ) ;
#41382=DIRECTION ( 'NONE',  ( -1.000000000000000000, 0.000000000000000000, 0.000000000000000000 ) ) ;
#41448=TOROIDAL_SURFACE ( 'NONE', #128923, 12.77500000000000036, 0.1000000000000000056 ) ;
#41460=EDGE_CURVE ( 'NONE', #68492, #128109, #149804, .T. ) ;
#41521=DIRECTION ( 'NONE',  ( 0.000000000000000000, 0.2128009952263403282, -0.9770955615653358350 ) ) ;
#41538=AXIS2_PLACEMENT_3D ( 'NONE', #142872, #182034, #140314 ) ;
#41543=EDGE_LOOP ( 'NONE', ( #5500, #250073, #4855 ) ) ;
#41557=CARTESIAN_POINT ( 'NONE',  ( -20.64999999999999858, 11.48697431424113446, -220.1440440112397994 ) ) ;
#41567=CARTESIAN_POINT ( 'NONE',  ( -23.15000000000000213, 8.882751598337867094, -187.0399955572217721 ) ) ;
#41577=ORIENTED_EDGE ( 'NONE', *, *, #63786, .F. ) ;
#41578=EDGE_CURVE ( 'NONE', #221067, #252116, #152302, .T. ) ;
#41599=AXIS2_PLACEMENT_3D ( 'NONE', #71069, #133584, #148022 ) ;
#41649=DIRECTION ( 'NONE',  ( 0.000000000000000000, -0.05689261644169250898, 0.9983803033886528011 ) ) ;
#41715=AXIS2_PLACEMENT_3D ( 'NONE', #236545, #57899, #117883 ) ;
#41729=DIRECTION ( 'NONE',  ( 0.000000000000000000, 0.9770955615653548199, 0.2128009952262535920 ) ) ;
#41745=ADVANCED_FACE ( 'NONE', ( #221653 ), #101691, .T. ) ;
#41746=DIRECTION ( 'NONE',  ( 0.000000000000000000, -0.9770955615653317272, -0.2128009952263598126 ) ) ;
#41751=DIRECTION ( 'NONE',  ( -1.000000000000000000, -0.000000000000000000, -0.000000000000000000 ) ) ;
#41754=AXIS2_PLACEMENT_3D ( 'NONE', #60361, #221979, #257232 ) ;
#41766=ORIENTED_EDGE ( 'NONE', *, *, #21790, .T. ) ;
#41798=CARTESIAN_POINT ( 'NONE',  ( -18.59999999999999787, 13.96869538424788004, -210.3925794786332233 ) ) ;
#41827=VERTEX_POINT ( 'NONE', #188972 ) ;
#41857=EDGE_LOOP ( 'NONE', ( #140118, #167724, #110091, #29134, #29088, #27199, #229357, #238217, #240956, #136978 ) ) ;
#41867=ORIENTED_EDGE ( 'NONE', *, *, #72305, .F. ) ;
#41870=ORIENTED_EDGE ( 'NONE', *, *, #200893, .T. ) ;
#41872=SPHERICAL_SURFACE ( 'NONE', #257026, 0.1000000000000000056 ) ;
#41913=ORIENTED_EDGE ( 'NONE', *, *, #70471, .F. ) ;
#41926=DIRECTION ( 'NONE',  ( 0.000000000000000000, -0.9770955615653316162, -0.2128009952263604232 ) ) ;
#41940=LINE ( 'NONE', #163163, #65875 ) ;
#42003=DIRECTION ( 'NONE',  ( 0.000000000000000000, 0.2128009952263485993, -0.9770955615653341697 ) ) ;
#42005=ORIENTED_EDGE ( 'NONE', *, *, #68755, .T. ) ;
#42011=CARTESIAN_POINT ( 'NONE',  ( -18.59999999999999787, 8.006782298343173565, -209.8034900594678618 ) ) ;
#42020=EDGE_CURVE ( 'NONE', #241077, #174819, #19090, .T. ) ;
#42054=ORIENTED_EDGE ( 'NONE', *, *, #42262, .F. ) ;
#42081=ADVANCED_FACE ( 'NONE', ( #60775 ), #180747, .F. ) ;
#42094=DIRECTION ( 'NONE',  ( -0.000000000000000000, 0.2128009952263604232, -0.9770955615653316162 ) ) ;
#42123=ORIENTED_EDGE ( 'NONE', *, *, #53023, .F. ) ;
#42130=ORIENTED_EDGE ( 'NONE', *, *, #27115, .T. ) ;
#42132=ORIENTED_EDGE ( 'NONE', *, *, #62711, .T. ) ;
#42141=TOROIDAL_SURFACE ( 'NONE', #79516, 6.258578643762712446, 0.1000000000000000056 ) ;
#42153=CARTESIAN_POINT ( 'NONE',  ( -21.05000000000000426, -1.362148144022342189, -194.8444205686345754 ) ) ;
#42161=ORIENTED_EDGE ( 'NONE', *, *, #126090, .F. ) ;
#42239=ORIENTED_EDGE ( 'NONE', *, *, #11716, .F. ) ;
#42251=VECTOR ( 'NONE', #235392, 999.9999999999998863 ) ;
#42262=EDGE_CURVE ( 'NONE', #221067, #139739, #28109, .T. ) ;
#42287=LINE ( 'NONE', #21456, #99130 ) ;
#42340=CYLINDRICAL_SURFACE ( 'NONE', #101214, 4.049999999999995381 ) ;
#42342=LINE ( 'NONE', #80137, #249802 ) ;
#42352=LINE ( 'NONE', #98420, #64421 ) ;
#42360=VECTOR ( 'NONE', #148141, 1000.000000000000227 ) ;
#42373=CARTESIAN_POINT ( 'NONE',  ( -22.48660254037842066, 11.47023279864282941, -198.4507335280135294 ) ) ;
#42383=DIRECTION ( 'NONE',  ( -1.000000000000000000, 0.000000000000000000, 0.000000000000000000 ) ) ;
#42385=ORIENTED_EDGE ( 'NONE', *, *, #43193, .T. ) ;
#42393=AXIS2_PLACEMENT_3D ( 'NONE', #63701, #222767, #203216 ) ;
#42413=LINE ( 'NONE', #84053, #134517 ) ;
#42414=ORIENTED_EDGE ( 'NONE', *, *, #209217, .T. ) ;
#42438=ORIENTED_EDGE ( 'NONE', *, *, #24617, .F. ) ;
#42471=CYLINDRICAL_SURFACE ( 'NONE', #56791, 0.09999999999999641120 ) ;
#42490=CARTESIAN_POINT ( 'NONE',  ( -20.64999999999999858, 2.739812813550878801, -213.5801053551551547 ) ) ;
#42503=FACE_OUTER_BOUND ( 'NONE', #248735, .T. ) ;
#42532=DIRECTION ( 'NONE',  ( 1.000000000000000000, 0.000000000000000000, 0.000000000000000000 ) ) ;
#42535=ADVANCED_FACE ( 'NONE', ( #247791 ), #141202, .T. ) ;
#42603=ORIENTED_EDGE ( 'NONE', *, *, #115456, .F. ) ;
#42617=CARTESIAN_POINT ( 'NONE',  ( 20.94999999999999929, 17.06838326776701109, -224.6250846885016870 ) ) ;
#42628=CARTESIAN_POINT ( 'NONE',  ( -20.94999999999999929, -4.714262876194486473, -233.3440214805475819 ) ) ;
#42633=CARTESIAN_POINT ( 'NONE',  ( -1.820710678118657944, -4.435039894044390252, -227.2960777983303160 ) ) ;
#42648=ADVANCED_FACE ( 'NONE', ( #48309 ), #41448, .T. ) ;
#42657=CARTESIAN_POINT ( 'NONE',  ( 21.30000000000002558, -0.8618440306552707098, -197.0427629756619297 ) ) ;
#42660=EDGE_LOOP ( 'NONE', ( #101318, #199850, #192009, #168492, #239834 ) ) ;
#42678=VECTOR ( 'NONE', #137414, 999.9999999999998863 ) ;
#42684=ORIENTED_EDGE ( 'NONE', *, *, #164339, .F. ) ;
#42686=CARTESIAN_POINT ( 'NONE',  ( -21.05000000000000071, 2.923777413779037548, -208.5507632484912222 ) ) ;
#42724=CARTESIAN_POINT ( 'NONE',  ( -23.15000000000000213, 7.128833340094563376, -233.7327013124401276 ) ) ;
#42729=CIRCLE ( 'NONE', #17761, 0.09999999999998866740 ) ;
#42734=ORIENTED_EDGE ( 'NONE', *, *, #244057, .F. ) ;
#42738=DIRECTION ( 'NONE',  ( -1.000000000000000000, -1.794895427898103559E-16, -3.909090864890002444E-17 ) ) ;
#42747=CARTESIAN_POINT ( 'NONE',  ( -23.25000000000000000, 7.128833340094563376, -233.7327013124401276 ) ) ;
#42751=CARTESIAN_POINT ( 'NONE',  ( -18.59999999999999787, 12.87592094156238609, -205.3750039893633073 ) ) ;
#42760=CYLINDRICAL_SURFACE ( 'NONE', #8773, 0.1000000000000056261 ) ;
#42761=TOROIDAL_SURFACE ( 'NONE', #184406, 11.70000000000000462, 0.1000000000000000056 ) ;
#42767=AXIS2_PLACEMENT_3D ( 'NONE', #181957, #64561, #99809 ) ;
#42843=DIRECTION ( 'NONE',  ( 0.000000000000000000, 0.2128009952263605342, -0.9770955615653315052 ) ) ;
#42854=ORIENTED_EDGE ( 'NONE', *, *, #24016, .F. ) ;
#42884=EDGE_CURVE ( 'NONE', #185772, #210485, #230499, .T. ) ;
#42887=CYLINDRICAL_SURFACE ( 'NONE', #75935, 0.1000000000000054040 ) ;
#42901=AXIS2_PLACEMENT_3D ( 'NONE', #186749, #159795, #8103 ) ;
#42905=CARTESIAN_POINT ( 'NONE',  ( -21.05000000000000071, 6.108674899944905867, -199.6368316019445501 ) ) ;
#42923=DIRECTION ( 'NONE',  ( 1.000000000000000000, 7.136802563874195162E-16, 1.554319503706929005E-16 ) ) ;
#42925=CARTESIAN_POINT ( 'NONE',  ( 23.14999999999999858, 11.03721558635588806, -232.8814973315346890 ) ) ;
#42926=ORIENTED_EDGE ( 'NONE', *, *, #632, .T. ) ;
#42954=CYLINDRICAL_SURFACE ( 'NONE', #131891, 0.1000000000000054040 ) ;
#42969=AXIS2_PLACEMENT_3D ( 'NONE', #204399, #84417, #7493 ) ;
#43012=ORIENTED_EDGE ( 'NONE', *, *, #181972, .T. ) ;
#43036=DIRECTION ( 'NONE',  ( 0.000000000000000000, -0.9964539953858966292, -0.08413937888696132461 ) ) ;
#43060=CARTESIAN_POINT ( 'NONE',  ( 19.80993210785516467, 16.75134015425318168, -222.6994291312944654 ) ) ;
#43063=CARTESIAN_POINT ( 'NONE',  ( 23.14999999999999858, 7.128833340094563376, -233.7327013124401276 ) ) ;
#43100=CIRCLE ( 'NONE', #22265, 0.09999999999999691080 ) ;
#43113=ADVANCED_FACE ( 'NONE', ( #233086 ), #91678, .F. ) ;
#43114=ORIENTED_EDGE ( 'NONE', *, *, #133837, .T. ) ;
#43126=AXIS2_PLACEMENT_3D ( 'NONE', #242635, #107942, #223075 ) ;
#43127=CARTESIAN_POINT ( 'NONE',  ( -20.05000000000000426, 13.56015509305096778, -219.7948714774209691 ) ) ;
#43128=CYLINDRICAL_SURFACE ( 'NONE', #11248, 0.09999999999999939493 ) ;
#43147=EDGE_CURVE ( 'NONE', #248011, #50999, #45893, .T. ) ;
#43193=EDGE_CURVE ( 'NONE', #39697, #212805, #180798, .T. ) ;
#43206=CARTESIAN_POINT ( 'NONE',  ( 21.05000000000000071, 11.84624361595474618, -206.1763227999733203 ) ) ;
#43251=PLANE ( 'NONE',  #228326 ) ;
#43265=SURFACE_STYLE_USAGE ( .BOTH. , #144906 ) ;
#43324=( BOUNDED_SURFACE ( )  B_SPLINE_SURFACE ( 3, 2, ( 
 ( #165173, #226402, #49069 ),
 ( #107761, #244693, #66065 ),
 ( #7375, #205562, #162618 ),
 ( #23119, #86893, #169066 ),
 ( #71229, #209425, #231576 ),
 ( #15097, #131173, #72509 ) ),
 .UNSPECIFIED., .F., .F., .F. ) 
 B_SPLINE_SURFACE_WITH_KNOTS ( ( 4, 2, 4 ),
 ( 3, 3 ),
 ( 0.0001381104793128029801, 0.0002947094729387742841, 0.0004513084665647455881 ),
 ( 0.000000000000000000, 1.000000000000000000 ),
 .UNSPECIFIED. ) 
 GEOMETRIC_REPRESENTATION_ITEM ( )  RATIONAL_B_SPLINE_SURFACE ( (
 ( 1.000000000000000000, 0.7071067811865601183, 1.000000000000000000),
 ( 1.000000000000000000, 0.6919563088096917225, 1.000000000000000000),
 ( 1.000000000000000000, 0.6959445945720270643, 1.000000000000000000),
 ( 1.000000000000000000, 0.7137882985309929040, 1.000000000000000000),
 ( 1.000000000000000000, 0.7257496306099716632, 1.000000000000000000),
 ( 1.000000000000000000, 0.7250110520819658122, 1.000000000000000000) ) ) 
 REPRESENTATION_ITEM ( '' )  SURFACE ( )  );
#43388=DIRECTION ( 'NONE',  ( -1.000000000000000000, -3.190570557967288949E-16, -6.948722487160392945E-17 ) ) ;
#43409=CIRCLE ( 'NONE', #126796, 0.09999999999999691080 ) ;
#43423=DIRECTION ( 'NONE',  ( 0.000000000000000000, 0.6728388485993177515, -0.7397890806274072251 ) ) ;
#43434=DIRECTION ( 'NONE',  ( 1.000000000000000000, 0.000000000000000000, 0.000000000000000000 ) ) ;
#43474=EDGE_LOOP ( 'NONE', ( #196981, #31332 ) ) ;
#43485=AXIS2_PLACEMENT_3D ( 'NONE', #206730, #249717, #247128 ) ;
#43488=ORIENTED_EDGE ( 'NONE', *, *, #242454, .F. ) ;
#43493=CYLINDRICAL_SURFACE ( 'NONE', #172141, 0.1000000000000007827 ) ;
#43501=ORIENTED_EDGE ( 'NONE', *, *, #134438, .T. ) ;
#43507=EDGE_CURVE ( 'NONE', #144682, #167762, #138740, .T. ) ;
#43509=PLANE ( 'NONE',  #41156 ) ;
#43530=ORIENTED_EDGE ( 'NONE', *, *, #143591, .T. ) ;
#43547=LINE ( 'NONE', #21433, #167148 ) ;
#43548=CARTESIAN_POINT ( 'NONE',  ( -23.25000000000000000, -4.892732937820631456, -233.2805462221312496 ) ) ;
#43550=PLANE ( 'NONE',  #198972 ) ;
#43600=CARTESIAN_POINT ( 'NONE',  ( 21.07094088545368038, -1.248309276978959437, -194.8035479807908530 ) ) ;
#43617=ORIENTED_EDGE ( 'NONE', *, *, #181619, .F. ) ;
#43654=TOROIDAL_SURFACE ( 'NONE', #151823, 0.2000000000000000111, 0.1000000000000000056 ) ;
#43655=CIRCLE ( 'NONE', #172885, 0.09999999999999939493 ) ;
#43701=DIRECTION ( 'NONE',  ( 0.000000000000000000, 0.9770955615653316162, 0.2128009952263597848 ) ) ;
#43729=VERTEX_POINT ( 'NONE', #209032 ) ;
#43751=AXIS2_PLACEMENT_3D ( 'NONE', #213180, #189781, #115368 ) ;
#43772=EDGE_CURVE ( 'NONE', #219574, #249430, #37908, .T. ) ;
#43778=VECTOR ( 'NONE', #100701, 1000.000000000000000 ) ;
#43779=AXIS2_PLACEMENT_3D ( 'NONE', #50146, #69741, #55260 ) ;
#43780=ORIENTED_EDGE ( 'NONE', *, *, #225846, .F. ) ;
#43786=CARTESIAN_POINT ( 'NONE',  ( -21.12230431290520016, 6.308551053831973121, -199.6207328664785052 ) ) ;
#43840=DIRECTION ( 'NONE',  ( -1.000000000000000000, 0.000000000000000000, 0.000000000000000000 ) ) ;
#43853=EDGE_CURVE ( 'NONE', #115361, #178200, #129467, .T. ) ;
#43865=CARTESIAN_POINT ( 'NONE',  ( -21.98333005346336577, -1.569210568885923696, -193.7948237253318098 ) ) ;
#43875=CARTESIAN_POINT ( 'NONE',  ( -23.25000000000000000, 7.128833340094563376, -233.7327013124401276 ) ) ;
#43900=FACE_OUTER_BOUND ( 'NONE', #190486, .T. ) ;
#43909=CARTESIAN_POINT ( 'NONE',  ( -21.02374657821594894, 16.98881331262127503, -224.4946931421776810 ) ) ;
#43922=CARTESIAN_POINT ( 'NONE',  ( 23.24999999999999289, 13.96869538424789070, -210.3925794786331949 ) ) ;
#43952=AXIS2_PLACEMENT_3D ( 'NONE', #65433, #27635, #50979 ) ;
#43983=ADVANCED_FACE ( 'NONE', ( #160642 ), #158094, .T. ) ;
#44006=DIRECTION ( 'NONE',  ( -0.000000000000000000, 0.9770955615653313941, 0.2128009952263603954 ) ) ;
#44040=DIRECTION ( 'NONE',  ( -0.000000000000000000, -0.9342891509276814999, -0.3565161741896601399 ) ) ;
#44059=AXIS2_PLACEMENT_3D ( 'NONE', #92273, #174441, #256419 ) ;
#44065=EDGE_CURVE ( 'NONE', #101102, #65554, #225683, .T. ) ;
#44068=ORIENTED_EDGE ( 'NONE', *, *, #176450, .T. ) ;
#44123=CIRCLE ( 'NONE', #77410, 0.1000000000000001305 ) ;
#44167=ORIENTED_EDGE ( 'NONE', *, *, #227428, .F. ) ;
#44168=AXIS2_PLACEMENT_3D ( 'NONE', #55806, #35039, #114539 ) ;
#44175=CARTESIAN_POINT ( 'NONE',  ( -21.05000000000000071, -10.47749788991998088, -206.4278944321438587 ) ) ;
#44191=CARTESIAN_POINT ( 'NONE',  ( -20.54999999999999716, 7.814782362862218612, -216.4406663269861610 ) ) ;
#44194=FACE_OUTER_BOUND ( 'NONE', #60709, .T. ) ;
#44218=CARTESIAN_POINT ( 'NONE',  ( -23.25000000000000000, 17.11694853917243364, -224.3781540347815451 ) ) ;
#44219=AXIS2_PLACEMENT_3D ( 'NONE', #179726, #194163, #18062 ) ;
#44259=VECTOR ( 'NONE', #200650, 1000.000000000000227 ) ;
#44262=CARTESIAN_POINT ( 'NONE',  ( -18.59999999999999787, 7.567413955921500346, -241.6205176796878504 ) ) ;
#44281=CARTESIAN_POINT ( 'NONE',  ( -18.50211644919735576, 18.36312997293285321, -236.9042258689304106 ) ) ;
#44303=PLANE ( 'NONE',  #138505 ) ;
#44333=ORIENTED_EDGE ( 'NONE', *, *, #221372, .F. ) ;
#44385=EDGE_CURVE ( 'NONE', #87224, #110507, #121491, .T. ) ;
#44393=CIRCLE ( 'NONE', #190144, 0.09999999999999600875 ) ;
#44396=VERTEX_POINT ( 'NONE', #200394 ) ;
#44398=CARTESIAN_POINT ( 'NONE',  ( -23.15000000000000213, 1.148907358139439339E-11, -201.0000000000015064 ) ) ;
#44404=ORIENTED_EDGE ( 'NONE', *, *, #66839, .T. ) ;
#44408=AXIS2_PLACEMENT_3D ( 'NONE', #130738, #233708, #55032 ) ;
#44422=ORIENTED_EDGE ( 'NONE', *, *, #42262, .T. ) ;
#44441=AXIS2_PLACEMENT_3D ( 'NONE', #176772, #198882, #151108 ) ;
#44444=DIRECTION ( 'NONE',  ( -1.000000000000000000, 0.000000000000000000, 0.000000000000000000 ) ) ;
#44455=CARTESIAN_POINT ( 'NONE',  ( -18.59999999999999787, 12.87592094156238609, -205.3750039893633073 ) ) ;
#44483=ORIENTED_EDGE ( 'NONE', *, *, #241530, .T. ) ;
#44488=CARTESIAN_POINT ( 'NONE',  ( 18.50000000000000000, -11.78281952876889527, -191.5407366062592871 ) ) ;
#44499=DIRECTION ( 'NONE',  ( 1.000000000000000000, 0.000000000000000000, 0.000000000000000000 ) ) ;
#44520=CARTESIAN_POINT ( 'NONE',  ( -18.50000000000000000, 6.440012694424540385, -187.5719980452876712 ) ) ;
#44596=CARTESIAN_POINT ( 'NONE',  ( 21.10710606213542562, 11.18076043846704692, -211.0928915918022426 ) ) ;
#44597=VERTEX_POINT ( 'NONE', #155844 ) ;
#44601=DIRECTION ( 'NONE',  ( -0.000000000000000000, 0.9770955615653313941, 0.2128009952263603954 ) ) ;
#44617=VECTOR ( 'NONE', #124060, 1000.000000000000227 ) ;
#44624=DIRECTION ( 'NONE',  ( -0.000000000000000000, 0.9983803033886520240, 0.05689261644170767740 ) ) ;
#44629=CARTESIAN_POINT ( 'NONE',  ( -21.46681500593131275, 6.700443717232317020, -199.5407148005083116 ) ) ;
#44650=ADVANCED_FACE ( 'NONE', ( #117978 ), #159077, .F. ) ;
#44676=CARTESIAN_POINT ( 'NONE',  ( 21.12757541349815682, 6.324013112643644519, -199.6174151709002444 ) ) ;
#44684=ORIENTED_EDGE ( 'NONE', *, *, #29103, .F. ) ;
#44685=CARTESIAN_POINT ( 'NONE',  ( 23.25000000000000000, -11.38316329222462464, -203.4791315943886048 ) ) ;
#44687=VERTEX_POINT ( 'NONE', #179263 ) ;
#44720=ORIENTED_EDGE ( 'NONE', *, *, #45774, .F. ) ;
#44737=EDGE_CURVE ( 'NONE', #236905, #217380, #92399, .T. ) ;
#44744=CARTESIAN_POINT ( 'NONE',  ( 23.24999999999999289, 14.06640494040442135, -210.3712993791105532 ) ) ;
#44750=CIRCLE ( 'NONE', #73429, 0.09999999999999130418 ) ;
#44775=DIRECTION ( 'NONE',  ( 0.000000000000000000, 0.2128009952263603954, -0.9770955615653315052 ) ) ;
#44786=FACE_OUTER_BOUND ( 'NONE', #39043, .T. ) ;
#44793=DIRECTION ( 'NONE',  ( 0.000000000000000000, -0.2128009952263604232, 0.9770955615653316162 ) ) ;
#44820=EDGE_LOOP ( 'NONE', ( #39949, #228161, #10493 ) ) ;
#44838=CARTESIAN_POINT ( 'NONE',  ( -18.40000000000000213, -0.6805341177324988333, -242.5179126613615495 ) ) ;
#44842=ORIENTED_EDGE ( 'NONE', *, *, #120629, .T. ) ;
#44864=FACE_OUTER_BOUND ( 'NONE', #47912, .T. ) ;
#44878=ORIENTED_EDGE ( 'NONE', *, *, #11974, .F. ) ;
#44883=LINE ( 'NONE', #240510, #176623 ) ;
#44901=VERTEX_POINT ( 'NONE', #68288 ) ;
#44945=DIRECTION ( 'NONE',  ( 1.000000000000000000, 0.000000000000000000, 0.000000000000000000 ) ) ;
#44951=AXIS2_PLACEMENT_3D ( 'NONE', #175448, #58017, #95868 ) ;
#44981=VERTEX_POINT ( 'NONE', #216769 ) ;
#44984=EDGE_CURVE ( 'NONE', #188047, #124170, #50879, .T. ) ;
#44987=AXIS2_PLACEMENT_3D ( 'NONE', #23188, #44006, #184795 ) ;
#45019=DIRECTION ( 'NONE',  ( 0.000000000000000000, 0.2128009952263603677, -0.9770955615653313941 ) ) ;
#45036=EDGE_CURVE ( 'NONE', #140605, #256115, #196633, .T. ) ;
#45067=AXIS2_PLACEMENT_3D ( 'NONE', #108662, #53826, #72120 ) ;
#45075=ORIENTED_EDGE ( 'NONE', *, *, #239080, .F. ) ;
#45090=CARTESIAN_POINT ( 'NONE',  ( 23.14999999999998437, -0.8618440306552707098, -197.0427629756619297 ) ) ;
#45093=PLANE ( 'NONE',  #47493 ) ;
#45108=AXIS2_PLACEMENT_3D ( 'NONE', #30401, #151649, #70827 ) ;
#45192=CARTESIAN_POINT ( 'NONE',  ( 22.39999999999999858, 7.591056067193225232, -199.2444047917219052 ) ) ;
#45204=DIRECTION ( 'NONE',  ( 1.000000000000000000, 0.000000000000000000, 0.000000000000000000 ) ) ;
#45233=AXIS2_PLACEMENT_3D ( 'NONE', #19764, #241377, #118865 ) ;
#45237=ORIENTED_EDGE ( 'NONE', *, *, #242448, .T. ) ;
#45238=CIRCLE ( 'NONE', #136823, 0.2000000000000111688 ) ;
#45243=DIRECTION ( 'NONE',  ( 1.000000000000000000, 0.000000000000000000, 0.000000000000000000 ) ) ;
#45277=EDGE_LOOP ( 'NONE', ( #20672, #19950, #155217, #62661 ) ) ;
#45302=ORIENTED_EDGE ( 'NONE', *, *, #128756, .T. ) ;
#45310=FACE_OUTER_BOUND ( 'NONE', #99612, .T. ) ;
#45315=DIRECTION ( 'NONE',  ( 0.000000000000000000, 0.2128009952263601734, -0.9770955615653316162 ) ) ;
#45345=VERTEX_POINT ( 'NONE', #121112 ) ;
#45388=ORIENTED_EDGE ( 'NONE', *, *, #22955, .T. ) ;
#45394=LINE ( 'NONE', #222734, #216285 ) ;
#45433=EDGE_CURVE ( 'NONE', #163312, #37415, #30255, .T. ) ;
#45455=CARTESIAN_POINT ( 'NONE',  ( 22.24259225415828922, -1.497494999994575471, -193.6585794405570766 ) ) ;
#45502=DIRECTION ( 'NONE',  ( -1.000000000000000000, 0.000000000000000000, 0.000000000000000000 ) ) ;
#45518=LINE ( 'NONE', #11542, #109927 ) ;
#45542=AXIS2_PLACEMENT_3D ( 'NONE', #29668, #229126, #90888 ) ;
#45575=CARTESIAN_POINT ( 'NONE',  ( -20.94999999999999929, -5.637547571910522137, -233.4427589080015650 ) ) ;
#45596=EDGE_CURVE ( 'NONE', #70740, #242169, #72449, .T. ) ;
#45597=CARTESIAN_POINT ( 'NONE',  ( -20.64999999999999858, 4.662003332185090443, -213.0075696128765514 ) ) ;
#45608=CARTESIAN_POINT ( 'NONE',  ( 21.05000000000000071, -0.9150442794618677267, -196.7984890852705746 ) ) ;
#45612=DIRECTION ( 'NONE',  ( 0.000000000000000000, -0.2128009952263604232, 0.9770955615653316162 ) ) ;
#45732=ORIENTED_EDGE ( 'NONE', *, *, #237083, .T. ) ;
#45744=EDGE_CURVE ( 'NONE', #220753, #92384, #134625, .T. ) ;
#45762=FACE_OUTER_BOUND ( 'NONE', #134763, .T. ) ;
#45771=PLANE ( 'NONE',  #157052 ) ;
#45774=EDGE_CURVE ( 'NONE', #256115, #199490, #55499, .T. ) ;
#45785=AXIS2_PLACEMENT_3D ( 'NONE', #105048, #184628, #225018 ) ;
#45797=DIRECTION ( 'NONE',  ( 1.000000000000000000, -0.000000000000000000, -0.000000000000000000 ) ) ;
#45824=DIRECTION ( 'NONE',  ( -1.000000000000000000, -0.000000000000000000, -0.000000000000000000 ) ) ;
#45828=LINE ( 'NONE', #27593, #255399 ) ;
#45843=CARTESIAN_POINT ( 'NONE',  ( -21.05000000000000071, 8.366615838327078336, -209.3410474610450080 ) ) ;
#45851=ORIENTED_EDGE ( 'NONE', *, *, #143489, .T. ) ;
#45870=ORIENTED_EDGE ( 'NONE', *, *, #23916, .T. ) ;
#45875=ORIENTED_EDGE ( 'NONE', *, *, #147919, .T. ) ;
#45893=CIRCLE ( 'NONE', #216576, 0.09999999999999939493 ) ;
#45931=DIRECTION ( 'NONE',  ( 0.000000000000000000, 0.9525900758537790836, -0.3042567129660269099 ) ) ;
#45946=CARTESIAN_POINT ( 'NONE',  ( 21.11101077988997332, 6.273301122770013727, -199.6180983270179468 ) ) ;
#45953=SPHERICAL_SURFACE ( 'NONE', #25585, 0.1000000000000000056 ) ;
#46046=CARTESIAN_POINT ( 'NONE',  ( 18.52928932188134326, 15.30185809848915746, -222.9551995274939316 ) ) ;
#46064=DIRECTION ( 'NONE',  ( 1.000000000000000000, 0.000000000000000000, 0.000000000000000000 ) ) ;
#46074=VERTEX_POINT ( 'NONE', #18250 ) ;
#46083=CARTESIAN_POINT ( 'NONE',  ( 21.14999999999999503, -1.330006220153263641, -194.8931527402181700 ) ) ;
#46133=CIRCLE ( 'NONE', #108494, 0.1000000000000003525 ) ;
#46139=DIRECTION ( 'NONE',  ( 1.734723475976817507E-14, 0.2128009952263604232, -0.9770955615653316162 ) ) ;
#46152=CIRCLE ( 'NONE', #245886, 0.09999999999999939493 ) ;
#46154=TOROIDAL_SURFACE ( 'NONE', #183724, 0.4000000000000010214, 0.1000000000000000056 ) ;
#46180=CARTESIAN_POINT ( 'NONE',  ( 21.05000000000000071, 0.3882413827466408840, -209.1776850584169551 ) ) ;
#46207=DIRECTION ( 'NONE',  ( -1.000000000000000000, -0.000000000000000000, -0.000000000000000000 ) ) ;
#46213=FACE_OUTER_BOUND ( 'NONE', #130376, .T. ) ;
#46247=ORIENTED_EDGE ( 'NONE', *, *, #180886, .F. ) ;
#46279=CARTESIAN_POINT ( 'NONE',  ( -18.50000000000000711, 12.97363049771892207, -205.3537238898406940 ) ) ;
#46284=ORIENTED_EDGE ( 'NONE', *, *, #60034, .F. ) ;
#46300=EDGE_LOOP ( 'NONE', ( #173428, #33382, #153297 ) ) ;
#46313=CARTESIAN_POINT ( 'NONE',  ( -23.25000000000000000, 7.575715430069919876, -235.7846019917273281 ) ) ;
#46351=CARTESIAN_POINT ( 'NONE',  ( -23.15000000000000213, -7.176961358819842651, -212.6889627706600834 ) ) ;
#46352=CARTESIAN_POINT ( 'NONE',  ( -23.25000000000000000, -0.8618440306552699326, -197.0427629756619297 ) ) ;
#46360=ORIENTED_EDGE ( 'NONE', *, *, #89406, .F. ) ;
#46438=ADVANCED_FACE ( 'NONE', ( #179598 ), #243160, .F. ) ;
#46439=DIRECTION ( 'NONE',  ( 0.000000000000000000, -0.9976611540403004241, -0.06835365183350541884 ) ) ;
#46453=AXIS2_PLACEMENT_3D ( 'NONE', #120116, #101759, #157968 ) ;
#46458=CARTESIAN_POINT ( 'NONE',  ( -20.87155475150660777, 17.14044013043752557, -224.4860178609578156 ) ) ;
#46460=AXIS2_PLACEMENT_3D ( 'NONE', #70533, #109615, #228300 ) ;
#46467=DIRECTION ( 'NONE',  ( 0.000000000000000000, 0.2128009952263603677, -0.9770955615653315052 ) ) ;
#46475=DIRECTION ( 'NONE',  ( 0.000000000000000000, 0.3042567129659888292, 0.9525900758537912960 ) ) ;
#46508=DIRECTION ( 'NONE',  ( -0.000000000000000000, 0.9770955615653316162, 0.2128009952263604232 ) ) ;
#46543=VECTOR ( 'NONE', #196866, 1000.000000000000000 ) ;
#46548=EDGE_CURVE ( 'NONE', #175208, #141902, #101669, .T. ) ;
#46569=CARTESIAN_POINT ( 'NONE',  ( -1.739115166359751170E-14, 13.98997548377050748, -210.4902890347897255 ) ) ;
#46614=DIRECTION ( 'NONE',  ( 0.000000000000000000, 0.2128009952263603122, -0.9770955615653315052 ) ) ;
#46651=CARTESIAN_POINT ( 'NONE',  ( 21.05000000000000071, 0.9150442794848463457, -205.2015109147324665 ) ) ;
#46663=AXIS2_PLACEMENT_3D ( 'NONE', #81783, #242173, #103922 ) ;
#46690=TOROIDAL_SURFACE ( 'NONE', #159170, 6.258578643762700899, 0.1000000000000000056 ) ;
#46694=B_SPLINE_CURVE_WITH_KNOTS ( 'NONE', 3,
 ( #6740, #27630, #187958, #26319, #86252, #5430, #203661, #163266, #65428, #64156, #48428, #44596, #224501, #108418, #165839, #129264 ),
 .UNSPECIFIED., .F., .F.,
 ( 4, 3, 3, 3, 3, 4 ),
 ( 0.000000000000000000, 2.372700795693673338E-05, 5.739057815866516020E-05, 9.073899019180219387E-05, 0.0001243544287365659932, 0.0001585386695601174523 ),
 .UNSPECIFIED. ) ;
#46697=CARTESIAN_POINT ( 'NONE',  ( 23.25000000000000000, -3.281532336344783030, -226.3283167004136942 ) ) ;
#46702=CARTESIAN_POINT ( 'NONE',  ( 22.39999999999999503, 11.45959274888150681, -198.4018787499352641 ) ) ;
#46709=VERTEX_POINT ( 'NONE', #52894 ) ;
#46710=ORIENTED_EDGE ( 'NONE', *, *, #217162, .T. ) ;
#46713=DIRECTION ( 'NONE',  ( 0.000000000000000000, 0.2128009952263485993, -0.9770955615653341697 ) ) ;
#46771=AXIS2_PLACEMENT_3D ( 'NONE', #36364, #115880, #195436 ) ;
#46782=AXIS2_PLACEMENT_3D ( 'NONE', #75045, #9893, #228956 ) ;
#46783=FACE_OUTER_BOUND ( 'NONE', #241974, .T. ) ;
#46797=CARTESIAN_POINT ( 'NONE',  ( 22.39999999999999503, -1.657885652111590780, -193.3876638332971538 ) ) ;
#46811=CARTESIAN_POINT ( 'NONE',  ( -18.55121869061588669, 18.40663661316795796, -236.9846611508999388 ) ) ;
#46817=TOROIDAL_SURFACE ( 'NONE', #125936, 0.2000000000000000111, 0.1000000000000000056 ) ;
#46858=CARTESIAN_POINT ( 'NONE',  ( -22.46246831459151494, -2.457692491805503643, -189.6123061134737497 ) ) ;
#46869=ORIENTED_EDGE ( 'NONE', *, *, #87563, .T. ) ;
#46879=CARTESIAN_POINT ( 'NONE',  ( 21.05000000000000071, 10.45765418377745526, -207.3040725013013912 ) ) ;
#46912=ORIENTED_EDGE ( 'NONE', *, *, #117350, .T. ) ;
#46915=ADVANCED_FACE ( 'NONE', ( #81424 ), #105954, .T. ) ;
#46936=DIRECTION ( 'NONE',  ( 0.000000000000000000, 0.2128009952263616722, -0.9770955615653312831 ) ) ;
#46955=CIRCLE ( 'NONE', #192734, 0.1000000000000054040 ) ;
#46957=ORIENTED_EDGE ( 'NONE', *, *, #151356, .F. ) ;
#47042=CIRCLE ( 'NONE', #163588, 0.1000000000000060424 ) ;
#47083=CARTESIAN_POINT ( 'NONE',  ( 21.07888907270776002, 13.08009968415031210, -210.6589686082192827 ) ) ;
#47098=EDGE_CURVE ( 'NONE', #38095, #194263, #59773, .T. ) ;
#47108=AXIS2_PLACEMENT_3D ( 'NONE', #16045, #134651, #91702 ) ;
#47112=ORIENTED_EDGE ( 'NONE', *, *, #102913, .F. ) ;
#47138=CIRCLE ( 'NONE', #209661, 0.1999999999999929334 ) ;
#47172=CARTESIAN_POINT ( 'NONE',  ( -23.15000000000000213, -6.688413578037177842, -212.5825622730469036 ) ) ;
#47198=CYLINDRICAL_SURFACE ( 'NONE', #234954, 12.87499999999999467 ) ;
#47227=CARTESIAN_POINT ( 'NONE',  ( -20.85000000000000142, 8.809961202382808665, -241.4517562488062481 ) ) ;
#47230=ORIENTED_EDGE ( 'NONE', *, *, #107891, .F. ) ;
#47263=DIRECTION ( 'NONE',  ( 0.000000000000000000, -0.2128009952263602012, 0.9770955615653315052 ) ) ;
#47277=ORIENTED_EDGE ( 'NONE', *, *, #79767, .F. ) ;
#47312=CARTESIAN_POINT ( 'NONE',  ( -18.39999999999999858, -11.68510997261236817, -191.5194565067366455 ) ) ;
#47331=FACE_OUTER_BOUND ( 'NONE', #214288, .T. ) ;
#47358=DIRECTION ( 'NONE',  ( 1.000000000000000000, 0.000000000000000000, 0.000000000000000000 ) ) ;
#47363=CARTESIAN_POINT ( 'NONE',  ( 20.85000000000000142, 14.83511725869332132, -235.8887435844146978 ) ) ;
#47415=CARTESIAN_POINT ( 'NONE',  ( -23.15000000000000213, 8.980461154494397746, -187.0187154576991304 ) ) ;
#47418=CARTESIAN_POINT ( 'NONE',  ( 18.50000000000000355, -7.664561988343767673, -210.0810037954756524 ) ) ;
#47438=DIRECTION ( 'NONE',  ( 0.000000000000000000, 0.2128009952263237581, -0.9770955615653394988 ) ) ;
#47488=EDGE_CURVE ( 'NONE', #106308, #155405, #174868, .T. ) ;
#47493=AXIS2_PLACEMENT_3D ( 'NONE', #107626, #28124, #187193 ) ;
#47515=ORIENTED_EDGE ( 'NONE', *, *, #134884, .F. ) ;
#47553=LINE ( 'NONE', #127107, #166100 ) ;
#47581=AXIS2_PLACEMENT_3D ( 'NONE', #131919, #211459, #35142 ) ;
#47606=EDGE_CURVE ( 'NONE', #109848, #150544, #1713, .T. ) ;
#47637=EDGE_LOOP ( 'NONE', ( #37816, #210160, #247053, #120861 ) ) ;
#47662=DIRECTION ( 'NONE',  ( 0.000000000000000000, 0.2128009952263601456, -0.9770955615653315052 ) ) ;
#47690=VERTEX_POINT ( 'NONE', #63854 ) ;
#47702=CIRCLE ( 'NONE', #193476, 0.1000000000000025591 ) ;
#47710=DIRECTION ( 'NONE',  ( 0.000000000000000000, 0.2128009952263603677, -0.9770955615653313941 ) ) ;
#47739=AXIS2_PLACEMENT_3D ( 'NONE', #13169, #152706, #92685 ) ;
#47741=CARTESIAN_POINT ( 'NONE',  ( -20.94560253601877164, 17.12224500340141020, -224.4024732428971731 ) ) ;
#47761=CARTESIAN_POINT ( 'NONE',  ( 21.05000000000000071, 9.459578591139306880, -220.9384041938172345 ) ) ;
#47794=CARTESIAN_POINT ( 'NONE',  ( -23.15000000000000213, 6.878457983866232972, -212.1414458560986986 ) ) ;
#47833=SPHERICAL_SURFACE ( 'NONE', #44987, 0.1000000000000000056 ) ;
#47859=EDGE_LOOP ( 'NONE', ( #88, #57658, #257367, #137807, #129739, #119793, #252679 ) ) ;
#47912=EDGE_LOOP ( 'NONE', ( #179348, #93806, #52684, #152424 ) ) ;
#47914=ORIENTED_EDGE ( 'NONE', *, *, #172092, .T. ) ;
#47929=ORIENTED_EDGE ( 'NONE', *, *, #33728, .F. ) ;
#47939=ORIENTED_EDGE ( 'NONE', *, *, #101204, .F. ) ;
#47943=DIRECTION ( 'NONE',  ( 0.000000000000000000, 0.3427706569149662763, -0.9394191166662954062 ) ) ;
#47965=CARTESIAN_POINT ( 'NONE',  ( 21.05000000000000071, 9.290509600414956992, -221.0404682250134840 ) ) ;
#47990=CARTESIAN_POINT ( 'NONE',  ( -20.94999999999999929, 0.7653315920341953182, -212.6731560895497353 ) ) ;
#48012=DIRECTION ( 'NONE',  ( 0.000000000000000000, 0.2128009952263618110, -0.9770955615653311721 ) ) ;
#48042=CARTESIAN_POINT ( 'NONE',  ( -20.64999999999999858, 1.148907358139439339E-11, -201.0000000000015064 ) ) ;
#48080=LINE ( 'NONE', #127627, #34966 ) ;
#48106=AXIS2_PLACEMENT_3D ( 'NONE', #76382, #112971, #232938 ) ;
#48109=AXIS2_PLACEMENT_3D ( 'NONE', #56001, #215107, #36499 ) ;
#48111=CARTESIAN_POINT ( 'NONE',  ( 18.59999999999997655, 8.809961202382808665, -241.4517562488062481 ) ) ;
#48120=CARTESIAN_POINT ( 'NONE',  ( 18.59999999999999432, 2.859758780633683273, -208.6670499591424459 ) ) ;
#48123=CARTESIAN_POINT ( 'NONE',  ( 18.37172112093794851, -0.7723029343291464288, -242.4300124561790426 ) ) ;
#48141=DIRECTION ( 'NONE',  ( 0.000000000000000000, -0.08413937888704772772, 0.9964539953858893018 ) ) ;
#48145=EDGE_LOOP ( 'NONE', ( #150547, #247648, #340, #47914 ) ) ;
#48187=ORIENTED_EDGE ( 'NONE', *, *, #23916, .F. ) ;
#48195=ADVANCED_FACE ( 'NONE', ( #89190 ), #218364, .T. ) ;
#48215=ORIENTED_EDGE ( 'NONE', *, *, #168013, .T. ) ;
#48251=ORIENTED_EDGE ( 'NONE', *, *, #75850, .F. ) ;
#48293=DIRECTION ( 'NONE',  ( 0.000000000000000000, 0.2128009952263603677, -0.9770955615653313941 ) ) ;
#48309=FACE_OUTER_BOUND ( 'NONE', #147598, .T. ) ;
#48337=DIRECTION ( 'NONE',  ( 1.000000000000000000, 0.000000000000000000, 0.000000000000000000 ) ) ;
#48338=FACE_OUTER_BOUND ( 'NONE', #230796, .T. ) ;
#48354=CARTESIAN_POINT ( 'NONE',  ( -18.59999999999999787, -7.558719773525646168, -210.9360835033311332 ) ) ;
#48407=EDGE_CURVE ( 'NONE', #35875, #138363, #102006, .T. ) ;
#48409=EDGE_LOOP ( 'NONE', ( #74583, #69396, #79937, #42684 ) ) ;
#48428=CARTESIAN_POINT ( 'NONE',  ( 21.09706851349341861, 11.17857743693056527, -211.0878094224673873 ) ) ;
#48489=CARTESIAN_POINT ( 'NONE',  ( 18.56308993302889832, 15.40745845255181301, -222.9635632280946993 ) ) ;
#48519=ADVANCED_FACE ( 'NONE', ( #30223 ), #8089, .T. ) ;
#48570=EDGE_LOOP ( 'NONE', ( #31686, #139272, #89239, #90857 ) ) ;
#48577=ORIENTED_EDGE ( 'NONE', *, *, #74999, .T. ) ;
#48605=FACE_OUTER_BOUND ( 'NONE', #181294, .T. ) ;
#48622=LINE ( 'NONE', #207724, #208305 ) ;
#48623=FACE_OUTER_BOUND ( 'NONE', #71615, .T. ) ;
#48630=CIRCLE ( 'NONE', #161075, 0.09999999999998904210 ) ;
#48671=ORIENTED_EDGE ( 'NONE', *, *, #56555, .F. ) ;
#48678=CARTESIAN_POINT ( 'NONE',  ( 22.39999999999999503, 11.36188319272497438, -198.4231588494578773 ) ) ;
#48706=FACE_OUTER_BOUND ( 'NONE', #239439, .T. ) ;
#48718=EDGE_LOOP ( 'NONE', ( #67818, #38788, #220254, #51076 ) ) ;
#48730=CARTESIAN_POINT ( 'NONE',  ( 20.97468175916148780, 12.98972486229050993, -210.7130060050627094 ) ) ;
#48732=CARTESIAN_POINT ( 'NONE',  ( 23.14999999999999858, 8.013878543493270001, -211.9507248933737458 ) ) ;
#48735=ORIENTED_EDGE ( 'NONE', *, *, #68579, .F. ) ;
#48749=DIRECTION ( 'NONE',  ( 2.952720810173289112E-16, -0.9770955615653316162, -0.2128009952263598403 ) ) ;
#48752=VERTEX_POINT ( 'NONE', #137012 ) ;
#48832=LINE ( 'NONE', #87936, #73805 ) ;
#48838=EDGE_CURVE ( 'NONE', #68130, #32779, #221664, .T. ) ;
#48851=FACE_OUTER_BOUND ( 'NONE', #77091, .T. ) ;
#48852=DIRECTION ( 'NONE',  ( -0.000000000000000000, -0.7397890806274223241, -0.6728388485993012091 ) ) ;
#48855=ORIENTED_EDGE ( 'NONE', *, *, #107595, .F. ) ;
#48877=AXIS2_PLACEMENT_3D ( 'NONE', #130119, #31067, #110560 ) ;
#48887=CARTESIAN_POINT ( 'NONE',  ( -18.59999999999999787, 0.8650195716890449749, -212.6652626294507229 ) ) ;
#48942=DIRECTION ( 'NONE',  ( -1.000000000000000000, 0.000000000000000000, 0.000000000000000000 ) ) ;
#48943=VERTEX_POINT ( 'NONE', #241269 ) ;
#48970=ORIENTED_EDGE ( 'NONE', *, *, #238869, .T. ) ;
#48978=CARTESIAN_POINT ( 'NONE',  ( -21.05000000000000071, -7.817436562502985353, -209.8389866834999395 ) ) ;
#48987=ORIENTED_EDGE ( 'NONE', *, *, #31919, .T. ) ;
#49007=ORIENTED_EDGE ( 'NONE', *, *, #132643, .F. ) ;
#49011=CARTESIAN_POINT ( 'NONE',  ( -21.05000000000000071, -10.74476030654554215, -206.4104182790846096 ) ) ;
#49026=CIRCLE ( 'NONE', #219895, 0.1000000000000016293 ) ;
#49034=CYLINDRICAL_SURFACE ( 'NONE', #76608, 0.1000000000000055844 ) ;
#49059=AXIS2_PLACEMENT_3D ( 'NONE', #59545, #60854, #21756 ) ;
#49064=VERTEX_POINT ( 'NONE', #86835 ) ;
#49069=CARTESIAN_POINT ( 'NONE',  ( 21.14999999999999858, 11.19216743630477673, -211.0996217964688526 ) ) ;
#49083=DIRECTION ( 'NONE',  ( 1.000000000000000000, -0.000000000000000000, 0.000000000000000000 ) ) ;
#49096=ORIENTED_EDGE ( 'NONE', *, *, #101630, .T. ) ;
#49101=AXIS2_PLACEMENT_3D ( 'NONE', #72279, #194809, #55235 ) ;
#49111=ORIENTED_EDGE ( 'NONE', *, *, #24067, .T. ) ;
#49121=EDGE_CURVE ( 'NONE', #77509, #247780, #239522, .T. ) ;
#49194=DIRECTION ( 'NONE',  ( 1.000000000000000000, 0.000000000000000000, 0.000000000000000000 ) ) ;
#49251=DIRECTION ( 'NONE',  ( -0.000000000000000000, 0.2128009952263604232, -0.9770955615653316162 ) ) ;
#49261=DIRECTION ( 'NONE',  ( 0.000000000000000000, 0.2128009952263603677, -0.9770955615653313941 ) ) ;
#49280=ORIENTED_EDGE ( 'NONE', *, *, #114406, .F. ) ;
#49285=ORIENTED_EDGE ( 'NONE', *, *, #1060, .F. ) ;
#49318=AXIS2_PLACEMENT_3D ( 'NONE', #227423, #44945, #249577 ) ;
#49333=LINE ( 'NONE', #105420, #144552 ) ;
#49351=DIRECTION ( 'NONE',  ( -1.000000000000000000, 0.000000000000000000, 0.000000000000000000 ) ) ;
#49386=CARTESIAN_POINT ( 'NONE',  ( -20.54999999999999716, 6.878457983866232972, -212.1414458560986986 ) ) ;
#49393=CARTESIAN_POINT ( 'NONE',  ( -22.16821283564876666, 7.385839301279057523, -199.3914429501938343 ) ) ;
#49395=ADVANCED_FACE ( 'NONE', ( #4123 ), #64108, .F. ) ;
#49402=DIRECTION ( 'NONE',  ( 0.000000000000000000, -0.2128009952263604232, 0.9770955615653316162 ) ) ;
#49405=DIRECTION ( 'NONE',  ( -1.000000000000000000, 0.000000000000000000, 0.000000000000000000 ) ) ;
#49413=CARTESIAN_POINT ( 'NONE',  ( 20.46382478191414833, 10.51603790215317602, -207.4557705628764666 ) ) ;
#49416=DIRECTION ( 'NONE',  ( -3.469446951953426755E-14, -0.2128009952263403282, 0.9770955615653358350 ) ) ;
#49439=CIRCLE ( 'NONE', #116088, 0.1000000000000050987 ) ;
#49477=ORIENTED_EDGE ( 'NONE', *, *, #211752, .T. ) ;
#49483=DIRECTION ( 'NONE',  ( 0.000000000000000000, 0.1678971852675816834, 0.9858045116447902156 ) ) ;
#49490=DIRECTION ( 'NONE',  ( 0.000000000000000000, 0.2128009952263678062, -0.9770955615653298398 ) ) ;
#49515=ORIENTED_EDGE ( 'NONE', *, *, #244160, .T. ) ;
#49552=DIRECTION ( 'NONE',  ( 0.000000000000000000, -0.2128009952263603954, 0.9770955615653315052 ) ) ;
#49561=EDGE_CURVE ( 'NONE', #76080, #204167, #11938, .T. ) ;
#49566=ORIENTED_EDGE ( 'NONE', *, *, #106138, .F. ) ;
#49572=CARTESIAN_POINT ( 'NONE',  ( -20.94999999999999929, 0.2428138352382497867, -200.9114032742886309 ) ) ;
#49581=CARTESIAN_POINT ( 'NONE',  ( -20.85000000000000142, -4.352039508298082282, -236.2331130063498676 ) ) ;
#49616=DIRECTION ( 'NONE',  ( 0.000000000000000000, -0.2128009952263604232, 0.9770955615653316162 ) ) ;
#49648=CARTESIAN_POINT ( 'NONE',  ( 21.09610168723073542, -1.324627966594374540, -194.7600028027378869 ) ) ;
#49655=LINE ( 'NONE', #169654, #129549 ) ;
#49669=ORIENTED_EDGE ( 'NONE', *, *, #220698, .F. ) ;
#49679=DIRECTION ( 'NONE',  ( 1.040834085586108490E-13, -0.9742838591452925856, -0.2253241261138180518 ) ) ;
#49727=ORIENTED_EDGE ( 'NONE', *, *, #24359, .F. ) ;
#49759=ORIENTED_EDGE ( 'NONE', *, *, #204528, .F. ) ;
#49770=FACE_OUTER_BOUND ( 'NONE', #118096, .T. ) ;
#49776=CARTESIAN_POINT ( 'NONE',  ( 18.50000000000000000, 15.30611090022306620, -222.9706416475797255 ) ) ;
#49793=CIRCLE ( 'NONE', #249710, 4.000000000000006217 ) ;
#49815=CARTESIAN_POINT ( 'NONE',  ( 23.14999999999999858, 9.480858690661944976, -221.0361137499737936 ) ) ;
#49820=DIRECTION ( 'NONE',  ( -0.000000000000000000, 0.07893460099012301889, -0.9968797965484754720 ) ) ;
#49836=CARTESIAN_POINT ( 'NONE',  ( -21.05000000000000071, 4.288595810029049993, -211.9930862808554934 ) ) ;
#49843=CARTESIAN_POINT ( 'NONE',  ( -20.64999999999999858, 11.50825441376376901, -220.2417535673963300 ) ) ;
#49848=ORIENTED_EDGE ( 'NONE', *, *, #70443, .T. ) ;
#49856=EDGE_CURVE ( 'NONE', #192844, #143815, #107763, .T. ) ;
#49901=ADVANCED_FACE ( 'NONE', ( #109322 ), #126333, .F. ) ;
#49910=ORIENTED_EDGE ( 'NONE', *, *, #91163, .T. ) ;
#49926=ORIENTED_EDGE ( 'NONE', *, *, #236764, .F. ) ;
#49973=EDGE_CURVE ( 'NONE', #401, #245998, #78705, .T. ) ;
#49998=EDGE_LOOP ( 'NONE', ( #134251, #2974, #222966 ) ) ;
#50035=AXIS2_PLACEMENT_3D ( 'NONE', #141015, #41926, #121469 ) ;
#50064=EDGE_LOOP ( 'NONE', ( #70393, #217263, #194947, #42132 ) ) ;
#50121=ADVANCED_FACE ( 'NONE', ( #233167 ), #253970, .F. ) ;
#50123=( BOUNDED_SURFACE ( )  B_SPLINE_SURFACE ( 3, 2, ( 
 ( #64750, #245970, #25633 ),
 ( #146838, #6054, #89443 ),
 ( #85557, #226369, #46458 ),
 ( #225087, #244664, #47741 ),
 ( #43909, #26947, #66033 ),
 ( #145565, #103858, #28232 ) ),
 .UNSPECIFIED., .F., .F., .F. ) 
 B_SPLINE_SURFACE_WITH_KNOTS ( ( 4, 2, 4 ),
 ( 3, 3 ),
 ( 1.570796326794897668, 2.356194490192346169, 3.141592653589794448 ),
 ( 0.000000000000000000, 1.000000000000000000 ),
 .UNSPECIFIED. ) 
 GEOMETRIC_REPRESENTATION_ITEM ( )  RATIONAL_B_SPLINE_SURFACE ( (
 ( 1.000000000000000000, 0.7071067811865806574, 1.000000000000000000),
 ( 1.000000000000000000, 0.6611148371769989263, 1.000000000000000000),
 ( 1.000000000000000000, 0.6092287576708182995, 1.000000000000000000),
 ( 1.000000000000000000, 0.5278258667044445351, 1.000000000000000000),
 ( 1.000000000000000000, 0.4993418825344856371, 1.000000000000000000),
 ( 1.000000000000000000, 0.5000000000000655032, 1.000000000000000000) ) ) 
 REPRESENTATION_ITEM ( '' )  SURFACE ( )  );
#50135=CARTESIAN_POINT ( 'NONE',  ( 20.85000000000000142, 7.804459559388681633, -245.4620200072988325 ) ) ;
#50146=CARTESIAN_POINT ( 'NONE',  ( 23.14999999999999858, 9.125777775466493935, -211.6520035670780544 ) ) ;
#50159=DIRECTION ( 'NONE',  ( 0.000000000000000000, 0.2128009952263605342, -0.9770955615653315052 ) ) ;
#50228=CIRCLE ( 'NONE', #183350, 0.5000000000000009992 ) ;
#50235=FACE_OUTER_BOUND ( 'NONE', #179675, .T. ) ;
#50247=DIRECTION ( 'NONE',  ( -0.000000000000000000, 0.9770955615653315052, 0.2128009952263602844 ) ) ;
#50322=VECTOR ( 'NONE', #147111, 1000.000000000000227 ) ;
#50362=B_SPLINE_CURVE_WITH_KNOTS ( 'NONE', 3,
 ( #103340, #87631, #124225, #83755, #244140, #128068, #66807, #107205 ),
 .UNSPECIFIED., .F., .F.,
 ( 4, 2, 2, 4 ),
 ( 0.000000000000000000, 0.0002181133598168996678, 0.0003271700397253495289, 0.0004362267196337993357 ),
 .UNSPECIFIED. ) ;
#50380=ORIENTED_EDGE ( 'NONE', *, *, #53819, .F. ) ;
#50407=AXIS2_PLACEMENT_3D ( 'NONE', #35380, #79577, #194438 ) ;
#50452=EDGE_LOOP ( 'NONE', ( #169785, #227032, #171685, #148168, #193428 ) ) ;
#50480=DIRECTION ( 'NONE',  ( 0.000000000000000000, -0.9770955615653315052, -0.2128009952263607008 ) ) ;
#50494=CARTESIAN_POINT ( 'NONE',  ( 21.05000000000000071, 11.83110912403452097, -206.0549139711134785 ) ) ;
#50514=B_SPLINE_CURVE_WITH_KNOTS ( 'NONE', 3,
 ( #250816, #35666, #209123, #55156, #214273, #10946, #133446, #52618, #233836, #12241, #149181, #111323, #173907, #253390, #228716, #91754, #72208, #53912, #231282 ),
 .UNSPECIFIED., .F., .F.,
 ( 4, 3, 3, 3, 3, 3, 4 ),
 ( -2.000416914658646987E-06, 0.000000000000000000, 4.714008503743518199E-05, 9.979203887776679231E-05, 0.0001372215519229392155, 0.0001635031576220894356, 0.0001900083748504071714 ),
 .UNSPECIFIED. ) ;
#50526=ORIENTED_EDGE ( 'NONE', *, *, #226283, .T. ) ;
#50612=ORIENTED_EDGE ( 'NONE', *, *, #26350, .F. ) ;
#50635=CARTESIAN_POINT ( 'NONE',  ( 21.04999999999999716, -1.448506596209664377, -194.7513623756925085 ) ) ;
#50641=CYLINDRICAL_SURFACE ( 'NONE', #190352, 0.1000000000000055844 ) ;
#50654=CIRCLE ( 'NONE', #83945, 3.900000000000000799 ) ;
#50676=ORIENTED_EDGE ( 'NONE', *, *, #18207, .T. ) ;
#50679=CARTESIAN_POINT ( 'NONE',  ( -22.59999999999999432, 11.46682355977092804, -198.4356847424421062 ) ) ;
#50683=DIRECTION ( 'NONE',  ( 1.000000000000000000, 0.000000000000000000, 0.000000000000000000 ) ) ;
#50736=DIRECTION ( 'NONE',  ( 0.000000000000000000, 0.2211802418851555596, -0.9752329468386637945 ) ) ;
#50739=CARTESIAN_POINT ( 'NONE',  ( -23.15000000000000213, -5.011722593499801093, -233.2041167654973322 ) ) ;
#50750=CARTESIAN_POINT ( 'NONE',  ( 23.24999999999999645, 9.273719881888197847, -221.1390486761779925 ) ) ;
#50758=B_SPLINE_CURVE_WITH_KNOTS ( 'NONE', 3,
 ( #166804, #49393, #145907, #225435, #128936, #165501, #88485 ),
 .UNSPECIFIED., .F., .F.,
 ( 4, 3, 4 ),
 ( 0.000000000000000000, 0.0009834301579440007414, 0.001767853679402678433 ),
 .UNSPECIFIED. ) ;
#50783=CARTESIAN_POINT ( 'NONE',  ( 23.14999999999998437, -11.48087284838115885, -203.5004116939112464 ) ) ;
#50797=ORIENTED_EDGE ( 'NONE', *, *, #12127, .T. ) ;
#50802=LINE ( 'NONE', #105638, #109367 ) ;
#50808=CARTESIAN_POINT ( 'NONE',  ( -20.94999999999999929, 14.76712877540431812, -235.7629163147296083 ) ) ;
#50832=CARTESIAN_POINT ( 'NONE',  ( -21.11833042828115126, -1.364701729829611798, -194.7004781828140665 ) ) ;
#50863=EDGE_LOOP ( 'NONE', ( #32135, #31116, #54248 ) ) ;
#50879=CIRCLE ( 'NONE', #238331, 0.09999999999999939493 ) ;
#50913=CARTESIAN_POINT ( 'NONE',  ( -20.94999999999999929, 7.872214528623318053, -209.6555322433423783 ) ) ;
#50932=CARTESIAN_POINT ( 'NONE',  ( 22.47809213839789066, -2.442448617817909451, -189.6088748368766517 ) ) ;
#50935=AXIS2_PLACEMENT_3D ( 'NONE', #152555, #91272, #134223 ) ;
#50937=CYLINDRICAL_SURFACE ( 'NONE', #185185, 0.09999999999999939493 ) ;
#50940=DIRECTION ( 'NONE',  ( 0.000000000000000000, 0.2128009952263403282, -0.9770955615653358350 ) ) ;
#50944=CARTESIAN_POINT ( 'NONE',  ( -21.08035267497491816, -1.266598828715301162, -194.7957211280704257 ) ) ;
#50960=DIRECTION ( 'NONE',  ( 1.000000000000000000, 0.000000000000000000, 0.000000000000000000 ) ) ;
#50979=DIRECTION ( 'NONE',  ( -1.000000000000000000, 0.000000000000000000, 0.000000000000000000 ) ) ;
#50999=VERTEX_POINT ( 'NONE', #11585 ) ;
#51005=EDGE_CURVE ( 'NONE', #89546, #111950, #224183, .T. ) ;
#51012=EDGE_LOOP ( 'NONE', ( #7577, #252561, #53967, #25081 ) ) ;
#51020=DIRECTION ( 'NONE',  ( 0.000000000000000000, -0.7397890806274222131, -0.6728388485993012091 ) ) ;
#51043=AXIS2_PLACEMENT_3D ( 'NONE', #146922, #187370, #227757 ) ;
#51056=ORIENTED_EDGE ( 'NONE', *, *, #152690, .F. ) ;
#51057=ORIENTED_EDGE ( 'NONE', *, *, #41578, .F. ) ;
#51076=ORIENTED_EDGE ( 'NONE', *, *, #99495, .F. ) ;
#51084=CARTESIAN_POINT ( 'NONE',  ( 18.50000324121758055, 18.34775554461876013, -236.8759397601554042 ) ) ;
#51093=EDGE_CURVE ( 'NONE', #200518, #236679, #53265, .T. ) ;
#51094=AXIS2_PLACEMENT_3D ( 'NONE', #123440, #145556, #227659 ) ;
#51103=ORIENTED_EDGE ( 'NONE', *, *, #121678, .F. ) ;
#51157=DIRECTION ( 'NONE',  ( 0.000000000000000000, -0.2128009952263604232, 0.9770955615653316162 ) ) ;
#51186=EDGE_CURVE ( 'NONE', #164707, #9130, #108333, .T. ) ;
#51199=CARTESIAN_POINT ( 'NONE',  ( -23.25000000000000000, 7.128833340094563376, -233.7327013124401276 ) ) ;
#51216=EDGE_CURVE ( 'NONE', #129923, #32161, #104383, .T. ) ;
#51228=AXIS2_PLACEMENT_3D ( 'NONE', #204983, #9364, #6806 ) ;
#51242=CARTESIAN_POINT ( 'NONE',  ( -18.50000000000000000, 14.86477715130881272, -235.7932433709592601 ) ) ;
#51244=ORIENTED_EDGE ( 'NONE', *, *, #106905, .F. ) ;
#51255=CARTESIAN_POINT ( 'NONE',  ( 20.94999999999999574, 10.52493806863738079, -207.3780514093641330 ) ) ;
#51256=ORIENTED_EDGE ( 'NONE', *, *, #232609, .F. ) ;
#51272=LINE ( 'NONE', #109987, #174092 ) ;
#51285=ORIENTED_EDGE ( 'NONE', *, *, #44385, .T. ) ;
#51303=CIRCLE ( 'NONE', #42969, 0.09999999999999939493 ) ;
#51327=ORIENTED_EDGE ( 'NONE', *, *, #245359, .T. ) ;
#51337=AXIS2_PLACEMENT_3D ( 'NONE', #78583, #179018, #254634 ) ;
#51357=CARTESIAN_POINT ( 'NONE',  ( -20.64999999999999858, 4.590145742703442444, -213.0289728181953706 ) ) ;
#51372=AXIS2_PLACEMENT_3D ( 'NONE', #113168, #192715, #93606 ) ;
#51385=CIRCLE ( 'NONE', #5603, 11.80000000000000959 ) ;
#51397=DIRECTION ( 'NONE',  ( 6.484947573744954877E-15, 0.9858045116447881062, -0.1678971852675942011 ) ) ;
#51404=VERTEX_POINT ( 'NONE', #103906 ) ;
#51412=AXIS2_PLACEMENT_3D ( 'NONE', #239587, #139165, #19247 ) ;
#51420=EDGE_CURVE ( 'NONE', #136449, #248593, #226422, .T. ) ;
#51438=B_SPLINE_CURVE_WITH_KNOTS ( 'NONE', 3,
 ( #13402, #92910, #232461, #113764, #134594, #155505, #193319, #216718 ),
 .UNSPECIFIED., .F., .F.,
 ( 4, 2, 2, 4 ),
 ( 0.000000000000000000, 0.0002114466876442107866, 0.0003171700314663170473, 0.0004228933752884233622 ),
 .UNSPECIFIED. ) ;
#51446=CARTESIAN_POINT ( 'NONE',  ( -22.50000000000000000, -1.330006220153263641, -194.8931527402181700 ) ) ;
#51478=EDGE_CURVE ( 'NONE', #204167, #178200, #210738, .T. ) ;
#51485=CIRCLE ( 'NONE', #168097, 0.1000000000000033223 ) ;
#51503=CARTESIAN_POINT ( 'NONE',  ( -23.25000000000000000, 14.70949956575304185, -235.9560995168023112 ) ) ;
#51556=ADVANCED_FACE ( 'NONE', ( #76339 ), #195710, .T. ) ;
#51588=TOROIDAL_SURFACE ( 'NONE', #126640, 11.65000000000000036, 0.1000000000000000056 ) ;
#51685=TOROIDAL_SURFACE ( 'NONE', #193204, 0.2000000000000000111, 0.1000000000000000056 ) ;
#51709=AXIS2_PLACEMENT_3D ( 'NONE', #246347, #207233, #111983 ) ;
#51747=CARTESIAN_POINT ( 'NONE',  ( -20.94999999999999929, 4.252251777740766236, -211.8999245327126744 ) ) ;
#51758=ORIENTED_EDGE ( 'NONE', *, *, #118426, .T. ) ;
#51820=CARTESIAN_POINT ( 'NONE',  ( -23.25000000000000000, 7.675662554762638479, -241.7139905447625381 ) ) ;
#51841=CARTESIAN_POINT ( 'NONE',  ( 20.93302460841142931, 18.38637412622486877, -236.9471295141160283 ) ) ;
#51886=DIRECTION ( 'NONE',  ( 0.000000000000000000, 0.2128009952263604232, -0.9770955615653316162 ) ) ;
#51901=VERTEX_POINT ( 'NONE', #252125 ) ;
#51935=EDGE_CURVE ( 'NONE', #9164, #3546, #33135, .T. ) ;
#51943=ORIENTED_EDGE ( 'NONE', *, *, #247634, .T. ) ;
#51976=AXIS2_PLACEMENT_3D ( 'NONE', #19007, #201492, #141523 ) ;
#52010=ORIENTED_EDGE ( 'NONE', *, *, #118057, .T. ) ;
#52044=EDGE_LOOP ( 'NONE', ( #70240, #206983, #230255, #1889, #124724 ) ) ;
#52058=ORIENTED_EDGE ( 'NONE', *, *, #72076, .T. ) ;
#52062=AXIS2_PLACEMENT_3D ( 'NONE', #118853, #198369, #140982 ) ;
#52071=TOROIDAL_SURFACE ( 'NONE', #227054, 0.2000000000000000111, 0.1000000000000000056 ) ;
#52090=ORIENTED_EDGE ( 'NONE', *, *, #24959, .F. ) ;
#52107=DIRECTION ( 'NONE',  ( 0.000000000000000000, 0.2128009952263603677, -0.9770955615653313941 ) ) ;
#52127=CARTESIAN_POINT ( 'NONE',  ( -21.09096482362077296, -1.315623836012118852, -194.7738144117574848 ) ) ;
#52134=ADVANCED_FACE ( 'NONE', ( #185440 ), #8097, .T. ) ;
#52138=VERTEX_POINT ( 'NONE', #5485 ) ;
#52147=AXIS2_PLACEMENT_3D ( 'NONE', #38204, #53899, #77301 ) ;
#52164=DIRECTION ( 'NONE',  ( 1.000000000000000000, 0.000000000000000000, 0.000000000000000000 ) ) ;
#52183=DIRECTION ( 'NONE',  ( 1.000000000000000000, 0.000000000000000000, 0.000000000000000000 ) ) ;
#52208=CIRCLE ( 'NONE', #143790, 11.65000000000001457 ) ;
#52218=ORIENTED_EDGE ( 'NONE', *, *, #191646, .F. ) ;
#52235=CARTESIAN_POINT ( 'NONE',  ( -21.08376601933334626, -1.287257433775161664, -194.7897398709591812 ) ) ;
#52243=DIRECTION ( 'NONE',  ( 0.000000000000000000, -0.9525900758537791946, 0.3042567129660269654 ) ) ;
#52252=CARTESIAN_POINT ( 'NONE',  ( -20.00857864376270001, 11.66622623553636018, -211.0987209794895421 ) ) ;
#52291=VERTEX_POINT ( 'NONE', #54577 ) ;
#52311=ORIENTED_EDGE ( 'NONE', *, *, #251507, .T. ) ;
#52325=CARTESIAN_POINT ( 'NONE',  ( 18.52928932188134326, 15.28939250479744771, -222.8979625946709007 ) ) ;
#52326=AXIS2_PLACEMENT_3D ( 'NONE', #6564, #204757, #140962 ) ;
#52330=ADVANCED_FACE ( 'NONE', ( #254056 ), #74188, .T. ) ;
#52350=VERTEX_POINT ( 'NONE', #168493 ) ;
#52367=ORIENTED_EDGE ( 'NONE', *, *, #166687, .T. ) ;
#52390=TOROIDAL_SURFACE ( 'NONE', #89998, 11.65000000000000036, 0.1000000000000000056 ) ;
#52405=DIRECTION ( 'NONE',  ( 0.000000000000000000, 0.2128009952263605065, -0.9770955615653315052 ) ) ;
#52407=ORIENTED_EDGE ( 'NONE', *, *, #193794, .T. ) ;
#52462=LINE ( 'NONE', #195870, #229252 ) ;
#52475=VECTOR ( 'NONE', #59352, 1000.000000000000227 ) ;
#52493=CIRCLE ( 'NONE', #227465, 0.1000000000000026840 ) ;
#52494=VERTEX_POINT ( 'NONE', #8733 ) ;
#52496=VECTOR ( 'NONE', #232932, 1000.000000000000000 ) ;
#52544=DIRECTION ( 'NONE',  ( -0.000000000000000000, 0.2128009952263603677, -0.9770955615653313941 ) ) ;
#52549=CARTESIAN_POINT ( 'NONE',  ( -18.52328366898032286, -0.8637155613953195754, -242.3456170079330150 ) ) ;
#52553=ORIENTED_EDGE ( 'NONE', *, *, #84789, .T. ) ;
#52561=ORIENTED_EDGE ( 'NONE', *, *, #255231, .F. ) ;
#52576=CIRCLE ( 'NONE', #73470, 0.09999999999999939493 ) ;
#52577=EDGE_CURVE ( 'NONE', #19725, #118478, #148235, .T. ) ;
#52587=DIRECTION ( 'NONE',  ( 1.000000000000000000, -0.000000000000000000, -0.000000000000000000 ) ) ;
#52592=ORIENTED_EDGE ( 'NONE', *, *, #69077, .F. ) ;
#52595=DIRECTION ( 'NONE',  ( 0.000000000000000000, -0.2128009952263604232, 0.9770955615653316162 ) ) ;
#52613=CIRCLE ( 'NONE', #252509, 11.65000000000000036 ) ;
#52618=CARTESIAN_POINT ( 'NONE',  ( -20.93975676684922504, 18.37846419038447010, -236.9325101954432853 ) ) ;
#52657=CIRCLE ( 'NONE', #198426, 0.09999999999999939493 ) ;
#52661=( GEOMETRIC_REPRESENTATION_CONTEXT ( 3 ) GLOBAL_UNCERTAINTY_ASSIGNED_CONTEXT ( ( #220031 ) ) GLOBAL_UNIT_ASSIGNED_CONTEXT ( ( #248138, #229865, #210312 ) ) REPRESENTATION_CONTEXT ( 'NONE', 'WORKASPACE' ) );
#52674=ORIENTED_EDGE ( 'NONE', *, *, #186013, .T. ) ;
#52684=ORIENTED_EDGE ( 'NONE', *, *, #160111, .F. ) ;
#52770=CARTESIAN_POINT ( 'NONE',  ( 21.05000000000000071, 6.724511449164477739, -231.8762197454659884 ) ) ;
#52773=LINE ( 'NONE', #12407, #257790 ) ;
#52803=AXIS2_PLACEMENT_3D ( 'NONE', #47794, #186050, #226427 ) ;
#52804=DIRECTION ( 'NONE',  ( 1.000000000000000000, 0.000000000000000000, 0.000000000000000000 ) ) ;
#52808=CARTESIAN_POINT ( 'NONE',  ( -23.15000000000000213, -6.688413578037177842, -212.5825622730469036 ) ) ;
#52815=DIRECTION ( 'NONE',  ( 1.000000000000000000, -0.000000000000000000, -0.000000000000000000 ) ) ;
#52884=CARTESIAN_POINT ( 'NONE',  ( 18.49999999999999289, 15.53922597307775000, -223.0482397989536025 ) ) ;
#52894=CARTESIAN_POINT ( 'NONE',  ( 20.85000000000000142, 8.809961202382808665, -241.4517562488062481 ) ) ;
#52907=CARTESIAN_POINT ( 'NONE',  ( 21.05000000000000071, 10.71906255309368383, -222.4921384173655383 ) ) ;
#52917=ORIENTED_EDGE ( 'NONE', *, *, #117924, .T. ) ;
#52934=CARTESIAN_POINT ( 'NONE',  ( 22.50000000000000000, 1.148907358139439339E-11, -201.0000000000015064 ) ) ;
#52960=ORIENTED_EDGE ( 'NONE', *, *, #125966, .F. ) ;
#53012=ORIENTED_EDGE ( 'NONE', *, *, #119328, .T. ) ;
#53023=EDGE_CURVE ( 'NONE', #136369, #207244, #246773, .T. ) ;
#53037=DIRECTION ( 'NONE',  ( 1.000000000000000000, -0.000000000000000000, -0.000000000000000000 ) ) ;
#53062=EDGE_CURVE ( 'NONE', #44396, #256585, #150939, .T. ) ;
#53084=ORIENTED_EDGE ( 'NONE', *, *, #54654, .F. ) ;
#53105=CARTESIAN_POINT ( 'NONE',  ( -20.54999999999999716, 4.768403829798271154, -213.4961173936592331 ) ) ;
#53112=CIRCLE ( 'NONE', #164975, 11.90000000000000213 ) ;
#53113=EDGE_CURVE ( 'NONE', #126073, #231419, #193577, .T. ) ;
#53124=DIRECTION ( 'NONE',  ( 0.000000000000000000, 0.2128009952263663074, -0.9770955615653301729 ) ) ;
#53159=CARTESIAN_POINT ( 'NONE',  ( -21.05000000000000071, 6.285074713407414748, -199.7187976872275499 ) ) ;
#53161=ORIENTED_EDGE ( 'NONE', *, *, #241162, .T. ) ;
#53176=CARTESIAN_POINT ( 'NONE',  ( 20.94999999999999929, 4.252251777740766236, -211.8999245327126744 ) ) ;
#53200=EDGE_CURVE ( 'NONE', #28455, #211815, #129699, .T. ) ;
#53243=ORIENTED_EDGE ( 'NONE', *, *, #143991, .T. ) ;
#53251=VECTOR ( 'NONE', #43434, 1000.000000000000000 ) ;
#53265=LINE ( 'NONE', #111967, #79255 ) ;
#53315=ORIENTED_EDGE ( 'NONE', *, *, #129665, .T. ) ;
#53331=DIRECTION ( 'NONE',  ( 0.000000000000000000, 0.9858045116447881062, -0.1678971852675942011 ) ) ;
#53334=CARTESIAN_POINT ( 'NONE',  ( 21.05000000000000071, -4.969162394454520459, -233.3995358778103935 ) ) ;
#53361=AXIS2_PLACEMENT_3D ( 'NONE', #61851, #217041, #141373 ) ;
#53370=AXIS2_PLACEMENT_3D ( 'NONE', #114659, #15589, #254151 ) ;
#53402=CARTESIAN_POINT ( 'NONE',  ( 21.03675099975490070, 11.29478665154959316, -211.1545853719440800 ) ) ;
#53403=DIRECTION ( 'NONE',  ( 0.000000000000000000, 0.9770955615653550419, 0.2128009952262526761 ) ) ;
#53413=ADVANCED_FACE ( 'NONE', ( #120486 ), #483, .T. ) ;
#53480=DIRECTION ( 'NONE',  ( 0.7071067811865474617, 0.6909108974501236844, 0.1504730267678057731 ) ) ;
#53501=EDGE_LOOP ( 'NONE', ( #44483, #173603, #226238, #194199 ) ) ;
#53528=CARTESIAN_POINT ( 'NONE',  ( 22.40736611211992368, -2.479040261793999722, -189.6172560698084624 ) ) ;
#53561=AXIS2_PLACEMENT_3D ( 'NONE', #96048, #59461, #15264 ) ;
#53582=DIRECTION ( 'NONE',  ( 0.000000000000000000, -0.9770955615653312831, -0.2128009952263614779 ) ) ;
#53609=FACE_OUTER_BOUND ( 'NONE', #237445, .T. ) ;
#53611=SHAPE_REPRESENTATION ( 'Injection Molded Chain Links 7', ( #2425 ), #52661 ) ;
#53628=CARTESIAN_POINT ( 'NONE',  ( 20.94999999999999929, 0.6656436123793473270, -212.6810495496487476 ) ) ;
#53643=CARTESIAN_POINT ( 'NONE',  ( 20.95576188350343116, 11.98566591433073647, -206.1793010702357947 ) ) ;
#53647=ORIENTED_EDGE ( 'NONE', *, *, #70388, .F. ) ;
#53664=CYLINDRICAL_SURFACE ( 'NONE', #192814, 0.09999999999999939493 ) ;
#53692=EDGE_LOOP ( 'NONE', ( #127680, #71389, #112219, #235474 ) ) ;
#53699=ORIENTED_EDGE ( 'NONE', *, *, #151633, .F. ) ;
#53701=VERTEX_POINT ( 'NONE', #25883 ) ;
#53710=AXIS2_PLACEMENT_3D ( 'NONE', #10476, #189110, #232104 ) ;
#53747=ORIENTED_EDGE ( 'NONE', *, *, #40381, .T. ) ;
#53757=AXIS2_PLACEMENT_3D ( 'NONE', #40461, #237344, #176106 ) ;
#53796=AXIS2_PLACEMENT_3D ( 'NONE', #169272, #153571, #233082 ) ;
#53819=EDGE_CURVE ( 'NONE', #76080, #253923, #217348, .T. ) ;
#53823=DIRECTION ( 'NONE',  ( 0.000000000000000000, 0.2128009952263601456, -0.9770955615653316162 ) ) ;
#53826=DIRECTION ( 'NONE',  ( -0.000000000000000000, -0.2128009952263604232, 0.9770955615653316162 ) ) ;
#53840=DIRECTION ( 'NONE',  ( 0.000000000000000000, -0.2128009952263485993, 0.9770955615653341697 ) ) ;
#53843=VERTEX_POINT ( 'NONE', #128829 ) ;
#53899=DIRECTION ( 'NONE',  ( 1.000000000000000000, -6.239415780002328221E-16, -5.674754385112861898E-16 ) ) ;
#53905=EDGE_CURVE ( 'NONE', #227863, #148073, #92638, .T. ) ;
#53912=CARTESIAN_POINT ( 'NONE',  ( -20.85882249326303040, 18.41524492703433324, -237.0006385043383546 ) ) ;
#53916=CARTESIAN_POINT ( 'NONE',  ( -22.50875500270928242, -2.598867398075993318, -189.5410127739348809 ) ) ;
#53939=SPHERICAL_SURFACE ( 'NONE', #176714, 0.1000000000000000056 ) ;
#53942=DIRECTION ( 'NONE',  ( -0.000000000000000000, 0.9770955615653313941, 0.2128009952263603954 ) ) ;
#53950=DIRECTION ( 'NONE',  ( 0.000000000000000000, 0.2128009952263601734, -0.9770955615653316162 ) ) ;
#53967=ORIENTED_EDGE ( 'NONE', *, *, #239650, .T. ) ;
#53972=CARTESIAN_POINT ( 'NONE',  ( -21.05000000000000071, 0.6656436123793491033, -212.6810495496487476 ) ) ;
#53982=VECTOR ( 'NONE', #56915, 1000.000000000000227 ) ;
#53998=CARTESIAN_POINT ( 'NONE',  ( -18.49719636458527106, -7.725155196047287731, -209.9198384750837931 ) ) ;
#54000=ORIENTED_EDGE ( 'NONE', *, *, #165653, .F. ) ;
#54039=ORIENTED_EDGE ( 'NONE', *, *, #189030, .F. ) ;
#54041=PLANE ( 'NONE',  #165142 ) ;
#54054=EDGE_CURVE ( 'NONE', #89222, #95759, #130047, .T. ) ;
#54081=VERTEX_POINT ( 'NONE', #205462 ) ;
#54128=AXIS2_PLACEMENT_3D ( 'NONE', #48120, #10303, #68998 ) ;
#54172=CARTESIAN_POINT ( 'NONE',  ( -23.25000000000000000, 7.675662554762638479, -241.7139905447625381 ) ) ;
#54192=AXIS2_PLACEMENT_3D ( 'NONE', #215114, #118602, #176017 ) ;
#54207=FACE_OUTER_BOUND ( 'NONE', #54547, .T. ) ;
#54210=AXIS2_PLACEMENT_3D ( 'NONE', #219276, #100585, #115358 ) ;
#54248=ORIENTED_EDGE ( 'NONE', *, *, #212490, .T. ) ;
#54255=DIRECTION ( 'NONE',  ( -1.000000000000000000, 0.000000000000000000, 0.000000000000000000 ) ) ;
#54259=EDGE_CURVE ( 'NONE', #222677, #195237, #129784, .T. ) ;
#54292=EDGE_CURVE ( 'NONE', #166165, #185482, #22121, .T. ) ;
#54321=CYLINDRICAL_SURFACE ( 'NONE', #36045, 12.87499999999999467 ) ;
#54334=VERTEX_POINT ( 'NONE', #98320 ) ;
#54351=VERTEX_POINT ( 'NONE', #18820 ) ;
#54363=ORIENTED_EDGE ( 'NONE', *, *, #130987, .T. ) ;
#54446=ADVANCED_FACE ( 'NONE', ( #116643 ), #42761, .F. ) ;
#54470=DIRECTION ( 'NONE',  ( 0.000000000000000000, 0.9770955615653551529, 0.2128009952262517601 ) ) ;
#54486=CARTESIAN_POINT ( 'NONE',  ( -21.14999999999999858, 12.92448621296781752, -205.1280733356431938 ) ) ;
#54521=EDGE_CURVE ( 'NONE', #16906, #118817, #145178, .T. ) ;
#54528=AXIS2_PLACEMENT_3D ( 'NONE', #218935, #160289, #139387 ) ;
#54534=DIRECTION ( 'NONE',  ( 0.000000000000000000, 0.2128009952263605342, -0.9770955615653315052 ) ) ;
#54547=EDGE_LOOP ( 'NONE', ( #148206, #67488, #256230, #75365 ) ) ;
#54572=DIRECTION ( 'NONE',  ( 0.000000000000000000, 0.2128009952263485993, -0.9770955615653341697 ) ) ;
#54577=CARTESIAN_POINT ( 'NONE',  ( 18.49999999999999289, 14.86477715130881272, -235.7932433709592601 ) ) ;
#54583=AXIS2_PLACEMENT_3D ( 'NONE', #144525, #205794, #127549 ) ;
#54608=DIRECTION ( 'NONE',  ( 0.000000000000000000, 0.2128009952263582305, -0.9770955615653319493 ) ) ;
#54627=ORIENTED_EDGE ( 'NONE', *, *, #212912, .T. ) ;
#54637=DIRECTION ( 'NONE',  ( -1.000000000000000000, -2.885090398161910739E-16, -6.283419270304611573E-17 ) ) ;
#54653=CARTESIAN_POINT ( 'NONE',  ( -18.50000000000000000, -0.5913595841389538421, -242.4574432119242999 ) ) ;
#54654=EDGE_CURVE ( 'NONE', #191384, #204466, #172183, .T. ) ;
#54655=EDGE_CURVE ( 'NONE', #148073, #241077, #231179, .T. ) ;
#54678=CARTESIAN_POINT ( 'NONE',  ( 23.14999999999999858, 3.318160649989770672, -234.5626251938229245 ) ) ;
#54701=EDGE_LOOP ( 'NONE', ( #235199, #35421, #190225, #253662 ) ) ;
#54703=ORIENTED_EDGE ( 'NONE', *, *, #168603, .F. ) ;
#54708=EDGE_CURVE ( 'NONE', #148702, #223782, #51438, .T. ) ;
#54720=CARTESIAN_POINT ( 'NONE',  ( 20.94999999999999929, 7.783179459866048866, -245.3643104511423303 ) ) ;
#54723=( BOUNDED_CURVE ( )  B_SPLINE_CURVE ( 3, ( #31174, #49413, #33748, #128957 ),
 .UNSPECIFIED., .F., .F. ) 
 B_SPLINE_CURVE_WITH_KNOTS ( ( 4, 4 ),
 ( 3.192897208853992641, 4.712388980384691450 ),
 .UNSPECIFIED. ) 
 CURVE ( )  GEOMETRIC_REPRESENTATION_ITEM ( )  RATIONAL_B_SPLINE_CURVE ( ( 1.000000000000000000, 0.8166740347213222728, 0.8166740347213222728, 1.000000000000000000 ) ) 
 REPRESENTATION_ITEM ( '' )  );
#54745=DIRECTION ( 'NONE',  ( 1.000000000000000000, 0.000000000000000000, 0.000000000000000000 ) ) ;
#54781=CARTESIAN_POINT ( 'NONE',  ( 22.49999999999999645, 11.36547683798393393, -198.4402660583091063 ) ) ;
#54803=DIRECTION ( 'NONE',  ( 0.000000000000000000, 0.2128009952263650861, -0.9770955615653305060 ) ) ;
#54813=FACE_OUTER_BOUND ( 'NONE', #21673, .T. ) ;
#54838=ORIENTED_EDGE ( 'NONE', *, *, #12376, .T. ) ;
#54850=ORIENTED_EDGE ( 'NONE', *, *, #2264, .T. ) ;
#54876=DIRECTION ( 'NONE',  ( -0.000000000000000000, 0.9770955615653313941, 0.2128009952263603954 ) ) ;
#54886=AXIS2_PLACEMENT_3D ( 'NONE', #32092, #225105, #46475 ) ;
#54972=ADVANCED_FACE ( 'NONE', ( #10527 ), #187885, .T. ) ;
#54977=EDGE_CURVE ( 'NONE', #241591, #38009, #185302, .T. ) ;
#55008=ORIENTED_EDGE ( 'NONE', *, *, #1312, .F. ) ;
#55021=ORIENTED_EDGE ( 'NONE', *, *, #192373, .F. ) ;
#55032=DIRECTION ( 'NONE',  ( 1.000000000000000000, 0.000000000000000000, 0.000000000000000000 ) ) ;
#55048=ORIENTED_EDGE ( 'NONE', *, *, #235471, .F. ) ;
#55087=CARTESIAN_POINT ( 'NONE',  ( 20.94999999999999574, 4.252251777740764460, -211.8999245327126744 ) ) ;
#55119=AXIS2_PLACEMENT_3D ( 'NONE', #204489, #244910, #182390 ) ;
#55139=FACE_OUTER_BOUND ( 'NONE', #204874, .T. ) ;
#55148=AXIS2_PLACEMENT_3D ( 'NONE', #160114, #203057, #165223 ) ;
#55156=CARTESIAN_POINT ( 'NONE',  ( -20.94999027547553894, 18.34807417603272128, -236.8765254748879556 ) ) ;
#55184=EDGE_LOOP ( 'NONE', ( #31653, #176661, #18685, #106687 ) ) ;
#55199=CARTESIAN_POINT ( 'NONE',  ( -18.50000000000000000, 18.51199663233067838, -231.2535697180530292 ) ) ;
#55205=AXIS2_PLACEMENT_3D ( 'NONE', #106093, #143953, #142656 ) ;
#55232=VERTEX_POINT ( 'NONE', #221525 ) ;
#55235=DIRECTION ( 'NONE',  ( 0.000000000000000000, 0.2128009952263485993, -0.9770955615653341697 ) ) ;
#55238=CARTESIAN_POINT ( 'NONE',  ( -20.94999999999999929, -4.557064143889601127, -233.1584191572127622 ) ) ;
#55245=ADVANCED_FACE ( 'NONE', ( #79458 ), #134855, .T. ) ;
#55260=DIRECTION ( 'NONE',  ( 2.952720810173289605E-16, -0.9770955615653357240, -0.2128009952263412996 ) ) ;
#55263=ORIENTED_EDGE ( 'NONE', *, *, #41460, .F. ) ;
#55308=ORIENTED_EDGE ( 'NONE', *, *, #239272, .F. ) ;
#55451=CYLINDRICAL_SURFACE ( 'NONE', #121191, 11.74999999999999289 ) ;
#55456=LINE ( 'NONE', #41099, #97146 ) ;
#55467=DIRECTION ( 'NONE',  ( -1.000000000000000000, -0.000000000000000000, -0.000000000000000000 ) ) ;
#55477=TOROIDAL_SURFACE ( 'NONE', #217997, 0.6000000000000013101, 0.1000000000000000056 ) ;
#55480=CARTESIAN_POINT ( 'NONE',  ( 20.85000000000000142, 7.128833340094563376, -233.7327013124401276 ) ) ;
#55497=CIRCLE ( 'NONE', #230530, 0.09999999999999939493 ) ;
#55499=CIRCLE ( 'NONE', #17935, 12.77500000000000924 ) ;
#55520=CARTESIAN_POINT ( 'NONE',  ( -20.94999999999999929, 12.97363049771892207, -205.3537238898406940 ) ) ;
#55537=ORIENTED_EDGE ( 'NONE', *, *, #128585, .T. ) ;
#55579=FACE_OUTER_BOUND ( 'NONE', #45277, .T. ) ;
#55581=CARTESIAN_POINT ( 'NONE',  ( -23.15000000000000213, 7.128833340094563376, -233.7327013124401276 ) ) ;
#55591=ADVANCED_FACE ( 'NONE', ( #64424 ), #189258, .T. ) ;
#55595=VERTEX_POINT ( 'NONE', #240485 ) ;
#55617=FACE_OUTER_BOUND ( 'NONE', #71674, .T. ) ;
#55633=DIRECTION ( 'NONE',  ( 1.000000000000000000, 0.000000000000000000, 0.000000000000000000 ) ) ;
#55636=VERTEX_POINT ( 'NONE', #241761 ) ;
#55684=DIRECTION ( 'NONE',  ( 1.000000000000000000, 0.000000000000000000, 0.000000000000000000 ) ) ;
#55699=FACE_OUTER_BOUND ( 'NONE', #107128, .T. ) ;
#55724=AXIS2_PLACEMENT_3D ( 'NONE', #187288, #28227, #148139 ) ;
#55729=DIRECTION ( 'NONE',  ( 0.000000000000000000, -0.9770955615653316162, -0.2128009952263604232 ) ) ;
#55730=AXIS2_PLACEMENT_3D ( 'NONE', #8960, #246293, #247568 ) ;
#55737=EDGE_LOOP ( 'NONE', ( #53084, #247382, #83465, #233748 ) ) ;
#55744=CARTESIAN_POINT ( 'NONE',  ( -20.64999999999999858, 6.268811756569107274, -220.3853799378769622 ) ) ;
#55774=EDGE_CURVE ( 'NONE', #242867, #19033, #219271, .T. ) ;
#55799=DIRECTION ( 'NONE',  ( -1.000000000000000000, 0.000000000000000000, 0.000000000000000000 ) ) ;
#55806=CARTESIAN_POINT ( 'NONE',  ( -23.15000000000000213, 17.01923898301589944, -224.3994341343041867 ) ) ;
#55831=ORIENTED_EDGE ( 'NONE', *, *, #3205, .F. ) ;
#55846=EDGE_LOOP ( 'NONE', ( #94213, #57779, #168838, #154175 ) ) ;
#55851=ORIENTED_EDGE ( 'NONE', *, *, #134384, .F. ) ;
#55905=CARTESIAN_POINT ( 'NONE',  ( 23.14999999999999858, 9.180734019381761257, -233.2858192224647382 ) ) ;
#55936=LINE ( 'NONE', #95088, #26966 ) ;
#55970=CARTESIAN_POINT ( 'NONE',  ( -21.05000000000000071, -1.362227297915485025, -194.8443758818181664 ) ) ;
#55995=AXIS2_PLACEMENT_3D ( 'NONE', #246985, #125750, #85321 ) ;
#56001=CARTESIAN_POINT ( 'NONE',  ( 23.14999999999999503, 8.882751598337874199, -187.0399955572217721 ) ) ;
#56016=VECTOR ( 'NONE', #98963, 1000.000000000000000 ) ;
#56024=ORIENTED_EDGE ( 'NONE', *, *, #66943, .F. ) ;
#56066=VECTOR ( 'NONE', #213955, 1000.000000000000227 ) ;
#56100=CIRCLE ( 'NONE', #76965, 0.2000000000000111688 ) ;
#56103=DIRECTION ( 'NONE',  ( -1.000000000000000000, 0.000000000000000000, 0.000000000000000000 ) ) ;
#56122=CARTESIAN_POINT ( 'NONE',  ( 23.15000000000000213, -4.756823075239758225, -233.1486023682345490 ) ) ;
#56129=DIRECTION ( 'NONE',  ( 0.000000000000000000, -0.9595780032479205301, 0.2814428106787130734 ) ) ;
#56142=CARTESIAN_POINT ( 'NONE',  ( 18.49999999999999645, -3.391987963166880338, -191.5331142350599691 ) ) ;
#56150=CARTESIAN_POINT ( 'NONE',  ( -21.55000000000000426, 12.05403912736948158, -220.1228874760914209 ) ) ;
#56166=DIRECTION ( 'NONE',  ( 1.000000000000000000, 2.885090398161910739E-16, 6.283419270304611573E-17 ) ) ;
#56187=CIRCLE ( 'NONE', #185201, 0.1000000000000066946 ) ;
#56213=CYLINDRICAL_SURFACE ( 'NONE', #118352, 0.1000000000000055844 ) ;
#56218=ORIENTED_EDGE ( 'NONE', *, *, #152951, .T. ) ;
#56333=ORIENTED_EDGE ( 'NONE', *, *, #107357, .F. ) ;
#56357=CARTESIAN_POINT ( 'NONE',  ( -21.05000000000000071, -4.557064143889599350, -233.1584191572127622 ) ) ;
#56377=CARTESIAN_POINT ( 'NONE',  ( 20.95346350065193519, 10.49492647445341831, -207.4255753433062353 ) ) ;
#56399=DIRECTION ( 'NONE',  ( 0.000000000000000000, -0.2128009952263603677, 0.9770955615653313941 ) ) ;
#56402=DIRECTION ( 'NONE',  ( 1.000000000000000000, 0.000000000000000000, 0.000000000000000000 ) ) ;
#56405=ORIENTED_EDGE ( 'NONE', *, *, #189513, .F. ) ;
#56418=CARTESIAN_POINT ( 'NONE',  ( -21.29999999999995808, 1.148907358139439339E-11, -201.0000000000015064 ) ) ;
#56425=CARTESIAN_POINT ( 'NONE',  ( -21.76363531954647357, -1.395625584870292979, -194.1266231281565524 ) ) ;
#56427=CARTESIAN_POINT ( 'NONE',  ( -21.05000000000000071, 4.193200906077805712, -212.0298262072164164 ) ) ;
#56429=CARTESIAN_POINT ( 'NONE',  ( 21.05000000000000071, -3.770473190032740174, -225.9805569534692324 ) ) ;
#56446=DIRECTION ( 'NONE',  ( 1.000000000000000000, 0.000000000000000000, 0.000000000000000000 ) ) ;
#56512=ORIENTED_EDGE ( 'NONE', *, *, #120084, .F. ) ;
#56553=FACE_OUTER_BOUND ( 'NONE', #169773, .T. ) ;
#56555=EDGE_CURVE ( 'NONE', #185405, #81280, #156512, .T. ) ;
#56561=CARTESIAN_POINT ( 'NONE',  ( 20.94999999999999929, 9.374458193048763377, -220.5475659691911119 ) ) ;
#56574=AXIS2_PLACEMENT_3D ( 'NONE', #15151, #73869, #54255 ) ;
#56601=CARTESIAN_POINT ( 'NONE',  ( 19.75857864376268935, 16.67126802362266247, -222.8016931105129004 ) ) ;
#56613=FACE_OUTER_BOUND ( 'NONE', #216068, .T. ) ;
#56617=AXIS2_PLACEMENT_3D ( 'NONE', #42724, #24477, #101360 ) ;
#56622=AXIS2_PLACEMENT_3D ( 'NONE', #107949, #110510, #85779 ) ;
#56642=AXIS2_PLACEMENT_3D ( 'NONE', #144805, #241371, #84813 ) ;
#56661=ORIENTED_EDGE ( 'NONE', *, *, #65029, .F. ) ;
#56665=LINE ( 'NONE', #214488, #78468 ) ;
#56677=DIRECTION ( 'NONE',  ( 0.000000000000000000, 0.2128009952263603122, -0.9770955615653315052 ) ) ;
#56683=CARTESIAN_POINT ( 'NONE',  ( 20.85000000000000142, 7.128833340094563376, -233.7327013124401276 ) ) ;
#56698=CARTESIAN_POINT ( 'NONE',  ( 21.53699400386439677, -1.444431824881390991, -194.3677569336561533 ) ) ;
#56705=CARTESIAN_POINT ( 'NONE',  ( 20.59588692710267921, 11.75683769346106011, -206.2576375686336405 ) ) ;
#56783=DIRECTION ( 'NONE',  ( 0.000000000000000000, -0.2128009952263603954, 0.9770955615653315052 ) ) ;
#56791=AXIS2_PLACEMENT_3D ( 'NONE', #62058, #28084, #124598 ) ;
#56796=CARTESIAN_POINT ( 'NONE',  ( -22.00356870069503046, -1.543709994182673739, -193.9119119858162037 ) ) ;
#56802=VERTEX_POINT ( 'NONE', #151189 ) ;
#56812=ORIENTED_EDGE ( 'NONE', *, *, #39483, .F. ) ;
#56832=ORIENTED_EDGE ( 'NONE', *, *, #120629, .F. ) ;
#56846=ORIENTED_EDGE ( 'NONE', *, *, #43507, .F. ) ;
#56857=CARTESIAN_POINT ( 'NONE',  ( -18.59999999999999787, 1.148907358139439339E-11, -201.0000000000015064 ) ) ;
#56862=FACE_OUTER_BOUND ( 'NONE', #163376, .T. ) ;
#56866=DIRECTION ( 'NONE',  ( 0.000000000000000000, 0.2128009952263568982, -0.9770955615653323934 ) ) ;
#56881=ORIENTED_EDGE ( 'NONE', *, *, #107374, .F. ) ;
#56884=ORIENTED_EDGE ( 'NONE', *, *, #212301, .F. ) ;
#56912=CIRCLE ( 'NONE', #11163, 0.09999999999999671652 ) ;
#56915=DIRECTION ( 'NONE',  ( 0.000000000000000000, 0.2128009952263603677, -0.9770955615653313941 ) ) ;
#56925=LINE ( 'NONE', #97335, #244098 ) ;
#56954=CARTESIAN_POINT ( 'NONE',  ( -20.64999999999999858, 11.48697431424113446, -220.1440440112397994 ) ) ;
#56983=SPHERICAL_SURFACE ( 'NONE', #212763, 0.1000000000000000056 ) ;
#57033=FACE_BOUND ( 'NONE', #152455, .T. ) ;
#57039=CARTESIAN_POINT ( 'NONE',  ( 18.39999999999999858, -7.785976468740638090, -209.8926132507865816 ) ) ;
#57078=DIRECTION ( 'NONE',  ( 1.000000000000000000, 0.000000000000000000, 0.000000000000000000 ) ) ;
#57085=EDGE_CURVE ( 'NONE', #94400, #61015, #156691, .T. ) ;
#57121=CARTESIAN_POINT ( 'NONE',  ( -21.05000000000000071, -10.60885044396467336, -206.2784744251879090 ) ) ;
#57134=ORIENTED_EDGE ( 'NONE', *, *, #45744, .T. ) ;
#57142=DIRECTION ( 'NONE',  ( 2.952720810173289112E-16, -0.9770955615653316162, -0.2128009952263604232 ) ) ;
#57158=VECTOR ( 'NONE', #204521, 1000.000000000000227 ) ;
#57166=CARTESIAN_POINT ( 'NONE',  ( -23.15000000000000213, -6.388372595096676321, -212.0629706944429813 ) ) ;
#57179=AXIS2_PLACEMENT_3D ( 'NONE', #39608, #193523, #176533 ) ;
#57191=CIRCLE ( 'NONE', #227914, 0.09999999999999895084 ) ;
#57204=ORIENTED_EDGE ( 'NONE', *, *, #193127, .T. ) ;
#57205=CARTESIAN_POINT ( 'NONE',  ( 20.84999999999998721, -4.352039508298082282, -236.2331130063498676 ) ) ;
#57207=AXIS2_PLACEMENT_3D ( 'NONE', #197852, #195324, #19225 ) ;
#57222=ORIENTED_EDGE ( 'NONE', *, *, #65527, .T. ) ;
#57259=ADVANCED_FACE ( 'NONE', ( #55579 ), #54321, .T. ) ;
#57268=EDGE_CURVE ( 'NONE', #242867, #97885, #212141, .T. ) ;
#57288=ORIENTED_EDGE ( 'NONE', *, *, #123444, .F. ) ;
#57302=DIRECTION ( 'NONE',  ( 1.000000000000000000, 0.000000000000000000, 0.000000000000000000 ) ) ;
#57305=AXIS2_PLACEMENT_3D ( 'NONE', #166227, #248295, #149218 ) ;
#57328=DIRECTION ( 'NONE',  ( 0.000000000000000000, -0.2128009952263403282, 0.9770955615653358350 ) ) ;
#57351=DIRECTION ( 'NONE',  ( 1.000000000000000000, 0.000000000000000000, 0.000000000000000000 ) ) ;
#57360=DIRECTION ( 'NONE',  ( 0.000000000000000000, 0.4599910535713788717, -0.8879235499941945386 ) ) ;
#57401=DIRECTION ( 'NONE',  ( 7.304098846218135653E-16, -0.9770955615653315052, -0.2128009952263603954 ) ) ;
#57443=AXIS2_PLACEMENT_3D ( 'NONE', #63558, #145661, #222618 ) ;
#57469=CIRCLE ( 'NONE', #74271, 11.80000000000000071 ) ;
#57470=CARTESIAN_POINT ( 'NONE',  ( 20.95561247346651967, 11.96829920165036043, -206.1652233253646216 ) ) ;
#57473=DIRECTION ( 'NONE',  ( 0.000000000000000000, 0.9770955615653316162, 0.2128009952263604232 ) ) ;
#57475=DIRECTION ( 'NONE',  ( -1.000000000000000000, 0.000000000000000000, 0.000000000000000000 ) ) ;
#57492=ADVANCED_FACE ( 'NONE', ( #107574 ), #243229, .F. ) ;
#57513=FACE_OUTER_BOUND ( 'NONE', #170441, .T. ) ;
#57520=LINE ( 'NONE', #155393, #157197 ) ;
#57521=CARTESIAN_POINT ( 'NONE',  ( 18.59999999999996945, 18.41524492703432614, -237.0006385043383546 ) ) ;
#57522=EDGE_LOOP ( 'NONE', ( #88828, #49566, #43617, #129288 ) ) ;
#57598=DIRECTION ( 'NONE',  ( -1.000000000000000000, 0.000000000000000000, 0.000000000000000000 ) ) ;
#57601=DIRECTION ( 'NONE',  ( 1.000000000000000000, 0.000000000000000000, 0.000000000000000000 ) ) ;
#57620=EDGE_CURVE ( 'NONE', #184847, #185482, #27316, .T. ) ;
#57622=EDGE_LOOP ( 'NONE', ( #20481, #207753, #51056, #212449, #187895 ) ) ;
#57651=VERTEX_POINT ( 'NONE', #174025 ) ;
#57658=ORIENTED_EDGE ( 'NONE', *, *, #157746, .T. ) ;
#57660=LINE ( 'NONE', #158113, #252481 ) ;
#57676=EDGE_LOOP ( 'NONE', ( #18873, #247296, #31964, #254448 ) ) ;
#57692=AXIS2_PLACEMENT_3D ( 'NONE', #66678, #148788, #245316 ) ;
#57695=AXIS2_PLACEMENT_3D ( 'NONE', #95256, #216486, #193088 ) ;
#57700=CIRCLE ( 'NONE', #124186, 0.09999999999999939493 ) ;
#57710=CARTESIAN_POINT ( 'NONE',  ( -22.50000000000000000, 0.09770955616802273758, -200.9787199004788931 ) ) ;
#57712=CARTESIAN_POINT ( 'NONE',  ( 20.85000000000000142, 8.788681102860174121, -241.3540466926497174 ) ) ;
#57742=VECTOR ( 'NONE', #66585, 999.9999999999998863 ) ;
#57753=AXIS2_PLACEMENT_3D ( 'NONE', #167380, #184331, #14408 ) ;
#57771=AXIS2_PLACEMENT_3D ( 'NONE', #126044, #45243, #123500 ) ;
#57779=ORIENTED_EDGE ( 'NONE', *, *, #199633, .F. ) ;
#57788=FACE_OUTER_BOUND ( 'NONE', #77603, .T. ) ;
#57830=VECTOR ( 'NONE', #83169, 1000.000000000000227 ) ;
#57831=ORIENTED_EDGE ( 'NONE', *, *, #4317, .F. ) ;
#57839=EDGE_CURVE ( 'NONE', #89812, #44396, #76150, .T. ) ;
#57841=ORIENTED_EDGE ( 'NONE', *, *, #24617, .T. ) ;
#57858=AXIS2_PLACEMENT_3D ( 'NONE', #8959, #185025, #6386 ) ;
#57885=ORIENTED_EDGE ( 'NONE', *, *, #44065, .F. ) ;
#57894=EDGE_LOOP ( 'NONE', ( #129407, #172917, #61254, #131328 ) ) ;
#57899=DIRECTION ( 'NONE',  ( 1.000000000000000000, 0.000000000000000000, 0.000000000000000000 ) ) ;
#57902=CIRCLE ( 'NONE', #137213, 7.900000000000002132 ) ;
#57917=VERTEX_POINT ( 'NONE', #104673 ) ;
#57957=CARTESIAN_POINT ( 'NONE',  ( -18.44232395690005433, -0.7486215172606220936, -242.4509705927298171 ) ) ;
#57985=DIRECTION ( 'NONE',  ( 1.000000000000000000, -0.000000000000000000, -0.000000000000000000 ) ) ;
#57998=CARTESIAN_POINT ( 'NONE',  ( 20.94999999999999574, 2.923777413779037548, -208.5507632484912222 ) ) ;
#58000=DIRECTION ( 'NONE',  ( -1.000000000000000000, -0.000000000000000000, -0.000000000000000000 ) ) ;
#58017=DIRECTION ( 'NONE',  ( -0.000000000000000000, 0.2128009952263597848, -0.9770955615653316162 ) ) ;
#58021=ORIENTED_EDGE ( 'NONE', *, *, #101947, .T. ) ;
#58027=DIRECTION ( 'NONE',  ( -1.000000000000000000, -2.885090398161910739E-16, -6.283419270304611573E-17 ) ) ;
#58048=CIRCLE ( 'NONE', #82983, 0.1000000000000054040 ) ;
#58068=DIRECTION ( 'NONE',  ( -1.000000000000000000, -0.000000000000000000, -0.000000000000000000 ) ) ;
#58128=ORIENTED_EDGE ( 'NONE', *, *, #113249, .T. ) ;
#58147=CIRCLE ( 'NONE', #208037, 0.1000000000000054040 ) ;
#58149=LINE ( 'NONE', #178145, #228101 ) ;
#58157=DIRECTION ( 'NONE',  ( 0.000000000000000000, -0.2128009952263603954, 0.9770955615653315052 ) ) ;
#58166=DIRECTION ( 'NONE',  ( 0.000000000000000000, -0.06430067914209719460, 0.9979305700607958851 ) ) ;
#58180=ADVANCED_FACE ( 'NONE', ( #159271 ), #58837, .F. ) ;
#58184=CIRCLE ( 'NONE', #87432, 7.791421356237341556 ) ;
#58187=VERTEX_POINT ( 'NONE', #198375 ) ;
#58190=ADVANCED_FACE ( 'NONE', ( #60135 ), #36777, .F. ) ;
#58213=DIRECTION ( 'NONE',  ( 0.000000000000000000, -0.9770955615653316162, -0.2128009952263604232 ) ) ;
#58246=DIRECTION ( 'NONE',  ( -1.000000000000000000, 0.000000000000000000, 0.000000000000000000 ) ) ;
#58248=FACE_OUTER_BOUND ( 'NONE', #132302, .T. ) ;
#58268=DIRECTION ( 'NONE',  ( 0.000000000000000000, -0.9770955615653315052, -0.2128009952263603954 ) ) ;
#58330=EDGE_CURVE ( 'NONE', #236182, #63493, #102425, .T. ) ;
#58364=CARTESIAN_POINT ( 'NONE',  ( 18.48197441911570138, -0.7048741502111930401, -242.4905267791219785 ) ) ;
#58408=EDGE_CURVE ( 'NONE', #200518, #204167, #256335, .T. ) ;
#58441=EDGE_CURVE ( 'NONE', #29274, #24822, #52576, .T. ) ;
#58494=CIRCLE ( 'NONE', #241679, 0.1000000000000055844 ) ;
#58503=EDGE_LOOP ( 'NONE', ( #20666, #238247, #186577, #65355 ) ) ;
#58551=EDGE_CURVE ( 'NONE', #20245, #169080, #90165, .T. ) ;
#58553=CARTESIAN_POINT ( 'NONE',  ( -18.45068461519106151, -7.764980607745699537, -209.9256088280441759 ) ) ;
#58579=CARTESIAN_POINT ( 'NONE',  ( -20.54999999999999716, 4.662003332185090443, -213.0075696128765514 ) ) ;
#58587=DIRECTION ( 'NONE',  ( -0.000000000000000000, 0.2128009952263603677, -0.9770955615653313941 ) ) ;
#58589=EDGE_CURVE ( 'NONE', #248782, #145377, #125893, .T. ) ;
#58611=VECTOR ( 'NONE', #131871, 1000.000000000000000 ) ;
#58642=CARTESIAN_POINT ( 'NONE',  ( -23.25000000000000000, 6.307392164054360428, -220.9841382799134522 ) ) ;
#58662=DIRECTION ( 'NONE',  ( 0.000000000000000000, 0.2128009952263601456, -0.9770955615653316162 ) ) ;
#58676=LINE ( 'NONE', #22164, #257274 ) ;
#58711=EDGE_CURVE ( 'NONE', #136982, #245093, #16260, .T. ) ;
#58741=EDGE_CURVE ( 'NONE', #253923, #200518, #89990, .T. ) ;
#58775=VECTOR ( 'NONE', #192180, 1000.000000000000000 ) ;
#58785=DIRECTION ( 'NONE',  ( 1.836970198721029934E-16, -0.9770955615653316162, -0.2128009952263604232 ) ) ;
#58788=EDGE_LOOP ( 'NONE', ( #90132, #166833, #129797, #124235 ) ) ;
#58791=ORIENTED_EDGE ( 'NONE', *, *, #211893, .F. ) ;
#58837=CYLINDRICAL_SURFACE ( 'NONE', #202433, 2.000000000000003109 ) ;
#58854=CARTESIAN_POINT ( 'NONE',  ( -21.05000000000000071, 0.4810385098657082859, -209.0827657365571213 ) ) ;
#58857=DIRECTION ( 'NONE',  ( 1.000000000000000000, -0.000000000000000000, -0.000000000000000000 ) ) ;
#58907=DIRECTION ( 'NONE',  ( 1.000000000000000000, 0.000000000000000000, 0.000000000000000000 ) ) ;
#58961=ADVANCED_FACE ( 'NONE', ( #44786 ), #68203, .F. ) ;
#58966=AXIS2_PLACEMENT_3D ( 'NONE', #50913, #30119, #88763 ) ;
#58970=CIRCLE ( 'NONE', #246438, 0.09999999999999939493 ) ;
#58991=DIRECTION ( 'NONE',  ( 0.000000000000000000, 0.2128009952263628102, -0.9770955615653308390 ) ) ;
#59006=CIRCLE ( 'NONE', #109090, 0.09999999999998714084 ) ;
#59069=EDGE_LOOP ( 'NONE', ( #49477, #92003, #36239, #127699 ) ) ;
#59070=VERTEX_POINT ( 'NONE', #151619 ) ;
#59097=ORIENTED_EDGE ( 'NONE', *, *, #123963, .F. ) ;
#59139=ADVANCED_FACE ( 'NONE', ( #154209 ), #133317, .F. ) ;
#59155=CARTESIAN_POINT ( 'NONE',  ( 18.59999999999999432, -1.102499207903924860, -187.8171010361417643 ) ) ;
#59184=EDGE_LOOP ( 'NONE', ( #159497, #149700, #110904, #242025 ) ) ;
#59189=AXIS2_PLACEMENT_3D ( 'NONE', #110991, #169723, #91433 ) ;
#59194=CARTESIAN_POINT ( 'NONE',  ( 18.49999999999999645, 0.6656436123793491033, -212.6810495496487476 ) ) ;
#59213=CARTESIAN_POINT ( 'NONE',  ( 20.04142135623731136, 16.75134856811735062, -222.6994677643232876 ) ) ;
#59216=CARTESIAN_POINT ( 'NONE',  ( -18.37151313414604203, -0.7723694306740864768, -242.4299537170358292 ) ) ;
#59232=CARTESIAN_POINT ( 'NONE',  ( 20.94999999999999929, 7.128833340094563376, -233.7327013124401276 ) ) ;
#59239=DIRECTION ( 'NONE',  ( 0.000000000000000000, 0.2128009952263604232, -0.9770955615653316162 ) ) ;
#59264=CARTESIAN_POINT ( 'NONE',  ( 20.54374330479332400, 11.90843211854532235, -206.3132545399801074 ) ) ;
#59265=CIRCLE ( 'NONE', #155216, 4.000000000000006217 ) ;
#59279=EDGE_CURVE ( 'NONE', #115133, #183380, #187458, .T. ) ;
#59280=CARTESIAN_POINT ( 'NONE',  ( -21.05000000000000071, 7.128833340094563376, -233.7327013124401276 ) ) ;
#59297=CIRCLE ( 'NONE', #176455, 0.2000000000000111688 ) ;
#59352=DIRECTION ( 'NONE',  ( 0.000000000000000000, 0.2128009952263603677, -0.9770955615653313941 ) ) ;
#59356=ADVANCED_FACE ( 'NONE', ( #45762 ), #114175, .F. ) ;
#59395=CARTESIAN_POINT ( 'NONE',  ( 22.40000000000000568, 7.612336166715867769, -199.3421143478784359 ) ) ;
#59418=EDGE_CURVE ( 'NONE', #79677, #145985, #21067, .T. ) ;
#59429=DIRECTION ( 'NONE',  ( -1.000000000000000000, -0.000000000000000000, -0.000000000000000000 ) ) ;
#59435=DIRECTION ( 'NONE',  ( 1.000000000000000000, 0.000000000000000000, 0.000000000000000000 ) ) ;
#59436=EDGE_LOOP ( 'NONE', ( #21984, #220060, #79930 ) ) ;
#59447=AXIS2_PLACEMENT_3D ( 'NONE', #11694, #31282, #232029 ) ;
#59461=DIRECTION ( 'NONE',  ( 0.000000000000000000, -0.9752329468386645717, -0.2211802418851520069 ) ) ;
#59486=VERTEX_POINT ( 'NONE', #36503 ) ;
#59492=AXIS2_PLACEMENT_3D ( 'NONE', #75958, #35574, #53823 ) ;
#59497=DIRECTION ( 'NONE',  ( -1.000000000000000000, -2.885090398161910739E-16, -6.283419270304611573E-17 ) ) ;
#59525=CARTESIAN_POINT ( 'NONE',  ( -23.15000000000000213, -4.756823075239758225, -233.1486023682345490 ) ) ;
#59545=CARTESIAN_POINT ( 'NONE',  ( -23.15000000000000213, 7.128833340094563376, -233.7327013124401276 ) ) ;
#59550=VERTEX_POINT ( 'NONE', #40368 ) ;
#59600=CARTESIAN_POINT ( 'NONE',  ( 20.94999999999999574, -10.86374996222470379, -206.3339888224507206 ) ) ;
#59622=AXIS2_PLACEMENT_3D ( 'NONE', #56418, #39481, #116424 ) ;
#59658=DIRECTION ( 'NONE',  ( 0.000000000000000000, 0.2128009952263775484, -0.9770955615653277304 ) ) ;
#59669=AXIS2_PLACEMENT_3D ( 'NONE', #44398, #207327, #165631 ) ;
#59746=ORIENTED_EDGE ( 'NONE', *, *, #232609, .T. ) ;
#59766=ORIENTED_EDGE ( 'NONE', *, *, #234889, .T. ) ;
#59773=CIRCLE ( 'NONE', #88820, 0.09999999999999939493 ) ;
#59777=ORIENTED_EDGE ( 'NONE', *, *, #151325, .F. ) ;
#59780=ORIENTED_EDGE ( 'NONE', *, *, #60614, .F. ) ;
#59785=VERTEX_POINT ( 'NONE', #200691 ) ;
#59792=AXIS2_PLACEMENT_3D ( 'NONE', #36580, #13137, #54803 ) ;
#59799=ADVANCED_FACE ( 'NONE', ( #2467 ), #3766, .F. ) ;
#59802=CARTESIAN_POINT ( 'NONE',  ( -18.50000000000000000, 7.675662554762638479, -241.7139905447625381 ) ) ;
#59807=DIRECTION ( 'NONE',  ( -0.000000000000000000, 0.9525900758537790836, -0.3042567129660269099 ) ) ;
#59819=TOROIDAL_SURFACE ( 'NONE', #205565, 11.65000000000000036, 0.1000000000000000056 ) ;
#59825=EDGE_LOOP ( 'NONE', ( #231626, #212806, #73133, #76166 ) ) ;
#59841=ORIENTED_EDGE ( 'NONE', *, *, #31508, .F. ) ;
#59850=ORIENTED_EDGE ( 'NONE', *, *, #84987, .T. ) ;
#59865=CARTESIAN_POINT ( 'NONE',  ( -21.14999999999999858, 6.390846877240203838, -199.6081416912452653 ) ) ;
#59886=AXIS2_PLACEMENT_3D ( 'NONE', #228742, #187053, #108770 ) ;
#59889=DIRECTION ( 'NONE',  ( 7.304098846218132695E-16, -0.9770955615653315052, -0.2128009952263603954 ) ) ;
#59905=CARTESIAN_POINT ( 'NONE',  ( 22.50046968638675793, -2.456286045658393036, -189.5094708429525099 ) ) ;
#59938=CARTESIAN_POINT ( 'NONE',  ( -23.15000000000000213, -0.8831241301779060304, -196.9450534195053706 ) ) ;
#59943=ORIENTED_EDGE ( 'NONE', *, *, #57268, .F. ) ;
#59959=VECTOR ( 'NONE', #105018, 1000.000000000000000 ) ;
#59962=SPHERICAL_SURFACE ( 'NONE', #143023, 0.1000000000000000056 ) ;
#59971=CIRCLE ( 'NONE', #143378, 0.09999999999999939493 ) ;
#59999=DIRECTION ( 'NONE',  ( 2.952720810173289112E-16, -0.9770955615653318382, -0.2128009952263588411 ) ) ;
#60034=EDGE_CURVE ( 'NONE', #107334, #98586, #67188, .T. ) ;
#60053=FACE_OUTER_BOUND ( 'NONE', #833, .T. ) ;
#60073=ORIENTED_EDGE ( 'NONE', *, *, #54655, .F. ) ;
#60100=CIRCLE ( 'NONE', #55995, 0.2000000000000003997 ) ;
#60115=DIRECTION ( 'NONE',  ( 0.000000000000000000, 0.2128009952263485993, -0.9770955615653341697 ) ) ;
#60132=DIRECTION ( 'NONE',  ( 1.000000000000000000, 0.000000000000000000, 0.000000000000000000 ) ) ;
#60135=FACE_OUTER_BOUND ( 'NONE', #146545, .T. ) ;
#60149=EDGE_CURVE ( 'NONE', #53843, #202387, #155116, .T. ) ;
#60166=AXIS2_PLACEMENT_3D ( 'NONE', #61647, #181609, #45931 ) ;
#60182=CARTESIAN_POINT ( 'NONE',  ( -20.64999999999999858, 1.148907358139439339E-11, -201.0000000000015064 ) ) ;
#60184=AXIS2_PLACEMENT_3D ( 'NONE', #83972, #164857, #120607 ) ;
#60258=ORIENTED_EDGE ( 'NONE', *, *, #216881, .T. ) ;
#60307=EDGE_CURVE ( 'NONE', #154129, #146487, #33661, .T. ) ;
#60314=EDGE_CURVE ( 'NONE', #64432, #241204, #136591, .T. ) ;
#60331=VERTEX_POINT ( 'NONE', #244678 ) ;
#60361=CARTESIAN_POINT ( 'NONE',  ( 21.05000000000000071, 2.761092913073515565, -213.6778149113116854 ) ) ;
#60366=DIRECTION ( 'NONE',  ( 0.000000000000000000, 0.2128009952263601456, -0.9770955615653316162 ) ) ;
#60392=DIRECTION ( 'NONE',  ( 6.938893903906840889E-14, -0.2128009952263485993, 0.9770955615653341697 ) ) ;
#60417=EDGE_LOOP ( 'NONE', ( #105961, #52561, #116463, #194168 ) ) ;
#60424=ORIENTED_EDGE ( 'NONE', *, *, #148300, .F. ) ;
#60557=ORIENTED_EDGE ( 'NONE', *, *, #39746, .T. ) ;
#60559=ADVANCED_FACE ( 'NONE', ( #131160 ), #210702, .T. ) ;
#60582=CARTESIAN_POINT ( 'NONE',  ( 20.52683494730048253, 10.58476304708173643, -207.3993787893872138 ) ) ;
#60589=EDGE_LOOP ( 'NONE', ( #68404, #24230, #257560, #89543 ) ) ;
#60597=CARTESIAN_POINT ( 'NONE',  ( 21.05000000000000071, 17.01923898301590654, -224.3994341343041867 ) ) ;
#60613=ORIENTED_EDGE ( 'NONE', *, *, #65029, .T. ) ;
#60614=EDGE_CURVE ( 'NONE', #179165, #232353, #75078, .T. ) ;
#60647=DIRECTION ( 'NONE',  ( -0.000000000000000000, -0.9770955615653313941, -0.2128009952263603677 ) ) ;
#60664=CARTESIAN_POINT ( 'NONE',  ( -21.53699400386206264, -1.444431824880774817, -194.3677569336538227 ) ) ;
#60709=EDGE_LOOP ( 'NONE', ( #186526, #17166, #126831, #137980 ) ) ;
#60711=ORIENTED_EDGE ( 'NONE', *, *, #170199, .T. ) ;
#60731=DIRECTION ( 'NONE',  ( 0.000000000000000000, 0.2128009952263603677, -0.9770955615653313941 ) ) ;
#60745=B_SPLINE_CURVE_WITH_KNOTS ( 'NONE', 3,
 ( #153152, #193533, #172723, #113970, #194831, #176545, #14902 ),
 .UNSPECIFIED., .F., .F.,
 ( 4, 3, 4 ),
 ( 0.000000000000000000, 1.860045280644813734E-05, 5.251155757305090734E-05 ),
 .UNSPECIFIED. ) ;
#60775=FACE_OUTER_BOUND ( 'NONE', #73480, .T. ) ;
#60794=ORIENTED_EDGE ( 'NONE', *, *, #176332, .F. ) ;
#60798=EDGE_LOOP ( 'NONE', ( #242246, #127804, #247245, #83292 ) ) ;
#60800=ORIENTED_EDGE ( 'NONE', *, *, #139801, .F. ) ;
#60823=CARTESIAN_POINT ( 'NONE',  ( -20.05000000000000426, 11.66622623553636018, -211.0987209794895421 ) ) ;
#60824=EDGE_CURVE ( 'NONE', #166449, #48752, #84062, .T. ) ;
#60843=CARTESIAN_POINT ( 'NONE',  ( -23.25000000000000000, 6.878457983866232972, -212.1414458560986986 ) ) ;
#60850=CARTESIAN_POINT ( 'NONE',  ( 21.05000000000000071, 12.10919762232931163, -206.2073353557311748 ) ) ;
#60854=DIRECTION ( 'NONE',  ( 1.000000000000000000, 0.000000000000000000, 0.000000000000000000 ) ) ;
#60908=DIRECTION ( 'NONE',  ( -0.000000000000000000, 0.2128009952263603677, -0.9770955615653313941 ) ) ;
#60910=ADVANCED_FACE ( 'NONE', ( #170045 ), #46690, .T. ) ;
#60997=EDGE_LOOP ( 'NONE', ( #217850, #112664, #222458, #177660 ) ) ;
#61006=AXIS2_PLACEMENT_3D ( 'NONE', #228057, #246334, #49416 ) ;
#61015=VERTEX_POINT ( 'NONE', #250805 ) ;
#61019=AXIS2_PLACEMENT_3D ( 'NONE', #178828, #214065, #136 ) ;
#61021=CARTESIAN_POINT ( 'NONE',  ( 20.94999999999999574, -10.72348020702289695, -206.5081278352411402 ) ) ;
#61029=CARTESIAN_POINT ( 'NONE',  ( 22.39999999999999858, -1.560176095955058129, -193.3663837337745122 ) ) ;
#61035=CYLINDRICAL_SURFACE ( 'NONE', #61500, 0.1000000000000054040 ) ;
#61037=AXIS2_PLACEMENT_3D ( 'NONE', #166317, #150573, #245820 ) ;
#61047=FACE_OUTER_BOUND ( 'NONE', #197719, .T. ) ;
#61060=DIRECTION ( 'NONE',  ( 3.697785493223492838E-32, -0.2128009952263605065, 0.9770955615653315052 ) ) ;
#61077=CIRCLE ( 'NONE', #190089, 0.1000000000000055844 ) ;
#61111=DIRECTION ( 'NONE',  ( 2.879366945564059217E-14, -0.9984213852963244040, -0.05616704890742151013 ) ) ;
#61141=DIRECTION ( 'NONE',  ( 3.697785493223492838E-32, -0.2128009952263605065, 0.9770955615653315052 ) ) ;
#61209=ADVANCED_FACE ( 'NONE', ( #131512 ), #180181, .F. ) ;
#61254=ORIENTED_EDGE ( 'NONE', *, *, #130369, .T. ) ;
#61267=CIRCLE ( 'NONE', #236047, 0.09999999999999939493 ) ;
#61301=CARTESIAN_POINT ( 'NONE',  ( -22.47071067811865319, 7.522163794833024220, -199.2603376134758832 ) ) ;
#61314=AXIS2_PLACEMENT_3D ( 'NONE', #65542, #222027, #43423 ) ;
#61370=ORIENTED_EDGE ( 'NONE', *, *, #86631, .F. ) ;
#61381=DIRECTION ( 'NONE',  ( -1.000000000000000000, 0.000000000000000000, 0.000000000000000000 ) ) ;
#61414=ORIENTED_EDGE ( 'NONE', *, *, #98880, .T. ) ;
#61445=CIRCLE ( 'NONE', #153067, 0.2000000000000021205 ) ;
#61462=CARTESIAN_POINT ( 'NONE',  ( 20.94999999999999929, 7.300274141770061398, -211.7264450054621534 ) ) ;
#61500=AXIS2_PLACEMENT_3D ( 'NONE', #16808, #76754, #181011 ) ;
#61504=FACE_OUTER_BOUND ( 'NONE', #89540, .T. ) ;
#61570=ORIENTED_EDGE ( 'NONE', *, *, #123444, .T. ) ;
#61583=CARTESIAN_POINT ( 'NONE',  ( 23.14999999999999147, 1.148907358139439339E-11, -201.0000000000015064 ) ) ;
#61590=DIRECTION ( 'NONE',  ( 1.000000000000000000, 0.000000000000000000, 0.000000000000000000 ) ) ;
#61612=CARTESIAN_POINT ( 'NONE',  ( 20.94999999999999929, 8.013878543493270001, -211.9507248933737458 ) ) ;
#61618=DIRECTION ( 'NONE',  ( 1.000000000000000000, 0.000000000000000000, 0.000000000000000000 ) ) ;
#61647=CARTESIAN_POINT ( 'NONE',  ( -20.94999999999999929, 19.68370618165487329, -225.3554403480446240 ) ) ;
#61655=AXIS2_PLACEMENT_3D ( 'NONE', #7260, #108931, #188472 ) ;
#61690=CARTESIAN_POINT ( 'NONE',  ( 21.05000000000000071, 0.02128009953412425548, -201.0977095561580370 ) ) ;
#61714=LINE ( 'NONE', #120440, #53251 ) ;
#61726=CIRCLE ( 'NONE', #136721, 0.1000000000000054040 ) ;
#61737=CIRCLE ( 'NONE', #53361, 0.1000000000000055844 ) ;
#61748=VERTEX_POINT ( 'NONE', #129906 ) ;
#61769=FACE_OUTER_BOUND ( 'NONE', #139627, .T. ) ;
#61778=LINE ( 'NONE', #141317, #62042 ) ;
#61840=CARTESIAN_POINT ( 'NONE',  ( -18.36527282682003204, -0.6805348922791804034, -242.5179119244810977 ) ) ;
#61851=CARTESIAN_POINT ( 'NONE',  ( 20.94999999999999929, 0.6656436123793473270, -212.6810495496487476 ) ) ;
#61885=DIRECTION ( 'NONE',  ( 1.000000000000000000, 0.000000000000000000, 0.000000000000000000 ) ) ;
#61887=CARTESIAN_POINT ( 'NONE',  ( 20.21567752745037794, 11.64196147963353134, -206.5319045250219858 ) ) ;
#61954=AXIS2_PLACEMENT_3D ( 'NONE', #248464, #108936, #148080 ) ;
#61959=EDGE_CURVE ( 'NONE', #118692, #148702, #209570, .T. ) ;
#61975=CIRCLE ( 'NONE', #16205, 0.1000000000000076938 ) ;
#61979=DIRECTION ( 'NONE',  ( 0.000000000000000000, 0.2128009952263650861, -0.9770955615653305060 ) ) ;
#61982=CARTESIAN_POINT ( 'NONE',  ( -23.15000000000000213, 17.11694853917243364, -224.3781540347815451 ) ) ;
#61985=AXIS2_PLACEMENT_3D ( 'NONE', #39123, #169359, #7688 ) ;
#62011=ADVANCED_FACE ( 'NONE', ( #198878 ), #101011, .T. ) ;
#62016=EDGE_LOOP ( 'NONE', ( #548, #96553, #93105, #1202 ) ) ;
#62025=EDGE_CURVE ( 'NONE', #200161, #252276, #97097, .T. ) ;
#62042=VECTOR ( 'NONE', #216981, 1000.000000000000227 ) ;
#62044=CARTESIAN_POINT ( 'NONE',  ( -18.50000000000000000, 7.128833340094563376, -233.7327013124401276 ) ) ;
#62045=ADVANCED_FACE ( 'NONE', ( #121925 ), #34812, .T. ) ;
#62058=CARTESIAN_POINT ( 'NONE',  ( -20.95000000000000284, 17.01923898301589588, -224.3994341343041867 ) ) ;
#62062=ORIENTED_EDGE ( 'NONE', *, *, #9101, .T. ) ;
#62079=DIRECTION ( 'NONE',  ( -0.000000000000000000, 0.9770955615653313941, 0.2128009952263603954 ) ) ;
#62091=AXIS2_PLACEMENT_3D ( 'NONE', #97959, #1446, #78415 ) ;
#62099=ORIENTED_EDGE ( 'NONE', *, *, #26350, .T. ) ;
#62117=AXIS2_PLACEMENT_3D ( 'NONE', #17225, #138407, #194590 ) ;
#62118=ADVANCED_FACE ( 'NONE', ( #107485 ), #226120, .T. ) ;
#62143=CARTESIAN_POINT ( 'NONE',  ( 22.39999999999999503, -2.576749817950531707, -189.6385361693310756 ) ) ;
#62148=DIRECTION ( 'NONE',  ( 0.000000000000000000, 0.2128009952263237581, -0.9770955615653394988 ) ) ;
#62149=AXIS2_PLACEMENT_3D ( 'NONE', #32276, #213442, #251281 ) ;
#62152=LINE ( 'NONE', #139077, #146769 ) ;
#62218=CYLINDRICAL_SURFACE ( 'NONE', #220272, 0.09999999999999939493 ) ;
#62224=ADVANCED_FACE ( 'NONE', ( #172655 ), #193465, .T. ) ;
#62230=CIRCLE ( 'NONE', #124594, 0.09999999999999939493 ) ;
#62237=DIRECTION ( 'NONE',  ( 0.000000000000000000, -0.2128009952263403282, 0.9770955615653358350 ) ) ;
#62238=EDGE_CURVE ( 'NONE', #5593, #141892, #35011, .T. ) ;
#62242=DIRECTION ( 'NONE',  ( 0.000000000000000000, 0.9770955615653316162, 0.2128009952263604232 ) ) ;
#62258=LINE ( 'NONE', #162652, #180245 ) ;
#62266=CIRCLE ( 'NONE', #108070, 0.1000000000000001305 ) ;
#62296=DIRECTION ( 'NONE',  ( -2.952720810173288126E-16, 0.9770955615653313941, 0.2128009952263603677 ) ) ;
#62329=CARTESIAN_POINT ( 'NONE',  ( 20.46382478191414833, 11.98971155215881801, -206.2465614625865271 ) ) ;
#62332=DIRECTION ( 'NONE',  ( 1.000000000000000000, 0.000000000000000000, 0.000000000000000000 ) ) ;
#62340=CIRCLE ( 'NONE', #95637, 0.1000000000000055844 ) ;
#62362=DIRECTION ( 'NONE',  ( 1.000000000000000000, 0.000000000000000000, 0.000000000000000000 ) ) ;
#62403=ADVANCED_FACE ( 'NONE', ( #220714 ), #81179, .T. ) ;
#62412=CARTESIAN_POINT ( 'NONE',  ( 21.05000000000000071, 7.128833340094563376, -233.7327013124401276 ) ) ;
#62427=CIRCLE ( 'NONE', #41599, 0.1000000000000055844 ) ;
#62430=ORIENTED_EDGE ( 'NONE', *, *, #145545, .T. ) ;
#62441=ORIENTED_EDGE ( 'NONE', *, *, #28737, .F. ) ;
#62470=CARTESIAN_POINT ( 'NONE',  ( -21.04999999999953531, 6.144922128657323235, -199.6090117692627928 ) ) ;
#62477=CYLINDRICAL_SURFACE ( 'NONE', #148865, 0.1000000000000054040 ) ;
#62553=EDGE_LOOP ( 'NONE', ( #225533, #243826, #1402, #129807 ) ) ;
#62624=CARTESIAN_POINT ( 'NONE',  ( 20.04142135391667168, 16.73759089399622013, -222.6362981240360739 ) ) ;
#62630=DIRECTION ( 'NONE',  ( 0.000000000000000000, -0.9770955615653318382, -0.2128009952263588411 ) ) ;
#62646=ORIENTED_EDGE ( 'NONE', *, *, #18814, .F. ) ;
#62659=ADVANCED_FACE ( 'NONE', ( #172347 ), #231008, .F. ) ;
#62661=ORIENTED_EDGE ( 'NONE', *, *, #15413, .T. ) ;
#62663=ORIENTED_EDGE ( 'NONE', *, *, #100459, .T. ) ;
#62711=EDGE_CURVE ( 'NONE', #81280, #16906, #110691, .T. ) ;
#62755=ORIENTED_EDGE ( 'NONE', *, *, #138338, .T. ) ;
#62766=CARTESIAN_POINT ( 'NONE',  ( 21.05000000000242721, 11.87050359475319716, -206.1507498716061946 ) ) ;
#62772=CARTESIAN_POINT ( 'NONE',  ( -18.59999999999999787, 6.440012694424540385, -187.5719980452876712 ) ) ;
#62820=AXIS2_PLACEMENT_3D ( 'NONE', #18537, #118934, #243 ) ;
#62834=CYLINDRICAL_SURFACE ( 'NONE', #257475, 0.09999999999999641120 ) ;
#62843=AXIS2_PLACEMENT_3D ( 'NONE', #160349, #99027, #123766 ) ;
#62858=AXIS2_PLACEMENT_3D ( 'NONE', #204226, #243352, #144238 ) ;
#62866=ORIENTED_EDGE ( 'NONE', *, *, #126828, .F. ) ;
#62887=ORIENTED_EDGE ( 'NONE', *, *, #121236, .T. ) ;
#62891=DIRECTION ( 'NONE',  ( -7.304098846218132695E-16, -0.9770955615653315052, -0.2128009952263603954 ) ) ;
#62907=ORIENTED_EDGE ( 'NONE', *, *, #155374, .F. ) ;
#62915=DIRECTION ( 'NONE',  ( 0.000000000000000000, 0.2128009952263603677, -0.9770955615653313941 ) ) ;
#62922=CYLINDRICAL_SURFACE ( 'NONE', #235355, 0.09999999999999641120 ) ;
#62952=ORIENTED_EDGE ( 'NONE', *, *, #80897, .T. ) ;
#62958=EDGE_CURVE ( 'NONE', #248782, #127836, #65178, .T. ) ;
#62972=DIRECTION ( 'NONE',  ( -1.000000000000000000, 0.000000000000000000, 0.000000000000000000 ) ) ;
#62982=CIRCLE ( 'NONE', #192353, 0.3999999999999952482 ) ;
#63003=CARTESIAN_POINT ( 'NONE',  ( 20.95512820512820440, 12.96604748760834092, -210.6109454999921411 ) ) ;
#63044=LINE ( 'NONE', #65617, #16683 ) ;
#63050=CARTESIAN_POINT ( 'NONE',  ( 21.05000000000000071, -0.09770955614504285569, -201.0212800995241764 ) ) ;
#63055=DIRECTION ( 'NONE',  ( 1.000000000000000000, 7.136802563874199107E-16, 1.554319503706929991E-16 ) ) ;
#63058=ORIENTED_EDGE ( 'NONE', *, *, #140901, .T. ) ;
#63059=CARTESIAN_POINT ( 'NONE',  ( 21.05000000000000071, 9.374458193048763377, -220.5475659691911119 ) ) ;
#63090=CARTESIAN_POINT ( 'NONE',  ( -23.25000000000000000, -11.48087284838115885, -203.5004116939112464 ) ) ;
#63109=DIRECTION ( 'NONE',  ( -1.000000000000000000, 0.000000000000000000, 0.000000000000000000 ) ) ;
#63116=DIRECTION ( 'NONE',  ( 2.952720810173289605E-16, -0.9770955615653357240, -0.2128009952263412996 ) ) ;
#63120=CARTESIAN_POINT ( 'NONE',  ( 23.14999999999999503, 8.882751598337874199, -187.0399955572217721 ) ) ;
#63158=EDGE_CURVE ( 'NONE', #245138, #166165, #124530, .T. ) ;
#63167=EDGE_CURVE ( 'NONE', #170209, #230954, #197064, .T. ) ;
#63189=EDGE_CURVE ( 'NONE', #48943, #98837, #42413, .T. ) ;
#63210=ORIENTED_EDGE ( 'NONE', *, *, #233881, .F. ) ;
#63224=CARTESIAN_POINT ( 'NONE',  ( 20.95263205890695701, 10.49856401425325281, -207.4020386360608086 ) ) ;
#63380=CARTESIAN_POINT ( 'NONE',  ( 18.59999999999999076, 11.04098673250373785, -220.4458636211660689 ) ) ;
#63387=DIRECTION ( 'NONE',  ( 0.000000000000000000, 0.9968797965484670343, 0.07893460099023179299 ) ) ;
#63434=CARTESIAN_POINT ( 'NONE',  ( 22.57320508075688537, 11.38316329224760359, -198.5208684056144079 ) ) ;
#63442=DIRECTION ( 'NONE',  ( 1.000000000000000000, 0.000000000000000000, 0.000000000000000000 ) ) ;
#63448=ORIENTED_EDGE ( 'NONE', *, *, #178765, .T. ) ;
#63466=ORIENTED_EDGE ( 'NONE', *, *, #59418, .T. ) ;
#63493=VERTEX_POINT ( 'NONE', #93086 ) ;
#63495=CYLINDRICAL_SURFACE ( 'NONE', #159929, 0.1000000000000122874 ) ;
#63524=EDGE_LOOP ( 'NONE', ( #24184, #227782, #35652, #20011, #25029 ) ) ;
#63527=LINE ( 'NONE', #83061, #100626 ) ;
#63532=DIRECTION ( 'NONE',  ( 0.000000000000000000, -0.9968797965484669232, -0.07893460099023200116 ) ) ;
#63547=EDGE_CURVE ( 'NONE', #125678, #43729, #30697, .T. ) ;
#63558=CARTESIAN_POINT ( 'NONE',  ( 23.14999999999999858, 7.128833340094563376, -233.7327013124401276 ) ) ;
#63584=CIRCLE ( 'NONE', #71983, 0.09999999999999810429 ) ;
#63592=CIRCLE ( 'NONE', #80121, 0.09999999999999810429 ) ;
#63606=ORIENTED_EDGE ( 'NONE', *, *, #15980, .T. ) ;
#63611=ORIENTED_EDGE ( 'NONE', *, *, #133531, .T. ) ;
#63658=EDGE_LOOP ( 'NONE', ( #107027, #44684, #47112 ) ) ;
#63666=VERTEX_POINT ( 'NONE', #30270 ) ;
#63679=VERTEX_POINT ( 'NONE', #47227 ) ;
#63701=CARTESIAN_POINT ( 'NONE',  ( 20.94999999999999929, 7.128833340094563376, -233.7327013124401276 ) ) ;
#63707=PLANE ( 'NONE',  #173068 ) ;
#63729=DIRECTION ( 'NONE',  ( 1.000000000000000000, 0.000000000000000000, 0.000000000000000000 ) ) ;
#63743=CARTESIAN_POINT ( 'NONE',  ( -21.05000000000000071, 6.284975638137225040, -199.7187985938684847 ) ) ;
#63757=CARTESIAN_POINT ( 'NONE',  ( -21.05000000000000071, 7.980037321000002848, -237.6410835587014390 ) ) ;
#63763=EDGE_CURVE ( 'NONE', #17245, #74531, #84990, .T. ) ;
#63786=EDGE_CURVE ( 'NONE', #230954, #2619, #97460, .T. ) ;
#63797=CARTESIAN_POINT ( 'NONE',  ( -20.94999999999999929, 0.6713328740235187109, -212.7808875799876205 ) ) ;
#63798=ADVANCED_FACE ( 'NONE', ( #176203 ), #56213, .F. ) ;
#63801=CARTESIAN_POINT ( 'NONE',  ( 21.09107601085545269, -1.315832710461172006, -194.7735184721627775 ) ) ;
#63811=ORIENTED_EDGE ( 'NONE', *, *, #32862, .T. ) ;
#63842=DIRECTION ( 'NONE',  ( 0.000000000000000000, -0.9770955615653316162, -0.2128009952263604232 ) ) ;
#63849=VERTEX_POINT ( 'NONE', #73267 ) ;
#63851=ORIENTED_EDGE ( 'NONE', *, *, #6625, .T. ) ;
#63853=DIRECTION ( 'NONE',  ( -1.000000000000000000, 0.000000000000000000, 0.000000000000000000 ) ) ;
#63854=CARTESIAN_POINT ( 'NONE',  ( 20.94999999999999929, 9.765296417674898422, -220.4624455711005737 ) ) ;
#63871=FACE_OUTER_BOUND ( 'NONE', #187474, .T. ) ;
#63892=DIRECTION ( 'NONE',  ( 0.000000000000000000, -0.2128009952263403282, 0.9770955615653358350 ) ) ;
#63896=EDGE_CURVE ( 'NONE', #254455, #189298, #214208, .T. ) ;
#63899=DIRECTION ( 'NONE',  ( 1.000000000000000000, 3.190570557967288949E-16, 6.948722487160392945E-17 ) ) ;
#63916=CARTESIAN_POINT ( 'NONE',  ( -21.05000000000000071, 4.288595810029049993, -211.9930862808554934 ) ) ;
#63962=CIRCLE ( 'NONE', #118118, 0.1000000000000054040 ) ;
#63970=AXIS2_PLACEMENT_3D ( 'NONE', #153776, #211129, #155035 ) ;
#63986=AXIS2_PLACEMENT_3D ( 'NONE', #126159, #67481, #87023 ) ;
#63992=ORIENTED_EDGE ( 'NONE', *, *, #125434, .T. ) ;
#64043=VERTEX_POINT ( 'NONE', #181047 ) ;
#64047=CARTESIAN_POINT ( 'NONE',  ( 20.12500000000000000, 14.04870287383362992, -219.6884709798077893 ) ) ;
#64059=CARTESIAN_POINT ( 'NONE',  ( 23.14999999999999503, 9.104497675943859392, -211.5542940109215522 ) ) ;
#64087=ORIENTED_EDGE ( 'NONE', *, *, #168610, .T. ) ;
#64108=CYLINDRICAL_SURFACE ( 'NONE', #70208, 0.09999999999999939493 ) ;
#64110=FILL_AREA_STYLE_COLOUR ( '', #32818 ) ;
#64113=ADVANCED_FACE ( 'NONE', ( #121091 ), #165317, .T. ) ;
#64151=AXIS2_PLACEMENT_3D ( 'NONE', #226573, #47943, #207036 ) ;
#64156=CARTESIAN_POINT ( 'NONE',  ( 21.08832698747859169, 11.17665284714344764, -211.0812192837269379 ) ) ;
#64164=ORIENTED_EDGE ( 'NONE', *, *, #212986, .T. ) ;
#64168=DIRECTION ( 'NONE',  ( 0.000000000000000000, -0.1975078988072421216, 0.9803012954743803853 ) ) ;
#64184=DIRECTION ( 'NONE',  ( 0.000000000000000000, 0.05689261644170980764, -0.9983803033886519129 ) ) ;
#64189=LINE ( 'NONE', #237689, #43778 ) ;
#64227=CARTESIAN_POINT ( 'NONE',  ( 21.08198257630413508, 6.176001972649067362, -199.5805864394077105 ) ) ;
#64237=DIRECTION ( 'NONE',  ( 0.000000000000000000, 0.9770955615653315052, 0.2128009952263607008 ) ) ;
#64264=FACE_OUTER_BOUND ( 'NONE', #29591, .T. ) ;
#64309=EDGE_CURVE ( 'NONE', #123636, #111449, #106022, .T. ) ;
#64318=ORIENTED_EDGE ( 'NONE', *, *, #85173, .T. ) ;
#64333=DIRECTION ( 'NONE',  ( 0.000000000000000000, 0.2128009952264685312, -0.9770955615653078574 ) ) ;
#64380=CARTESIAN_POINT ( 'NONE',  ( 20.94999999999999574, 1.148907358139439339E-11, -201.0000000000015064 ) ) ;
#64381=DIRECTION ( 'NONE',  ( 0.000000000000000000, 0.2128009952263605897, -0.9770955615653315052 ) ) ;
#64421=VECTOR ( 'NONE', #217106, 1000.000000000000000 ) ;
#64424=FACE_OUTER_BOUND ( 'NONE', #210626, .T. ) ;
#64432=VERTEX_POINT ( 'NONE', #85424 ) ;
#64475=ORIENTED_EDGE ( 'NONE', *, *, #12419, .F. ) ;
#64477=AXIS2_PLACEMENT_3D ( 'NONE', #255670, #238724, #234886 ) ;
#64484=FACE_OUTER_BOUND ( 'NONE', #220277, .T. ) ;
#64494=AXIS2_PLACEMENT_3D ( 'NONE', #108113, #231924, #187668 ) ;
#64561=DIRECTION ( 'NONE',  ( 1.000000000000000000, 0.000000000000000000, 0.000000000000000000 ) ) ;
#64605=AXIS2_PLACEMENT_3D ( 'NONE', #43127, #125227, #66540 ) ;
#64610=EDGE_LOOP ( 'NONE', ( #24775, #37292, #91026 ) ) ;
#64624=EDGE_CURVE ( 'NONE', #633, #115886, #168817, .T. ) ;
#64636=DIRECTION ( 'NONE',  ( 1.000000000000000000, 0.000000000000000000, 0.000000000000000000 ) ) ;
#64658=ORIENTED_EDGE ( 'NONE', *, *, #104113, .T. ) ;
#64659=DIRECTION ( 'NONE',  ( -1.000000000000000000, 0.000000000000000000, 0.000000000000000000 ) ) ;
#64669=ORIENTED_EDGE ( 'NONE', *, *, #231641, .T. ) ;
#64691=FACE_OUTER_BOUND ( 'NONE', #53501, .T. ) ;
#64699=CARTESIAN_POINT ( 'NONE',  ( -20.94999999999999929, 2.953700692300310848, -208.6327728934509764 ) ) ;
#64706=CARTESIAN_POINT ( 'NONE',  ( 23.15000000000000213, -4.756823075239756449, -233.1486023682345490 ) ) ;
#64721=EDGE_LOOP ( 'NONE', ( #23034, #234999, #175961 ) ) ;
#64750=CARTESIAN_POINT ( 'NONE',  ( -20.94999999999999929, 17.06838326776700399, -224.6250846885016870 ) ) ;
#64754=CARTESIAN_POINT ( 'NONE',  ( 18.59999999999999076, 8.531609279343539853, -209.3937462695851366 ) ) ;
#64842=CIRCLE ( 'NONE', #210600, 0.1000000000000054040 ) ;
#64861=CARTESIAN_POINT ( 'NONE',  ( 21.05000000000000071, -4.871452838297987142, -233.3782557782877518 ) ) ;
#64865=CARTESIAN_POINT ( 'NONE',  ( -23.15000000000000213, 4.768403829798271154, -213.4961173936592331 ) ) ;
#64867=CIRCLE ( 'NONE', #139877, 7.800000000000002487 ) ;
#64877=DIRECTION ( 'NONE',  ( 0.000000000000000000, 0.2128009952263601456, -0.9770955615653315052 ) ) ;
#64881=DIRECTION ( 'NONE',  ( 0.000000000000000000, -0.2128009952263506810, 0.9770955615653337256 ) ) ;
#64897=VERTEX_POINT ( 'NONE', #190390 ) ;
#64924=EDGE_CURVE ( 'NONE', #45345, #87352, #252902, .T. ) ;
#64933=ORIENTED_EDGE ( 'NONE', *, *, #39908, .F. ) ;
#65026=ADVANCED_FACE ( 'NONE', ( #175967 ), #156415, .T. ) ;
#65029=EDGE_CURVE ( 'NONE', #206404, #22410, #78108, .T. ) ;
#65050=ORIENTED_EDGE ( 'NONE', *, *, #192038, .F. ) ;
#65057=AXIS2_PLACEMENT_3D ( 'NONE', #206726, #67215, #248425 ) ;
#65072=CARTESIAN_POINT ( 'NONE',  ( 21.87500000000000355, 14.04870287383362992, -219.6884709798077893 ) ) ;
#65101=DIRECTION ( 'NONE',  ( -1.000000000000000000, -0.000000000000000000, -0.000000000000000000 ) ) ;
#65102=AXIS2_PLACEMENT_3D ( 'NONE', #105715, #165747, #122768 ) ;
#65109=CARTESIAN_POINT ( 'NONE',  ( -18.56579813702275672, 18.41141989892753017, -236.9935361838138022 ) ) ;
#65124=VERTEX_POINT ( 'NONE', #204473 ) ;
#65144=ORIENTED_EDGE ( 'NONE', *, *, #143356, .T. ) ;
#65157=ORIENTED_EDGE ( 'NONE', *, *, #237792, .T. ) ;
#65168=DIRECTION ( 'NONE',  ( 0.000000000000000000, 0.9770955615653313941, 0.2128009952263603677 ) ) ;
#65170=DIRECTION ( 'NONE',  ( 0.000000000000000000, -0.2128009952263603677, 0.9770955615653313941 ) ) ;
#65178=LINE ( 'NONE', #226822, #238781 ) ;
#65194=AXIS2_PLACEMENT_3D ( 'NONE', #45192, #165151, #124744 ) ;
#65201=TOROIDAL_SURFACE ( 'NONE', #202578, 0.2000000000000000111, 0.1000000000000000056 ) ;
#65237=AXIS2_PLACEMENT_3D ( 'NONE', #202028, #222860, #28574 ) ;
#65242=PLANE ( 'NONE',  #64605 ) ;
#65251=ORIENTED_EDGE ( 'NONE', *, *, #185820, .F. ) ;
#65255=DIRECTION ( 'NONE',  ( 1.000000000000000000, 0.000000000000000000, 0.000000000000000000 ) ) ;
#65275=ORIENTED_EDGE ( 'NONE', *, *, #27971, .T. ) ;
#65278=LINE ( 'NONE', #99251, #106036 ) ;
#65342=DIRECTION ( 'NONE',  ( 1.000000000000000000, 2.885090398161910739E-16, 6.283419270304611573E-17 ) ) ;
#65344=ORIENTED_EDGE ( 'NONE', *, *, #146564, .F. ) ;
#65348=ADVANCED_FACE ( 'NONE', ( #149673 ), #33605, .F. ) ;
#65355=ORIENTED_EDGE ( 'NONE', *, *, #175234, .F. ) ;
#65365=CARTESIAN_POINT ( 'NONE',  ( 20.85000000000000142, 7.783179459866048866, -245.3643104511423019 ) ) ;
#65383=CARTESIAN_POINT ( 'NONE',  ( 21.05000000000000071, 13.06362847850371622, -210.5896934006125889 ) ) ;
#65386=CARTESIAN_POINT ( 'NONE',  ( 21.05000000000000071, 9.374458193048763377, -220.5475659691911119 ) ) ;
#65424=CIRCLE ( 'NONE', #140426, 0.8750000000000007772 ) ;
#65427=CYLINDRICAL_SURFACE ( 'NONE', #66440, 0.09999999999999939493 ) ;
#65428=CARTESIAN_POINT ( 'NONE',  ( 21.07964655665547227, 11.17474170846107029, -211.0746752039685248 ) ) ;
#65433=CARTESIAN_POINT ( 'NONE',  ( -22.39999999999999858, -1.560176095955062348, -193.3663837337744837 ) ) ;
#65454=DIRECTION ( 'NONE',  ( 1.000000000000000000, 0.000000000000000000, 0.000000000000000000 ) ) ;
#65457=EDGE_CURVE ( 'NONE', #129320, #187942, #236882, .T. ) ;
#65460=LINE ( 'NONE', #126727, #199426 ) ;
#65464=VECTOR ( 'NONE', #208403, 1000.000000000000000 ) ;
#65475=CARTESIAN_POINT ( 'NONE',  ( 21.14999999999999503, -2.598867842139046314, -189.5410128746472083 ) ) ;
#65500=AXIS2_PLACEMENT_3D ( 'NONE', #242177, #102640, #63532 ) ;
#65509=FACE_OUTER_BOUND ( 'NONE', #179092, .T. ) ;
#65522=AXIS2_PLACEMENT_3D ( 'NONE', #55744, #37518, #32405 ) ;
#65527=EDGE_CURVE ( 'NONE', #44687, #229705, #240065, .T. ) ;
#65542=CARTESIAN_POINT ( 'NONE',  ( 20.94999999999999574, 8.299331953467152800, -209.2670685529822663 ) ) ;
#65554=VERTEX_POINT ( 'NONE', #81623 ) ;
#65568=EDGE_CURVE ( 'NONE', #154626, #156652, #210832, .T. ) ;
#65571=EDGE_CURVE ( 'NONE', #258000, #189298, #85471, .T. ) ;
#65579=EDGE_CURVE ( 'NONE', #17245, #154129, #240746, .T. ) ;
#65595=ORIENTED_EDGE ( 'NONE', *, *, #40051, .F. ) ;
#65615=DIRECTION ( 'NONE',  ( 0.000000000000000000, -0.2128009952263603677, 0.9770955615653313941 ) ) ;
#65617=CARTESIAN_POINT ( 'NONE',  ( 21.05000000000000071, 9.863005973831429074, -220.4411654715779321 ) ) ;
#65637=EDGE_CURVE ( 'NONE', #27458, #167415, #142823, .T. ) ;
#65642=CIRCLE ( 'NONE', #211402, 12.97499999999999964 ) ;
#65647=EDGE_CURVE ( 'NONE', #79677, #235545, #13675, .T. ) ;
#65680=EDGE_LOOP ( 'NONE', ( #180902, #163328, #103958, #204984 ) ) ;
#65754=DIRECTION ( 'NONE',  ( -0.000000000000000000, -0.08413937888704771384, 0.9964539953858891908 ) ) ;
#65801=EDGE_CURVE ( 'NONE', #192844, #21650, #185880, .T. ) ;
#65829=DIRECTION ( 'NONE',  ( 0.000000000000000000, -0.2128009952263403282, 0.9770955615653358350 ) ) ;
#65848=ORIENTED_EDGE ( 'NONE', *, *, #90270, .F. ) ;
#65861=CARTESIAN_POINT ( 'NONE',  ( 20.85000000000000142, 7.668827189579289438, -241.6142244293585009 ) ) ;
#65871=CARTESIAN_POINT ( 'NONE',  ( -18.59999999999999787, 7.128833340094563376, -233.7327013124401276 ) ) ;
#65875=VECTOR ( 'NONE', #44499, 1000.000000000000000 ) ;
#65876=ADVANCED_FACE ( 'NONE', ( #153226 ), #256564, .T. ) ;
#65915=ORIENTED_EDGE ( 'NONE', *, *, #8706, .T. ) ;
#65916=CARTESIAN_POINT ( 'NONE',  ( -20.54999999999999716, 6.294532028225942710, -220.7845521659012888 ) ) ;
#65962=ORIENTED_EDGE ( 'NONE', *, *, #89946, .F. ) ;
#65968=DIRECTION ( 'NONE',  ( 0.000000000000000000, 0.2128009952263485993, -0.9770955615653341697 ) ) ;
#65982=ORIENTED_EDGE ( 'NONE', *, *, #44984, .F. ) ;
#66033=CARTESIAN_POINT ( 'NONE',  ( -20.99749315643146730, 17.11694853957537887, -224.3781540366317131 ) ) ;
#66040=DIRECTION ( 'NONE',  ( 0.000000000000000000, 0.2128009952263403282, -0.9770955615653358350 ) ) ;
#66042=FACE_OUTER_BOUND ( 'NONE', #200834, .T. ) ;
#66062=EDGE_CURVE ( 'NONE', #16906, #53843, #165220, .T. ) ;
#66065=CARTESIAN_POINT ( 'NONE',  ( 21.12400222705969099, 11.18425721308768850, -211.1013445587443869 ) ) ;
#66116=CARTESIAN_POINT ( 'NONE',  ( -23.15000000000000213, -4.756823075239756449, -233.1486023682345490 ) ) ;
#66139=FACE_OUTER_BOUND ( 'NONE', #63524, .T. ) ;
#66202=EDGE_CURVE ( 'NONE', #214314, #83582, #156770, .T. ) ;
#66204=AXIS2_PLACEMENT_3D ( 'NONE', #27330, #204623, #28627 ) ;
#66220=DIRECTION ( 'NONE',  ( 0.000000000000000000, -0.9770955615653315052, -0.2128009952263603954 ) ) ;
#66232=DIRECTION ( 'NONE',  ( 1.000000000000000000, 2.885090398161910739E-16, 6.283419270304611573E-17 ) ) ;
#66248=PLANE ( 'NONE',  #242920 ) ;
#66255=DIRECTION ( 'NONE',  ( 0.000000000000000000, -0.9550021345545530727, 0.2965989261549131228 ) ) ;
#66263=VERTEX_POINT ( 'NONE', #143267 ) ;
#66284=CARTESIAN_POINT ( 'NONE',  ( 23.24999999999999289, 8.882751598337874199, -187.0399955572217721 ) ) ;
#66325=ORIENTED_EDGE ( 'NONE', *, *, #920, .F. ) ;
#66366=DIRECTION ( 'NONE',  ( 0.000000000000000000, -0.9770955615653316162, -0.2128009952263604232 ) ) ;
#66370=CARTESIAN_POINT ( 'NONE',  ( 20.94999999999999574, 11.84624361595475506, -206.1763227999733203 ) ) ;
#66385=AXIS2_PLACEMENT_3D ( 'NONE', #250409, #167064, #30108 ) ;
#66399=CARTESIAN_POINT ( 'NONE',  ( 21.05000000000000071, 2.585532092011767702, -212.8717110730202933 ) ) ;
#66421=ORIENTED_EDGE ( 'NONE', *, *, #177558, .F. ) ;
#66440=AXIS2_PLACEMENT_3D ( 'NONE', #142395, #225767, #165838 ) ;
#66445=CARTESIAN_POINT ( 'NONE',  ( -22.50000000000000000, -2.388551469052506260, -189.5974192130969698 ) ) ;
#66462=AXIS2_PLACEMENT_3D ( 'NONE', #97128, #93318, #215814 ) ;
#66466=DIRECTION ( 'NONE',  ( -3.265361837132813586E-16, 0.9770955615653313941, 0.2128009952263610061 ) ) ;
#66467=ORIENTED_EDGE ( 'NONE', *, *, #128615, .F. ) ;
#66509=ORIENTED_EDGE ( 'NONE', *, *, #114406, .T. ) ;
#66515=EDGE_LOOP ( 'NONE', ( #250505, #62099, #22688, #6876, #153716 ) ) ;
#66516=CARTESIAN_POINT ( 'NONE',  ( 21.30000000000002558, 1.148907358139439339E-11, -201.0000000000015064 ) ) ;
#66526=ADVANCED_FACE ( 'NONE', ( #150982 ), #190562, .T. ) ;
#66538=EDGE_LOOP ( 'NONE', ( #109455, #173684, #230897, #255729 ) ) ;
#66540=DIRECTION ( 'NONE',  ( 0.7071067811865474617, 0.6909108974501236844, 0.1504730267678055788 ) ) ;
#66562=DIRECTION ( 'NONE',  ( 1.000000000000000000, 0.000000000000000000, 0.000000000000000000 ) ) ;
#66563=VECTOR ( 'NONE', #170223, 1000.000000000000000 ) ;
#66569=ORIENTED_EDGE ( 'NONE', *, *, #233721, .F. ) ;
#66585=DIRECTION ( 'NONE',  ( 2.827886303505248766E-16, -0.7397890806274223241, -0.6728388485993012091 ) ) ;
#66657=EDGE_CURVE ( 'NONE', #162009, #110145, #211201, .T. ) ;
#66677=CARTESIAN_POINT ( 'NONE',  ( 21.06490991615909536, 13.07620565549636993, -210.6419246457020620 ) ) ;
#66678=CARTESIAN_POINT ( 'NONE',  ( 21.05000000000000071, 7.533155231024649012, -235.5891828794142384 ) ) ;
#66681=( LENGTH_UNIT ( ) NAMED_UNIT ( * ) SI_UNIT ( .MILLI., .METRE. ) );
#66692=LINE ( 'NONE', #148802, #207487 ) ;
#66713=DIRECTION ( 'NONE',  ( -4.336808689942052446E-15, -0.7397890806274316500, -0.6728388485992908841 ) ) ;
#66753=ORIENTED_EDGE ( 'NONE', *, *, #248140, .T. ) ;
#66778=DIRECTION ( 'NONE',  ( -1.000000000000000000, 0.000000000000000000, 0.000000000000000000 ) ) ;
#66801=EDGE_LOOP ( 'NONE', ( #33858, #221364, #209206, #144957 ) ) ;
#66807=CARTESIAN_POINT ( 'NONE',  ( 18.43709777086139923, -0.9152171842606990904, -242.2974985173726736 ) ) ;
#66825=ADVANCED_FACE ( 'NONE', ( #93248 ), #103209, .T. ) ;
#66839=EDGE_CURVE ( 'NONE', #222677, #52138, #240599, .T. ) ;
#66848=DIRECTION ( 'NONE',  ( 0.000000000000000000, 0.2128009952263485993, -0.9770955615653341697 ) ) ;
#66881=CIRCLE ( 'NONE', #245958, 12.87499999999999467 ) ;
#66882=AXIS2_PLACEMENT_3D ( 'NONE', #217250, #238106, #85102 ) ;
#66903=DIRECTION ( 'NONE',  ( 1.000000000000000000, 0.000000000000000000, 0.000000000000000000 ) ) ;
#66921=ORIENTED_EDGE ( 'NONE', *, *, #149382, .T. ) ;
#66934=CARTESIAN_POINT ( 'NONE',  ( -21.05000000000000071, 4.273531877263400780, -211.9976340888692050 ) ) ;
#66943=EDGE_CURVE ( 'NONE', #170209, #2619, #124097, .T. ) ;
#66949=DIRECTION ( 'NONE',  ( 2.952720810173288126E-16, -0.9770955615653313941, -0.2128009952263603677 ) ) ;
#66970=ADVANCED_FACE ( 'NONE', ( #214477 ), #147685, .T. ) ;
#66972=DIRECTION ( 'NONE',  ( 0.000000000000000000, -0.2128009952263603677, 0.9770955615653313941 ) ) ;
#66993=VECTOR ( 'NONE', #101424, 1000.000000000000000 ) ;
#67001=ORIENTED_EDGE ( 'NONE', *, *, #188089, .T. ) ;
#67021=CARTESIAN_POINT ( 'NONE',  ( -21.07928932188134041, 6.162520550847337297, -199.5566553493351307 ) ) ;
#67030=ORIENTED_EDGE ( 'NONE', *, *, #128318, .T. ) ;
#67033=ORIENTED_EDGE ( 'NONE', *, *, #218113, .F. ) ;
#67081=DIRECTION ( 'NONE',  ( -1.000000000000000000, -2.885090398161910739E-16, -6.283419270304611573E-17 ) ) ;
#67085=DIRECTION ( 'NONE',  ( 0.000000000000000000, -0.2128009952263602012, 0.9770955615653315052 ) ) ;
#67139=ORIENTED_EDGE ( 'NONE', *, *, #195714, .F. ) ;
#67159=ADVANCED_FACE ( 'NONE', ( #171257 ), #73420, .T. ) ;
#67172=CARTESIAN_POINT ( 'NONE',  ( -18.59999999999999787, 0.5876173420563349792, -209.1618981382189588 ) ) ;
#67180=DIRECTION ( 'NONE',  ( 0.000000000000000000, -0.2128009952263603677, 0.9770955615653313941 ) ) ;
#67188=CIRCLE ( 'NONE', #17145, 0.1000000000000054040 ) ;
#67196=CYLINDRICAL_SURFACE ( 'NONE', #162386, 0.09999999999999895084 ) ;
#67215=DIRECTION ( 'NONE',  ( 0.000000000000000000, -0.2128009952263603954, 0.9770955615653315052 ) ) ;
#67225=LINE ( 'NONE', #222417, #30614 ) ;
#67231=ADVANCED_FACE ( 'NONE', ( #177658 ), #133369, .F. ) ;
#67238=CIRCLE ( 'NONE', #250582, 0.1000000000000055844 ) ;
#67262=ORIENTED_EDGE ( 'NONE', *, *, #217683, .T. ) ;
#67303=LINE ( 'NONE', #226353, #150674 ) ;
#67313=CARTESIAN_POINT ( 'NONE',  ( 18.39999999999999858, -0.6821283177418837607, -242.5105927437468836 ) ) ;
#67328=DIRECTION ( 'NONE',  ( 0.000000000000000000, -0.9770955615653316162, -0.2128009952263604232 ) ) ;
#67331=ADVANCED_FACE ( 'NONE', ( #242717 ), #43251, .F. ) ;
#67362=ORIENTED_EDGE ( 'NONE', *, *, #144235, .T. ) ;
#67405=ORIENTED_EDGE ( 'NONE', *, *, #134694, .F. ) ;
#67431=ORIENTED_EDGE ( 'NONE', *, *, #130394, .T. ) ;
#67444=CARTESIAN_POINT ( 'NONE',  ( 20.95512820512820440, 12.01161663143393632, -206.2285874551107554 ) ) ;
#67447=CARTESIAN_POINT ( 'NONE',  ( -23.25000000000000000, 1.148907358139439339E-11, -201.0000000000015064 ) ) ;
#67448=ORIENTED_EDGE ( 'NONE', *, *, #78800, .F. ) ;
#67455=ADVANCED_FACE ( 'NONE', ( #209743 ), #50641, .F. ) ;
#67481=DIRECTION ( 'NONE',  ( 1.000000000000000000, 0.000000000000000000, 0.000000000000000000 ) ) ;
#67486=LINE ( 'NONE', #244836, #241019 ) ;
#67488=ORIENTED_EDGE ( 'NONE', *, *, #221581, .F. ) ;
#67502=ORIENTED_EDGE ( 'NONE', *, *, #175832, .T. ) ;
#67503=AXIS2_PLACEMENT_3D ( 'NONE', #115737, #51886, #74077 ) ;
#67513=CARTESIAN_POINT ( 'NONE',  ( 21.14999999999999858, 14.06640494040442135, -210.3712993791105532 ) ) ;
#67620=LINE ( 'NONE', #71504, #22787 ) ;
#67644=DIRECTION ( 'NONE',  ( 1.000000000000000000, 0.000000000000000000, 0.000000000000000000 ) ) ;
#67651=CARTESIAN_POINT ( 'NONE',  ( -23.15000000000000213, 6.878457983866232972, -212.1414458560986986 ) ) ;
#67673=VECTOR ( 'NONE', #108263, 1000.000000000000000 ) ;
#67676=CARTESIAN_POINT ( 'NONE',  ( -18.53317502108577131, 18.39833411442327460, -236.9692678682430369 ) ) ;
#67683=DIRECTION ( 'NONE',  ( 1.000000000000000000, 0.000000000000000000, 0.000000000000000000 ) ) ;
#67693=CARTESIAN_POINT ( 'NONE',  ( 18.39999999999999858, -0.7490476236415669620, -242.2033265267442061 ) ) ;
#67697=ORIENTED_EDGE ( 'NONE', *, *, #27844, .T. ) ;
#67727=CARTESIAN_POINT ( 'NONE',  ( -22.43310005002225438, -2.473551863546898932, -189.6159672949451362 ) ) ;
#67803=DIRECTION ( 'NONE',  ( 0.000000000000000000, -0.2965989261549410450, -0.9550021345545443019 ) ) ;
#67818=ORIENTED_EDGE ( 'NONE', *, *, #125210, .F. ) ;
#67825=CARTESIAN_POINT ( 'NONE',  ( 21.08489247129321242, 11.30242931707484821, -211.1779520694198311 ) ) ;
#67851=DIRECTION ( 'NONE',  ( 0.000000000000000000, 0.2128009952263604232, -0.9770955615653316162 ) ) ;
#67875=AXIS2_PLACEMENT_3D ( 'NONE', #137654, #112989, #132553 ) ;
#67876=DIRECTION ( 'NONE',  ( 0.000000000000000000, 0.9770955615653548199, 0.2128009952262535920 ) ) ;
#67898=CARTESIAN_POINT ( 'NONE',  ( 21.05000000000012150, 12.00928618750723231, -206.1912950450977746 ) ) ;
#67910=VECTOR ( 'NONE', #39427, 1000.000000000000000 ) ;
#67945=DIRECTION ( 'NONE',  ( -1.000000000000000000, 0.000000000000000000, -0.000000000000000000 ) ) ;
#67966=CARTESIAN_POINT ( 'NONE',  ( -21.07971444708686093, -1.261174164707013157, -194.7964993367602062 ) ) ;
#67973=CARTESIAN_POINT ( 'NONE',  ( 20.94999999999999929, 13.06362847850371978, -210.5896934006125889 ) ) ;
#67983=ORIENTED_EDGE ( 'NONE', *, *, #187033, .T. ) ;
#68032=CARTESIAN_POINT ( 'NONE',  ( 23.14999999999999858, 7.525330762710603416, -212.0571253909869256 ) ) ;
#68044=DIRECTION ( 'NONE',  ( 1.000000000000000000, 0.000000000000000000, 0.000000000000000000 ) ) ;
#68053=LINE ( 'NONE', #165895, #174720 ) ;
#68067=FACE_OUTER_BOUND ( 'NONE', #116134, .T. ) ;
#68073=VECTOR ( 'NONE', #168666, 1000.000000000000000 ) ;
#68089=DIRECTION ( 'NONE',  ( -0.000000000000000000, 0.9770955615653313941, 0.2128009952263603954 ) ) ;
#68127=ORIENTED_EDGE ( 'NONE', *, *, #253642, .F. ) ;
#68130=VERTEX_POINT ( 'NONE', #244069 ) ;
#68171=EDGE_LOOP ( 'NONE', ( #164877, #35807, #104910, #191729 ) ) ;
#68178=CIRCLE ( 'NONE', #126443, 0.8750000000000007772 ) ;
#68189=FACE_OUTER_BOUND ( 'NONE', #18730, .T. ) ;
#68203=CYLINDRICAL_SURFACE ( 'NONE', #165189, 0.1000000000000057648 ) ;
#68205=DIRECTION ( 'NONE',  ( -0.000000000000000000, 0.9770955615653313941, 0.2128009952263603954 ) ) ;
#68217=EDGE_CURVE ( 'NONE', #143709, #190923, #123897, .T. ) ;
#68243=CIRCLE ( 'NONE', #213996, 2.000000000000003109 ) ;
#68250=VECTOR ( 'NONE', #75868, 1000.000000000000227 ) ;
#68256=LINE ( 'NONE', #124384, #145238 ) ;
#68264=DIRECTION ( 'NONE',  ( 1.000000000000000000, 2.885090398161910739E-16, 6.283419270304611573E-17 ) ) ;
#68288=CARTESIAN_POINT ( 'NONE',  ( 18.59999999999997655, 18.60970618848720903, -231.2322896185303875 ) ) ;
#68293=CARTESIAN_POINT ( 'NONE',  ( 18.49713797159835948, -7.725302628690933204, -209.9197111851193256 ) ) ;
#68307=EDGE_CURVE ( 'NONE', #95409, #54081, #178262, .T. ) ;
#68315=CARTESIAN_POINT ( 'NONE',  ( 21.05000000000000071, 1.148907358139439339E-11, -201.0000000000015064 ) ) ;
#68317=VERTEX_POINT ( 'NONE', #178701 ) ;
#68341=CIRCLE ( 'NONE', #193237, 2.000000000000003109 ) ;
#68368=CARTESIAN_POINT ( 'NONE',  ( 21.04999999999998650, 9.104497675943859392, -211.5542940109215522 ) ) ;
#68391=ORIENTED_EDGE ( 'NONE', *, *, #3417, .T. ) ;
#68404=ORIENTED_EDGE ( 'NONE', *, *, #182471, .T. ) ;
#68450=DIRECTION ( 'NONE',  ( 0.000000000000000000, -0.9770955615653551529, -0.2128009952262517601 ) ) ;
#68490=ORIENTED_EDGE ( 'NONE', *, *, #135584, .F. ) ;
#68492=VERTEX_POINT ( 'NONE', #242476 ) ;
#68497=DIRECTION ( 'NONE',  ( 0.000000000000000000, -0.2128009952263650861, 0.9770955615653305060 ) ) ;
#68529=EDGE_CURVE ( 'NONE', #31563, #229898, #40891, .T. ) ;
#68562=FACE_OUTER_BOUND ( 'NONE', #218551, .T. ) ;
#68563=CYLINDRICAL_SURFACE ( 'NONE', #159340, 0.09999999999999641120 ) ;
#68564=EDGE_LOOP ( 'NONE', ( #239455, #138357, #207371, #38408 ) ) ;
#68579=EDGE_CURVE ( 'NONE', #112587, #77509, #153322, .T. ) ;
#68583=DIRECTION ( 'NONE',  ( 1.000000000000000000, 0.000000000000000000, 0.000000000000000000 ) ) ;
#68649=CARTESIAN_POINT ( 'NONE',  ( -23.25000000000000000, 8.809961202382810441, -241.4517562488062481 ) ) ;
#68667=FACE_OUTER_BOUND ( 'NONE', #55846, .T. ) ;
#68684=VECTOR ( 'NONE', #255928, 1000.000000000000000 ) ;
#68699=CARTESIAN_POINT ( 'NONE',  ( 21.05000000000000071, -4.656943609564678788, -233.1535107627236414 ) ) ;
#68700=AXIS2_PLACEMENT_3D ( 'NONE', #157420, #182086, #221187 ) ;
#68738=CARTESIAN_POINT ( 'NONE',  ( -23.15000000000000213, 1.148907358139439339E-11, -201.0000000000015064 ) ) ;
#68755=EDGE_CURVE ( 'NONE', #235714, #115133, #145731, .T. ) ;
#68768=CARTESIAN_POINT ( 'NONE',  ( -20.94999999999999929, -4.871452838297996024, -233.3782557782877518 ) ) ;
#68775=CONICAL_SURFACE ( 'NONE', #72905, 4.049999999999995381, 0.7853981633974604915 ) ;
#68782=EDGE_CURVE ( 'NONE', #256147, #122770, #120642, .T. ) ;
#68796=CIRCLE ( 'NONE', #14654, 0.1000000000000057648 ) ;
#68798=DIRECTION ( 'NONE',  ( 0.000000000000000000, 0.2128009952263403282, -0.9770955615653358350 ) ) ;
#68824=VERTEX_POINT ( 'NONE', #223875 ) ;
#68895=ORIENTED_EDGE ( 'NONE', *, *, #97523, .T. ) ;
#68899=DIRECTION ( 'NONE',  ( 0.000000000000000000, 0.9770955615653551529, 0.2128009952262517601 ) ) ;
#68947=VERTEX_POINT ( 'NONE', #212053 ) ;
#68955=CARTESIAN_POINT ( 'NONE',  ( -20.05000000000000426, 13.53887499352833146, -219.6971619212644669 ) ) ;
#68998=DIRECTION ( 'NONE',  ( 0.000000000000000000, -0.2128009952263485993, 0.9770955615653341697 ) ) ;
#69001=LINE ( 'NONE', #205913, #28985 ) ;
#69002=CARTESIAN_POINT ( 'NONE',  ( 18.43466021071417060, -0.7397809587360789640, -242.2185760212437629 ) ) ;
#69030=EDGE_CURVE ( 'NONE', #200569, #51404, #213305, .T. ) ;
#69063=ORIENTED_EDGE ( 'NONE', *, *, #183324, .F. ) ;
#69072=DIRECTION ( 'NONE',  ( -1.000000000000000000, -2.885090398161910739E-16, -6.283419270304611573E-17 ) ) ;
#69077=EDGE_CURVE ( 'NONE', #68824, #95409, #78912, .T. ) ;
#69082=AXIS2_PLACEMENT_3D ( 'NONE', #251556, #127778, #9108 ) ;
#69097=VECTOR ( 'NONE', #206655, 1000.000000000000000 ) ;
#69101=VERTEX_POINT ( 'NONE', #176781 ) ;
#69119=CARTESIAN_POINT ( 'NONE',  ( 21.05000000000000071, 6.511710453938116316, -230.8991241839006534 ) ) ;
#69176=ORIENTED_EDGE ( 'NONE', *, *, #61959, .F. ) ;
#69256=EDGE_CURVE ( 'NONE', #226256, #219487, #205768, .T. ) ;
#69259=CARTESIAN_POINT ( 'NONE',  ( 22.47110162079220785, -2.450980137404201731, -189.6107711856424203 ) ) ;
#69305=ORIENTED_EDGE ( 'NONE', *, *, #104933, .T. ) ;
#69323=CARTESIAN_POINT ( 'NONE',  ( 20.95000000000000284, 16.98881331171930498, -224.4946931418895417 ) ) ;
#69351=CARTESIAN_POINT ( 'NONE',  ( -20.85000000000000142, 7.783179459866048866, -245.3643104511423303 ) ) ;
#69352=CYLINDRICAL_SURFACE ( 'NONE', #171005, 0.09999999999999691080 ) ;
#69357=VECTOR ( 'NONE', #226260, 1000.000000000000000 ) ;
#69372=ADVANCED_FACE ( 'NONE', ( #114880 ), #234829, .T. ) ;
#69381=AXIS2_PLACEMENT_3D ( 'NONE', #51199, #130765, #210319 ) ;
#69383=CARTESIAN_POINT ( 'NONE',  ( 21.07928932188134397, 6.162520550847347955, -199.5566553493351307 ) ) ;
#69396=ORIENTED_EDGE ( 'NONE', *, *, #138889, .F. ) ;
#69415=ORIENTED_EDGE ( 'NONE', *, *, #195964, .T. ) ;
#69446=CIRCLE ( 'NONE', #161019, 7.799999999999998046 ) ;
#69488=ORIENTED_EDGE ( 'NONE', *, *, #166570, .F. ) ;
#69507=DIRECTION ( 'NONE',  ( 1.000000000000000000, 0.000000000000000000, 0.000000000000000000 ) ) ;
#69537=ORIENTED_EDGE ( 'NONE', *, *, #177970, .F. ) ;
#69580=ORIENTED_EDGE ( 'NONE', *, *, #119522, .F. ) ;
#69599=CARTESIAN_POINT ( 'NONE',  ( -18.50000000000000000, 8.980461154494397746, -187.0187154576991304 ) ) ;
#69605=CARTESIAN_POINT ( 'NONE',  ( -21.22070241538126112, 6.300705718653867748, -199.5265356483836570 ) ) ;
#69617=CARTESIAN_POINT ( 'NONE',  ( -23.15000000000000213, 6.683038871553167226, -212.1840060551439819 ) ) ;
#69677=EDGE_CURVE ( 'NONE', #83539, #242544, #26215, .T. ) ;
#69692=ORIENTED_EDGE ( 'NONE', *, *, #64624, .T. ) ;
#69730=CARTESIAN_POINT ( 'NONE',  ( -18.50000000000000355, -7.631834139420990759, -210.1304494778855485 ) ) ;
#69741=DIRECTION ( 'NONE',  ( -1.000000000000000000, -2.885090398161910739E-16, -6.283419270304611573E-17 ) ) ;
#69760=ORIENTED_EDGE ( 'NONE', *, *, #121032, .T. ) ;
#69774=CIRCLE ( 'NONE', #215504, 0.1000000000000054040 ) ;
#69795=DIRECTION ( 'NONE',  ( -1.000000000000000000, 0.000000000000000000, 0.000000000000000000 ) ) ;
#69807=DIRECTION ( 'NONE',  ( 0.000000000000000000, 0.2128009952263604232, -0.9770955615653316162 ) ) ;
#69828=DIRECTION ( 'NONE',  ( 0.000000000000000000, -0.2128009952263602012, 0.9770955615653315052 ) ) ;
#69854=DIRECTION ( 'NONE',  ( 0.000000000000000000, -0.3427706569149636118, 0.9394191166662962944 ) ) ;
#69894=DIRECTION ( 'NONE',  ( 1.000000000000000000, 0.000000000000000000, 0.000000000000000000 ) ) ;
#69916=CARTESIAN_POINT ( 'NONE',  ( -18.50000000000000000, -0.5844187615853587703, -242.4893126442242703 ) ) ;
#69943=EDGE_CURVE ( 'NONE', #55595, #256235, #81820, .T. ) ;
#69994=LINE ( 'NONE', #89518, #114854 ) ;
#70004=AXIS2_PLACEMENT_3D ( 'NONE', #65386, #45824, #131778 ) ;
#70028=CIRCLE ( 'NONE', #136619, 0.09999999999999553690 ) ;
#70043=CIRCLE ( 'NONE', #94956, 0.09999999999999939493 ) ;
#70049=EDGE_LOOP ( 'NONE', ( #186143, #231127, #108246, #229429 ) ) ;
#70067=DIRECTION ( 'NONE',  ( 1.000000000000000000, 0.000000000000000000, 0.000000000000000000 ) ) ;
#70079=AXIS2_PLACEMENT_3D ( 'NONE', #218118, #198568, #99451 ) ;
#70107=EDGE_LOOP ( 'NONE', ( #17802, #197434, #117077, #88610 ) ) ;
#70119=DIRECTION ( 'NONE',  ( -1.000000000000000000, 0.000000000000000000, 0.000000000000000000 ) ) ;
#70198=CIRCLE ( 'NONE', #3508, 0.09999999999999939493 ) ;
#70201=CARTESIAN_POINT ( 'NONE',  ( 22.50000000000000000, -2.381330705637465961, -189.5959759702857923 ) ) ;
#70208=AXIS2_PLACEMENT_3D ( 'NONE', #99352, #78516, #1547 ) ;
#70238=CLOSED_SHELL ( 'NONE', ( #156038, #151986, #165286, #181173, #146567, #207141, #249737, #205129, #18393, #44650, #133858, #120687, #223274, #6449, #128237, #30548, #132912, #225481, #199328, #251166, #105409, #90641, #147609, #216265, #18409, #17482, #192662, #116996, #10778, #196810, #62403, #106446, #16128, #201043, #113839, #163083, #161744, #254672, #162233, #205281, #242621, #91417, #26779, #113582, #111580, #127960, #205772, #227763, #140719, #172187, #236461, #59799, #170825, #243974, #153698, #196579, #245799, #241565, #19371, #23255, #212151, #3662, #136327, #191387, #208938, #152479, #173711, #58190, #129451, #12907, #177928, #118972, #71449, #253888, #131366, #9865, #140709, #224927, #104081, #243341, #225738, #140622, #71109, #240405, #187385, #40796, #203202, #90873, #220736, #162076, #126135, #239465, #176225, #14445, #169993, #17552, #219992, #93244, #49901, #226583, #36319, #67331, #221472, #163281, #230359, #254607, #87071, #188957, #108193, #128620, #110308, #28749, #213422, #205385, #9438, #39809, #96174, #80471, #140876, #156329, #82434, #210405, #28583, #241645, #57259, #216479, #64113, #125527, #120207, #72999, #101243, #97025, #190102, #83958, #129697, #207316, #245022, #109985, #52330, #79855, #58180, #221057, #8076, #257676, #102523, #62659, #231135, #251882, #199868, #181607, #232372, #222181, #162131, #39959, #148593, #150214, #723, #37610, #165890, #109978, #215486, #142594, #105914, #169005, #140769, #193877, #165182, #81565, #58961, #49395, #185634, #178632, #188665, #220859, #11782, #72615, #60559, #25431, #42081, #117702, #212759, #89176, #175527, #247333, #256135, #67455, #245990, #218963, #100151, #121508, #91360, #215715, #190450, #102046, #80806, #127688, #119727, #199554, #1730, #36489, #62224, #13470, #111695, #12189, #236541, #90217, #247793, #9359, #114692, #103946, #199131, #226484, #41365, #6154, #84769, #169053, #87690, #65026, #120079, #240797, #186487, #87227, #31235, #182973, #168629, #96005, #931, #133012, #85615, #244815, #220009, #59356, #123072, #216318, #79889, #202435, #249432, #38096, #136429, #33912, #98722, #89208, #195214, #160506, #204508, #103026, #102403, #234356, #89417, #210163, #180895, #248202, #83738, #112719, #143124, #178962, #205746, #75569, #245451, #208831, #75444, #77561, #152142, #115003, #55591, #128217, #175903, #252383, #43983, #172380, #197018, #254688, #200389, #142712, #8674, #94029, #3009, #241790, #10245, #196793, #121018, #208080, #226909, #78302, #18102, #28568, #42535, #1572, #24061, #174012, #28563, #10877, #253470, #125097, #133275, #139995, #48519, #186563, #123860, #231152, #41745, #168119, #151789, #165499, #79172, #69372, #46915, #118317, #188310, #206747, #237929, #147128, #211542, #105023, #5477, #150560, #15204, #255558, #122162, #232861, #43113, #149571, #210523, #175100, #206671, #222796, #198429, #39262, #112868, #231015, #66970, #133228, #223131, #215980, #185027, #244029, #54972, #96299, #249509, #251307, #62011, #88497, #162105, #136233, #84808, #237779, #200684, #133456, #158047, #63798, #53413, #133854, #66526, #140066, #89660, #52134, #110244, #208461, #186593, #218767, #121445, #195674, #46438, #57492, #145845, #84008, #78179, #229672, #79036, #148754, #80899, #72417, #99409, #70534, #50121, #231661, #241013, #208269, #37120, #76359, #250561, #54446, #66825, #148092, #108452, #255947, #82684, #115628, #227992, #38258, #96190, #141692, #209556, #5638, #6081, #122112, #214565, #158480, #160784, #215383, #164492, #87923, #23694, #188899, #239224, #61209, #67231, #191276, #226732, #222364, #156149, #24318, #239898, #90190, #29694, #62118, #239918, #142235, #102811, #108812, #232910, #65876, #12901, #228208, #62045, #20515, #196655, #143696, #137067, #42648, #241644, #135258, #160098, #60910, #112611, #100813, #74549, #65348, #183445, #223860, #98614, #104690, #155015, #135009, #16457, #59139, #91971, #129482, #179861, #138032, #110862, #114493, #32102, #217089, #121943, #2742, #51556, #48195, #88127, #171155, #128298, #187810, #32018, #180009, #12167, #26673, #151350, #67159, #26238, #170925, #113540, #137183, #252828, #55245, #138360, #119977, #219783, #26375 ) ) ;
#70240=ORIENTED_EDGE ( 'NONE', *, *, #80755, .T. ) ;
#70245=LINE ( 'NONE', #113189, #244927 ) ;
#70250=DIRECTION ( 'NONE',  ( 1.000000000000000000, 0.000000000000000000, 0.000000000000000000 ) ) ;
#70276=DIRECTION ( 'NONE',  ( 1.000000000000000000, 0.000000000000000000, 0.000000000000000000 ) ) ;
#70286=DIRECTION ( 'NONE',  ( 1.000000000000000000, 0.000000000000000000, 0.000000000000000000 ) ) ;
#70301=ORIENTED_EDGE ( 'NONE', *, *, #21347, .T. ) ;
#70356=DIRECTION ( 'NONE',  ( 0.000000000000000000, -0.2128009952263601456, 0.9770955615653316162 ) ) ;
#70388=EDGE_CURVE ( 'NONE', #185684, #168941, #10521, .T. ) ;
#70393=ORIENTED_EDGE ( 'NONE', *, *, #54521, .T. ) ;
#70427=EDGE_LOOP ( 'NONE', ( #102076, #135568, #165334 ) ) ;
#70438=EDGE_CURVE ( 'NONE', #13347, #213820, #110452, .T. ) ;
#70443=EDGE_CURVE ( 'NONE', #126094, #44687, #256142, .T. ) ;
#70471=EDGE_CURVE ( 'NONE', #102565, #3257, #139666, .T. ) ;
#70485=EDGE_LOOP ( 'NONE', ( #2025, #9443, #115537, #40172 ) ) ;
#70497=FACE_OUTER_BOUND ( 'NONE', #243674, .T. ) ;
#70503=CARTESIAN_POINT ( 'NONE',  ( 23.14999999999999858, 10.71906255309368383, -222.4921384173655383 ) ) ;
#70514=VECTOR ( 'NONE', #107614, 1000.000000000000227 ) ;
#70533=CARTESIAN_POINT ( 'NONE',  ( -23.15000000000000213, 10.74948822439028895, -222.3968794097801549 ) ) ;
#70534=ADVANCED_FACE ( 'NONE', ( #209192 ), #211781, .F. ) ;
#70549=B_SPLINE_CURVE_WITH_KNOTS ( 'NONE', 3,
 ( #83663, #76649, #14143, #33732, #114501, #216155 ),
 .UNSPECIFIED., .F., .F.,
 ( 4, 2, 4 ),
 ( 0.000000000000000000, 0.0001895189928937408147, 0.0003790379857874816294 ),
 .UNSPECIFIED. ) ;
#70552=EDGE_LOOP ( 'NONE', ( #226646, #110523, #85493, #20118 ) ) ;
#70584=CARTESIAN_POINT ( 'NONE',  ( -20.94999999999999929, 12.80863705670245700, -205.3010250813005655 ) ) ;
#70585=AXIS2_PLACEMENT_3D ( 'NONE', #164106, #87110, #226621 ) ;
#70596=EDGE_CURVE ( 'NONE', #245608, #145681, #73269, .T. ) ;
#70616=ORIENTED_EDGE ( 'NONE', *, *, #233721, .T. ) ;
#70621=AXIS2_PLACEMENT_3D ( 'NONE', #130256, #113273, #230664 ) ;
#70700=DIRECTION ( 'NONE',  ( 0.000000000000000000, -0.2128009952263485993, 0.9770955615653341697 ) ) ;
#70702=CARTESIAN_POINT ( 'NONE',  ( 21.05000000000000071, 0.6736784609442970639, -212.7825231506076875 ) ) ;
#70740=VERTEX_POINT ( 'NONE', #142488 ) ;
#70745=AXIS2_PLACEMENT_3D ( 'NONE', #8580, #50247, #151963 ) ;
#70808=VERTEX_POINT ( 'NONE', #104621 ) ;
#70814=DIRECTION ( 'NONE',  ( -1.000000000000000000, -1.794895427898102820E-16, -3.909090864890033875E-17 ) ) ;
#70827=DIRECTION ( 'NONE',  ( 0.000000000000000000, 0.2128009952263485993, -0.9770955615653341697 ) ) ;
#70854=ORIENTED_EDGE ( 'NONE', *, *, #198946, .T. ) ;
#70879=CARTESIAN_POINT ( 'NONE',  ( 21.05000000000000071, 7.244009986534929446, -211.6437749090809177 ) ) ;
#70886=FACE_OUTER_BOUND ( 'NONE', #94640, .T. ) ;
#70897=EDGE_CURVE ( 'NONE', #123919, #169080, #64842, .T. ) ;
#70902=PLANE ( 'NONE',  #32627 ) ;
#70904=EDGE_CURVE ( 'NONE', #148979, #103023, #243917, .T. ) ;
#70913=EDGE_CURVE ( 'NONE', #31696, #179904, #228480, .T. ) ;
#70943=CARTESIAN_POINT ( 'NONE',  ( -22.39999999999999858, -2.500503813844232592, -189.5187041743089367 ) ) ;
#70976=CARTESIAN_POINT ( 'NONE',  ( -23.15000000000000213, 13.96869538424788360, -210.3925794786331949 ) ) ;
#70990=DIRECTION ( 'NONE',  ( 1.000000000000000000, 0.000000000000000000, 0.000000000000000000 ) ) ;
#71024=EDGE_LOOP ( 'NONE', ( #23995, #194880, #34976, #247472 ) ) ;
#71034=VERTEX_POINT ( 'NONE', #27288 ) ;
#71060=ORIENTED_EDGE ( 'NONE', *, *, #186283, .F. ) ;
#71067=CIRCLE ( 'NONE', #62858, 0.1000000000000054040 ) ;
#71069=CARTESIAN_POINT ( 'NONE',  ( 21.14999999999999503, -2.576749817950531707, -189.6385361693310756 ) ) ;
#71078=CARTESIAN_POINT ( 'NONE',  ( -20.85000000000000142, 14.80545736607782814, -235.9842437978701639 ) ) ;
#71084=ORIENTED_EDGE ( 'NONE', *, *, #74838, .F. ) ;
#71088=CARTESIAN_POINT ( 'NONE',  ( 23.25000000000000000, 9.028068219309963283, -211.6732836666006961 ) ) ;
#71109=ADVANCED_FACE ( 'NONE', ( #221571 ), #146962, .T. ) ;
#71142=DIRECTION ( 'NONE',  ( 1.000000000000000000, -7.136802563874199107E-16, -1.554319503706925307E-16 ) ) ;
#71168=EDGE_CURVE ( 'NONE', #141902, #156342, #194256, .T. ) ;
#71209=ORIENTED_EDGE ( 'NONE', *, *, #197435, .T. ) ;
#71217=AXIS2_PLACEMENT_3D ( 'NONE', #141057, #220592, #58907 ) ;
#71229=CARTESIAN_POINT ( 'NONE',  ( 20.95512828230154767, 11.26953735574613447, -211.0340866196924026 ) ) ;
#71269=CIRCLE ( 'NONE', #112754, 0.1000000000000054040 ) ;
#71274=CARTESIAN_POINT ( 'NONE',  ( 21.05000000000000071, 17.11694853917244075, -224.3781540347815451 ) ) ;
#71280=ORIENTED_EDGE ( 'NONE', *, *, #79484, .T. ) ;
#71291=AXIS2_PLACEMENT_3D ( 'NONE', #55581, #38629, #118165 ) ;
#71306=TOROIDAL_SURFACE ( 'NONE', #171107, 7.800000000000000711, 0.1000000000000000056 ) ;
#71340=ORIENTED_EDGE ( 'NONE', *, *, #234889, .F. ) ;
#71358=AXIS2_PLACEMENT_3D ( 'NONE', #23686, #26237, #221823 ) ;
#71382=ORIENTED_EDGE ( 'NONE', *, *, #142347, .T. ) ;
#71386=DIRECTION ( 'NONE',  ( -5.603264701231743991E-32, 0.2128009952263606175, -0.9770955615653316162 ) ) ;
#71389=ORIENTED_EDGE ( 'NONE', *, *, #108187, .F. ) ;
#71408=DIRECTION ( 'NONE',  ( -1.000000000000000000, -0.000000000000000000, -0.000000000000000000 ) ) ;
#71441=ORIENTED_EDGE ( 'NONE', *, *, #205150, .F. ) ;
#71449=ADVANCED_FACE ( 'NONE', ( #16478 ), #37320, .T. ) ;
#71453=CARTESIAN_POINT ( 'NONE',  ( 20.94999675878240808, 18.34775554461856828, -236.8759397601555179 ) ) ;
#71482=EDGE_CURVE ( 'NONE', #233023, #164661, #123481, .T. ) ;
#71504=CARTESIAN_POINT ( 'NONE',  ( -21.05000000000000071, -4.990442493977163885, -233.3018263216538628 ) ) ;
#71506=( BOUNDED_SURFACE ( )  B_SPLINE_SURFACE ( 3, 2, ( 
 ( #94205, #75943, #211606 ),
 ( #73404, #254540, #212887 ),
 ( #13409, #155512, #172526 ),
 ( #195905, #95495, #253278 ),
 ( #115066, #232468, #215443 ),
 ( #15994, #92919, #154241 ) ),
 .UNSPECIFIED., .F., .F., .F. ) 
 B_SPLINE_SURFACE_WITH_KNOTS ( ( 4, 2, 4 ),
 ( 3, 3 ),
 ( 0.0001792624049599645341, 0.0003686986002124761691, 0.0005581347954649877770 ),
 ( 0.000000000000000000, 1.000000000000000000 ),
 .UNSPECIFIED. ) 
 GEOMETRIC_REPRESENTATION_ITEM ( )  RATIONAL_B_SPLINE_SURFACE ( (
 ( 1.000000000000000000, 0.9238795325112807433, 1.000000000000000000),
 ( 1.000000000000000000, 0.9229318695232904268, 1.000000000000000000),
 ( 1.000000000000000000, 0.8926288119238101615, 1.000000000000000000),
 ( 1.000000000000000000, 0.8123777807263494743, 1.000000000000000000),
 ( 1.000000000000000000, 0.7629087100937503862, 1.000000000000000000),
 ( 1.000000000000000000, 0.7071067811865467956, 1.000000000000000000) ) ) 
 REPRESENTATION_ITEM ( '' )  SURFACE ( )  );
#71545=CARTESIAN_POINT ( 'NONE',  ( 20.04142135623730070, 16.02417409648693081, -219.3605785455116006 ) ) ;
#71551=CARTESIAN_POINT ( 'NONE',  ( 21.00000000000000000, 14.02742277431099538, -219.5907614236512870 ) ) ;
#71571=CARTESIAN_POINT ( 'NONE',  ( 18.39999999999999858, -0.9152171842606988683, -242.2974985173726452 ) ) ;
#71593=ORIENTED_EDGE ( 'NONE', *, *, #153902, .F. ) ;
#71611=FACE_OUTER_BOUND ( 'NONE', #180376, .T. ) ;
#71612=ORIENTED_EDGE ( 'NONE', *, *, #149677, .F. ) ;
#71615=EDGE_LOOP ( 'NONE', ( #28298, #227045, #250911, #48987, #112882, #207904, #74338, #89133, #213347, #31482, #176139, #92330, #24481, #253463, #71209, #44068 ) ) ;
#71628=AXIS2_PLACEMENT_3D ( 'NONE', #221034, #70990, #211765 ) ;
#71674=EDGE_LOOP ( 'NONE', ( #112542, #171555, #200699, #168832 ) ) ;
#71695=EDGE_CURVE ( 'NONE', #230675, #242544, #108820, .T. ) ;
#71710=PLANE ( 'NONE',  #178551 ) ;
#71711=EDGE_LOOP ( 'NONE', ( #3388, #96024, #74150, #161170 ) ) ;
#71718=DIRECTION ( 'NONE',  ( -1.000000000000000000, 0.000000000000000000, 0.000000000000000000 ) ) ;
#71725=CARTESIAN_POINT ( 'NONE',  ( -21.05000000000000782, -1.244299762474067705, -194.8241018385128314 ) ) ;
#71757=EDGE_CURVE ( 'NONE', #74028, #64043, #127959, .T. ) ;
#71804=EDGE_LOOP ( 'NONE', ( #145429, #207875, #256911, #173690 ) ) ;
#71831=EDGE_CURVE ( 'NONE', #257097, #232829, #215430, .T. ) ;
#71832=LINE ( 'NONE', #86209, #14529 ) ;
#71840=CARTESIAN_POINT ( 'NONE',  ( -21.14999999999999858, -1.391858308744747807, -194.6091531227727955 ) ) ;
#71852=ORIENTED_EDGE ( 'NONE', *, *, #211752, .F. ) ;
#71861=DIRECTION ( 'NONE',  ( 0.000000000000000000, 0.6728388485993177515, -0.7397890806274072251 ) ) ;
#71862=EDGE_LOOP ( 'NONE', ( #188718, #131825, #50612, #126405 ) ) ;
#71865=FACE_OUTER_BOUND ( 'NONE', #210375, .T. ) ;
#71869=LINE ( 'NONE', #151409, #144782 ) ;
#71891=CARTESIAN_POINT ( 'NONE',  ( 18.59999999999999076, 7.128833340094563376, -233.7327013124401276 ) ) ;
#71912=VERTEX_POINT ( 'NONE', #125525 ) ;
#71924=CARTESIAN_POINT ( 'NONE',  ( 21.14999999999999858, -1.391858308744748696, -194.6091531227727955 ) ) ;
#71929=CIRCLE ( 'NONE', #105172, 0.1999999999999987899 ) ;
#71983=AXIS2_PLACEMENT_3D ( 'NONE', #55905, #61060, #139299 ) ;
#71991=ORIENTED_EDGE ( 'NONE', *, *, #107357, .T. ) ;
#71993=DIRECTION ( 'NONE',  ( 0.000000000000000000, 0.9736512643735623085, 0.2280421351061316382 ) ) ;
#72019=DIRECTION ( 'NONE',  ( -0.7071067811865302533, 0.6909108974501196876, 0.1504730267679053324 ) ) ;
#72057=LINE ( 'NONE', #151608, #212148 ) ;
#72076=EDGE_CURVE ( 'NONE', #168569, #203210, #17155, .T. ) ;
#72079=AXIS2_PLACEMENT_3D ( 'NONE', #202358, #219348, #224479 ) ;
#72089=EDGE_CURVE ( 'NONE', #87043, #136449, #57520, .T. ) ;
#72104=EDGE_CURVE ( 'NONE', #190072, #51901, #44750, .T. ) ;
#72119=DIRECTION ( 'NONE',  ( 0.000000000000000000, 0.2128009952263604232, -0.9770955615653316162 ) ) ;
#72120=DIRECTION ( 'NONE',  ( -1.000000000000000000, -3.295974604355953674E-13, 0.000000000000000000 ) ) ;
#72129=EDGE_CURVE ( 'NONE', #173624, #72705, #223230, .T. ) ;
#72140=LINE ( 'NONE', #34311, #129674 ) ;
#72157=CARTESIAN_POINT ( 'NONE',  ( -18.59999999999999787, 11.62724406944293598, -220.3181830240302190 ) ) ;
#72193=EDGE_CURVE ( 'NONE', #127544, #74110, #252442, .T. ) ;
#72200=DIRECTION ( 'NONE',  ( -0.7071067811865474617, -0.6909108974501236844, -0.1504730267678055788 ) ) ;
#72208=CARTESIAN_POINT ( 'NONE',  ( -20.86777300164945004, 18.41441690808118281, -236.9991004306322964 ) ) ;
#72229=CARTESIAN_POINT ( 'NONE',  ( 20.94999999999999929, -4.656943609564680564, -233.1535107627236414 ) ) ;
#72243=FACE_OUTER_BOUND ( 'NONE', #113639, .T. ) ;
#72279=CARTESIAN_POINT ( 'NONE',  ( 18.39999999999999858, -0.8467571797981052750, -242.2246066262668194 ) ) ;
#72305=EDGE_CURVE ( 'NONE', #72705, #1104, #53112, .T. ) ;
#72327=DIRECTION ( 'NONE',  ( 0.000000000000000000, 0.9788861828082167094, 0.2044060691544132835 ) ) ;
#72349=CARTESIAN_POINT ( 'NONE',  ( -23.15000000000000213, 6.307392164054360428, -220.9841382799134522 ) ) ;
#72352=CIRCLE ( 'NONE', #43126, 0.1000000000000008937 ) ;
#72364=DIRECTION ( 'NONE',  ( 0.000000000000000000, 0.2128009952263485993, -0.9770955615653341697 ) ) ;
#72369=ORIENTED_EDGE ( 'NONE', *, *, #87040, .T. ) ;
#72417=ADVANCED_FACE ( 'NONE', ( #219824 ), #65201, .F. ) ;
#72449=LINE ( 'NONE', #148121, #34535 ) ;
#72457=DIRECTION ( 'NONE',  ( 0.000000000000000000, -0.2128009952263744675, 0.9770955615653283965 ) ) ;
#72491=AXIS2_PLACEMENT_3D ( 'NONE', #221933, #107139, #141153 ) ;
#72507=DIRECTION ( 'NONE',  ( -1.000000000000000000, 0.000000000000000000, 0.000000000000000000 ) ) ;
#72509=CARTESIAN_POINT ( 'NONE',  ( 21.05000000000000071, 11.16079915604378492, -211.0041093385139561 ) ) ;
#72514=VECTOR ( 'NONE', #92083, 1000.000000000000114 ) ;
#72543=ORIENTED_EDGE ( 'NONE', *, *, #209217, .F. ) ;
#72575=EDGE_CURVE ( 'NONE', #183349, #116714, #11043, .T. ) ;
#72576=EDGE_CURVE ( 'NONE', #202387, #175179, #48630, .T. ) ;
#72580=DIRECTION ( 'NONE',  ( 0.000000000000000000, -0.9770955615653291737, -0.2128009952263710536 ) ) ;
#72589=LINE ( 'NONE', #172997, #3341 ) ;
#72604=DIRECTION ( 'NONE',  ( 1.000000000000000000, 0.000000000000000000, 0.000000000000000000 ) ) ;
#72607=EDGE_LOOP ( 'NONE', ( #235326, #161901, #232381, #157702, #21292, #229433, #180593, #62430, #211410, #250564, #152268, #100186, #111103, #244382, #4986, #230974, #13336, #35678, #229741, #206561, #49285, #153285, #99192, #46247, #65915, #152231, #236707 ) ) ;
#72615=ADVANCED_FACE ( 'NONE', ( #182000 ), #42471, .T. ) ;
#72621=DIRECTION ( 'NONE',  ( -0.000000000000000000, -0.2128009952263604232, 0.9770955615653316162 ) ) ;
#72652=FACE_OUTER_BOUND ( 'NONE', #68564, .T. ) ;
#72667=CIRCLE ( 'NONE', #81004, 0.1000000000000073330 ) ;
#72688=EDGE_CURVE ( 'NONE', #30925, #162306, #227508, .T. ) ;
#72698=EDGE_CURVE ( 'NONE', #48752, #24784, #84113, .T. ) ;
#72705=VERTEX_POINT ( 'NONE', #204110 ) ;
#72706=DIRECTION ( 'NONE',  ( -1.000000000000000000, -0.000000000000000000, -0.000000000000000000 ) ) ;
#72712=CIRCLE ( 'NONE', #189393, 0.1000000000000055844 ) ;
#72724=CARTESIAN_POINT ( 'NONE',  ( 20.94999999999999929, 7.128833340094563376, -233.7327013124401276 ) ) ;
#72761=CARTESIAN_POINT ( 'NONE',  ( -21.05000000000000782, 6.100991474439140028, -199.6040273627268107 ) ) ;
#72767=AXIS2_PLACEMENT_3D ( 'NONE', #102117, #4318, #1748 ) ;
#72778=CARTESIAN_POINT ( 'NONE',  ( -20.94999999999999929, 0.6656436123793491033, -212.6810495496487476 ) ) ;
#72820=CARTESIAN_POINT ( 'NONE',  ( 21.05000000000000071, 1.148907358139439339E-11, -201.0000000000015064 ) ) ;
#72869=DIRECTION ( 'NONE',  ( 0.000000000000000000, 0.2128009952263485993, -0.9770955615653341697 ) ) ;
#72884=CARTESIAN_POINT ( 'NONE',  ( -22.59999999999999787, 11.36146383068193444, -198.4232501820394816 ) ) ;
#72886=ORIENTED_EDGE ( 'NONE', *, *, #29103, .T. ) ;
#72889=SPHERICAL_SURFACE ( 'NONE', #5070, 0.1000000000000000056 ) ;
#72898=EDGE_CURVE ( 'NONE', #225466, #17954, #11229, .T. ) ;
#72905=AXIS2_PLACEMENT_3D ( 'NONE', #143735, #230670, #170741 ) ;
#72908=DIRECTION ( 'NONE',  ( -3.265361837132813586E-16, 0.9770955615653357240, 0.2128009952263412996 ) ) ;
#72916=CARTESIAN_POINT ( 'NONE',  ( 21.14999999999999503, 1.148907358139439339E-11, -201.0000000000015064 ) ) ;
#72917=CIRCLE ( 'NONE', #218598, 12.87499999999999467 ) ;
#72922=CARTESIAN_POINT ( 'NONE',  ( -21.05000000000000071, 7.128833340094563376, -233.7327013124401276 ) ) ;
#72937=LINE ( 'NONE', #75495, #1603 ) ;
#72938=CARTESIAN_POINT ( 'NONE',  ( 20.85000000000000142, 7.675662554762638479, -241.7139905447625381 ) ) ;
#72973=VECTOR ( 'NONE', #226714, 1000.000000000000000 ) ;
#72981=CARTESIAN_POINT ( 'NONE',  ( -18.49999999999999645, -0.6211011429738022560, -242.4105644729049232 ) ) ;
#72997=CARTESIAN_POINT ( 'NONE',  ( -20.85000000000000142, 7.675662554762638479, -241.7139905447625381 ) ) ;
#72999=ADVANCED_FACE ( 'NONE', ( #220808 ), #81273, .F. ) ;
#73041=VERTEX_POINT ( 'NONE', #124294 ) ;
#73055=CIRCLE ( 'NONE', #210395, 0.1000000000000005468 ) ;
#73101=VECTOR ( 'NONE', #179849, 1000.000000000000000 ) ;
#73133=ORIENTED_EDGE ( 'NONE', *, *, #12419, .T. ) ;
#73193=ORIENTED_EDGE ( 'NONE', *, *, #202996, .T. ) ;
#73224=ORIENTED_EDGE ( 'NONE', *, *, #75333, .F. ) ;
#73230=CARTESIAN_POINT ( 'NONE',  ( 18.49999999999999289, 15.39038045630036855, -223.0585967715782090 ) ) ;
#73234=ORIENTED_EDGE ( 'NONE', *, *, #47098, .F. ) ;
#73267=CARTESIAN_POINT ( 'NONE',  ( -20.15000000000000568, 11.68541875934721297, -210.9921969175020706 ) ) ;
#73269=CIRCLE ( 'NONE', #173241, 11.80000000000000959 ) ;
#73353=ORIENTED_EDGE ( 'NONE', *, *, #38107, .F. ) ;
#73404=CARTESIAN_POINT ( 'NONE',  ( 21.07954763557415490, 6.170303673189042826, -199.5887535105479174 ) ) ;
#73418=CIRCLE ( 'NONE', #40284, 11.74999999999999289 ) ;
#73420=CYLINDRICAL_SURFACE ( 'NONE', #81969, 0.09999999999999939493 ) ;
#73426=FACE_OUTER_BOUND ( 'NONE', #128387, .T. ) ;
#73429=AXIS2_PLACEMENT_3D ( 'NONE', #138332, #13287, #137077 ) ;
#73444=DIRECTION ( 'NONE',  ( 1.000000000000000000, 0.000000000000000000, 0.000000000000000000 ) ) ;
#73447=CARTESIAN_POINT ( 'NONE',  ( 18.59999999999999076, 8.433899723187009201, -209.4150263691077782 ) ) ;
#73454=CARTESIAN_POINT ( 'NONE',  ( 18.41789779300693652, -7.785976411356864801, -209.8926135142695273 ) ) ;
#73470=AXIS2_PLACEMENT_3D ( 'NONE', #110826, #67851, #187826 ) ;
#73476=CARTESIAN_POINT ( 'NONE',  ( 21.53551880898956838, 6.608334920795639000, -199.4594853955832434 ) ) ;
#73480=EDGE_LOOP ( 'NONE', ( #32584, #109280, #192956 ) ) ;
#73482=EDGE_LOOP ( 'NONE', ( #252614, #111497, #229190, #118189, #174121, #109295, #129728 ) ) ;
#73523=CARTESIAN_POINT ( 'NONE',  ( -18.50000000000000000, 0.8650195716890449749, -212.6652626294507229 ) ) ;
#73525=EDGE_LOOP ( 'NONE', ( #62663, #215578, #83084, #28313 ) ) ;
#73532=CARTESIAN_POINT ( 'NONE',  ( 21.05000000000000071, 7.525330762710603416, -212.0571253909869256 ) ) ;
#73543=SPHERICAL_SURFACE ( 'NONE', #213889, 0.1000000000000000056 ) ;
#73546=DIRECTION ( 'NONE',  ( 1.000000000000000000, 0.000000000000000000, 0.000000000000000000 ) ) ;
#73571=DIRECTION ( 'NONE',  ( -1.000000000000000000, 0.000000000000000000, 0.000000000000000000 ) ) ;
#73594=ORIENTED_EDGE ( 'NONE', *, *, #129172, .F. ) ;
#73675=LINE ( 'NONE', #35822, #76549 ) ;
#73697=DIRECTION ( 'NONE',  ( 1.000000000000000000, 0.000000000000000000, 0.000000000000000000 ) ) ;
#73699=CARTESIAN_POINT ( 'NONE',  ( -18.50000000000000000, 11.50215294792677057, -198.5972978622482970 ) ) ;
#73728=DIRECTION ( 'NONE',  ( 0.000000000000000000, -0.2128009952263403282, 0.9770955615653358350 ) ) ;
#73746=ORIENTED_EDGE ( 'NONE', *, *, #224436, .F. ) ;
#73805=VECTOR ( 'NONE', #8435, 1000.000000000000227 ) ;
#73848=DIRECTION ( 'NONE',  ( 1.000000000000000000, 0.000000000000000000, 0.000000000000000000 ) ) ;
#73869=DIRECTION ( 'NONE',  ( 3.469446951953635015E-14, -0.2128009952263604232, 0.9770955615653316162 ) ) ;
#73886=ORIENTED_EDGE ( 'NONE', *, *, #9559, .T. ) ;
#73977=DIRECTION ( 'NONE',  ( -0.000000000000000000, -0.3427706569149635007, 0.9394191166662961834 ) ) ;
#74005=VECTOR ( 'NONE', #18822, 1000.000000000000000 ) ;
#74028=VERTEX_POINT ( 'NONE', #3069 ) ;
#74030=CIRCLE ( 'NONE', #28229, 0.1000000000000054040 ) ;
#74034=CARTESIAN_POINT ( 'NONE',  ( 20.84999999999998721, 18.41524492703432614, -237.0006385043383546 ) ) ;
#74040=FACE_OUTER_BOUND ( 'NONE', #79890, .T. ) ;
#74060=CARTESIAN_POINT ( 'NONE',  ( -20.94999999999999929, -4.735542975717121905, -233.2463119243910796 ) ) ;
#74077=DIRECTION ( 'NONE',  ( -1.000000000000000000, 0.000000000000000000, 0.000000000000000000 ) ) ;
#74094=ORIENTED_EDGE ( 'NONE', *, *, #232926, .F. ) ;
#74110=VERTEX_POINT ( 'NONE', #242977 ) ;
#74150=ORIENTED_EDGE ( 'NONE', *, *, #60307, .F. ) ;
#74160=EDGE_CURVE ( 'NONE', #192351, #5146, #74361, .T. ) ;
#74166=AXIS2_PLACEMENT_3D ( 'NONE', #105042, #144196, #243303 ) ;
#74188=CYLINDRICAL_SURFACE ( 'NONE', #121569, 4.000000000000006217 ) ;
#74193=DIRECTION ( 'NONE',  ( -3.469446951953738513E-14, 0.9770955615653543758, 0.2128009952262553683 ) ) ;
#74271=AXIS2_PLACEMENT_3D ( 'NONE', #181194, #24697, #27273 ) ;
#74283=DIRECTION ( 'NONE',  ( 1.000000000000000000, 0.000000000000000000, 0.000000000000000000 ) ) ;
#74287=ORIENTED_EDGE ( 'NONE', *, *, #128428, .F. ) ;
#74290=CARTESIAN_POINT ( 'NONE',  ( -22.39999999999999858, -1.560176095955062348, -193.3663837337744837 ) ) ;
#74303=EDGE_CURVE ( 'NONE', #232474, #96897, #116032, .T. ) ;
#74308=VERTEX_POINT ( 'NONE', #168191 ) ;
#74310=CARTESIAN_POINT ( 'NONE',  ( 18.49999999999999289, 7.474345188812916874, -187.3467314563696107 ) ) ;
#74317=TOROIDAL_SURFACE ( 'NONE', #157715, 0.4000000000000005773, 0.1000000000000000056 ) ;
#74322=EDGE_LOOP ( 'NONE', ( #212481, #209558, #75993, #196765 ) ) ;
#74338=ORIENTED_EDGE ( 'NONE', *, *, #177845, .F. ) ;
#74347=ORIENTED_EDGE ( 'NONE', *, *, #74570, .T. ) ;
#74361=CIRCLE ( 'NONE', #3563, 0.09999999999999939493 ) ;
#74377=CARTESIAN_POINT ( 'NONE',  ( 21.00000000000000000, 14.04870287383362992, -219.6884709798077893 ) ) ;
#74400=CARTESIAN_POINT ( 'NONE',  ( 22.49999999999999289, 11.45898712536580710, -198.4011321578509808 ) ) ;
#74402=ORIENTED_EDGE ( 'NONE', *, *, #188861, .T. ) ;
#74439=AXIS2_PLACEMENT_3D ( 'NONE', #204795, #183965, #26189 ) ;
#74466=ORIENTED_EDGE ( 'NONE', *, *, #240014, .F. ) ;
#74472=DIRECTION ( 'NONE',  ( -1.836970198721029934E-16, 0.9770955615653316162, 0.2128009952263604232 ) ) ;
#74481=LINE ( 'NONE', #154032, #56066 ) ;
#74531=VERTEX_POINT ( 'NONE', #83705 ) ;
#74535=CARTESIAN_POINT ( 'NONE',  ( 20.95575313997065336, 11.99325116692322268, -206.1879418114507985 ) ) ;
#74549=ADVANCED_FACE ( 'NONE', ( #88857 ), #31210, .F. ) ;
#74556=ORIENTED_EDGE ( 'NONE', *, *, #218245, .T. ) ;
#74570=EDGE_CURVE ( 'NONE', #227863, #166449, #65460, .T. ) ;
#74571=VERTEX_POINT ( 'NONE', #87578 ) ;
#74579=DIRECTION ( 'NONE',  ( -0.000000000000000000, -0.9316174814283004757, -0.3634403228828502752 ) ) ;
#74583=ORIENTED_EDGE ( 'NONE', *, *, #225704, .T. ) ;
#74585=CARTESIAN_POINT ( 'NONE',  ( -18.50000000000000000, 14.06640494040441247, -210.3712993791105532 ) ) ;
#74671=CARTESIAN_POINT ( 'NONE',  ( -21.05000000000000071, 4.617781596423511381, -222.2029736859691980 ) ) ;
#74699=DIRECTION ( 'NONE',  ( 1.000000000000000000, -0.000000000000000000, -0.000000000000000000 ) ) ;
#74737=DIRECTION ( 'NONE',  ( -0.000000000000000000, -0.9770955615653316162, -0.2128009952263604232 ) ) ;
#74793=VECTOR ( 'NONE', #11758, 1000.000000000000227 ) ;
#74824=DIRECTION ( 'NONE',  ( 0.000000000000000000, 0.2128009952263601456, -0.9770955615653316162 ) ) ;
#74827=DIRECTION ( 'NONE',  ( 1.000000000000000000, 7.136802563874199107E-16, 1.554319503706929991E-16 ) ) ;
#74837=DIRECTION ( 'NONE',  ( 0.7071067811865474617, 0.6909108974501236844, 0.1504730267678055788 ) ) ;
#74838=EDGE_CURVE ( 'NONE', #102935, #200910, #141312, .T. ) ;
#74888=ORIENTED_EDGE ( 'NONE', *, *, #68529, .T. ) ;
#74919=( BOUNDED_CURVE ( )  B_SPLINE_CURVE ( 3, ( #126584, #209983, #206121, #151301 ),
 .UNSPECIFIED., .F., .T. ) 
 B_SPLINE_CURVE_WITH_KNOTS ( ( 4, 4 ),
 ( 1.570796326794899223, 3.141592653589871276 ),
 .UNSPECIFIED. ) 
 CURVE ( )  GEOMETRIC_REPRESENTATION_ITEM ( )  RATIONAL_B_SPLINE_CURVE ( ( 1.000000000000000000, 0.8047378541243471739, 0.8047378541243471739, 1.000000000000000000 ) ) 
 REPRESENTATION_ITEM ( '' )  );
#74926=EDGE_CURVE ( 'NONE', #98560, #222722, #166295, .T. ) ;
#74947=CARTESIAN_POINT ( 'NONE',  ( -21.05000000000000071, -10.58757034444203704, -206.3761839813444396 ) ) ;
#74950=AXIS2_PLACEMENT_3D ( 'NONE', #142410, #22493, #202393 ) ;
#74959=DIRECTION ( 'NONE',  ( 1.000000000000000000, 0.000000000000000000, 0.000000000000000000 ) ) ;
#74962=FACE_OUTER_BOUND ( 'NONE', #33495, .T. ) ;
#74971=AXIS2_PLACEMENT_3D ( 'NONE', #224858, #42383, #67085 ) ;
#74999=EDGE_CURVE ( 'NONE', #52494, #28807, #8059, .T. ) ;
#75000=CARTESIAN_POINT ( 'NONE',  ( -23.25000000000000000, 2.718532714028242925, -213.4823957989985956 ) ) ;
#75022=EDGE_CURVE ( 'NONE', #235545, #18136, #99585, .T. ) ;
#75037=CARTESIAN_POINT ( 'NONE',  ( 18.49999999999999289, 14.51805813080544638, -219.6885945441820809 ) ) ;
#75045=CARTESIAN_POINT ( 'NONE',  ( -23.24999999999999645, -0.8467571797981052750, -242.2246066262668194 ) ) ;
#75051=VERTEX_POINT ( 'NONE', #229383 ) ;
#75053=LINE ( 'NONE', #57998, #151697 ) ;
#75077=EDGE_CURVE ( 'NONE', #20649, #136330, #57902, .T. ) ;
#75078=LINE ( 'NONE', #33390, #42251 ) ;
#75111=FACE_OUTER_BOUND ( 'NONE', #80345, .T. ) ;
#75163=VERTEX_POINT ( 'NONE', #57121 ) ;
#75177=DIRECTION ( 'NONE',  ( 1.000000000000000000, 0.000000000000000000, 0.000000000000000000 ) ) ;
#75181=CARTESIAN_POINT ( 'NONE',  ( 23.14999999999999503, 17.04051908253854108, -224.4971436904607174 ) ) ;
#75202=CIRCLE ( 'NONE', #220911, 0.1000000000000089151 ) ;
#75207=PLANE ( 'NONE',  #215821 ) ;
#75221=CIRCLE ( 'NONE', #54528, 11.75000000000000355 ) ;
#75248=DIRECTION ( 'NONE',  ( 1.000000000000000000, 0.000000000000000000, 0.000000000000000000 ) ) ;
#75263=DIRECTION ( 'NONE',  ( 0.000000000000000000, 0.2128009952263485993, -0.9770955615653341697 ) ) ;
#75270=TOROIDAL_SURFACE ( 'NONE', #12730, 11.70000000000000462, 0.1000000000000000056 ) ;
#75290=DIRECTION ( 'NONE',  ( 0.000000000000000000, 0.2128009952263485993, -0.9770955615653341697 ) ) ;
#75292=CARTESIAN_POINT ( 'NONE',  ( -20.54999999999999716, 7.128833340094563376, -233.7327013124401276 ) ) ;
#75315=PLANE ( 'NONE',  #161664 ) ;
#75333=EDGE_CURVE ( 'NONE', #230954, #224326, #196038, .T. ) ;
#75335=AXIS2_PLACEMENT_3D ( 'NONE', #98071, #35602, #197203 ) ;
#75343=LINE ( 'NONE', #19186, #94089 ) ;
#75365=ORIENTED_EDGE ( 'NONE', *, *, #48407, .F. ) ;
#75367=CARTESIAN_POINT ( 'NONE',  ( 21.13507111622890022, 13.07883613358315245, -210.6878745673258493 ) ) ;
#75370=CARTESIAN_POINT ( 'NONE',  ( -21.00250684356853270, 12.97363049731598039, -205.3537238879905544 ) ) ;
#75379=CARTESIAN_POINT ( 'NONE',  ( 20.94999999999999574, 0.3813505302108621264, -209.0906591966561336 ) ) ;
#75381=CARTESIAN_POINT ( 'NONE',  ( -20.99142135623731065, 16.98881331171929787, -224.4946931418895701 ) ) ;
#75444=ADVANCED_FACE ( 'NONE', ( #28327 ), #20716, .F. ) ;
#75456=CARTESIAN_POINT ( 'NONE',  ( -23.15000000000000213, -7.176961358819843539, -212.6889627706600834 ) ) ;
#75478=CARTESIAN_POINT ( 'NONE',  ( -22.57848426163148048, -2.504590758878124213, -189.5199776337204867 ) ) ;
#75495=CARTESIAN_POINT ( 'NONE',  ( -21.05000000000000071, 0.2428138352382497867, -200.9114032742886309 ) ) ;
#75513=EDGE_CURVE ( 'NONE', #102386, #102873, #187494, .T. ) ;
#75532=EDGE_CURVE ( 'NONE', #138363, #247713, #20911, .T. ) ;
#75551=DIRECTION ( 'NONE',  ( 0.000000000000000000, 0.2128009952263403282, -0.9770955615653358350 ) ) ;
#75569=ADVANCED_FACE ( 'NONE', ( #39563 ), #83389, .T. ) ;
#75573=AXIS2_PLACEMENT_3D ( 'NONE', #27368, #224228, #28663 ) ;
#75579=FACE_OUTER_BOUND ( 'NONE', #179384, .T. ) ;
#75595=VERTEX_POINT ( 'NONE', #216865 ) ;
#75601=DIRECTION ( 'NONE',  ( 1.000000000000000000, 0.000000000000000000, 0.000000000000000000 ) ) ;
#75606=ORIENTED_EDGE ( 'NONE', *, *, #58330, .T. ) ;
#75618=VERTEX_POINT ( 'NONE', #247989 ) ;
#75640=VERTEX_POINT ( 'NONE', #208871 ) ;
#75641=CARTESIAN_POINT ( 'NONE',  ( -20.64999999999999858, 6.759468328187065111, -212.0650163994647812 ) ) ;
#75655=DIRECTION ( 'NONE',  ( 0.000000000000000000, 0.9770955615653316162, 0.2128009952263604232 ) ) ;
#75666=FACE_OUTER_BOUND ( 'NONE', #84820, .T. ) ;
#75694=CARTESIAN_POINT ( 'NONE',  ( -20.94999999999999929, 12.97363049771892207, -205.3537238898406940 ) ) ;
#75752=DIRECTION ( 'NONE',  ( 1.000000000000000000, 0.000000000000000000, 0.000000000000000000 ) ) ;
#75760=ORIENTED_EDGE ( 'NONE', *, *, #86508, .T. ) ;
#75762=DIRECTION ( 'NONE',  ( 0.000000000000000000, 0.2128009952263601179, -0.9770955615653315052 ) ) ;
#75777=ORIENTED_EDGE ( 'NONE', *, *, #248648, .T. ) ;
#75780=CARTESIAN_POINT ( 'NONE',  ( 20.95566103547454517, 11.99910583982818224, -206.1974635114572720 ) ) ;
#75783=CARTESIAN_POINT ( 'NONE',  ( -23.15000000000000213, 17.95002310328549200, -228.2032933776778520 ) ) ;
#75788=CARTESIAN_POINT ( 'NONE',  ( 18.59999999999999432, 0.8650195716890449749, -212.6652626294507229 ) ) ;
#75798=FACE_OUTER_BOUND ( 'NONE', #201355, .T. ) ;
#75828=DIRECTION ( 'NONE',  ( 0.000000000000000000, 0.9770955615653313941, 0.2128009952263606730 ) ) ;
#75830=EDGE_LOOP ( 'NONE', ( #189290, #73594, #246992, #84380 ) ) ;
#75844=ORIENTED_EDGE ( 'NONE', *, *, #90028, .F. ) ;
#75850=EDGE_CURVE ( 'NONE', #142529, #183742, #233469, .T. ) ;
#75868=DIRECTION ( 'NONE',  ( -0.000000000000000000, -0.3427706569149635007, 0.9394191166662961834 ) ) ;
#75873=EDGE_LOOP ( 'NONE', ( #178723, #152473, #44167, #132592, #79264 ) ) ;
#75885=CARTESIAN_POINT ( 'NONE',  ( -20.64999999999999858, 7.128833340094563376, -233.7327013124401276 ) ) ;
#75930=SURFACE_STYLE_FILL_AREA ( #115054 ) ;
#75933=VECTOR ( 'NONE', #196247, 1000.000000000000000 ) ;
#75935=AXIS2_PLACEMENT_3D ( 'NONE', #139390, #3753, #200681 ) ;
#75943=CARTESIAN_POINT ( 'NONE',  ( 21.05000000000000071, 6.134002965564945065, -199.5633345488327848 ) ) ;
#75958=CARTESIAN_POINT ( 'NONE',  ( 21.05000000000000071, 7.128833340094563376, -233.7327013124401276 ) ) ;
#75980=CARTESIAN_POINT ( 'NONE',  ( -20.64999999999999858, 7.554435330547284444, -235.6868924355707691 ) ) ;
#75992=CARTESIAN_POINT ( 'NONE',  ( 18.43473516226064746, -7.778091709709652690, -209.9050494981294435 ) ) ;
#75993=ORIENTED_EDGE ( 'NONE', *, *, #129772, .F. ) ;
#76022=CARTESIAN_POINT ( 'NONE',  ( 20.85000000000000142, 7.783179459866048866, -245.3643104511423303 ) ) ;
#76074=DIRECTION ( 'NONE',  ( 3.265361837132812600E-16, -0.9770955615653313941, -0.2128009952263603677 ) ) ;
#76080=VERTEX_POINT ( 'NONE', #108191 ) ;
#76109=DIRECTION ( 'NONE',  ( -1.000000000000000000, -0.000000000000000000, -0.000000000000000000 ) ) ;
#76139=EDGE_LOOP ( 'NONE', ( #246300, #164853 ) ) ;
#76150=LINE ( 'NONE', #166004, #227180 ) ;
#76166=ORIENTED_EDGE ( 'NONE', *, *, #16749, .F. ) ;
#76189=DIRECTION ( 'NONE',  ( 1.000000000000000000, 0.000000000000000000, 0.000000000000000000 ) ) ;
#76287=CARTESIAN_POINT ( 'NONE',  ( 22.47071067811864964, -1.546016791165053306, -193.4356622592197255 ) ) ;
#76289=CARTESIAN_POINT ( 'NONE',  ( 18.41416235934318735, -0.7490476236415684053, -242.2033265267442061 ) ) ;
#76292=CARTESIAN_POINT ( 'NONE',  ( 20.11144452913633884, 11.38514937259154713, -206.5956884379970688 ) ) ;
#76305=DIRECTION ( 'NONE',  ( 1.000000000000000000, -0.000000000000000000, -0.000000000000000000 ) ) ;
#76312=CIRCLE ( 'NONE', #35245, 0.1000000000000065004 ) ;
#76336=CARTESIAN_POINT ( 'NONE',  ( -21.05000000000000071, -4.756823075239758225, -233.1486023682345490 ) ) ;
#76339=FACE_OUTER_BOUND ( 'NONE', #70049, .T. ) ;
#76355=ORIENTED_EDGE ( 'NONE', *, *, #51216, .F. ) ;
#76359=ADVANCED_FACE ( 'NONE', ( #203113 ), #42760, .F. ) ;
#76382=CARTESIAN_POINT ( 'NONE',  ( -20.85000000000000142, 7.675662554762638479, -241.7139905447625381 ) ) ;
#76395=EDGE_CURVE ( 'NONE', #174683, #237270, #171341, .T. ) ;
#76414=VECTOR ( 'NONE', #113344, 1000.000000000000114 ) ;
#76433=VECTOR ( 'NONE', #210013, 1000.000000000000000 ) ;
#76438=CARTESIAN_POINT ( 'NONE',  ( -23.25000000000000000, 6.857177884343597540, -212.0437362999421680 ) ) ;
#76467=DIRECTION ( 'NONE',  ( 0.000000000000000000, -0.9770955615652943127, -0.2128009952265311755 ) ) ;
#76510=AXIS2_PLACEMENT_3D ( 'NONE', #122060, #97316, #118205 ) ;
#76517=DIRECTION ( 'NONE',  ( 1.000000000000000000, 0.000000000000000000, 0.000000000000000000 ) ) ;
#76533=FACE_OUTER_BOUND ( 'NONE', #32418, .T. ) ;
#76549=VECTOR ( 'NONE', #74959, 1000.000000000000000 ) ;
#76560=AXIS2_PLACEMENT_3D ( 'NONE', #63059, #26531, #22689 ) ;
#76581=CARTESIAN_POINT ( 'NONE',  ( 20.94999999999999574, 4.287142817744433287, -211.9955491415249469 ) ) ;
#76595=AXIS2_PLACEMENT_3D ( 'NONE', #204616, #125113, #122544 ) ;
#76600=VECTOR ( 'NONE', #56103, 1000.000000000000000 ) ;
#76605=CARTESIAN_POINT ( 'NONE',  ( -20.15000000000000568, 13.60062771638445511, -219.7860569715900567 ) ) ;
#76608=AXIS2_PLACEMENT_3D ( 'NONE', #9905, #108997, #125998 ) ;
#76610=TOROIDAL_SURFACE ( 'NONE', #209907, 11.65000000000000036, 0.1000000000000000056 ) ;
#76649=CARTESIAN_POINT ( 'NONE',  ( 21.05000000000000071, 6.349993537836307489, -199.7193832479148625 ) ) ;
#76685=EDGE_LOOP ( 'NONE', ( #198577, #78908, #103993, #2088 ) ) ;
#76718=VECTOR ( 'NONE', #223181, 999.9999999999998863 ) ;
#76729=VERTEX_POINT ( 'NONE', #180688 ) ;
#76754=DIRECTION ( 'NONE',  ( 0.000000000000000000, -0.9770955615653317272, -0.2128009952263598126 ) ) ;
#76830=ORIENTED_EDGE ( 'NONE', *, *, #250758, .T. ) ;
#76866=CARTESIAN_POINT ( 'NONE',  ( -18.50000000000000000, 11.56851667937982775, -211.1200010790121553 ) ) ;
#76868=LINE ( 'NONE', #58579, #73101 ) ;
#76917=CARTESIAN_POINT ( 'NONE',  ( 22.49544290803765634, 11.46684760846049578, -198.4357998940971868 ) ) ;
#76937=CARTESIAN_POINT ( 'NONE',  ( 21.14999999999999858, 13.07482039728799528, -210.6896000549707537 ) ) ;
#76965=AXIS2_PLACEMENT_3D ( 'NONE', #1486, #178893, #160604 ) ;
#76968=EDGE_CURVE ( 'NONE', #119503, #156593, #162706, .T. ) ;
#77016=DIRECTION ( 'NONE',  ( 1.000000000000000000, 0.000000000000000000, 0.000000000000000000 ) ) ;
#77053=CYLINDRICAL_SURFACE ( 'NONE', #91010, 2.000000000000003109 ) ;
#77062=EDGE_CURVE ( 'NONE', #27420, #59785, #218192, .T. ) ;
#77072=EDGE_LOOP ( 'NONE', ( #160841, #34824, #221701, #157418 ) ) ;
#77075=DIRECTION ( 'NONE',  ( -1.000000000000000000, 0.000000000000000000, 0.000000000000000000 ) ) ;
#77083=AXIS2_PLACEMENT_3D ( 'NONE', #14234, #212426, #235813 ) ;
#77091=EDGE_LOOP ( 'NONE', ( #186607, #91085, #58791, #65275 ) ) ;
#77101=CARTESIAN_POINT ( 'NONE',  ( 18.59999999999999787, 4.324939842317335525, -212.0862480289983409 ) ) ;
#77110=ORIENTED_EDGE ( 'NONE', *, *, #227664, .F. ) ;
#77195=EDGE_CURVE ( 'NONE', #200910, #143844, #189, .T. ) ;
#77196=FACE_OUTER_BOUND ( 'NONE', #186858, .T. ) ;
#77209=DIRECTION ( 'NONE',  ( 0.000000000000000000, -0.2128009952257606530, 0.9770955615654620674 ) ) ;
#77214=DIRECTION ( 'NONE',  ( 0.000000000000000000, -0.9987946567507778317, 0.04908394489133698774 ) ) ;
#77275=EDGE_CURVE ( 'NONE', #227551, #150544, #237640, .T. ) ;
#77276=AXIS2_PLACEMENT_3D ( 'NONE', #190570, #182558, #43036 ) ;
#77284=DIRECTION ( 'NONE',  ( 0.000000000000000000, -0.2128009952263603677, 0.9770955615653313941 ) ) ;
#77287=ORIENTED_EDGE ( 'NONE', *, *, #63896, .T. ) ;
#77301=DIRECTION ( 'NONE',  ( 0.000000000000000000, 0.9770955615653551529, 0.2128009952262517601 ) ) ;
#77310=ORIENTED_EDGE ( 'NONE', *, *, #99495, .T. ) ;
#77318=EDGE_CURVE ( 'NONE', #212023, #19725, #21264, .T. ) ;
#77319=B_SPLINE_CURVE_WITH_KNOTS ( 'NONE', 3,
 ( #249055, #89952, #232058, #53402, #67825, #147369 ),
 .UNSPECIFIED., .F., .F.,
 ( 4, 2, 4 ),
 ( 0.000000000000000000, 0.0001496588209255951573, 0.0002993176418511903146 ),
 .UNSPECIFIED. ) ;
#77324=EDGE_CURVE ( 'NONE', #225466, #286, #216853, .T. ) ;
#77326=LINE ( 'NONE', #154362, #145874 ) ;
#77394=ORIENTED_EDGE ( 'NONE', *, *, #245685, .T. ) ;
#77395=DIRECTION ( 'NONE',  ( 2.952720810173289112E-16, -0.9770955615653302839, -0.2128009952263658355 ) ) ;
#77410=AXIS2_PLACEMENT_3D ( 'NONE', #212066, #133789, #37284 ) ;
#77443=AXIS2_PLACEMENT_3D ( 'NONE', #149304, #31926, #9760 ) ;
#77466=ORIENTED_EDGE ( 'NONE', *, *, #126321, .T. ) ;
#77477=VERTEX_POINT ( 'NONE', #119798 ) ;
#77478=CIRCLE ( 'NONE', #227527, 11.89999999999999858 ) ;
#77509=VERTEX_POINT ( 'NONE', #57205 ) ;
#77511=DIRECTION ( 'NONE',  ( -0.000000000000000000, 0.2128009952263604232, -0.9770955615653316162 ) ) ;
#77542=CARTESIAN_POINT ( 'NONE',  ( -20.64999999999999858, 11.60596396992030144, -220.2204734678737168 ) ) ;
#77561=ADVANCED_FACE ( 'NONE', ( #243568 ), #4923, .T. ) ;
#77576=EDGE_CURVE ( 'NONE', #50999, #13347, #242273, .T. ) ;
#77581=VERTEX_POINT ( 'NONE', #85739 ) ;
#77603=EDGE_LOOP ( 'NONE', ( #126513, #143157, #100374, #204002 ) ) ;
#77607=AXIS2_PLACEMENT_3D ( 'NONE', #209783, #46207, #25391 ) ;
#77614=AXIS2_PLACEMENT_3D ( 'NONE', #179353, #141485, #223573 ) ;
#77615=CARTESIAN_POINT ( 'NONE',  ( -22.49533356619861735, 11.36930514850286222, -198.4572374200818672 ) ) ;
#77622=EDGE_LOOP ( 'NONE', ( #234273, #104034 ) ) ;
#77712=CARTESIAN_POINT ( 'NONE',  ( 20.94999999999999929, 10.39655183198267707, -207.4949966697317620 ) ) ;
#77716=AXIS2_PLACEMENT_3D ( 'NONE', #148760, #208739, #5352 ) ;
#77725=FACE_OUTER_BOUND ( 'NONE', #54701, .T. ) ;
#77739=ORIENTED_EDGE ( 'NONE', *, *, #133370, .F. ) ;
#77761=FACE_OUTER_BOUND ( 'NONE', #113116, .T. ) ;
#77784=CARTESIAN_POINT ( 'NONE',  ( -18.59999999999999787, -7.567701079425722455, -210.0537230116848662 ) ) ;
#77789=LINE ( 'NONE', #157383, #38790 ) ;
#77824=EDGE_LOOP ( 'NONE', ( #30469, #110810, #77110, #117977 ) ) ;
#77827=CYLINDRICAL_SURFACE ( 'NONE', #68700, 12.87499999999999467 ) ;
#77829=ORIENTED_EDGE ( 'NONE', *, *, #237762, .F. ) ;
#77867=AXIS2_PLACEMENT_3D ( 'NONE', #226618, #224053, #8874 ) ;
#77885=CIRCLE ( 'NONE', #82153, 0.1999999999999987899 ) ;
#77910=TOROIDAL_SURFACE ( 'NONE', #77716, 11.65000000000000036, 0.1000000000000000056 ) ;
#77915=FACE_OUTER_BOUND ( 'NONE', #220858, .T. ) ;
#77957=CARTESIAN_POINT ( 'NONE',  ( -23.25000000000000000, 15.92646454033039660, -219.3818586450342423 ) ) ;
#78005=DIRECTION ( 'NONE',  ( 1.000000000000000000, 0.000000000000000000, 0.000000000000000000 ) ) ;
#78075=ORIENTED_EDGE ( 'NONE', *, *, #130394, .F. ) ;
#78077=DIRECTION ( 'NONE',  ( -0.000000000000000000, 0.9770955615653313941, 0.2128009952263603954 ) ) ;
#78088=ORIENTED_EDGE ( 'NONE', *, *, #121032, .F. ) ;
#78090=DIRECTION ( 'NONE',  ( 0.000000000000000000, -0.2128009952263603677, 0.9770955615653313941 ) ) ;
#78108=LINE ( 'NONE', #98936, #231330 ) ;
#78122=CARTESIAN_POINT ( 'NONE',  ( 21.14999999999999503, -10.76604040606816959, -206.3127087229280789 ) ) ;
#78131=ORIENTED_EDGE ( 'NONE', *, *, #1005, .F. ) ;
#78179=ADVANCED_FACE ( 'NONE', ( #216966 ), #43493, .T. ) ;
#78186=ORIENTED_EDGE ( 'NONE', *, *, #175307, .T. ) ;
#78222=CARTESIAN_POINT ( 'NONE',  ( -20.94999999999999929, -5.011722593499800205, -233.2041167654973322 ) ) ;
#78278=ORIENTED_EDGE ( 'NONE', *, *, #109540, .T. ) ;
#78302=ADVANCED_FACE ( 'NONE', ( #68189 ), #105418, .T. ) ;
#78327=ORIENTED_EDGE ( 'NONE', *, *, #189791, .F. ) ;
#78349=CARTESIAN_POINT ( 'NONE',  ( 21.14999999999999503, -13.88357498613435048, -191.9982587459959689 ) ) ;
#78390=ORIENTED_EDGE ( 'NONE', *, *, #225914, .T. ) ;
#78395=AXIS2_PLACEMENT_3D ( 'NONE', #222437, #123376, #84178 ) ;
#78415=DIRECTION ( 'NONE',  ( 0.000000000000000000, 0.2128009952263603954, -0.9770955615653315052 ) ) ;
#78448=ORIENTED_EDGE ( 'NONE', *, *, #132687, .F. ) ;
#78468=VECTOR ( 'NONE', #35879, 1000.000000000000000 ) ;
#78512=CARTESIAN_POINT ( 'NONE',  ( 21.05000000000000071, 8.575267064043504917, -199.1323982654951976 ) ) ;
#78516=DIRECTION ( 'NONE',  ( -6.938893903907222856E-15, 0.9770955615653315052, 0.2128009952263607008 ) ) ;
#78551=VERTEX_POINT ( 'NONE', #238822 ) ;
#78552=CARTESIAN_POINT ( 'NONE',  ( -23.15000000000000213, -4.735542975717121905, -233.2463119243910796 ) ) ;
#78559=DIRECTION ( 'NONE',  ( 1.000000000000000000, -7.136802563874199107E-16, -1.554319503706929991E-16 ) ) ;
#78576=EDGE_LOOP ( 'NONE', ( #105955, #169772, #155908, #257469 ) ) ;
#78583=CARTESIAN_POINT ( 'NONE',  ( 23.15000000000000213, -8.895340756380869962, -215.3721227669300049 ) ) ;
#78585=EDGE_LOOP ( 'NONE', ( #195060, #45851, #45870, #106946, #187508 ) ) ;
#78605=VECTOR ( 'NONE', #21309, 1000.000000000000114 ) ;
#78614=FACE_OUTER_BOUND ( 'NONE', #205888, .T. ) ;
#78615=DIRECTION ( 'NONE',  ( 1.000000000000000000, -0.000000000000000000, -0.000000000000000000 ) ) ;
#78617=FACE_OUTER_BOUND ( 'NONE', #14479, .T. ) ;
#78619=CARTESIAN_POINT ( 'NONE',  ( -18.59999999999999787, 7.783179459866048866, -245.3643104511423303 ) ) ;
#78621=DIRECTION ( 'NONE',  ( 0.000000000000000000, -0.9770955615652966442, -0.2128009952265203508 ) ) ;
#78624=FACE_OUTER_BOUND ( 'NONE', #14730, .T. ) ;
#78672=CARTESIAN_POINT ( 'NONE',  ( 22.39999999999999503, -1.560176095955058129, -193.3663837337745122 ) ) ;
#78676=ORIENTED_EDGE ( 'NONE', *, *, #125494, .T. ) ;
#78695=AXIS2_PLACEMENT_3D ( 'NONE', #228931, #30751, #93254 ) ;
#78705=CIRCLE ( 'NONE', #12125, 0.5000000000000007772 ) ;
#78747=AXIS2_PLACEMENT_3D ( 'NONE', #191746, #193007, #92594 ) ;
#78754=CARTESIAN_POINT ( 'NONE',  ( -21.05000000000000071, -2.576749817950531707, -189.6385361693310756 ) ) ;
#78775=DIRECTION ( 'NONE',  ( 0.000000000000000000, -0.5626415523514111117, 0.8267009638119422466 ) ) ;
#78800=EDGE_CURVE ( 'NONE', #165216, #120023, #114971, .T. ) ;
#78801=CARTESIAN_POINT ( 'NONE',  ( -18.59999999999999787, -0.6576273345615599730, -242.5323337003318898 ) ) ;
#78812=CYLINDRICAL_SURFACE ( 'NONE', #178095, 0.09999999999999939493 ) ;
#78815=EDGE_CURVE ( 'NONE', #57917, #115133, #6640, .T. ) ;
#78853=FACE_OUTER_BOUND ( 'NONE', #57622, .T. ) ;
#78861=EDGE_LOOP ( 'NONE', ( #9325, #79011, #12351, #230121 ) ) ;
#78868=CARTESIAN_POINT ( 'NONE',  ( -18.50000000000000000, 0.7653315920341953182, -212.6731560895497353 ) ) ;
#78873=CARTESIAN_POINT ( 'NONE',  ( -18.59999999999999787, 12.80863705670246411, -205.3010250813005655 ) ) ;
#78908=ORIENTED_EDGE ( 'NONE', *, *, #237705, .F. ) ;
#78909=CYLINDRICAL_SURFACE ( 'NONE', #162085, 0.09999999999999939493 ) ;
#78912=LINE ( 'NONE', #80187, #101495 ) ;
#78914=DIRECTION ( 'NONE',  ( -1.000000000000000000, 6.239415780002328221E-16, 5.674754385112861898E-16 ) ) ;
#78920=CARTESIAN_POINT ( 'NONE',  ( 20.95512820512820085, 10.49413282287805949, -207.4737445703522383 ) ) ;
#78934=CARTESIAN_POINT ( 'NONE',  ( 20.94999999999999574, -10.56629024491939894, -206.4738935375009703 ) ) ;
#78980=ORIENTED_EDGE ( 'NONE', *, *, #69943, .T. ) ;
#79011=ORIENTED_EDGE ( 'NONE', *, *, #131424, .F. ) ;
#79023=LINE ( 'NONE', #253826, #124057 ) ;
#79024=VECTOR ( 'NONE', #236697, 1000.000000000000000 ) ;
#79036=ADVANCED_FACE ( 'NONE', ( #50235 ), #26871, .F. ) ;
#79038=CARTESIAN_POINT ( 'NONE',  ( 18.50000000000000000, -4.317402351199911337, -229.8357552817742260 ) ) ;
#79104=ORIENTED_EDGE ( 'NONE', *, *, #28311, .F. ) ;
#79126=CIRCLE ( 'NONE', #34, 0.09999999999999810429 ) ;
#79131=DIRECTION ( 'NONE',  ( 1.000000000000000000, 0.000000000000000000, 0.000000000000000000 ) ) ;
#79141=AXIS2_PLACEMENT_3D ( 'NONE', #69599, #228675, #149138 ) ;
#79163=EDGE_CURVE ( 'NONE', #24047, #227863, #235300, .T. ) ;
#79172=ADVANCED_FACE ( 'NONE', ( #157074 ), #37134, .T. ) ;
#79255=VECTOR ( 'NONE', #135343, 1000.000000000000000 ) ;
#79264=ORIENTED_EDGE ( 'NONE', *, *, #237083, .F. ) ;
#79284=VECTOR ( 'NONE', #137382, 1000.000000000000000 ) ;
#79295=CARTESIAN_POINT ( 'NONE',  ( 22.57320508075687115, 11.48087284840413425, -198.4995883060917663 ) ) ;
#79312=ORIENTED_EDGE ( 'NONE', *, *, #174552, .F. ) ;
#79338=DIRECTION ( 'NONE',  ( -0.000000000000000000, 0.9770955615653312831, 0.2128009952263620053 ) ) ;
#79358=CARTESIAN_POINT ( 'NONE',  ( -18.59999999999999787, 4.252251777740764460, -211.8999245327126744 ) ) ;
#79395=EDGE_CURVE ( 'NONE', #183742, #29761, #94302, .T. ) ;
#79458=FACE_OUTER_BOUND ( 'NONE', #218072, .T. ) ;
#79459=AXIS2_PLACEMENT_3D ( 'NONE', #23519, #104278, #63892 ) ;
#79484=EDGE_CURVE ( 'NONE', #250869, #46074, #181792, .T. ) ;
#79492=LINE ( 'NONE', #159076, #145160 ) ;
#79516=AXIS2_PLACEMENT_3D ( 'NONE', #85439, #88019, #244543 ) ;
#79540=DIRECTION ( 'NONE',  ( 1.000000000000000000, 0.000000000000000000, 0.000000000000000000 ) ) ;
#79577=DIRECTION ( 'NONE',  ( -0.000000000000000000, -0.9770955615653316162, -0.2128009952263604232 ) ) ;
#79620=ORIENTED_EDGE ( 'NONE', *, *, #33315, .T. ) ;
#79677=VERTEX_POINT ( 'NONE', #100591 ) ;
#79688=ORIENTED_EDGE ( 'NONE', *, *, #210687, .F. ) ;
#79721=PLANE ( 'NONE',  #107896 ) ;
#79763=ORIENTED_EDGE ( 'NONE', *, *, #143489, .F. ) ;
#79767=EDGE_CURVE ( 'NONE', #118980, #7608, #143605, .T. ) ;
#79780=ORIENTED_EDGE ( 'NONE', *, *, #209234, .F. ) ;
#79833=DIRECTION ( 'NONE',  ( -1.000000000000000000, -2.885090398161910739E-16, -6.283419270304611573E-17 ) ) ;
#79843=FACE_OUTER_BOUND ( 'NONE', #143758, .T. ) ;
#79849=CARTESIAN_POINT ( 'NONE',  ( 23.24999999999999645, 7.128833340094563376, -233.7327013124401276 ) ) ;
#79855=ADVANCED_FACE ( 'NONE', ( #207450 ), #88748, .F. ) ;
#79857=ORIENTED_EDGE ( 'NONE', *, *, #35809, .F. ) ;
#79871=CIRCLE ( 'NONE', #179882, 4.150000000000000355 ) ;
#79889=ADVANCED_FACE ( 'NONE', ( #247844 ), #77910, .T. ) ;
#79890=EDGE_LOOP ( 'NONE', ( #105552, #234953, #122567, #142694 ) ) ;
#79901=ORIENTED_EDGE ( 'NONE', *, *, #129390, .T. ) ;
#79926=DIRECTION ( 'NONE',  ( 0.000000000000000000, 0.2128009952263604232, -0.9770955615653316162 ) ) ;
#79930=ORIENTED_EDGE ( 'NONE', *, *, #92632, .F. ) ;
#79937=ORIENTED_EDGE ( 'NONE', *, *, #59418, .F. ) ;
#79962=FACE_OUTER_BOUND ( 'NONE', #156356, .T. ) ;
#79992=ORIENTED_EDGE ( 'NONE', *, *, #38458, .T. ) ;
#79998=CARTESIAN_POINT ( 'NONE',  ( -20.85000000000000142, 14.80545736607782814, -235.9842437978701639 ) ) ;
#80040=CIRCLE ( 'NONE', #234188, 0.1000000000000054040 ) ;
#80090=DIRECTION ( 'NONE',  ( -0.000000000000000000, 0.9770955615653313941, 0.2128009952263603954 ) ) ;
#80096=VERTEX_POINT ( 'NONE', #42925 ) ;
#80109=DIRECTION ( 'NONE',  ( 0.000000000000000000, -0.3427706569149636118, 0.9394191166662961834 ) ) ;
#80114=CARTESIAN_POINT ( 'NONE',  ( 20.74897398619114242, 11.98716974373489208, -206.2486471196630191 ) ) ;
#80121=AXIS2_PLACEMENT_3D ( 'NONE', #94878, #212288, #54470 ) ;
#80137=CARTESIAN_POINT ( 'NONE',  ( -20.85000000000000142, 7.567413955921500346, -241.6205176796878504 ) ) ;
#80154=CARTESIAN_POINT ( 'NONE',  ( -21.55000000000000426, 10.20058289318835953, -211.4179224723290815 ) ) ;
#80158=EDGE_CURVE ( 'NONE', #147767, #81634, #49333, .T. ) ;
#80164=AXIS2_PLACEMENT_3D ( 'NONE', #108108, #209775, #132815 ) ;
#80174=CARTESIAN_POINT ( 'NONE',  ( -21.14999999999999858, -2.479040261793999722, -189.6172560698084624 ) ) ;
#80186=ORIENTED_EDGE ( 'NONE', *, *, #256442, .F. ) ;
#80187=CARTESIAN_POINT ( 'NONE',  ( -21.05000000000000071, 2.953700692300310848, -208.6327728934509764 ) ) ;
#80196=CARTESIAN_POINT ( 'NONE',  ( -21.44999999999999929, 9.809744668562228043, -211.5030428704195913 ) ) ;
#80204=CYLINDRICAL_SURFACE ( 'NONE', #42901, 0.1000000000000008937 ) ;
#80232=EDGE_CURVE ( 'NONE', #61015, #164661, #222826, .T. ) ;
#80233=EDGE_CURVE ( 'NONE', #98769, #210485, #194664, .T. ) ;
#80237=VECTOR ( 'NONE', #75177, 1000.000000000000000 ) ;
#80256=DIRECTION ( 'NONE',  ( 0.000000000000000000, -0.2128009952263485993, 0.9770955615653341697 ) ) ;
#80276=EDGE_CURVE ( 'NONE', #193505, #208696, #210986, .T. ) ;
#80313=DIRECTION ( 'NONE',  ( 0.000000000000000000, 0.2128009952263605620, -0.9770955615653315052 ) ) ;
#80345=EDGE_LOOP ( 'NONE', ( #243598, #127474, #240249, #104796, #220950, #132621, #234668, #229325 ) ) ;
#80346=DIRECTION ( 'NONE',  ( 2.694716079187273439E-16, -0.9770955615653316162, -0.2128009952263598958 ) ) ;
#80347=CARTESIAN_POINT ( 'NONE',  ( 23.14999999999999858, 7.128833340094563376, -233.7327013124401276 ) ) ;
#80447=CARTESIAN_POINT ( 'NONE',  ( -22.39999999999999858, -2.598867842139048090, -189.5410128746472083 ) ) ;
#80471=ADVANCED_FACE ( 'NONE', ( #17900 ), #38768, .T. ) ;
#80504=CARTESIAN_POINT ( 'NONE',  ( -20.64999999999999858, -6.794814075650357665, -212.0940144922642219 ) ) ;
#80532=DIRECTION ( 'NONE',  ( -1.000000000000000000, -0.000000000000000000, -0.000000000000000000 ) ) ;
#80540=ORIENTED_EDGE ( 'NONE', *, *, #149800, .T. ) ;
#80551=UNCERTAINTY_MEASURE_WITH_UNIT (LENGTH_MEASURE( 1.000000000000000082E-05 ), #66681, 'distance_accuracy_value', 'NONE');
#80611=DIRECTION ( 'NONE',  ( 0.000000000000000000, 0.2128009952263604510, -0.9770955615653315052 ) ) ;
#80632=ORIENTED_EDGE ( 'NONE', *, *, #63786, .T. ) ;
#80635=DIRECTION ( 'NONE',  ( 1.000000000000000000, -0.000000000000000000, -0.000000000000000000 ) ) ;
#80718=CARTESIAN_POINT ( 'NONE',  ( -21.07928932188134041, 6.162520550852570445, -199.5566553493337665 ) ) ;
#80754=CARTESIAN_POINT ( 'NONE',  ( -20.54999999999999716, 7.128833340094563376, -233.7327013124401276 ) ) ;
#80755=EDGE_CURVE ( 'NONE', #257455, #109848, #158168, .T. ) ;
#80760=CYLINDRICAL_SURFACE ( 'NONE', #212054, 0.1000000000000055844 ) ;
#80764=CARTESIAN_POINT ( 'NONE',  ( 21.14999999999999858, -11.38316329222461754, -203.4791315943886048 ) ) ;
#80770=CARTESIAN_POINT ( 'NONE',  ( 21.05000000000000071, -1.335782702529562771, -194.7974669479901593 ) ) ;
#80798=DIRECTION ( 'NONE',  ( 0.000000000000000000, 0.2128009952263056614, -0.9770955615653434956 ) ) ;
#80806=ADVANCED_FACE ( 'NONE', ( #122827 ), #62834, .T. ) ;
#80818=CARTESIAN_POINT ( 'NONE',  ( 20.94999999999999574, 4.158309866074138661, -211.9342015984041439 ) ) ;
#80845=EDGE_CURVE ( 'NONE', #218469, #44901, #24330, .T. ) ;
#80864=DIRECTION ( 'NONE',  ( -1.000000000000000000, 0.000000000000000000, 0.000000000000000000 ) ) ;
#80883=AXIS2_PLACEMENT_3D ( 'NONE', #236868, #58213, #75263 ) ;
#80897=EDGE_CURVE ( 'NONE', #117463, #63493, #66692, .T. ) ;
#80899=ADVANCED_FACE ( 'NONE', ( #127949 ), #95031, .T. ) ;
#80924=VERTEX_POINT ( 'NONE', #5395 ) ;
#80952=FACE_OUTER_BOUND ( 'NONE', #49998, .T. ) ;
#80989=ORIENTED_EDGE ( 'NONE', *, *, #19899, .T. ) ;
#80997=CIRCLE ( 'NONE', #114330, 12.97499999999998899 ) ;
#81000=AXIS2_PLACEMENT_3D ( 'NONE', #183781, #27311, #128948 ) ;
#81004=AXIS2_PLACEMENT_3D ( 'NONE', #128046, #129323, #107180 ) ;
#81020=DIRECTION ( 'NONE',  ( 1.000000000000000000, 0.000000000000000000, 0.000000000000000000 ) ) ;
#81062=ORIENTED_EDGE ( 'NONE', *, *, #54655, .T. ) ;
#81078=CARTESIAN_POINT ( 'NONE',  ( 21.11701782572533048, 13.08179283168479579, -210.6830026332638681 ) ) ;
#81124=CARTESIAN_POINT ( 'NONE',  ( 23.24999999999999645, 8.111588099649802430, -211.9294447938511325 ) ) ;
#81151=DIRECTION ( 'NONE',  ( 1.000000000000000000, 6.779962435680481854E-15, 1.476603528521582099E-15 ) ) ;
#81165=ORIENTED_EDGE ( 'NONE', *, *, #207633, .T. ) ;
#81179=SPHERICAL_SURFACE ( 'NONE', #30905, 0.1000000000000000056 ) ;
#81198=CARTESIAN_POINT ( 'NONE',  ( -21.14999999999999858, -2.576749817950531707, -189.6385361693310756 ) ) ;
#81202=ORIENTED_EDGE ( 'NONE', *, *, #149184, .T. ) ;
#81210=VERTEX_POINT ( 'NONE', #241182 ) ;
#81217=DIRECTION ( 'NONE',  ( 1.000000000000000000, 0.000000000000000000, 0.000000000000000000 ) ) ;
#81222=EDGE_CURVE ( 'NONE', #163761, #159106, #195208, .T. ) ;
#81223=AXIS2_PLACEMENT_3D ( 'NONE', #81198, #141203, #220733 ) ;
#81224=TOROIDAL_SURFACE ( 'NONE', #135405, 0.2000000000000000111, 0.1000000000000000056 ) ;
#81236=CARTESIAN_POINT ( 'NONE',  ( -21.55000000000000071, 11.68239342655420110, -220.1014838121945161 ) ) ;
#81253=EDGE_CURVE ( 'NONE', #86372, #27420, #177378, .T. ) ;
#81261=AXIS2_PLACEMENT_3D ( 'NONE', #136275, #138831, #114170 ) ;
#81273=CYLINDRICAL_SURFACE ( 'NONE', #256874, 0.5000000000000007772 ) ;
#81280=VERTEX_POINT ( 'NONE', #46797 ) ;
#81304=DIRECTION ( 'NONE',  ( 0.000000000000000000, 0.2128009952263603677, -0.9770955615653313941 ) ) ;
#81343=DIRECTION ( 'NONE',  ( 0.000000000000000000, 0.2128009952263485993, -0.9770955615653341697 ) ) ;
#81344=( BOUNDED_SURFACE ( )  B_SPLINE_SURFACE ( 3, 2, ( 
 ( #253005, #177363, #114787 ),
 ( #194352, #215167, #15720 ),
 ( #36573, #16988, #183753 ),
 ( #63801, #80770, #241168 ),
 ( #224145, #85895, #164195 ),
 ( #162924, #243721, #22127 ) ),
 .UNSPECIFIED., .F., .F., .F. ) 
 B_SPLINE_SURFACE_WITH_KNOTS ( ( 4, 2, 4 ),
 ( 3, 3 ),
 ( 0.0001300404313046926664, 0.0003183318589266920175, 0.0005066232865486913414 ),
 ( 0.000000000000000000, 1.000000000000000000 ),
 .UNSPECIFIED. ) 
 GEOMETRIC_REPRESENTATION_ITEM ( )  RATIONAL_B_SPLINE_SURFACE ( (
 ( 1.000000000000000000, 0.7071067811865597852, 1.000000000000000000),
 ( 1.000000000000000000, 0.7625113560540101032, 1.000000000000000000),
 ( 1.000000000000000000, 0.8126073484688884907, 1.000000000000000000),
 ( 1.000000000000000000, 0.8923049332732615468, 1.000000000000000000),
 ( 1.000000000000000000, 0.9231914937769579721, 1.000000000000000000),
 ( 1.000000000000000000, 0.9238795325112791890, 1.000000000000000000) ) ) 
 REPRESENTATION_ITEM ( '' )  SURFACE ( )  );
#81375=FACE_OUTER_BOUND ( 'NONE', #32547, .T. ) ;
#81384=LINE ( 'NONE', #3150, #22022 ) ;
#81394=ORIENTED_EDGE ( 'NONE', *, *, #87929, .F. ) ;
#81406=CARTESIAN_POINT ( 'NONE',  ( 20.94999999999999574, 0.5876173420563349792, -209.1618981382189588 ) ) ;
#81408=CARTESIAN_POINT ( 'NONE',  ( 20.86036036209902633, 12.00918032940415969, -206.2305865399390257 ) ) ;
#81424=FACE_OUTER_BOUND ( 'NONE', #98737, .T. ) ;
#81425=AXIS2_PLACEMENT_3D ( 'NONE', #78672, #236476, #98210 ) ;
#81428=DIRECTION ( 'NONE',  ( 1.000000000000000000, 0.000000000000000000, 0.000000000000000000 ) ) ;
#81442=DIRECTION ( 'NONE',  ( -1.000000000000000000, 0.000000000000000000, 0.000000000000000000 ) ) ;
#81459=ORIENTED_EDGE ( 'NONE', *, *, #103614, .F. ) ;
#81465=CARTESIAN_POINT ( 'NONE',  ( 21.14999999999999858, 11.40444339177024169, -198.6185779617709670 ) ) ;
#81472=ORIENTED_EDGE ( 'NONE', *, *, #1344, .F. ) ;
#81481=CARTESIAN_POINT ( 'NONE',  ( 21.05000000000000071, 10.39655183198267530, -207.4949966697317620 ) ) ;
#81490=LINE ( 'NONE', #39860, #117884 ) ;
#81512=EDGE_CURVE ( 'NONE', #162009, #137285, #157504, .T. ) ;
#81524=CARTESIAN_POINT ( 'NONE',  ( -20.54999999999999716, 4.768403829798271154, -213.4961173936592331 ) ) ;
#81565=ADVANCED_FACE ( 'NONE', ( #77915 ), #237009, .F. ) ;
#81568=CARTESIAN_POINT ( 'NONE',  ( 18.59999999999999787, 7.783179459866048866, -245.3643104511423019 ) ) ;
#81591=DIRECTION ( 'NONE',  ( 1.000000000000000000, 0.000000000000000000, 0.000000000000000000 ) ) ;
#81593=AXIS2_PLACEMENT_3D ( 'NONE', #127457, #227832, #6210 ) ;
#81597=ORIENTED_EDGE ( 'NONE', *, *, #27608, .F. ) ;
#81610=AXIS2_PLACEMENT_3D ( 'NONE', #112171, #229539, #232113 ) ;
#81614=AXIS2_PLACEMENT_3D ( 'NONE', #228614, #108648, #169956 ) ;
#81618=ORIENTED_EDGE ( 'NONE', *, *, #155847, .T. ) ;
#81623=CARTESIAN_POINT ( 'NONE',  ( -21.05000000000000071, -4.735542975717121905, -233.2463119243910796 ) ) ;
#81627=EDGE_CURVE ( 'NONE', #215393, #110145, #7943, .T. ) ;
#81634=VERTEX_POINT ( 'NONE', #103880 ) ;
#81682=DIRECTION ( 'NONE',  ( -1.000000000000000000, 0.000000000000000000, 0.000000000000000000 ) ) ;
#81691=CARTESIAN_POINT ( 'NONE',  ( -18.59999999999999787, 2.859758780633683273, -208.6670499591424459 ) ) ;
#81735=EDGE_CURVE ( 'NONE', #164130, #24822, #206845, .T. ) ;
#81783=CARTESIAN_POINT ( 'NONE',  ( -21.05000000000000071, 2.859758780633683273, -208.6670499591424459 ) ) ;
#81820=LINE ( 'NONE', #240941, #85306 ) ;
#81823=CIRCLE ( 'NONE', #61006, 0.1000000000000054040 ) ;
#81835=ORIENTED_EDGE ( 'NONE', *, *, #156392, .T. ) ;
#81839=B_SPLINE_CURVE_WITH_KNOTS ( 'NONE', 3,
 ( #28718, #229443, #42153, #88615, #87340, #29982 ),
 .UNSPECIFIED., .F., .F.,
 ( 4, 2, 4 ),
 ( 0.000000000000000000, 0.0001891491689349495266, 0.0003782983378698990531 ),
 .UNSPECIFIED. ) ;
#81846=LINE ( 'NONE', #178452, #30590 ) ;
#81865=EDGE_CURVE ( 'NONE', #39697, #156342, #62266, .T. ) ;
#81913=DIRECTION ( 'NONE',  ( 0.000000000000000000, -0.2128009952263603677, 0.9770955615653313941 ) ) ;
#81942=CARTESIAN_POINT ( 'NONE',  ( 22.47071067811865319, -1.546016791165055304, -193.4356622592196970 ) ) ;
#81950=DIRECTION ( 'NONE',  ( 0.000000000000000000, -0.9770955615653548199, -0.2128009952262535920 ) ) ;
#81951=CARTESIAN_POINT ( 'NONE',  ( 18.59999999999998721, 19.88098775990103562, -199.0038892813511779 ) ) ;
#81952=EDGE_CURVE ( 'NONE', #198456, #95913, #49793, .T. ) ;
#81969=AXIS2_PLACEMENT_3D ( 'NONE', #250732, #72119, #132081 ) ;
#81983=CARTESIAN_POINT ( 'NONE',  ( 20.94999999999999929, -3.770473190032740174, -225.9805569534692324 ) ) ;
#81984=DIRECTION ( 'NONE',  ( 1.000000000000000000, 0.000000000000000000, 0.000000000000000000 ) ) ;
#82014=ORIENTED_EDGE ( 'NONE', *, *, #132726, .F. ) ;
#82020=DIRECTION ( 'NONE',  ( 1.000000000000000000, -0.000000000000000000, -0.000000000000000000 ) ) ;
#82035=FACE_OUTER_BOUND ( 'NONE', #246227, .T. ) ;
#82059=DIRECTION ( 'NONE',  ( 0.000000000000000000, 0.2128009952263598958, -0.9770955615653316162 ) ) ;
#82129=AXIS2_PLACEMENT_3D ( 'NONE', #199063, #235605, #238169 ) ;
#82153=AXIS2_PLACEMENT_3D ( 'NONE', #59600, #40106, #41382 ) ;
#82211=ORIENTED_EDGE ( 'NONE', *, *, #118886, .T. ) ;
#82214=CARTESIAN_POINT ( 'NONE',  ( 18.59999999999999076, 10.90071697730193456, -220.2717246083756208 ) ) ;
#82226=CARTESIAN_POINT ( 'NONE',  ( 22.39999999999999503, 11.38316329224760892, -198.5208684056144079 ) ) ;
#82231=DIRECTION ( 'NONE',  ( 0.000000000000000000, 0.2128009952263604787, -0.9770955615653315052 ) ) ;
#82331=DIRECTION ( 'NONE',  ( -1.000000000000000000, -0.000000000000000000, -0.000000000000000000 ) ) ;
#82345=CARTESIAN_POINT ( 'NONE',  ( -21.55000000000000426, 10.16011026985487398, -211.4267369781599939 ) ) ;
#82365=DIRECTION ( 'NONE',  ( 0.000000000000000000, 0.6728388485993177515, -0.7397890806274072251 ) ) ;
#82383=CARTESIAN_POINT ( 'NONE',  ( 22.50000000000000000, -2.402702137741712818, -189.4978470520862288 ) ) ;
#82396=CIRCLE ( 'NONE', #219975, 0.1999999999999987899 ) ;
#82414=DIRECTION ( 'NONE',  ( 0.000000000000000000, 0.2128009952263485993, -0.9770955615653340587 ) ) ;
#82419=EDGE_LOOP ( 'NONE', ( #68391, #202775, #250876, #99761 ) ) ;
#82434=ADVANCED_FACE ( 'NONE', ( #55139 ), #194715, .F. ) ;
#82439=DIRECTION ( 'NONE',  ( 0.000000000000000000, -0.9770955615653318382, -0.2128009952263588411 ) ) ;
#82482=CARTESIAN_POINT ( 'NONE',  ( 23.14999999999999858, 5.174642216963899699, -234.1583033028928753 ) ) ;
#82493=EDGE_LOOP ( 'NONE', ( #50797, #166166, #79992, #247577 ) ) ;
#82500=EDGE_CURVE ( 'NONE', #214061, #225466, #120741, .T. ) ;
#82502=ORIENTED_EDGE ( 'NONE', *, *, #57085, .T. ) ;
#82509=EDGE_CURVE ( 'NONE', #37909, #176555, #83275, .T. ) ;
#82539=CARTESIAN_POINT ( 'NONE',  ( 20.97224591636398827, 12.98858666785727323, -210.7083050095600925 ) ) ;
#82556=DIRECTION ( 'NONE',  ( -0.000000000000000000, -0.2128009952263605620, 0.9770955615653313941 ) ) ;
#82558=ORIENTED_EDGE ( 'NONE', *, *, #92021, .T. ) ;
#82592=FACE_OUTER_BOUND ( 'NONE', #248765, .T. ) ;
#82593=ORIENTED_EDGE ( 'NONE', *, *, #93575, .F. ) ;
#82607=VECTOR ( 'NONE', #234769, 1000.000000000000000 ) ;
#82626=DIRECTION ( 'NONE',  ( 0.000000000000000000, 0.2128009952263485993, -0.9770955615653341697 ) ) ;
#82684=ADVANCED_FACE ( 'NONE', ( #95278 ), #220840, .T. ) ;
#82691=CARTESIAN_POINT ( 'NONE',  ( 21.11344571971334361, 12.98064790059219575, -210.7060374374014771 ) ) ;
#82707=LINE ( 'NONE', #162301, #161490 ) ;
#82747=ORIENTED_EDGE ( 'NONE', *, *, #187578, .T. ) ;
#82761=CARTESIAN_POINT ( 'NONE',  ( 21.05000000000061888, 10.48215802087101700, -207.4378900153776328 ) ) ;
#82773=ORIENTED_EDGE ( 'NONE', *, *, #1928, .F. ) ;
#82825=CIRCLE ( 'NONE', #33033, 2.100000000000004974 ) ;
#82892=VECTOR ( 'NONE', #100520, 1000.000000000000000 ) ;
#82944=ORIENTED_EDGE ( 'NONE', *, *, #184073, .T. ) ;
#82962=TOROIDAL_SURFACE ( 'NONE', #8008, 4.149999999999999467, 0.1000000000000000056 ) ;
#82983=AXIS2_PLACEMENT_3D ( 'NONE', #83866, #22683, #163456 ) ;
#82990=CARTESIAN_POINT ( 'NONE',  ( 20.94999999999999218, 17.16609282392353109, -224.6038045889790453 ) ) ;
#83026=CARTESIAN_POINT ( 'NONE',  ( -18.59999999999999787, 13.98997548377051459, -210.4902890347897255 ) ) ;
#83032=EDGE_CURVE ( 'NONE', #7989, #138601, #158714, .T. ) ;
#83061=CARTESIAN_POINT ( 'NONE',  ( -21.05000000000000071, -0.9150442794618510733, -196.7984890852706030 ) ) ;
#83067=B_SPLINE_CURVE_WITH_KNOTS ( 'NONE', 3,
 ( #144222, #102510, #43865, #41321 ),
 .UNSPECIFIED., .F., .F.,
 ( 4, 4 ),
 ( 0.000000000000000000, 0.001767853679387137913 ),
 .UNSPECIFIED. ) ;
#83084=ORIENTED_EDGE ( 'NONE', *, *, #249637, .F. ) ;
#83112=DIRECTION ( 'NONE',  ( 0.000000000000000000, 0.9770955615653259541, 0.2128009952263860971 ) ) ;
#83169=DIRECTION ( 'NONE',  ( 0.000000000000000000, -0.07893460099012301889, 0.9968797965484754720 ) ) ;
#83180=DIRECTION ( 'NONE',  ( -0.000000000000000000, 0.9770955615653313941, 0.2128009952263606730 ) ) ;
#83246=DIRECTION ( 'NONE',  ( 7.304098846218132695E-16, -0.9770955615653315052, -0.2128009952263603954 ) ) ;
#83275=CIRCLE ( 'NONE', #116614, 0.09999999999998904210 ) ;
#83292=ORIENTED_EDGE ( 'NONE', *, *, #180886, .T. ) ;
#83296=DIRECTION ( 'NONE',  ( 1.000000000000000000, 3.190570557967288949E-16, 6.948722487160392945E-17 ) ) ;
#83315=CARTESIAN_POINT ( 'NONE',  ( -21.05000000000000071, 2.859758780633683273, -208.6670499591424459 ) ) ;
#83317=AXIS2_PLACEMENT_3D ( 'NONE', #239809, #201961, #40356 ) ;
#83340=DIRECTION ( 'NONE',  ( 1.000000000000000000, 0.000000000000000000, 0.000000000000000000 ) ) ;
#83361=VERTEX_POINT ( 'NONE', #73523 ) ;
#83377=ORIENTED_EDGE ( 'NONE', *, *, #19429, .F. ) ;
#83389=TOROIDAL_SURFACE ( 'NONE', #8414, 7.800000000000000711, 0.1000000000000000056 ) ;
#83393=ORIENTED_EDGE ( 'NONE', *, *, #172982, .F. ) ;
#83409=AXIS2_PLACEMENT_3D ( 'NONE', #202524, #256328, #76467 ) ;
#83414=EDGE_LOOP ( 'NONE', ( #189884, #231122, #111556, #70301 ) ) ;
#83427=EDGE_LOOP ( 'NONE', ( #206200, #170352, #162774, #219964 ) ) ;
#83444=ORIENTED_EDGE ( 'NONE', *, *, #218085, .T. ) ;
#83465=ORIENTED_EDGE ( 'NONE', *, *, #136536, .F. ) ;
#83472=VERTEX_POINT ( 'NONE', #160765 ) ;
#83483=ORIENTED_EDGE ( 'NONE', *, *, #17839, .F. ) ;
#83488=ORIENTED_EDGE ( 'NONE', *, *, #163470, .T. ) ;
#83519=VECTOR ( 'NONE', #120245, 1000.000000000000227 ) ;
#83539=VERTEX_POINT ( 'NONE', #163310 ) ;
#83582=VERTEX_POINT ( 'NONE', #65475 ) ;
#83589=DIRECTION ( 'NONE',  ( 1.000000000000000000, 0.000000000000000000, 0.000000000000000000 ) ) ;
#83595=TOROIDAL_SURFACE ( 'NONE', #220985, 0.4000000000000015210, 0.1000000000000000056 ) ;
#83634=VERTEX_POINT ( 'NONE', #26364 ) ;
#83658=DIRECTION ( 'NONE',  ( 1.000000000000000000, -0.000000000000000000, -0.000000000000000000 ) ) ;
#83663=CARTESIAN_POINT ( 'NONE',  ( 21.05000000000000071, 6.412126976762841046, -199.7058512474018244 ) ) ;
#83668=LINE ( 'NONE', #4164, #241423 ) ;
#83679=DIRECTION ( 'NONE',  ( 0.000000000000000000, -0.2128009952263403282, 0.9770955615653358350 ) ) ;
#83685=FACE_OUTER_BOUND ( 'NONE', #126919, .T. ) ;
#83705=CARTESIAN_POINT ( 'NONE',  ( 18.59999999999999432, -0.6576273345615495369, -242.5323337003318898 ) ) ;
#83706=EDGE_CURVE ( 'NONE', #222722, #69101, #221954, .T. ) ;
#83710=CIRCLE ( 'NONE', #79459, 0.1000000000000054040 ) ;
#83738=ADVANCED_FACE ( 'NONE', ( #49770 ), #69352, .F. ) ;
#83746=CARTESIAN_POINT ( 'NONE',  ( 21.14250536705908345, 6.368877103560281583, -199.6129264737045048 ) ) ;
#83753=ORIENTED_EDGE ( 'NONE', *, *, #169239, .F. ) ;
#83755=CARTESIAN_POINT ( 'NONE',  ( 18.54286124688533732, -0.8401192457767151511, -242.3674794292616923 ) ) ;
#83762=ORIENTED_EDGE ( 'NONE', *, *, #240635, .F. ) ;
#83866=CARTESIAN_POINT ( 'NONE',  ( -18.59999999999999787, 15.92646454033039305, -219.3818586450342707 ) ) ;
#83938=DIRECTION ( 'NONE',  ( 0.000000000000000000, 0.9550021345545507412, -0.2965989261549202838 ) ) ;
#83945=AXIS2_PLACEMENT_3D ( 'NONE', #185299, #65342, #180178 ) ;
#83953=CARTESIAN_POINT ( 'NONE',  ( 21.00000000000000000, 14.04870287383362992, -219.6884709798077893 ) ) ;
#83958=ADVANCED_FACE ( 'NONE', ( #160461 ), #24806, .T. ) ;
#83972=CARTESIAN_POINT ( 'NONE',  ( 20.85000000000000142, 7.128833340094563376, -233.7327013124401276 ) ) ;
#83976=CARTESIAN_POINT ( 'NONE',  ( -23.25000000000000000, 1.148907358139439339E-11, -201.0000000000015064 ) ) ;
#83994=DIRECTION ( 'NONE',  ( -6.938893903907221278E-15, 0.9770955615653313941, 0.2128009952263606730 ) ) ;
#84008=ADVANCED_FACE ( 'NONE', ( #145992 ), #245782, .T. ) ;
#84035=VECTOR ( 'NONE', #193626, 1000.000000000000227 ) ;
#84036=ORIENTED_EDGE ( 'NONE', *, *, #122668, .T. ) ;
#84041=CARTESIAN_POINT ( 'NONE',  ( -23.25000000000000000, 14.73746888278882494, -235.8584165281851028 ) ) ;
#84053=CARTESIAN_POINT ( 'NONE',  ( -21.05000000000000071, 0.9150442794848296924, -205.2015109147324097 ) ) ;
#84062=CIRCLE ( 'NONE', #234131, 0.09999999999999939493 ) ;
#84094=ORIENTED_EDGE ( 'NONE', *, *, #108317, .T. ) ;
#84103=EDGE_CURVE ( 'NONE', #83582, #114637, #108417, .T. ) ;
#84113=LINE ( 'NONE', #3329, #2653 ) ;
#84139=ORIENTED_EDGE ( 'NONE', *, *, #82509, .T. ) ;
#84142=DIRECTION ( 'NONE',  ( -3.265361837132813093E-16, 0.9770955615653316162, 0.2128009952263604232 ) ) ;
#84172=LINE ( 'NONE', #244583, #94481 ) ;
#84178=DIRECTION ( 'NONE',  ( 0.000000000000000000, 0.2128009952263598958, -0.9770955615653316162 ) ) ;
#84193=DIRECTION ( 'NONE',  ( 0.000000000000000000, -0.2128009952263603677, 0.9770955615653313941 ) ) ;
#84220=DIRECTION ( 'NONE',  ( 1.000000000000000000, 0.000000000000000000, 0.000000000000000000 ) ) ;
#84233=DIRECTION ( 'NONE',  ( -0.8660254037844884456, -0.1064004976131806557, 0.4885477807825773788 ) ) ;
#84281=AXIS2_PLACEMENT_3D ( 'NONE', #95834, #155857, #175426 ) ;
#84295=EDGE_CURVE ( 'NONE', #127544, #246315, #179347, .T. ) ;
#84302=EDGE_CURVE ( 'NONE', #30925, #184847, #236983, .T. ) ;
#84380=ORIENTED_EDGE ( 'NONE', *, *, #99395, .F. ) ;
#84392=DIRECTION ( 'NONE',  ( -1.000000000000000000, -0.000000000000000000, -0.000000000000000000 ) ) ;
#84396=CARTESIAN_POINT ( 'NONE',  ( 20.12500000000000000, 11.25287472715600146, -206.8511660127314826 ) ) ;
#84398=DIRECTION ( 'NONE',  ( 0.000000000000000000, -0.2128009952263361926, 0.9770955615653368342 ) ) ;
#84410=ORIENTED_EDGE ( 'NONE', *, *, #129387, .F. ) ;
#84417=DIRECTION ( 'NONE',  ( -0.000000000000000000, -0.2128009952263604232, 0.9770955615653316162 ) ) ;
#84427=DIRECTION ( 'NONE',  ( 1.000000000000000000, 1.794895427898103559E-16, 3.909090864890002444E-17 ) ) ;
#84454=DIRECTION ( 'NONE',  ( 0.000000000000000000, -0.9770955615653307280, -0.2128009952263641702 ) ) ;
#84455=ORIENTED_EDGE ( 'NONE', *, *, #86411, .F. ) ;
#84482=FACE_OUTER_BOUND ( 'NONE', #47637, .T. ) ;
#84542=CARTESIAN_POINT ( 'NONE',  ( -21.04999999999999361, 6.134002965570138244, -199.5633345488312784 ) ) ;
#84556=DIRECTION ( 'NONE',  ( 0.000000000000000000, 0.9964539953858966292, 0.08413937888696132461 ) ) ;
#84593=DIRECTION ( 'NONE',  ( 0.000000000000000000, 0.2128009952263608395, -0.9770955615653315052 ) ) ;
#84651=ORIENTED_EDGE ( 'NONE', *, *, #134485, .F. ) ;
#84731=ORIENTED_EDGE ( 'NONE', *, *, #122669, .F. ) ;
#84732=ORIENTED_EDGE ( 'NONE', *, *, #197142, .T. ) ;
#84766=CIRCLE ( 'NONE', #118120, 0.09999999999999939493 ) ;
#84769=ADVANCED_FACE ( 'NONE', ( #142476 ), #27719, .T. ) ;
#84775=AXIS2_PLACEMENT_3D ( 'NONE', #1672, #18683, #387 ) ;
#84780=VERTEX_POINT ( 'NONE', #44685 ) ;
#84781=ORIENTED_EDGE ( 'NONE', *, *, #28656, .F. ) ;
#84789=EDGE_CURVE ( 'NONE', #74531, #87436, #50362, .T. ) ;
#84808=ADVANCED_FACE ( 'NONE', ( #65509 ), #45953, .T. ) ;
#84813=DIRECTION ( 'NONE',  ( 0.000000000000000000, 0.2128009952263982818, -0.9770955615653232895 ) ) ;
#84820=EDGE_LOOP ( 'NONE', ( #6760, #59097, #13903, #194861 ) ) ;
#84845=DIRECTION ( 'NONE',  ( -1.000000000000000000, 0.000000000000000000, 0.000000000000000000 ) ) ;
#84852=CARTESIAN_POINT ( 'NONE',  ( 20.95595624212472075, 12.00415041844581054, -206.1941058355727989 ) ) ;
#84871=EDGE_LOOP ( 'NONE', ( #31571, #124117, #42854, #15901 ) ) ;
#84888=CIRCLE ( 'NONE', #9909, 0.09999999999999939493 ) ;
#84958=AXIS2_PLACEMENT_3D ( 'NONE', #205868, #70250, #229302 ) ;
#84959=CARTESIAN_POINT ( 'NONE',  ( -18.59999999999999787, 7.783179459866048866, -245.3643104511423019 ) ) ;
#84968=EDGE_CURVE ( 'NONE', #63666, #209650, #62982, .T. ) ;
#84987=EDGE_CURVE ( 'NONE', #81210, #96897, #166779, .T. ) ;
#84990=CIRCLE ( 'NONE', #22687, 0.09999999999999753530 ) ;
#84992=AXIS2_PLACEMENT_3D ( 'NONE', #83953, #163542, #243072 ) ;
#84993=LINE ( 'NONE', #241532, #121486 ) ;
#85010=DIRECTION ( 'NONE',  ( -1.000000000000000000, -0.000000000000000000, -0.000000000000000000 ) ) ;
#85102=DIRECTION ( 'NONE',  ( -1.000000000000000000, 0.000000000000000000, 0.000000000000000000 ) ) ;
#85131=AXIS2_PLACEMENT_3D ( 'NONE', #226250, #84142, #69795 ) ;
#85154=FACE_BOUND ( 'NONE', #163782, .T. ) ;
#85173=EDGE_CURVE ( 'NONE', #13347, #106308, #213011, .T. ) ;
#85185=CARTESIAN_POINT ( 'NONE',  ( -23.15000000000000213, -6.794814075650357665, -212.0940144922642219 ) ) ;
#85186=CARTESIAN_POINT ( 'NONE',  ( 21.05000000000000071, 9.765296417674898422, -220.4624455711005737 ) ) ;
#85206=EDGE_CURVE ( 'NONE', #30038, #89812, #133889, .T. ) ;
#85229=LINE ( 'NONE', #163521, #100402 ) ;
#85256=ORIENTED_EDGE ( 'NONE', *, *, #242454, .T. ) ;
#85266=CARTESIAN_POINT ( 'NONE',  ( -23.15000000000000213, 13.98997548377051814, -210.4902890347897255 ) ) ;
#85303=CIRCLE ( 'NONE', #64494, 0.1000000000000054040 ) ;
#85306=VECTOR ( 'NONE', #62296, 1000.000000000000227 ) ;
#85311=CIRCLE ( 'NONE', #81223, 0.1000000000000099282 ) ;
#85321=DIRECTION ( 'NONE',  ( 0.000000000000000000, 0.9770955615653259541, 0.2128009952263860971 ) ) ;
#85361=DIRECTION ( 'NONE',  ( 0.000000000000000000, -0.2128009952263628934, 0.9770955615653310611 ) ) ;
#85376=FACE_OUTER_BOUND ( 'NONE', #26019, .T. ) ;
#85424=CARTESIAN_POINT ( 'NONE',  ( 21.05000000000000071, -10.76604040606816959, -206.3127087229280789 ) ) ;
#85425=ORIENTED_EDGE ( 'NONE', *, *, #221941, .F. ) ;
#85431=ORIENTED_EDGE ( 'NONE', *, *, #215235, .T. ) ;
#85439=CARTESIAN_POINT ( 'NONE',  ( 21.14999999999999858, 1.148907358139439339E-11, -201.0000000000015064 ) ) ;
#85447=CARTESIAN_POINT ( 'NONE',  ( 20.85000000000000142, 18.60970618848721259, -231.2322896185303875 ) ) ;
#85457=DIRECTION ( 'NONE',  ( 0.000000000000000000, -0.9770955615653317272, -0.2128009952263598126 ) ) ;
#85464=ORIENTED_EDGE ( 'NONE', *, *, #104113, .F. ) ;
#85471=LINE ( 'NONE', #141633, #206732 ) ;
#85490=FACE_OUTER_BOUND ( 'NONE', #253593, .T. ) ;
#85493=ORIENTED_EDGE ( 'NONE', *, *, #209862, .F. ) ;
#85506=CIRCLE ( 'NONE', #181430, 0.1000000000000026840 ) ;
#85537=DIRECTION ( 'NONE',  ( 0.000000000000000000, -0.9394191166662618775, -0.3427706569150580362 ) ) ;
#85551=SPHERICAL_SURFACE ( 'NONE', #105469, 0.1000000000000000056 ) ;
#85552=CARTESIAN_POINT ( 'NONE',  ( 20.95000000000000284, 17.04749343158541919, -224.5908524457890678 ) ) ;
#85557=CARTESIAN_POINT ( 'NONE',  ( -20.96077737575358668, 17.02684875966442846, -224.5570219545468262 ) ) ;
#85567=CARTESIAN_POINT ( 'NONE',  ( -23.25000000000000000, 6.855069093508307176, -220.2576993407411692 ) ) ;
#85577=PLANE ( 'NONE',  #160637 ) ;
#85592=DIRECTION ( 'NONE',  ( 1.000000000000000000, 0.000000000000000000, 0.000000000000000000 ) ) ;
#85597=DIRECTION ( 'NONE',  ( 4.504528286903031644E-15, 0.08413937888703756918, -0.9964539953858901900 ) ) ;
#85607=AXIS2_PLACEMENT_3D ( 'NONE', #26324, #224508, #127987 ) ;
#85615=ADVANCED_FACE ( 'NONE', ( #162450 ), #98557, .T. ) ;
#85623=PLANE ( 'NONE',  #185295 ) ;
#85624=DIRECTION ( 'NONE',  ( 0.000000000000000000, 0.2128009952263650861, -0.9770955615653305060 ) ) ;
#85636=AXIS2_PLACEMENT_3D ( 'NONE', #227443, #29296, #100604 ) ;
#85686=CARTESIAN_POINT ( 'NONE',  ( -18.59999999999999787, 4.273531877263399892, -211.9976340888692050 ) ) ;
#85739=CARTESIAN_POINT ( 'NONE',  ( 19.75857864376268935, 16.76897757977919312, -222.7804130109902871 ) ) ;
#85747=VERTEX_POINT ( 'NONE', #25500 ) ;
#85763=EDGE_CURVE ( 'NONE', #64432, #102962, #196612, .T. ) ;
#85765=DIRECTION ( 'NONE',  ( -1.000000000000000000, 0.000000000000000000, 0.000000000000000000 ) ) ;
#85779=DIRECTION ( 'NONE',  ( 0.000000000000000000, -0.2128009952263511806, 0.9770955615653335036 ) ) ;
#85867=ORIENTED_EDGE ( 'NONE', *, *, #62958, .T. ) ;
#85877=AXIS2_PLACEMENT_3D ( 'NONE', #124408, #27901, #150402 ) ;
#85895=CARTESIAN_POINT ( 'NONE',  ( 21.05000000000000071, -1.290380839962420589, -194.8331666543516292 ) ) ;
#85916=CARTESIAN_POINT ( 'NONE',  ( -21.05000000000000071, -10.56629024491939894, -206.4738935375009703 ) ) ;
#85924=LINE ( 'NONE', #66399, #33925 ) ;
#85938=CARTESIAN_POINT ( 'NONE',  ( 18.58725287972316664, -0.7668395408905932520, -242.4347282044658698 ) ) ;
#85962=CARTESIAN_POINT ( 'NONE',  ( 20.94999999999999574, -10.74476030654553504, -206.4104182790846096 ) ) ;
#85969=( GEOMETRIC_REPRESENTATION_CONTEXT ( 3 ) GLOBAL_UNCERTAINTY_ASSIGNED_CONTEXT ( ( #141761 ) ) GLOBAL_UNIT_ASSIGNED_CONTEXT ( ( #133337, #251988, #173800 ) ) REPRESENTATION_CONTEXT ( 'NONE', 'WORKASPACE' ) );
#86080=FACE_OUTER_BOUND ( 'NONE', #166163, .T. ) ;
#86102=DIRECTION ( 'NONE',  ( 0.000000000000000000, -0.2128009952263485993, 0.9770955615653341697 ) ) ;
#86122=CARTESIAN_POINT ( 'NONE',  ( -18.50000000000000000, 3.132039894996826224, -190.2813437854022993 ) ) ;
#86124=EDGE_CURVE ( 'NONE', #29396, #185772, #175305, .T. ) ;
#86145=DIRECTION ( 'NONE',  ( -1.000000000000000000, 0.000000000000000000, 0.000000000000000000 ) ) ;
#86146=DIRECTION ( 'NONE',  ( 1.000000000000000000, 0.000000000000000000, 0.000000000000000000 ) ) ;
#86154=AXIS2_PLACEMENT_3D ( 'NONE', #15456, #36303, #97504 ) ;
#86160=AXIS2_PLACEMENT_3D ( 'NONE', #64706, #223765, #142935 ) ;
#86168=VERTEX_POINT ( 'NONE', #244209 ) ;
#86209=CARTESIAN_POINT ( 'NONE',  ( 20.94999999999999929, -4.254329952141543636, -236.2118329068271976 ) ) ;
#86252=CARTESIAN_POINT ( 'NONE',  ( 21.05543885634738643, 11.16761608078845924, -211.0378151740945611 ) ) ;
#86320=CIRCLE ( 'NONE', #169620, 0.5000000000000076605 ) ;
#86327=ORIENTED_EDGE ( 'NONE', *, *, #134985, .F. ) ;
#86348=VECTOR ( 'NONE', #45019, 1000.000000000000227 ) ;
#86371=ORIENTED_EDGE ( 'NONE', *, *, #43147, .T. ) ;
#86372=VERTEX_POINT ( 'NONE', #191679 ) ;
#86386=EDGE_LOOP ( 'NONE', ( #184650, #84731, #223155, #241095 ) ) ;
#86393=VERTEX_POINT ( 'NONE', #162802 ) ;
#86411=EDGE_CURVE ( 'NONE', #212886, #196267, #130338, .T. ) ;
#86442=FACE_OUTER_BOUND ( 'NONE', #257255, .T. ) ;
#86471=DIRECTION ( 'NONE',  ( 0.000000000000000000, 0.4599910535713788717, -0.8879235499941945386 ) ) ;
#86506=AXIS2_PLACEMENT_3D ( 'NONE', #163763, #69807, #88034 ) ;
#86508=EDGE_CURVE ( 'NONE', #52291, #23148, #22232, .T. ) ;
#86514=ORIENTED_EDGE ( 'NONE', *, *, #72089, .T. ) ;
#86540=CARTESIAN_POINT ( 'NONE',  ( 21.00023020733502577, -1.359983335743155886, -194.7555100259054086 ) ) ;
#86571=ORIENTED_EDGE ( 'NONE', *, *, #116960, .T. ) ;
#86631=EDGE_CURVE ( 'NONE', #96897, #254455, #68178, .T. ) ;
#86674=AXIS2_PLACEMENT_3D ( 'NONE', #159522, #241612, #257267 ) ;
#86691=DIRECTION ( 'NONE',  ( 3.697785493223492838E-32, -0.2128009952263605065, 0.9770955615653315052 ) ) ;
#86765=EDGE_CURVE ( 'NONE', #198700, #125678, #51385, .T. ) ;
#86775=CARTESIAN_POINT ( 'NONE',  ( -18.43569575749025446, -7.817436562502987130, -209.8389866834998827 ) ) ;
#86835=CARTESIAN_POINT ( 'NONE',  ( -20.54999999999999716, -6.488386256076843495, -212.2361678873109838 ) ) ;
#86842=CARTESIAN_POINT ( 'NONE',  ( 21.14999999999999503, 11.38316329224760892, -198.5208684056144079 ) ) ;
#86867=DIRECTION ( 'NONE',  ( -0.000000000000000000, -0.2128009952263603677, 0.9770955615653313941 ) ) ;
#86893=CARTESIAN_POINT ( 'NONE',  ( 21.06277459767474980, 11.26665768069844553, -211.0363194868302799 ) ) ;
#86932=DIRECTION ( 'NONE',  ( 1.000000000000000000, -0.000000000000000000, -0.000000000000000000 ) ) ;
#87002=ORIENTED_EDGE ( 'NONE', *, *, #16392, .F. ) ;
#87021=DIRECTION ( 'NONE',  ( 1.000000000000000000, 0.000000000000000000, 0.000000000000000000 ) ) ;
#87023=DIRECTION ( 'NONE',  ( 0.000000000000000000, 0.2128009952263485993, -0.9770955615653341697 ) ) ;
#87040=EDGE_CURVE ( 'NONE', #80924, #90864, #183327, .T. ) ;
#87043=VERTEX_POINT ( 'NONE', #5941 ) ;
#87066=ORIENTED_EDGE ( 'NONE', *, *, #228883, .T. ) ;
#87071=ADVANCED_FACE ( 'NONE', ( #247129 ), #45093, .T. ) ;
#87073=DIRECTION ( 'NONE',  ( 0.000000000000000000, -0.2128009952263485993, 0.9770955615653341697 ) ) ;
#87110=DIRECTION ( 'NONE',  ( -0.000000000000000000, -0.9984213852963228497, -0.05616704890745022327 ) ) ;
#87112=EDGE_CURVE ( 'NONE', #257455, #87436, #73675, .T. ) ;
#87135=DIRECTION ( 'NONE',  ( 0.000000000000000000, 0.2128009952263603677, -0.9770955615653313941 ) ) ;
#87212=ORIENTED_EDGE ( 'NONE', *, *, #252110, .F. ) ;
#87222=EDGE_CURVE ( 'NONE', #89391, #77509, #84888, .T. ) ;
#87224=VERTEX_POINT ( 'NONE', #102160 ) ;
#87225=CARTESIAN_POINT ( 'NONE',  ( -20.94999999999999929, 7.128833340094563376, -233.7327013124401276 ) ) ;
#87227=ADVANCED_FACE ( 'NONE', ( #82592 ), #117896, .T. ) ;
#87229=LINE ( 'NONE', #148515, #112069 ) ;
#87230=DIRECTION ( 'NONE',  ( 0.000000000000000000, -0.2128009952263605065, 0.9770955615653315052 ) ) ;
#87237=CARTESIAN_POINT ( 'NONE',  ( 18.44206774312973351, -0.7347395580569413553, -242.2268588646078626 ) ) ;
#87239=LINE ( 'NONE', #242470, #176946 ) ;
#87253=PLANE ( 'NONE',  #214926 ) ;
#87256=ORIENTED_EDGE ( 'NONE', *, *, #102025, .T. ) ;
#87272=CIRCLE ( 'NONE', #133093, 0.5000000000000007772 ) ;
#87307=CARTESIAN_POINT ( 'NONE',  ( 21.97500000000000497, 12.15477401631902232, -210.9923204818763622 ) ) ;
#87340=CARTESIAN_POINT ( 'NONE',  ( -21.05000000000000426, -1.476035864388226537, -194.6925666612220027 ) ) ;
#87352=VERTEX_POINT ( 'NONE', #103456 ) ;
#87380=CARTESIAN_POINT ( 'NONE',  ( -20.54999999999999716, 11.60596396992030144, -220.2204734678737168 ) ) ;
#87432=AXIS2_PLACEMENT_3D ( 'NONE', #95905, #55467, #97153 ) ;
#87436=VERTEX_POINT ( 'NONE', #34252 ) ;
#87447=CARTESIAN_POINT ( 'NONE',  ( 21.05000000000000071, 11.90759680182680924, -206.0382519879416918 ) ) ;
#87456=ORIENTED_EDGE ( 'NONE', *, *, #195356, .T. ) ;
#87463=DIRECTION ( 'NONE',  ( 0.000000000000000000, -0.2128009952263603954, 0.9770955615653315052 ) ) ;
#87466=DIRECTION ( 'NONE',  ( 0.000000000000000000, 0.2128009952263485993, -0.9770955615653341697 ) ) ;
#87473=ORIENTED_EDGE ( 'NONE', *, *, #201813, .T. ) ;
#87474=DIRECTION ( 'NONE',  ( 1.000000000000000000, 0.000000000000000000, 0.000000000000000000 ) ) ;
#87490=CARTESIAN_POINT ( 'NONE',  ( -23.25000000000000000, -11.38316329222462464, -203.4791315943886048 ) ) ;
#87497=CARTESIAN_POINT ( 'NONE',  ( 21.14999999999999858, 13.07482039728799528, -210.6896000549707537 ) ) ;
#87505=LINE ( 'NONE', #246590, #127370 ) ;
#87542=DIRECTION ( 'NONE',  ( 1.000000000000000000, 0.000000000000000000, 0.000000000000000000 ) ) ;
#87560=CARTESIAN_POINT ( 'NONE',  ( -18.50000000000000000, 8.882751598337863541, -187.0399955572217721 ) ) ;
#87563=EDGE_CURVE ( 'NONE', #110507, #165216, #189449, .T. ) ;
#87578=CARTESIAN_POINT ( 'NONE',  ( -21.64999999999999858, 11.70367352607683564, -220.1991933683510467 ) ) ;
#87631=CARTESIAN_POINT ( 'NONE',  ( 18.59999999999999787, -0.7124699236739290287, -242.4838055749970351 ) ) ;
#87642=ORIENTED_EDGE ( 'NONE', *, *, #144235, .F. ) ;
#87647=DIRECTION ( 'NONE',  ( 0.000000000000000000, 0.06835365183351375939, -0.9976611540402997580 ) ) ;
#87650=AXIS2_PLACEMENT_3D ( 'NONE', #23818, #85010, #125463 ) ;
#87651=AXIS2_PLACEMENT_3D ( 'NONE', #145833, #105402, #68899 ) ;
#87659=CYLINDRICAL_SURFACE ( 'NONE', #23157, 4.049999999999995381 ) ;
#87690=ADVANCED_FACE ( 'NONE', ( #48338 ), #207437, .T. ) ;
#87735=CARTESIAN_POINT ( 'NONE',  ( 20.85000000000000142, 14.86477715130881272, -235.7932433709592601 ) ) ;
#87740=EDGE_CURVE ( 'NONE', #211554, #252276, #23446, .T. ) ;
#87767=DIRECTION ( 'NONE',  ( 1.000000000000000000, 0.000000000000000000, 0.000000000000000000 ) ) ;
#87773=ORIENTED_EDGE ( 'NONE', *, *, #240521, .F. ) ;
#87823=CYLINDRICAL_SURFACE ( 'NONE', #192059, 0.09999999999999939493 ) ;
#87837=ORIENTED_EDGE ( 'NONE', *, *, #210687, .T. ) ;
#87847=EDGE_LOOP ( 'NONE', ( #7044, #134411, #133219, #32108 ) ) ;
#87921=DIRECTION ( 'NONE',  ( 0.000000000000000000, 0.2965989261549202283, 0.9550021345545507412 ) ) ;
#87923=ADVANCED_FACE ( 'NONE', ( #255476 ), #23036, .F. ) ;
#87929=EDGE_CURVE ( 'NONE', #224443, #256147, #19311, .T. ) ;
#87936=CARTESIAN_POINT ( 'NONE',  ( -20.54999999999999716, 7.368416211812038874, -223.5546256078887097 ) ) ;
#87949=DIRECTION ( 'NONE',  ( 0.000000000000000000, 0.2128009952263403282, -0.9770955615653358350 ) ) ;
#87998=DIRECTION ( 'NONE',  ( 0.000000000000000000, 0.5795995782408065455, 0.8149014228132623883 ) ) ;
#88005=ORIENTED_EDGE ( 'NONE', *, *, #201811, .F. ) ;
#88019=DIRECTION ( 'NONE',  ( 1.000000000000000000, 0.000000000000000000, 0.000000000000000000 ) ) ;
#88020=DIRECTION ( 'NONE',  ( 0.000000000000000000, -0.2128009952263604232, 0.9770955615653316162 ) ) ;
#88034=DIRECTION ( 'NONE',  ( -1.000000000000000000, 0.000000000000000000, 0.000000000000000000 ) ) ;
#88070=LINE ( 'NONE', #208071, #23207 ) ;
#88076=SPHERICAL_SURFACE ( 'NONE', #242201, 0.1000000000000000056 ) ;
#88098=DIRECTION ( 'NONE',  ( 1.000000000000000000, 0.000000000000000000, 0.000000000000000000 ) ) ;
#88101=LINE ( 'NONE', #167701, #200923 ) ;
#88102=FACE_OUTER_BOUND ( 'NONE', #9653, .T. ) ;
#88126=CARTESIAN_POINT ( 'NONE',  ( -21.05000000000000071, -0.9150442794618510733, -196.7984890852706030 ) ) ;
#88127=ADVANCED_FACE ( 'NONE', ( #68562 ), #148097, .T. ) ;
#88138=CIRCLE ( 'NONE', #179778, 0.1000000000000055844 ) ;
#88216=ORIENTED_EDGE ( 'NONE', *, *, #47606, .F. ) ;
#88226=DIRECTION ( 'NONE',  ( 1.000000000000000000, 0.000000000000000000, 0.000000000000000000 ) ) ;
#88242=ORIENTED_EDGE ( 'NONE', *, *, #190179, .T. ) ;
#88245=VERTEX_POINT ( 'NONE', #75000 ) ;
#88300=DIRECTION ( 'NONE',  ( 1.000000000000000000, 0.000000000000000000, 0.000000000000000000 ) ) ;
#88376=ORIENTED_EDGE ( 'NONE', *, *, #164431, .F. ) ;
#88416=CARTESIAN_POINT ( 'NONE',  ( 21.14999999999999858, 8.985508020264692419, -211.4778645542876347 ) ) ;
#88450=CIRCLE ( 'NONE', #46771, 0.1000000000000055844 ) ;
#88472=CARTESIAN_POINT ( 'NONE',  ( 21.05000000000000426, -1.300211140951535116, -194.8661069862146178 ) ) ;
#88474=CARTESIAN_POINT ( 'NONE',  ( -21.14999999999999858, -2.576749817950532595, -189.6385361693310756 ) ) ;
#88485=CARTESIAN_POINT ( 'NONE',  ( -21.14999999999999858, 6.390846877240202950, -199.6081416912452653 ) ) ;
#88491=DIRECTION ( 'NONE',  ( -1.000000000000000000, -7.136802563874199107E-16, -1.554319503706929991E-16 ) ) ;
#88496=CARTESIAN_POINT ( 'NONE',  ( -18.50596464788227635, 18.37039103902859694, -236.9176190769589141 ) ) ;
#88497=ADVANCED_FACE ( 'NONE', ( #229892 ), #231195, .F. ) ;
#88513=AXIS2_PLACEMENT_3D ( 'NONE', #174681, #254145, #75551 ) ;
#88544=DIRECTION ( 'NONE',  ( -0.000000000000000000, 0.9770955615653313941, 0.2128009952263603954 ) ) ;
#88550=CARTESIAN_POINT ( 'NONE',  ( -20.94999999999999929, -10.72348020702290583, -206.5081278352411402 ) ) ;
#88593=CARTESIAN_POINT ( 'NONE',  ( 23.24999999999999645, 1.148907358139439339E-11, -201.0000000000015064 ) ) ;
#88606=ORIENTED_EDGE ( 'NONE', *, *, #66657, .T. ) ;
#88610=ORIENTED_EDGE ( 'NONE', *, *, #8157, .T. ) ;
#88612=VECTOR ( 'NONE', #131119, 1000.000000000000227 ) ;
#88615=CARTESIAN_POINT ( 'NONE',  ( -21.04999999999999716, -1.448645706476685335, -194.7513245572836809 ) ) ;
#88617=CARTESIAN_POINT ( 'NONE',  ( 20.94999999999999929, -3.770473190032740174, -225.9805569534692324 ) ) ;
#88619=EDGE_LOOP ( 'NONE', ( #18016, #157721, #177555, #175563 ) ) ;
#88628=ORIENTED_EDGE ( 'NONE', *, *, #77324, .F. ) ;
#88652=VECTOR ( 'NONE', #249486, 1000.000000000000000 ) ;
#88719=DIRECTION ( 'NONE',  ( 0.000000000000000000, -0.2128009952263604232, 0.9770955615653316162 ) ) ;
#88748=PLANE ( 'NONE',  #94476 ) ;
#88752=ORIENTED_EDGE ( 'NONE', *, *, #252105, .T. ) ;
#88763=DIRECTION ( 'NONE',  ( 0.000000000000000000, -0.6728388485993130885, 0.7397890806274115549 ) ) ;
#88768=DIRECTION ( 'NONE',  ( 0.000000000000000000, -0.2128009952263602289, 0.9770955615653315052 ) ) ;
#88771=EDGE_CURVE ( 'NONE', #17857, #83361, #212459, .T. ) ;
#88809=DIRECTION ( 'NONE',  ( 1.000000000000000000, 0.000000000000000000, 0.000000000000000000 ) ) ;
#88820=AXIS2_PLACEMENT_3D ( 'NONE', #69617, #52595, #13493 ) ;
#88828=ORIENTED_EDGE ( 'NONE', *, *, #240711, .T. ) ;
#88841=ORIENTED_EDGE ( 'NONE', *, *, #65571, .T. ) ;
#88857=FACE_OUTER_BOUND ( 'NONE', #91140, .T. ) ;
#88861=CARTESIAN_POINT ( 'NONE',  ( -18.59999999999999787, 7.675662554762638479, -241.7139905447625381 ) ) ;
#88876=AXIS2_PLACEMENT_3D ( 'NONE', #49572, #148688, #103100 ) ;
#88884=CARTESIAN_POINT ( 'NONE',  ( 18.50000000000062883, 15.26868426882366592, -222.9405159379593613 ) ) ;
#88934=CIRCLE ( 'NONE', #39091, 0.09999999999999939493 ) ;
#88942=DIRECTION ( 'NONE',  ( 1.000000000000000000, 0.000000000000000000, 0.000000000000000000 ) ) ;
#88945=DIRECTION ( 'NONE',  ( -1.000000000000000000, -2.885090398161910739E-16, -6.283419270304611573E-17 ) ) ;
#88970=AXIS2_PLACEMENT_3D ( 'NONE', #71551, #49402, #70276 ) ;
#88973=VERTEX_POINT ( 'NONE', #18085 ) ;
#89009=CIRCLE ( 'NONE', #14036, 12.87499999999999822 ) ;
#89031=EDGE_LOOP ( 'NONE', ( #197554, #198998, #90161, #194548, #186418 ) ) ;
#89033=DIRECTION ( 'NONE',  ( 0.000000000000000000, 0.2128009952263568982, -0.9770955615653323934 ) ) ;
#89055=CIRCLE ( 'NONE', #243179, 0.1000000000000054040 ) ;
#89059=CARTESIAN_POINT ( 'NONE',  ( -21.44999999999999929, 9.614325556249161409, -211.5456030694648746 ) ) ;
#89100=DIRECTION ( 'NONE',  ( -0.000000000000000000, -0.2128009952263607285, 0.9770955615653316162 ) ) ;
#89128=VERTEX_POINT ( 'NONE', #122501 ) ;
#89133=ORIENTED_EDGE ( 'NONE', *, *, #187616, .T. ) ;
#89151=ORIENTED_EDGE ( 'NONE', *, *, #206914, .F. ) ;
#89157=CARTESIAN_POINT ( 'NONE',  ( 22.39999999999999503, 11.50215294792677767, -198.5972978622482970 ) ) ;
#89165=EDGE_CURVE ( 'NONE', #256420, #202021, #143254, .T. ) ;
#89174=DIRECTION ( 'NONE',  ( 0.000000000000000000, 0.2128009952263485993, -0.9770955615653341697 ) ) ;
#89176=ADVANCED_FACE ( 'NONE', ( #46783 ), #27278, .T. ) ;
#89187=AXIS2_PLACEMENT_3D ( 'NONE', #24199, #3308, #219801 ) ;
#89190=FACE_OUTER_BOUND ( 'NONE', #127482, .T. ) ;
#89208=ADVANCED_FACE ( 'NONE', ( #106761 ), #114011, .F. ) ;
#89213=EDGE_CURVE ( 'NONE', #29274, #164555, #45518, .T. ) ;
#89222=VERTEX_POINT ( 'NONE', #170654 ) ;
#89238=DIRECTION ( 'NONE',  ( 1.000000000000000000, 0.000000000000000000, 0.000000000000000000 ) ) ;
#89239=ORIENTED_EDGE ( 'NONE', *, *, #38869, .F. ) ;
#89255=CIRCLE ( 'NONE', #31057, 0.1000000000000054040 ) ;
#89279=EDGE_CURVE ( 'NONE', #117008, #188047, #48080, .T. ) ;
#89378=LINE ( 'NONE', #48978, #121213 ) ;
#89391=VERTEX_POINT ( 'NONE', #12834 ) ;
#89394=DIRECTION ( 'NONE',  ( -1.836970198721029934E-16, 0.9770955615653316162, 0.2128009952263604232 ) ) ;
#89406=EDGE_CURVE ( 'NONE', #191384, #135942, #34984, .T. ) ;
#89407=ORIENTED_EDGE ( 'NONE', *, *, #101559, .T. ) ;
#89413=DIRECTION ( 'NONE',  ( -1.000000000000000000, 0.000000000000000000, 0.000000000000000000 ) ) ;
#89417=ADVANCED_FACE ( 'NONE', ( #122191 ), #143000, .T. ) ;
#89421=FACE_OUTER_BOUND ( 'NONE', #229161, .T. ) ;
#89428=FACE_OUTER_BOUND ( 'NONE', #15166, .T. ) ;
#89443=CARTESIAN_POINT ( 'NONE',  ( -20.85000000106584750, 17.15319076756266981, -224.5445635972164951 ) ) ;
#89445=ORIENTED_EDGE ( 'NONE', *, *, #6655, .F. ) ;
#89488=DIRECTION ( 'NONE',  ( -1.836970198721029934E-16, 0.9770955615653316162, 0.2128009952263604232 ) ) ;
#89490=DIRECTION ( 'NONE',  ( -0.000000000000000000, 0.9770955615653313941, 0.2128009952263603677 ) ) ;
#89518=CARTESIAN_POINT ( 'NONE',  ( -18.59999999999999787, 16.00289399696429271, -219.2628689893550700 ) ) ;
#89532=DIRECTION ( 'NONE',  ( 0.000000000000000000, 0.2128009952263604787, -0.9770955615653313941 ) ) ;
#89540=EDGE_LOOP ( 'NONE', ( #242869, #249428, #188796, #141016, #221748, #217134 ) ) ;
#89543=ORIENTED_EDGE ( 'NONE', *, *, #24231, .F. ) ;
#89546=VERTEX_POINT ( 'NONE', #109016 ) ;
#89608=DIRECTION ( 'NONE',  ( 0.000000000000000000, -0.9550021345545507412, 0.2965989261549202283 ) ) ;
#89619=CIRCLE ( 'NONE', #222901, 0.1000000000000030170 ) ;
#89620=CARTESIAN_POINT ( 'NONE',  ( -18.59999999999999787, -6.696875742858878766, -214.8933205276707099 ) ) ;
#89660=ADVANCED_FACE ( 'NONE', ( #163883 ), #243402, .F. ) ;
#89699=CYLINDRICAL_SURFACE ( 'NONE', #156903, 0.5000000000000009992 ) ;
#89719=ORIENTED_EDGE ( 'NONE', *, *, #41460, .T. ) ;
#89724=EDGE_CURVE ( 'NONE', #46709, #182231, #89255, .T. ) ;
#89733=DIRECTION ( 'NONE',  ( 0.000000000000000000, 0.2128009952263613391, -0.9770955615653312831 ) ) ;
#89742=AXIS2_PLACEMENT_3D ( 'NONE', #109685, #169718, #249221 ) ;
#89745=ORIENTED_EDGE ( 'NONE', *, *, #120084, .T. ) ;
#89812=VERTEX_POINT ( 'NONE', #81124 ) ;
#89816=CARTESIAN_POINT ( 'NONE',  ( 20.85000000000000142, 7.128833340094563376, -233.7327013124401276 ) ) ;
#89819=LINE ( 'NONE', #110682, #164183 ) ;
#89844=DIRECTION ( 'NONE',  ( 0.000000000000000000, -0.2128009952263604232, 0.9770955615653316162 ) ) ;
#89846=EDGE_CURVE ( 'NONE', #231604, #87043, #1383, .T. ) ;
#89884=ORIENTED_EDGE ( 'NONE', *, *, #140979, .F. ) ;
#89946=EDGE_CURVE ( 'NONE', #39697, #175208, #101899, .T. ) ;
#89952=CARTESIAN_POINT ( 'NONE',  ( 20.95512820512820085, 11.26905698129511357, -211.0318809171001249 ) ) ;
#89965=EDGE_LOOP ( 'NONE', ( #52367, #190635, #166290, #15792 ) ) ;
#89990=CIRCLE ( 'NONE', #235729, 0.1000000000000055844 ) ;
#89998=AXIS2_PLACEMENT_3D ( 'NONE', #9562, #249478, #185643 ) ;
#90016=DIRECTION ( 'NONE',  ( 1.000000000000000000, 2.885090398161910739E-16, 6.283419270304611573E-17 ) ) ;
#90026=DIRECTION ( 'NONE',  ( 0.000000000000000000, 0.7397890806274222131, 0.6728388485993012091 ) ) ;
#90028=EDGE_CURVE ( 'NONE', #172105, #138363, #193522, .T. ) ;
#90054=DIRECTION ( 'NONE',  ( 0.000000000000000000, 0.2128009952263603677, -0.9770955615653313941 ) ) ;
#90132=ORIENTED_EDGE ( 'NONE', *, *, #524, .T. ) ;
#90159=DIRECTION ( 'NONE',  ( -0.000000000000000000, 0.9770955615653313941, 0.2128009952263603954 ) ) ;
#90161=ORIENTED_EDGE ( 'NONE', *, *, #9559, .F. ) ;
#90165=CIRCLE ( 'NONE', #65057, 0.09999999999999939493 ) ;
#90177=FACE_OUTER_BOUND ( 'NONE', #236343, .T. ) ;
#90186=VECTOR ( 'NONE', #14998, 1000.000000000000000 ) ;
#90190=ADVANCED_FACE ( 'NONE', ( #15761 ), #95261, .F. ) ;
#90193=CARTESIAN_POINT ( 'NONE',  ( -20.54999999999999716, 11.48697431424113446, -220.1440440112397994 ) ) ;
#90201=DIRECTION ( 'NONE',  ( 0.000000000000000000, -0.6626775042260681925, -0.7489048840758811831 ) ) ;
#90217=ADVANCED_FACE ( 'NONE', ( #104227 ), #59962, .T. ) ;
#90219=ORIENTED_EDGE ( 'NONE', *, *, #254605, .T. ) ;
#90244=EDGE_CURVE ( 'NONE', #27420, #237840, #159816, .T. ) ;
#90270=EDGE_CURVE ( 'NONE', #187404, #16838, #89055, .T. ) ;
#90289=EDGE_CURVE ( 'NONE', #149075, #123919, #155740, .T. ) ;
#90325=EDGE_CURVE ( 'NONE', #135756, #227551, #130761, .T. ) ;
#90332=EDGE_CURVE ( 'NONE', #31299, #7157, #255612, .T. ) ;
#90368=ORIENTED_EDGE ( 'NONE', *, *, #223848, .T. ) ;
#90400=ORIENTED_EDGE ( 'NONE', *, *, #84968, .F. ) ;
#90406=CARTESIAN_POINT ( 'NONE',  ( 18.43579564894472966, -7.817436314305575173, -209.8389869030123407 ) ) ;
#90432=FACE_OUTER_BOUND ( 'NONE', #214760, .T. ) ;
#90502=AXIS2_PLACEMENT_3D ( 'NONE', #81568, #101108, #257610 ) ;
#90511=CARTESIAN_POINT ( 'NONE',  ( -22.48660254037843487, 11.37252324248628632, -198.4720136275361710 ) ) ;
#90526=EDGE_LOOP ( 'NONE', ( #198124, #256001, #250692, #15982 ) ) ;
#90532=CARTESIAN_POINT ( 'NONE',  ( 21.05000000000000071, 13.96869538424789070, -210.3925794786331949 ) ) ;
#90611=CARTESIAN_POINT ( 'NONE',  ( -21.05000000000000071, 2.838478681111047841, -208.5693404029859437 ) ) ;
#90629=ORIENTED_EDGE ( 'NONE', *, *, #166810, .F. ) ;
#90641=ADVANCED_FACE ( 'NONE', ( #102619 ), #120960, .F. ) ;
#90670=CARTESIAN_POINT ( 'NONE',  ( -18.50000000000000000, 11.40444339177023458, -198.6185779617709670 ) ) ;
#90682=CARTESIAN_POINT ( 'NONE',  ( 23.25000000000000000, -4.356730526971940520, -226.1082375506050539 ) ) ;
#90688=CARTESIAN_POINT ( 'NONE',  ( -20.64999999999999858, 11.48697431424113446, -220.1440440112397994 ) ) ;
#90710=DIRECTION ( 'NONE',  ( 0.000000000000000000, -0.2128009952263485993, 0.9770955615653341697 ) ) ;
#90749=EDGE_LOOP ( 'NONE', ( #134433, #16934, #161383 ) ) ;
#90759=ORIENTED_EDGE ( 'NONE', *, *, #196399, .F. ) ;
#90772=CARTESIAN_POINT ( 'NONE',  ( -22.49999999999999289, 11.45898712536581066, -198.4011321578509808 ) ) ;
#90837=DIRECTION ( 'NONE',  ( -0.000000000000000000, -0.9550021345545507412, 0.2965989261549202838 ) ) ;
#90857=ORIENTED_EDGE ( 'NONE', *, *, #214227, .F. ) ;
#90864=VERTEX_POINT ( 'NONE', #174224 ) ;
#90873=ADVANCED_FACE ( 'NONE', ( #75111 ), #116770, .T. ) ;
#90888=DIRECTION ( 'NONE',  ( 0.000000000000000000, 0.2128009952263403282, -0.9770955615653358350 ) ) ;
#90928=ORIENTED_EDGE ( 'NONE', *, *, #229534, .F. ) ;
#90929=FACE_OUTER_BOUND ( 'NONE', #249776, .T. ) ;
#90944=VERTEX_POINT ( 'NONE', #138862 ) ;
#90949=DIRECTION ( 'NONE',  ( 0.000000000000000000, 0.04908394489122551441, 0.9987946567507833828 ) ) ;
#90952=FACE_OUTER_BOUND ( 'NONE', #177549, .T. ) ;
#90965=EDGE_LOOP ( 'NONE', ( #182079, #19272, #251202, #160835 ) ) ;
#90975=CARTESIAN_POINT ( 'NONE',  ( 18.52928932188133970, 15.31067260432008403, -222.9956721508274029 ) ) ;
#90977=ORIENTED_EDGE ( 'NONE', *, *, #149438, .F. ) ;
#90994=DIRECTION ( 'NONE',  ( 1.000000000000000000, 0.000000000000000000, 0.000000000000000000 ) ) ;
#91010=AXIS2_PLACEMENT_3D ( 'NONE', #117480, #217829, #236133 ) ;
#91026=ORIENTED_EDGE ( 'NONE', *, *, #232511, .F. ) ;
#91033=DIRECTION ( 'NONE',  ( -0.7071067811865474617, -0.6909108974501236844, -0.1504730267678055788 ) ) ;
#91041=CARTESIAN_POINT ( 'NONE',  ( 21.05000000000000071, 2.817198581588411077, -208.4716308468294130 ) ) ;
#91049=ORIENTED_EDGE ( 'NONE', *, *, #126555, .T. ) ;
#91085=ORIENTED_EDGE ( 'NONE', *, *, #174180, .T. ) ;
#91087=CIRCLE ( 'NONE', #103700, 0.1000000000000050293 ) ;
#91114=DIRECTION ( 'NONE',  ( 1.000000000000000000, 0.000000000000000000, 0.000000000000000000 ) ) ;
#91140=EDGE_LOOP ( 'NONE', ( #117680, #59841, #209914, #174985 ) ) ;
#91153=LINE ( 'NONE', #250228, #7454 ) ;
#91163=EDGE_CURVE ( 'NONE', #107334, #258000, #246987, .T. ) ;
#91164=CARTESIAN_POINT ( 'NONE',  ( -23.25000000000000000, 0.8618440306782485516, -204.9572370243411115 ) ) ;
#91190=ORIENTED_EDGE ( 'NONE', *, *, #214708, .F. ) ;
#91198=ORIENTED_EDGE ( 'NONE', *, *, #204368, .F. ) ;
#91272=DIRECTION ( 'NONE',  ( 0.000000000000000000, -0.2128009952263604232, 0.9770955615653316162 ) ) ;
#91276=LINE ( 'NONE', #134227, #34754 ) ;
#91290=ORIENTED_EDGE ( 'NONE', *, *, #226265, .F. ) ;
#91296=DIRECTION ( 'NONE',  ( -1.000000000000000000, 0.000000000000000000, 0.000000000000000000 ) ) ;
#91325=DIRECTION ( 'NONE',  ( 1.000000000000000000, 3.190570557967288949E-16, 6.948722487160392945E-17 ) ) ;
#91360=ADVANCED_FACE ( 'NONE', ( #78617 ), #62922, .T. ) ;
#91368=ORIENTED_EDGE ( 'NONE', *, *, #125671, .F. ) ;
#91391=CARTESIAN_POINT ( 'NONE',  ( -21.09316766718152891, -1.317210868494001375, -194.7673961808032459 ) ) ;
#91415=CARTESIAN_POINT ( 'NONE',  ( 20.84999999999998721, 18.60970618848720903, -231.2322896185303875 ) ) ;
#91417=ADVANCED_FACE ( 'NONE', ( #104585 ), #68775, .F. ) ;
#91428=VERTEX_POINT ( 'NONE', #229387 ) ;
#91433=DIRECTION ( 'NONE',  ( 0.000000000000000000, 0.2128009952263600346, -0.9770955615653315052 ) ) ;
#91441=DIRECTION ( 'NONE',  ( -0.000000000000000000, -0.2128009952263603677, 0.9770955615653313941 ) ) ;
#91463=DIRECTION ( 'NONE',  ( -1.000000000000000000, 0.000000000000000000, 0.000000000000000000 ) ) ;
#91469=DIRECTION ( 'NONE',  ( 0.000000000000000000, 0.2128009952263601734, -0.9770955615653315052 ) ) ;
#91486=CARTESIAN_POINT ( 'NONE',  ( 23.14999999999999503, 9.028068219309963283, -211.6732836666006961 ) ) ;
#91505=CIRCLE ( 'NONE', #24892, 0.4000000000000044631 ) ;
#91518=VERTEX_POINT ( 'NONE', #35065 ) ;
#91557=CARTESIAN_POINT ( 'NONE',  ( 20.94999999999999929, -3.664072692419559907, -226.4691047342518857 ) ) ;
#91632=CYLINDRICAL_SURFACE ( 'NONE', #140180, 0.09999999999999810429 ) ;
#91642=AXIS2_PLACEMENT_3D ( 'NONE', #35513, #133296, #234968 ) ;
#91643=ORIENTED_EDGE ( 'NONE', *, *, #107843, .T. ) ;
#91678=TOROIDAL_SURFACE ( 'NONE', #20979, 11.70000000000000639, 0.1000000000000000056 ) ;
#91702=DIRECTION ( 'NONE',  ( 2.715809747126116015E-16, -0.9770955615653309501, -0.2128009952263628102 ) ) ;
#91729=EDGE_LOOP ( 'NONE', ( #90219, #104199, #206577, #67033 ) ) ;
#91740=EDGE_CURVE ( 'NONE', #51901, #90864, #4843, .T. ) ;
#91743=DIRECTION ( 'NONE',  ( -1.000000000000000000, -1.794895427898102820E-16, -3.909090864890033875E-17 ) ) ;
#91754=CARTESIAN_POINT ( 'NONE',  ( -20.87600722750343252, 18.41291479239798079, -236.9963116028434058 ) ) ;
#91766=ORIENTED_EDGE ( 'NONE', *, *, #18418, .F. ) ;
#91767=VECTOR ( 'NONE', #192304, 1000.000000000000227 ) ;
#91775=CARTESIAN_POINT ( 'NONE',  ( 20.94999999999999929, 12.10919762232931163, -206.2073353557311748 ) ) ;
#91842=ORIENTED_EDGE ( 'NONE', *, *, #30635, .T. ) ;
#91845=CARTESIAN_POINT ( 'NONE',  ( -18.59999996769639097, -7.620584189787890317, -210.0095198070081324 ) ) ;
#91861=AXIS2_PLACEMENT_3D ( 'NONE', #130814, #112552, #9577 ) ;
#91871=DIRECTION ( 'NONE',  ( 0.000000000000000000, -0.2044060691543873876, 0.9788861828082220384 ) ) ;
#91872=DIRECTION ( 'NONE',  ( 0.000000000000000000, -0.2128009952263603677, 0.9770955615653313941 ) ) ;
#91894=CARTESIAN_POINT ( 'NONE',  ( 21.05000000000000071, -7.079251802663310222, -212.6676826711374417 ) ) ;
#91904=LINE ( 'NONE', #90611, #66563 ) ;
#91906=DIRECTION ( 'NONE',  ( -1.000000000000000000, -0.000000000000000000, -0.000000000000000000 ) ) ;
#91933=EDGE_LOOP ( 'NONE', ( #74466, #34348, #25252, #137761 ) ) ;
#91945=DIRECTION ( 'NONE',  ( 0.000000000000000000, 0.2128009952263568427, -0.9770955615653322823 ) ) ;
#91958=ORIENTED_EDGE ( 'NONE', *, *, #66943, .T. ) ;
#91971=ADVANCED_FACE ( 'NONE', ( #231643 ), #193861, .F. ) ;
#91999=AXIS2_PLACEMENT_3D ( 'NONE', #59525, #236909, #139057 ) ;
#92003=ORIENTED_EDGE ( 'NONE', *, *, #151325, .T. ) ;
#92004=ORIENTED_EDGE ( 'NONE', *, *, #72104, .F. ) ;
#92005=AXIS2_PLACEMENT_3D ( 'NONE', #115877, #197964, #195433 ) ;
#92021=EDGE_CURVE ( 'NONE', #176927, #163980, #202241, .T. ) ;
#92063=CARTESIAN_POINT ( 'NONE',  ( 21.05000000000000071, -4.871452838297987142, -233.3782557782877518 ) ) ;
#92083=DIRECTION ( 'NONE',  ( 0.000000000000000000, -0.9770955615653313941, -0.2128009952263606730 ) ) ;
#92116=CARTESIAN_POINT ( 'NONE',  ( 18.49999999999999645, 4.064367954407507533, -211.9684786640956418 ) ) ;
#92147=CARTESIAN_POINT ( 'NONE',  ( -18.59999999999999787, 0.4810385098657082859, -209.0827657365571213 ) ) ;
#92164=CIRCLE ( 'NONE', #246305, 0.09999999999999213685 ) ;
#92185=VERTEX_POINT ( 'NONE', #90511 ) ;
#92196=ORIENTED_EDGE ( 'NONE', *, *, #94937, .T. ) ;
#92206=ORIENTED_EDGE ( 'NONE', *, *, #101421, .T. ) ;
#92257=DIRECTION ( 'NONE',  ( 1.000000000000000000, 0.000000000000000000, 0.000000000000000000 ) ) ;
#92264=CARTESIAN_POINT ( 'NONE',  ( 20.94983749550516450, 18.35558276679135048, -236.8903279188150464 ) ) ;
#92273=CARTESIAN_POINT ( 'NONE',  ( -18.59999999999999787, 14.80545736607782814, -235.9842437978701639 ) ) ;
#92288=AXIS2_PLACEMENT_3D ( 'NONE', #233255, #211097, #74193 ) ;
#92330=ORIENTED_EDGE ( 'NONE', *, *, #167121, .T. ) ;
#92334=EDGE_LOOP ( 'NONE', ( #158483, #6973, #237357, #248587 ) ) ;
#92384=VERTEX_POINT ( 'NONE', #34440 ) ;
#92385=DIRECTION ( 'NONE',  ( 0.000000000000000000, 0.2128009952263403282, -0.9770955615653358350 ) ) ;
#92399=CIRCLE ( 'NONE', #134090, 0.09999999999999939493 ) ;
#92425=DIRECTION ( 'NONE',  ( 3.469446951953635015E-14, -0.2128009952263604232, 0.9770955615653316162 ) ) ;
#92459=CIRCLE ( 'NONE', #213082, 2.000000000000004885 ) ;
#92465=CIRCLE ( 'NONE', #154866, 0.1000000000000065004 ) ;
#92475=ORIENTED_EDGE ( 'NONE', *, *, #58441, .F. ) ;
#92512=ORIENTED_EDGE ( 'NONE', *, *, #115998, .T. ) ;
#92514=CARTESIAN_POINT ( 'NONE',  ( -2.995603634470829482E-16, -6.958851699820998604, -224.2636923771745501 ) ) ;
#92529=ORIENTED_EDGE ( 'NONE', *, *, #2264, .F. ) ;
#92531=PLANE ( 'NONE',  #34425 ) ;
#92540=FACE_OUTER_BOUND ( 'NONE', #62553, .T. ) ;
#92545=CARTESIAN_POINT ( 'NONE',  ( 21.05000000000000071, -6.438379425586758131, -212.1495692908769684 ) ) ;
#92560=CARTESIAN_POINT ( 'NONE',  ( 22.60000000000000142, 11.45898712536580177, -198.4011321578509808 ) ) ;
#92575=CARTESIAN_POINT ( 'NONE',  ( 21.05000000000000071, -5.011722593499792211, -233.2041167654973322 ) ) ;
#92584=AXIS2_PLACEMENT_3D ( 'NONE', #26615, #220920, #185673 ) ;
#92594=DIRECTION ( 'NONE',  ( 0.000000000000000000, -0.2128009952263734406, 0.9770955615653287296 ) ) ;
#92597=EDGE_CURVE ( 'NONE', #6661, #232107, #223425, .T. ) ;
#92632=EDGE_CURVE ( 'NONE', #179904, #75051, #44393, .T. ) ;
#92638=CIRCLE ( 'NONE', #100971, 0.1000000000000054040 ) ;
#92685=DIRECTION ( 'NONE',  ( 0.000000000000000000, -0.9770955615653259541, -0.2128009952263860971 ) ) ;
#92703=DIRECTION ( 'NONE',  ( 0.000000000000000000, -0.2128009952263678062, 0.9770955615653298398 ) ) ;
#92727=AXIS2_PLACEMENT_3D ( 'NONE', #154970, #237046, #59658 ) ;
#92744=CARTESIAN_POINT ( 'NONE',  ( 18.49999999999999289, 15.51794587355511723, -222.9505302427970719 ) ) ;
#92768=EDGE_CURVE ( 'NONE', #11889, #171420, #7125, .T. ) ;
#92771=ORIENTED_EDGE ( 'NONE', *, *, #173940, .F. ) ;
#92797=ORIENTED_EDGE ( 'NONE', *, *, #245146, .T. ) ;
#92802=CARTESIAN_POINT ( 'NONE',  ( 18.58222699835054570, 18.41441690808118992, -236.9991004306322964 ) ) ;
#92831=AXIS2_PLACEMENT_3D ( 'NONE', #251828, #194453, #94030 ) ;
#92877=DIRECTION ( 'NONE',  ( 1.000000000000000000, 0.000000000000000000, 0.000000000000000000 ) ) ;
#92910=CARTESIAN_POINT ( 'NONE',  ( 18.60000000000001208, -7.621788160715480487, -210.0085134484000946 ) ) ;
#92919=CARTESIAN_POINT ( 'NONE',  ( 21.05000000000000071, 6.390846877240204726, -199.6081416912452653 ) ) ;
#92942=EDGE_CURVE ( 'NONE', #123636, #136369, #240217, .T. ) ;
#92949=CARTESIAN_POINT ( 'NONE',  ( 18.59999999999999076, 4.273531877263399892, -211.9976340888692050 ) ) ;
#92965=CARTESIAN_POINT ( 'NONE',  ( -21.64999999999999858, 11.68239342655420110, -220.1014838121945161 ) ) ;
#92979=VERTEX_POINT ( 'NONE', #164103 ) ;
#92997=DIRECTION ( 'NONE',  ( 0.000000000000000000, 0.9770955615653316162, 0.2128009952263597848 ) ) ;
#93012=CARTESIAN_POINT ( 'NONE',  ( -23.25000000000000000, 7.783179459866048866, -245.3643104511423019 ) ) ;
#93072=DIRECTION ( 'NONE',  ( -1.000000000000000000, 0.000000000000000000, 0.000000000000000000 ) ) ;
#93073=CIRCLE ( 'NONE', #226136, 0.1000000000000055844 ) ;
#93083=EDGE_CURVE ( 'NONE', #157859, #85747, #248562, .T. ) ;
#93086=CARTESIAN_POINT ( 'NONE',  ( 21.05000000000000071, -4.735542975717121905, -233.2463119243910796 ) ) ;
#93091=FACE_OUTER_BOUND ( 'NONE', #115643, .T. ) ;
#93095=CARTESIAN_POINT ( 'NONE',  ( -21.05000000000000071, 7.128833340094563376, -233.7327013124401276 ) ) ;
#93105=ORIENTED_EDGE ( 'NONE', *, *, #193679, .F. ) ;
#93119=CARTESIAN_POINT ( 'NONE',  ( -18.43599941264911024, -7.817436179055779810, -209.8389870226308744 ) ) ;
#93122=AXIS2_PLACEMENT_3D ( 'NONE', #180455, #254795, #197436 ) ;
#93124=EDGE_LOOP ( 'NONE', ( #191097, #162591, #79688, #11309 ) ) ;
#93156=AXIS2_PLACEMENT_3D ( 'NONE', #228052, #32450, #130211 ) ;
#93158=ORIENTED_EDGE ( 'NONE', *, *, #225082, .T. ) ;
#93176=FACE_OUTER_BOUND ( 'NONE', #238772, .T. ) ;
#93192=CIRCLE ( 'NONE', #230590, 0.3999999999999952482 ) ;
#93244=ADVANCED_FACE ( 'NONE', ( #58248 ), #159957, .F. ) ;
#93248=FACE_OUTER_BOUND ( 'NONE', #82419, .T. ) ;
#93254=DIRECTION ( 'NONE',  ( 0.000000000000000000, -0.2128009952263601456, 0.9770955615653316162 ) ) ;
#93292=CARTESIAN_POINT ( 'NONE',  ( 18.47688499308726051, -0.6931819285577012213, -242.2946892244310959 ) ) ;
#93298=LINE ( 'NONE', #69916, #229792 ) ;
#93299=AXIS2_PLACEMENT_3D ( 'NONE', #173590, #253058, #193106 ) ;
#93308=DIRECTION ( 'NONE',  ( -0.7071067811865474617, -0.6909108974501236844, -0.1504730267678055788 ) ) ;
#93318=DIRECTION ( 'NONE',  ( 0.000000000000000000, 0.2128009952263607008, -0.9770955615653315052 ) ) ;
#93389=ORIENTED_EDGE ( 'NONE', *, *, #63189, .F. ) ;
#93423=CARTESIAN_POINT ( 'NONE',  ( 20.94999999999999574, -10.82118976317943115, -206.5294079347637819 ) ) ;
#93460=CIRCLE ( 'NONE', #130883, 0.09999999999999939493 ) ;
#93461=DIRECTION ( 'NONE',  ( 0.000000000000000000, 0.2965989261549202283, 0.9550021345545507412 ) ) ;
#93505=LINE ( 'NONE', #12721, #3128 ) ;
#93516=CARTESIAN_POINT ( 'NONE',  ( -22.50000000000000000, -2.381330705637465961, -189.5959759702857923 ) ) ;
#93573=AXIS2_PLACEMENT_3D ( 'NONE', #112731, #192280, #12370 ) ;
#93575=EDGE_CURVE ( 'NONE', #94400, #365, #31999, .T. ) ;
#93585=CARTESIAN_POINT ( 'NONE',  ( 23.24999999999999645, 7.128833340094563376, -233.7327013124401276 ) ) ;
#93590=DIRECTION ( 'NONE',  ( -0.000000000000000000, 0.9770955615653313941, 0.2128009952263603677 ) ) ;
#93599=VECTOR ( 'NONE', #73977, 1000.000000000000227 ) ;
#93606=DIRECTION ( 'NONE',  ( -1.000000000000000000, -1.794895427898103559E-16, -3.909090864890002444E-17 ) ) ;
#93611=CARTESIAN_POINT ( 'NONE',  ( -18.59999999999999787, 13.63658454968486389, -219.6758818217417968 ) ) ;
#93645=VERTEX_POINT ( 'NONE', #180478 ) ;
#93664=CARTESIAN_POINT ( 'NONE',  ( -18.39999999999999858, -0.8467571797981087167, -242.2246066262668194 ) ) ;
#93690=VECTOR ( 'NONE', #29589, 1000.000000000000000 ) ;
#93729=EDGE_CURVE ( 'NONE', #73041, #48943, #232396, .T. ) ;
#93740=CARTESIAN_POINT ( 'NONE',  ( 21.05000000000000071, 9.307299318941717914, -220.9418877738490039 ) ) ;
#93762=ORIENTED_EDGE ( 'NONE', *, *, #115998, .F. ) ;
#93777=VERTEX_POINT ( 'NONE', #206454 ) ;
#93780=CARTESIAN_POINT ( 'NONE',  ( 23.14999999999999858, 7.128833340094563376, -233.7327013124401276 ) ) ;
#93786=EDGE_CURVE ( 'NONE', #24784, #137793, #201314, .T. ) ;
#93806=ORIENTED_EDGE ( 'NONE', *, *, #17941, .F. ) ;
#93841=ORIENTED_EDGE ( 'NONE', *, *, #195029, .T. ) ;
#93862=DIRECTION ( 'NONE',  ( 0.000000000000000000, -0.9342891509276819439, -0.3565161741896589742 ) ) ;
#93917=CARTESIAN_POINT ( 'NONE',  ( 22.49533356619853564, 11.36930514850300611, -198.4572374200820093 ) ) ;
#93918=CARTESIAN_POINT ( 'NONE',  ( 22.40000000000010516, -2.500503813845274870, -189.5187041743088230 ) ) ;
#93925=ORIENTED_EDGE ( 'NONE', *, *, #149064, .F. ) ;
#93934=CARTESIAN_POINT ( 'NONE',  ( 22.50000000000000000, -2.381330705637465961, -189.5959759702857923 ) ) ;
#93935=EDGE_CURVE ( 'NONE', #131400, #159106, #128499, .T. ) ;
#93936=CYLINDRICAL_SURFACE ( 'NONE', #40229, 0.5000000000000007772 ) ;
#93990=VECTOR ( 'NONE', #184721, 1000.000000000000227 ) ;
#93995=CIRCLE ( 'NONE', #248127, 4.049999999999995381 ) ;
#94011=AXIS2_PLACEMENT_3D ( 'NONE', #240641, #101075, #120724 ) ;
#94012=ORIENTED_EDGE ( 'NONE', *, *, #58408, .T. ) ;
#94023=EDGE_LOOP ( 'NONE', ( #87002, #78131, #61414, #153086 ) ) ;
#94028=AXIS2_PLACEMENT_3D ( 'NONE', #10320, #225472, #230644 ) ;
#94029=ADVANCED_FACE ( 'NONE', ( #215438 ), #95183, .T. ) ;
#94030=DIRECTION ( 'NONE',  ( 0.000000000000000000, 0.2128009952263603677, -0.9770955615653313941 ) ) ;
#94042=DIRECTION ( 'NONE',  ( 0.000000000000000000, -0.2128009952263403282, 0.9770955615653358350 ) ) ;
#94045=AXIS2_PLACEMENT_3D ( 'NONE', #178966, #18573, #42003 ) ;
#94058=DIRECTION ( 'NONE',  ( 1.000000000000000000, 0.000000000000000000, 0.000000000000000000 ) ) ;
#94068=ORIENTED_EDGE ( 'NONE', *, *, #119171, .T. ) ;
#94089=VECTOR ( 'NONE', #177010, 1000.000000000000227 ) ;
#94153=DIRECTION ( 'NONE',  ( -0.000000000000000000, -0.2128009952263604787, 0.9770955615653313941 ) ) ;
#94205=CARTESIAN_POINT ( 'NONE',  ( 21.07928932188134397, 6.162520550847358614, -199.5566553493351307 ) ) ;
#94213=ORIENTED_EDGE ( 'NONE', *, *, #75513, .F. ) ;
#94219=ORIENTED_EDGE ( 'NONE', *, *, #208760, .F. ) ;
#94228=ORIENTED_EDGE ( 'NONE', *, *, #148751, .T. ) ;
#94255=CARTESIAN_POINT ( 'NONE',  ( 18.59999999999999432, 0.5876173420563349792, -209.1618981382189588 ) ) ;
#94264=AXIS2_PLACEMENT_3D ( 'NONE', #121671, #237740, #98188 ) ;
#94282=ORIENTED_EDGE ( 'NONE', *, *, #58408, .F. ) ;
#94302=CIRCLE ( 'NONE', #135987, 0.2000000000000010658 ) ;
#94327=ORIENTED_EDGE ( 'NONE', *, *, #209234, .T. ) ;
#94328=DIRECTION ( 'NONE',  ( -1.000000000000000000, 0.000000000000000000, 0.000000000000000000 ) ) ;
#94353=CARTESIAN_POINT ( 'NONE',  ( -21.44999999999999929, 9.809744668562228043, -211.5030428704195913 ) ) ;
#94375=AXIS2_PLACEMENT_3D ( 'NONE', #78934, #222292, #61979 ) ;
#94398=CARTESIAN_POINT ( 'NONE',  ( 23.14999999999999858, 9.374458193048763377, -220.5475659691911119 ) ) ;
#94400=VERTEX_POINT ( 'NONE', #234707 ) ;
#94476=AXIS2_PLACEMENT_3D ( 'NONE', #108344, #129191, #169642 ) ;
#94481=VECTOR ( 'NONE', #42532, 1000.000000000000000 ) ;
#94484=DIRECTION ( 'NONE',  ( 1.000000000000000000, 7.136802563874199107E-16, 1.554319503706929991E-16 ) ) ;
#94557=CARTESIAN_POINT ( 'NONE',  ( -23.25000000000000000, -5.011722593499800205, -233.2041167654973322 ) ) ;
#94589=DIRECTION ( 'NONE',  ( 1.000000000000000000, 0.000000000000000000, 0.000000000000000000 ) ) ;
#94599=DIRECTION ( 'NONE',  ( 0.000000000000000000, -0.9770955615653318382, -0.2128009952263588411 ) ) ;
#94617=DIRECTION ( 'NONE',  ( 2.952720810173289112E-16, -0.9770955615653316162, -0.2128009952263604232 ) ) ;
#94636=CARTESIAN_POINT ( 'NONE',  ( 18.49999999999999289, 10.99842653345846699, -220.2504445088529792 ) ) ;
#94640=EDGE_LOOP ( 'NONE', ( #101247, #200532, #65848, #101775 ) ) ;
#94644=ORIENTED_EDGE ( 'NONE', *, *, #12959, .F. ) ;
#94665=ORIENTED_EDGE ( 'NONE', *, *, #58551, .F. ) ;
#94671=DIRECTION ( 'NONE',  ( 0.000000000000000000, 0.2128009952263601179, -0.9770955615653315052 ) ) ;
#94703=CARTESIAN_POINT ( 'NONE',  ( 22.47071067811866030, 7.522163794833009121, -199.2603376134759117 ) ) ;
#94799=DIRECTION ( 'NONE',  ( 0.000000000000000000, 0.2128009952264106608, -0.9770955615653206250 ) ) ;
#94830=VECTOR ( 'NONE', #237955, 1000.000000000000227 ) ;
#94844=CARTESIAN_POINT ( 'NONE',  ( -21.05000000000000426, 6.195222845121298505, -199.6891624788988224 ) ) ;
#94871=CONICAL_SURFACE ( 'NONE', #194859, 7.750000000000013323, 0.7853981633974531640 ) ;
#94878=CARTESIAN_POINT ( 'NONE',  ( 18.59999999999996945, 14.80545736607782814, -235.9842437978701639 ) ) ;
#94891=CARTESIAN_POINT ( 'NONE',  ( -21.03922262424674017, 12.81730801556627952, -205.2285241112374194 ) ) ;
#94910=TOROIDAL_SURFACE ( 'NONE', #128249, 0.2000000000000000111, 0.1000000000000000056 ) ;
#94925=AXIS2_PLACEMENT_3D ( 'NONE', #164670, #248046, #66848 ) ;
#94937=EDGE_CURVE ( 'NONE', #74571, #147215, #244807, .T. ) ;
#94956=AXIS2_PLACEMENT_3D ( 'NONE', #48678, #152966, #232487 ) ;
#94967=AXIS2_PLACEMENT_3D ( 'NONE', #137781, #58246, #201619 ) ;
#95020=ORIENTED_EDGE ( 'NONE', *, *, #24391, .T. ) ;
#95031=TOROIDAL_SURFACE ( 'NONE', #240794, 0.2000000000000000111, 0.1000000000000000056 ) ;
#95070=ORIENTED_EDGE ( 'NONE', *, *, #247552, .F. ) ;
#95080=ORIENTED_EDGE ( 'NONE', *, *, #121500, .F. ) ;
#95088=CARTESIAN_POINT ( 'NONE',  ( -20.94999999999999929, 7.980037321000004624, -237.6410835587014390 ) ) ;
#95128=EDGE_CURVE ( 'NONE', #126771, #87224, #252806, .T. ) ;
#95182=AXIS2_PLACEMENT_3D ( 'NONE', #232786, #193646, #196203 ) ;
#95183=TOROIDAL_SURFACE ( 'NONE', #153490, 11.65000000000000036, 0.1000000000000000056 ) ;
#95184=ORIENTED_EDGE ( 'NONE', *, *, #82500, .T. ) ;
#95186=CIRCLE ( 'NONE', #236640, 0.09999999999999600875 ) ;
#95250=CARTESIAN_POINT ( 'NONE',  ( -18.39999999999999858, -7.817436562502981801, -209.8389866834999111 ) ) ;
#95256=CARTESIAN_POINT ( 'NONE',  ( -23.15000000000000213, 4.768403829798271154, -213.4961173936592331 ) ) ;
#95261=CYLINDRICAL_SURFACE ( 'NONE', #9770, 0.09999999999999724387 ) ;
#95278=FACE_OUTER_BOUND ( 'NONE', #134541, .T. ) ;
#95312=DIRECTION ( 'NONE',  ( 0.000000000000000000, 0.2128009952263603677, -0.9770955615653313941 ) ) ;
#95318=AXIS2_PLACEMENT_3D ( 'NONE', #218905, #40326, #161534 ) ;
#95336=CARTESIAN_POINT ( 'NONE',  ( 20.95420533658165141, 11.91469018375357436, -206.1500060891886505 ) ) ;
#95349=EDGE_CURVE ( 'NONE', #37909, #69101, #38072, .T. ) ;
#95367=CARTESIAN_POINT ( 'NONE',  ( 18.49999999999999645, 1.148907358139439339E-11, -201.0000000000015064 ) ) ;
#95374=FACE_OUTER_BOUND ( 'NONE', #118519, .T. ) ;
#95400=CARTESIAN_POINT ( 'NONE',  ( 20.94999999999999929, 6.724511449164476851, -231.8762197454659884 ) ) ;
#95409=VERTEX_POINT ( 'NONE', #16998 ) ;
#95416=CYLINDRICAL_SURFACE ( 'NONE', #216894, 0.09999999999999939493 ) ;
#95435=ORIENTED_EDGE ( 'NONE', *, *, #93575, .T. ) ;
#95495=CARTESIAN_POINT ( 'NONE',  ( 21.04999999999999716, 6.297325973826397139, -199.6466443475954122 ) ) ;
#95520=CARTESIAN_POINT ( 'NONE',  ( 20.95083306685154056, 10.51659053420942413, -207.3856434995966538 ) ) ;
#95523=AXIS2_PLACEMENT_3D ( 'NONE', #139830, #120327, #58991 ) ;
#95547=CYLINDRICAL_SURFACE ( 'NONE', #222063, 0.1000000000000054040 ) ;
#95549=ORIENTED_EDGE ( 'NONE', *, *, #240711, .F. ) ;
#95563=CARTESIAN_POINT ( 'NONE',  ( -22.14074124539699895, -1.475831776601470802, -193.7581091773087110 ) ) ;
#95581=DIRECTION ( 'NONE',  ( 1.000000000000000000, 0.000000000000000000, 0.000000000000000000 ) ) ;
#95598=AXIS2_PLACEMENT_3D ( 'NONE', #176042, #195605, #233448 ) ;
#95633=CARTESIAN_POINT ( 'NONE',  ( -1.820710678118658388, -4.456319993567025683, -227.1983682421737569 ) ) ;
#95637=AXIS2_PLACEMENT_3D ( 'NONE', #59938, #136930, #238602 ) ;
#95662=AXIS2_PLACEMENT_3D ( 'NONE', #103783, #102493, #165070 ) ;
#95668=CARTESIAN_POINT ( 'NONE',  ( 18.39999999999999858, -7.817436562502981801, -209.8389866834999395 ) ) ;
#95689=CARTESIAN_POINT ( 'NONE',  ( -18.59999999999999787, 7.783179459866048866, -245.3643104511423019 ) ) ;
#95710=DIRECTION ( 'NONE',  ( 0.000000000000000000, 0.2128009952263630322, -0.9770955615653309501 ) ) ;
#95734=DIRECTION ( 'NONE',  ( 0.000000000000000000, -0.3634403228828347321, 0.9316174814283063599 ) ) ;
#95736=DIRECTION ( 'NONE',  ( 0.000000000000000000, -0.9770955615653315052, -0.2128009952263603954 ) ) ;
#95739=ORIENTED_EDGE ( 'NONE', *, *, #49973, .F. ) ;
#95743=DIRECTION ( 'NONE',  ( -0.000000000000000000, 0.9770955615653316162, 0.2128009952263603122 ) ) ;
#95756=FACE_OUTER_BOUND ( 'NONE', #210243, .T. ) ;
#95759=VERTEX_POINT ( 'NONE', #7702 ) ;
#95800=CARTESIAN_POINT ( 'NONE',  ( -18.58744394320964943, -0.7665302784960944527, -242.4350121447238280 ) ) ;
#95834=CARTESIAN_POINT ( 'NONE',  ( -22.39999999999999858, -0.02128009951114784304, -200.9022904438449757 ) ) ;
#95836=AXIS2_PLACEMENT_3D ( 'NONE', #157765, #36509, #57302 ) ;
#95843=CARTESIAN_POINT ( 'NONE',  ( -18.59999999999999787, 0.6656436123793491033, -212.6810495496487476 ) ) ;
#95845=CARTESIAN_POINT ( 'NONE',  ( 18.49999999999999645, -0.6210911348947316668, -242.4105802476707936 ) ) ;
#95862=CARTESIAN_POINT ( 'NONE',  ( 20.85000000000000142, 7.576017155224048061, -241.7224044826512284 ) ) ;
#95868=DIRECTION ( 'NONE',  ( 0.000000000000000000, 0.9770955615653316162, 0.2128009952263597848 ) ) ;
#95873=ORIENTED_EDGE ( 'NONE', *, *, #157746, .F. ) ;
#95896=CARTESIAN_POINT ( 'NONE',  ( 21.05000000000000071, 2.739812813550880577, -213.5801053551551547 ) ) ;
#95905=CARTESIAN_POINT ( 'NONE',  ( -22.50000000000000000, 1.148907358139439339E-11, -201.0000000000015064 ) ) ;
#95913=VERTEX_POINT ( 'NONE', #36262 ) ;
#95930=AXIS2_PLACEMENT_3D ( 'NONE', #96535, #74472, #34060 ) ;
#95958=CARTESIAN_POINT ( 'NONE',  ( 20.85000000000000142, 7.476371755685457643, -241.7308184205399471 ) ) ;
#96005=ADVANCED_FACE ( 'NONE', ( #244684 ), #62218, .T. ) ;
#96024=ORIENTED_EDGE ( 'NONE', *, *, #12127, .F. ) ;
#96048=CARTESIAN_POINT ( 'NONE',  ( 21.14999999999999503, -2.576749817950531707, -189.6385361693310756 ) ) ;
#96053=CARTESIAN_POINT ( 'NONE',  ( -20.64999999999999858, 6.878457983866232972, -212.1414458560986986 ) ) ;
#96107=CARTESIAN_POINT ( 'NONE',  ( 20.94788355080264353, 18.36312997293286031, -236.9042258689303821 ) ) ;
#96118=CARTESIAN_POINT ( 'NONE',  ( -21.04999999999999361, 6.349973371233773811, -199.7193876399858254 ) ) ;
#96160=AXIS2_PLACEMENT_3D ( 'NONE', #188519, #68583, #47710 ) ;
#96168=CARTESIAN_POINT ( 'NONE',  ( -21.04999999999999361, 12.92448621296781930, -205.1280733356431938 ) ) ;
#96174=ADVANCED_FACE ( 'NONE', ( #219370 ), #213264, .F. ) ;
#96180=DIRECTION ( 'NONE',  ( 0.000000000000000000, -0.2128009952263485993, 0.9770955615653341697 ) ) ;
#96190=ADVANCED_FACE ( 'NONE', ( #79843 ), #108015, .F. ) ;
#96194=EDGE_LOOP ( 'NONE', ( #111454, #64475, #139569, #128714 ) ) ;
#96215=ORIENTED_EDGE ( 'NONE', *, *, #252515, .F. ) ;
#96216=CARTESIAN_POINT ( 'NONE',  ( -20.64999999999999858, 9.614325556249161409, -211.5456030694648746 ) ) ;
#96218=EDGE_CURVE ( 'NONE', #203210, #28455, #12350, .T. ) ;
#96222=CARTESIAN_POINT ( 'NONE',  ( -21.05000000000000071, 1.148907358139439339E-11, -201.0000000000015064 ) ) ;
#96234=ORIENTED_EDGE ( 'NONE', *, *, #172287, .F. ) ;
#96256=DIRECTION ( 'NONE',  ( 1.000000000000000000, 0.000000000000000000, 0.000000000000000000 ) ) ;
#96274=CARTESIAN_POINT ( 'NONE',  ( -22.39999999999999858, -2.598867842139048090, -189.5410128746472083 ) ) ;
#96299=ADVANCED_FACE ( 'NONE', ( #133732 ), #119012, .F. ) ;
#96338=VERTEX_POINT ( 'NONE', #210279 ) ;
#96384=CARTESIAN_POINT ( 'NONE',  ( -21.14999999999999858, -1.391858308744749140, -194.6091531227727955 ) ) ;
#96404=DIRECTION ( 'NONE',  ( -1.000000000000000000, -2.885090398161910739E-16, -6.283419270304611573E-17 ) ) ;
#96477=DIRECTION ( 'NONE',  ( 0.000000000000000000, -0.2128009952263651694, 0.9770955615653305060 ) ) ;
#96514=CARTESIAN_POINT ( 'NONE',  ( -18.59999999999999787, 12.97363049771892207, -205.3537238898406940 ) ) ;
#96516=FACE_OUTER_BOUND ( 'NONE', #75873, .T. ) ;
#96531=ORIENTED_EDGE ( 'NONE', *, *, #189791, .T. ) ;
#96533=CARTESIAN_POINT ( 'NONE',  ( 21.05000000000000071, -7.176961358819842651, -212.6889627706600834 ) ) ;
#96535=CARTESIAN_POINT ( 'NONE',  ( 20.94999999999999574, -10.76604040606816959, -206.3127087229280789 ) ) ;
#96548=EDGE_LOOP ( 'NONE', ( #134041, #207331, #27720, #71340 ) ) ;
#96553=ORIENTED_EDGE ( 'NONE', *, *, #111069, .F. ) ;
#96554=CARTESIAN_POINT ( 'NONE',  ( 23.15000000000000213, -3.770473190032740174, -225.9805569534692324 ) ) ;
#96571=ORIENTED_EDGE ( 'NONE', *, *, #98211, .T. ) ;
#96625=ORIENTED_EDGE ( 'NONE', *, *, #181972, .F. ) ;
#96644=CARTESIAN_POINT ( 'NONE',  ( 23.15000000000000213, -5.637547571910521249, -233.4427589080015650 ) ) ;
#96652=TOROIDAL_SURFACE ( 'NONE', #246531, 0.4000000000000005773, 0.1000000000000000056 ) ;
#96679=B_SPLINE_CURVE_WITH_KNOTS ( 'NONE', 3,
 ( #231255, #252074, #31785, #34346, #109990, #30484, #192129, #73476, #113851, #232545 ),
 .UNSPECIFIED., .F., .F.,
 ( 4, 3, 3, 4 ),
 ( 0.000000000000000000, 0.0002000000000002894374, 0.001000000000045112372, 0.001967863649472102218 ),
 .UNSPECIFIED. ) ;
#96772=LINE ( 'NONE', #78512, #227654 ) ;
#96801=DIRECTION ( 'NONE',  ( 1.000000000000000000, 0.000000000000000000, 0.000000000000000000 ) ) ;
#96831=DIRECTION ( 'NONE',  ( -1.000000000000000000, -2.885090398161910739E-16, -6.283419270304611573E-17 ) ) ;
#96886=CARTESIAN_POINT ( 'NONE',  ( 18.59999999999999076, 15.28205413790855971, -223.0019049476732675 ) ) ;
#96897=VERTEX_POINT ( 'NONE', #140579 ) ;
#97024=EDGE_LOOP ( 'NONE', ( #42130, #230465, #61570, #110086 ) ) ;
#97025=ADVANCED_FACE ( 'NONE', ( #6200 ), #128738, .F. ) ;
#97029=ORIENTED_EDGE ( 'NONE', *, *, #223705, .F. ) ;
#97060=CARTESIAN_POINT ( 'NONE',  ( -18.49372193242242446, -0.6578241932036854589, -242.3519091605612630 ) ) ;
#97097=CIRCLE ( 'NONE', #1456, 0.09999999999999939493 ) ;
#97111=CARTESIAN_POINT ( 'NONE',  ( -18.59999999999999787, 7.661991824395936845, -241.5144583139544636 ) ) ;
#97127=EDGE_LOOP ( 'NONE', ( #52674, #112089, #164312, #200559 ) ) ;
#97128=CARTESIAN_POINT ( 'NONE',  ( -20.54999999999999716, 9.690755012883057518, -211.4266134137857023 ) ) ;
#97146=VECTOR ( 'NONE', #98427, 999.9999999999998863 ) ;
#97153=DIRECTION ( 'NONE',  ( 0.000000000000000000, 0.2128009952263602567, -0.9770955615653315052 ) ) ;
#97162=DIRECTION ( 'NONE',  ( 1.000000000000000000, 0.000000000000000000, 0.000000000000000000 ) ) ;
#97179=TOROIDAL_SURFACE ( 'NONE', #59792, 0.2000000000000000111, 0.1000000000000000056 ) ;
#97192=CARTESIAN_POINT ( 'NONE',  ( -21.07016717457010557, -1.345102501103331294, -194.8238367621760858 ) ) ;
#97219=FACE_OUTER_BOUND ( 'NONE', #177383, .T. ) ;
#97222=AXIS2_PLACEMENT_3D ( 'NONE', #181177, #82020, #164174 ) ;
#97233=CARTESIAN_POINT ( 'NONE',  ( 20.94999999999999929, 9.290509600414956992, -221.0404682250134840 ) ) ;
#97266=DIRECTION ( 'NONE',  ( 1.000000000000000000, 0.000000000000000000, 0.000000000000000000 ) ) ;
#97271=DIRECTION ( 'NONE',  ( 0.000000000000000000, 0.9803012954743849372, 0.1975078988072195840 ) ) ;
#97316=DIRECTION ( 'NONE',  ( 1.000000000000000000, 0.000000000000000000, 0.000000000000000000 ) ) ;
#97327=VECTOR ( 'NONE', #246316, 1000.000000000000000 ) ;
#97331=CIRCLE ( 'NONE', #76510, 0.1000000000000054040 ) ;
#97335=CARTESIAN_POINT ( 'NONE',  ( 20.94999999999999929, -4.259020970815407203, -226.0869574510824123 ) ) ;
#97398=CYLINDRICAL_SURFACE ( 'NONE', #197327, 0.1000000000000035305 ) ;
#97427=CIRCLE ( 'NONE', #64151, 0.1000000000000035305 ) ;
#97460=CIRCLE ( 'NONE', #239143, 0.1000000000000054040 ) ;
#97479=CARTESIAN_POINT ( 'NONE',  ( -20.85000000000000142, 7.675662554762638479, -241.7139905447625381 ) ) ;
#97504=DIRECTION ( 'NONE',  ( 0.000000000000000000, 0.2128009952263601456, -0.9770955615653316162 ) ) ;
#97521=ORIENTED_EDGE ( 'NONE', *, *, #148429, .F. ) ;
#97523=EDGE_CURVE ( 'NONE', #237457, #142313, #154134, .T. ) ;
#97558=EDGE_LOOP ( 'NONE', ( #207152, #207755 ) ) ;
#97559=DIRECTION ( 'NONE',  ( 1.000000000000000000, 0.000000000000000000, 0.000000000000000000 ) ) ;
#97586=DIRECTION ( 'NONE',  ( 0.000000000000000000, 0.7397890806274223241, 0.6728388485993012091 ) ) ;
#97599=EDGE_LOOP ( 'NONE', ( #92206, #87066, #70616, #49007 ) ) ;
#97608=VERTEX_POINT ( 'NONE', #174986 ) ;
#97636=EDGE_LOOP ( 'NONE', ( #71593, #149221, #184177, #80186, #73746 ) ) ;
#97660=DIRECTION ( 'NONE',  ( -1.000000000000000000, -0.000000000000000000, -0.000000000000000000 ) ) ;
#97672=CARTESIAN_POINT ( 'NONE',  ( -18.41353343127311248, -7.785976468740646084, -209.8926132507865816 ) ) ;
#97686=DIRECTION ( 'NONE',  ( 0.000000000000000000, 0.2128009952263603954, -0.9770955615653315052 ) ) ;
#97694=VERTEX_POINT ( 'NONE', #180084 ) ;
#97703=EDGE_CURVE ( 'NONE', #10248, #45345, #100954, .T. ) ;
#97717=ORIENTED_EDGE ( 'NONE', *, *, #34693, .F. ) ;
#97753=CIRCLE ( 'NONE', #18676, 0.1000000000000054040 ) ;
#97754=EDGE_CURVE ( 'NONE', #43729, #233023, #50802, .T. ) ;
#97793=CIRCLE ( 'NONE', #114403, 0.1000000000000055844 ) ;
#97828=FACE_OUTER_BOUND ( 'NONE', #244883, .T. ) ;
#97840=ORIENTED_EDGE ( 'NONE', *, *, #247634, .F. ) ;
#97885=VERTEX_POINT ( 'NONE', #232053 ) ;
#97897=VERTEX_POINT ( 'NONE', #115945 ) ;
#97909=CARTESIAN_POINT ( 'NONE',  ( -20.54999999999999716, 6.780748427709700543, -212.1627259556213403 ) ) ;
#97954=EDGE_LOOP ( 'NONE', ( #230332, #154508, #186553, #140619 ) ) ;
#97959=CARTESIAN_POINT ( 'NONE',  ( -20.54999999999999716, 1.148907358139439339E-11, -201.0000000000015064 ) ) ;
#97982=EDGE_CURVE ( 'NONE', #121315, #103565, #167677, .T. ) ;
#97988=ORIENTED_EDGE ( 'NONE', *, *, #138659, .T. ) ;
#98018=DIRECTION ( 'NONE',  ( -1.000000000000000000, -0.000000000000000000, -0.000000000000000000 ) ) ;
#98020=CARTESIAN_POINT ( 'NONE',  ( -23.15000000000000213, 1.554534886597881638, -188.6360030214194694 ) ) ;
#98021=CARTESIAN_POINT ( 'NONE',  ( -20.85000000000000142, 7.225717546301074989, -233.4207493275448257 ) ) ;
#98038=ORIENTED_EDGE ( 'NONE', *, *, #197607, .F. ) ;
#98041=VERTEX_POINT ( 'NONE', #20707 ) ;
#98045=AXIS2_PLACEMENT_3D ( 'NONE', #23386, #83296, #159039 ) ;
#98047=DIRECTION ( 'NONE',  ( 0.000000000000000000, -0.2128009952263604232, 0.9770955615653316162 ) ) ;
#98065=LINE ( 'NONE', #202337, #194028 ) ;
#98068=ORIENTED_EDGE ( 'NONE', *, *, #54977, .F. ) ;
#98071=CARTESIAN_POINT ( 'NONE',  ( -23.25000000000000000, 14.80545736607782814, -235.9842437978701639 ) ) ;
#98087=EDGE_CURVE ( 'NONE', #65554, #145681, #105439, .T. ) ;
#98094=CARTESIAN_POINT ( 'NONE',  ( -18.50000000000000000, 8.980461154494397746, -187.0187154576991304 ) ) ;
#98099=AXIS2_PLACEMENT_3D ( 'NONE', #129278, #208816, #150143 ) ;
#98122=CYLINDRICAL_SURFACE ( 'NONE', #52147, 0.09999999999999810429 ) ;
#98127=ORIENTED_EDGE ( 'NONE', *, *, #252118, .F. ) ;
#98188=DIRECTION ( 'NONE',  ( 0.000000000000000000, 0.2128009952263604510, -0.9770955615653315052 ) ) ;
#98205=ORIENTED_EDGE ( 'NONE', *, *, #63167, .F. ) ;
#98210=DIRECTION ( 'NONE',  ( 1.000000000000000000, 0.000000000000000000, 0.000000000000000000 ) ) ;
#98211=EDGE_CURVE ( 'NONE', #241077, #92185, #146961, .T. ) ;
#98220=ORIENTED_EDGE ( 'NONE', *, *, #250429, .F. ) ;
#98224=VERTEX_POINT ( 'NONE', #226565 ) ;
#98306=DIRECTION ( 'NONE',  ( 0.000000000000000000, 0.2128009952263568427, -0.9770955615653322823 ) ) ;
#98307=CARTESIAN_POINT ( 'NONE',  ( -20.85000000000000142, 7.128833340094563376, -233.7327013124401276 ) ) ;
#98320=CARTESIAN_POINT ( 'NONE',  ( 21.05000000000000071, 9.083217576421224848, -211.4565844547649931 ) ) ;
#98350=VECTOR ( 'NONE', #145476, 1000.000000000000227 ) ;
#98352=AXIS2_PLACEMENT_3D ( 'NONE', #248930, #48141, #28640 ) ;
#98382=CARTESIAN_POINT ( 'NONE',  ( 21.93340585897773920, -1.558585775483465552, -193.8436084524194314 ) ) ;
#98386=CARTESIAN_POINT ( 'NONE',  ( -21.05000000000000071, 0.4879293624014888198, -209.1697915983179428 ) ) ;
#98390=CARTESIAN_POINT ( 'NONE',  ( 20.22483756094572271, 11.01637091542799674, -206.9310927836460507 ) ) ;
#98403=ORIENTED_EDGE ( 'NONE', *, *, #220773, .T. ) ;
#98406=AXIS2_PLACEMENT_3D ( 'NONE', #128218, #243011, #82626 ) ;
#98415=CIRCLE ( 'NONE', #190047, 0.1000000000000022399 ) ;
#98420=CARTESIAN_POINT ( 'NONE',  ( -23.25000000000000000, -2.598867842139046314, -189.5410128746472083 ) ) ;
#98427=DIRECTION ( 'NONE',  ( -0.7071067811865475727, -0.6909108974501237954, -0.1504730267678056066 ) ) ;
#98434=AXIS2_PLACEMENT_3D ( 'NONE', #233216, #214906, #92385 ) ;
#98470=AXIS2_PLACEMENT_3D ( 'NONE', #200274, #19062, #58166 ) ;
#98515=EDGE_LOOP ( 'NONE', ( #96625, #87642, #197007, #233496 ) ) ;
#98523=ORIENTED_EDGE ( 'NONE', *, *, #69030, .T. ) ;
#98553=DIRECTION ( 'NONE',  ( 0.000000000000000000, -0.1975078988072421216, 0.9803012954743803853 ) ) ;
#98557=SPHERICAL_SURFACE ( 'NONE', #180067, 0.1000000000000000056 ) ;
#98560=VERTEX_POINT ( 'NONE', #24246 ) ;
#98566=DIRECTION ( 'NONE',  ( 0.000000000000000000, 0.5000683049008606273, 0.8659859643398268858 ) ) ;
#98586=VERTEX_POINT ( 'NONE', #149332 ) ;
#98602=CIRCLE ( 'NONE', #86154, 0.5000000000000007772 ) ;
#98614=ADVANCED_FACE ( 'NONE', ( #108889 ), #42141, .T. ) ;
#98647=VERTEX_POINT ( 'NONE', #7209 ) ;
#98655=DIRECTION ( 'NONE',  ( -1.000000000000000000, -0.000000000000000000, -0.000000000000000000 ) ) ;
#98670=ORIENTED_EDGE ( 'NONE', *, *, #132052, .F. ) ;
#98686=CARTESIAN_POINT ( 'NONE',  ( -23.15000000000000213, -4.656943609564678788, -233.1535107627236414 ) ) ;
#98699=ORIENTED_EDGE ( 'NONE', *, *, #132689, .T. ) ;
#98706=EDGE_CURVE ( 'NONE', #168941, #185684, #8804, .T. ) ;
#98720=CARTESIAN_POINT ( 'NONE',  ( -21.44999999999999929, 11.60596396992030144, -220.2204734678737168 ) ) ;
#98722=ADVANCED_FACE ( 'NONE', ( #93176 ), #110170, .T. ) ;
#98728=AXIS2_PLACEMENT_3D ( 'NONE', #40046, #157434, #236928 ) ;
#98737=EDGE_LOOP ( 'NONE', ( #100699, #48735, #27807, #31273 ) ) ;
#98740=ORIENTED_EDGE ( 'NONE', *, *, #165695, .T. ) ;
#98769=VERTEX_POINT ( 'NONE', #30673 ) ;
#98785=ORIENTED_EDGE ( 'NONE', *, *, #146572, .T. ) ;
#98800=CYLINDRICAL_SURFACE ( 'NONE', #143902, 0.1000000000000055844 ) ;
#98837=VERTEX_POINT ( 'NONE', #237831 ) ;
#98879=DIRECTION ( 'NONE',  ( -1.000000000000000000, -2.885090398161910739E-16, -6.283419270304611573E-17 ) ) ;
#98880=EDGE_CURVE ( 'NONE', #205753, #157859, #67238, .T. ) ;
#98893=ORIENTED_EDGE ( 'NONE', *, *, #163516, .F. ) ;
#98911=CARTESIAN_POINT ( 'NONE',  ( 21.05000000000000071, 7.128833340094563376, -233.7327013124401276 ) ) ;
#98915=ORIENTED_EDGE ( 'NONE', *, *, #183614, .T. ) ;
#98936=CARTESIAN_POINT ( 'NONE',  ( 20.85000000000000142, 7.891440239059407169, -245.4579275668733942 ) ) ;
#98961=ORIENTED_EDGE ( 'NONE', *, *, #224203, .F. ) ;
#98963=DIRECTION ( 'NONE',  ( 1.000000000000000000, 0.000000000000000000, 0.000000000000000000 ) ) ;
#98983=CARTESIAN_POINT ( 'NONE',  ( -21.07954640115345768, 6.170272409895004806, -199.5886254415383974 ) ) ;
#98994=CIRCLE ( 'NONE', #152655, 0.1000000000000055844 ) ;
#99025=CARTESIAN_POINT ( 'NONE',  ( 22.45463910399147878, -2.479040262357760760, -189.6172560672240479 ) ) ;
#99027=DIRECTION ( 'NONE',  ( 1.000000000000000000, 0.000000000000000000, 0.000000000000000000 ) ) ;
#99105=DIRECTION ( 'NONE',  ( 0.000000000000000000, 0.2128009952263605897, -0.9770955615653315052 ) ) ;
#99117=DIRECTION ( 'NONE',  ( 0.000000000000000000, 0.2128009952263604787, -0.9770955615653315052 ) ) ;
#99130=VECTOR ( 'NONE', #564, 1000.000000000000000 ) ;
#99144=VECTOR ( 'NONE', #172109, 1000.000000000000000 ) ;
#99159=TOROIDAL_SURFACE ( 'NONE', #215677, 0.2000000000000000111, 0.1000000000000000056 ) ;
#99192=ORIENTED_EDGE ( 'NONE', *, *, #189513, .T. ) ;
#99194=CIRCLE ( 'NONE', #144990, 0.1000000000000003109 ) ;
#99217=CIRCLE ( 'NONE', #32654, 0.09999999999999939493 ) ;
#99223=EDGE_LOOP ( 'NONE', ( #98205, #191173, #97840, #73224 ) ) ;
#99251=CARTESIAN_POINT ( 'NONE',  ( -20.94999999999999929, 18.51199663233067483, -231.2535697180530292 ) ) ;
#99256=LINE ( 'NONE', #157, #82892 ) ;
#99268=ORIENTED_EDGE ( 'NONE', *, *, #152094, .F. ) ;
#99348=ORIENTED_EDGE ( 'NONE', *, *, #44737, .F. ) ;
#99352=CARTESIAN_POINT ( 'NONE',  ( -21.65000000000000213, 10.20058289318835953, -211.4179224723290815 ) ) ;
#99367=CARTESIAN_POINT ( 'NONE',  ( -20.54999999999999716, -6.688413578037177842, -212.5825622730469036 ) ) ;
#99373=SPHERICAL_SURFACE ( 'NONE', #196896, 0.1000000000000000056 ) ;
#99395=EDGE_CURVE ( 'NONE', #257097, #248650, #175655, .T. ) ;
#99399=DIRECTION ( 'NONE',  ( 0.000000000000000000, 0.2128009952263403282, -0.9770955615653358350 ) ) ;
#99409=ADVANCED_FACE ( 'NONE', ( #76533 ), #75270, .F. ) ;
#99414=CARTESIAN_POINT ( 'NONE',  ( 20.94999999999999929, -6.688413578037176066, -212.5825622730469036 ) ) ;
#99419=CYLINDRICAL_SURFACE ( 'NONE', #51337, 0.09999999999999939493 ) ;
#99451=DIRECTION ( 'NONE',  ( -3.265361837132813586E-16, 0.9770955615653357240, 0.2128009952263412996 ) ) ;
#99469=VECTOR ( 'NONE', #86867, 1000.000000000000227 ) ;
#99472=CIRCLE ( 'NONE', #149415, 0.09999999999999810429 ) ;
#99495=EDGE_CURVE ( 'NONE', #7157, #31299, #245937, .T. ) ;
#99523=EDGE_LOOP ( 'NONE', ( #125143, #33140, #110519, #220774 ) ) ;
#99526=CARTESIAN_POINT ( 'NONE',  ( 22.39999999999999503, 7.591056067193221679, -199.2444047917219052 ) ) ;
#99585=CIRCLE ( 'NONE', #37280, 0.09999999999999939493 ) ;
#99612=EDGE_LOOP ( 'NONE', ( #86571, #43501, #7779, #15876 ) ) ;
#99658=ORIENTED_EDGE ( 'NONE', *, *, #221880, .F. ) ;
#99662=PLANE ( 'NONE',  #254165 ) ;
#99694=CARTESIAN_POINT ( 'NONE',  ( -20.94999999999999929, 17.06838326776700399, -224.6250846885016870 ) ) ;
#99723=CARTESIAN_POINT ( 'NONE',  ( 21.14999999999999858, 13.96869538424789070, -210.3925794786331949 ) ) ;
#99750=CARTESIAN_POINT ( 'NONE',  ( -22.50014994444028460, 11.46291945964633818, -198.4184706950396446 ) ) ;
#99761=ORIENTED_EDGE ( 'NONE', *, *, #233881, .T. ) ;
#99771=ORIENTED_EDGE ( 'NONE', *, *, #127761, .T. ) ;
#99809=DIRECTION ( 'NONE',  ( 0.000000000000000000, 0.2128009952263485993, -0.9770955615653341697 ) ) ;
#99843=CARTESIAN_POINT ( 'NONE',  ( -20.54999999999999716, -7.916456178339619676, -219.8667623501305570 ) ) ;
#99891=DIRECTION ( 'NONE',  ( 0.000000000000000000, 0.2128009952263485993, -0.9770955615653341697 ) ) ;
#99898=CIRCLE ( 'NONE', #54128, 0.1000000000000055844 ) ;
#99948=ORIENTED_EDGE ( 'NONE', *, *, #101559, .F. ) ;
#99968=FACE_OUTER_BOUND ( 'NONE', #91729, .T. ) ;
#99976=VECTOR ( 'NONE', #156043, 1000.000000000000000 ) ;
#100008=FACE_OUTER_BOUND ( 'NONE', #115470, .T. ) ;
#100040=ORIENTED_EDGE ( 'NONE', *, *, #186580, .T. ) ;
#100071=DIRECTION ( 'NONE',  ( 1.000000000000000000, 0.000000000000000000, 0.000000000000000000 ) ) ;
#100074=EDGE_CURVE ( 'NONE', #30038, #44687, #92164, .T. ) ;
#100107=ORIENTED_EDGE ( 'NONE', *, *, #21347, .F. ) ;
#100112=CIRCLE ( 'NONE', #237524, 0.09999999999998866740 ) ;
#100150=EDGE_CURVE ( 'NONE', #145361, #103375, #21459, .T. ) ;
#100151=ADVANCED_FACE ( 'NONE', ( #244279 ), #8265, .F. ) ;
#100169=DIRECTION ( 'NONE',  ( -1.000000000000000000, -0.000000000000000000, -0.000000000000000000 ) ) ;
#100186=ORIENTED_EDGE ( 'NONE', *, *, #238453, .T. ) ;
#100196=CARTESIAN_POINT ( 'NONE',  ( -18.59999999999999787, 11.56851667937982775, -211.1200010790121553 ) ) ;
#100223=CARTESIAN_POINT ( 'NONE',  ( -21.37071067811865532, 10.49266777380207216, -211.2519653646891413 ) ) ;
#100228=ORIENTED_EDGE ( 'NONE', *, *, #117352, .F. ) ;
#100244=DIRECTION ( 'NONE',  ( 2.952720810173289112E-16, -0.9770955615653316162, -0.2128009952263598403 ) ) ;
#100255=CARTESIAN_POINT ( 'NONE',  ( 21.05000000000000071, -10.56629024491939894, -206.4738935375009703 ) ) ;
#100267=DIRECTION ( 'NONE',  ( 0.000000000000000000, -0.2128009952263604232, 0.9770955615653316162 ) ) ;
#100269=CARTESIAN_POINT ( 'NONE',  ( 18.49999999999999289, 14.61354176542825201, -235.9279552357344016 ) ) ;
#100292=ORIENTED_EDGE ( 'NONE', *, *, #42020, .F. ) ;
#100298=VECTOR ( 'NONE', #241261, 1000.000000000000114 ) ;
#100320=ORIENTED_EDGE ( 'NONE', *, *, #24231, .T. ) ;
#100374=ORIENTED_EDGE ( 'NONE', *, *, #219703, .T. ) ;
#100402=VECTOR ( 'NONE', #106085, 1000.000000000000114 ) ;
#100453=EDGE_LOOP ( 'NONE', ( #720, #213410, #71991, #60258, #195301, #245845, #53243, #236046, #190671, #151, #58128 ) ) ;
#100459=EDGE_CURVE ( 'NONE', #248008, #27458, #59006, .T. ) ;
#100471=AXIS2_PLACEMENT_3D ( 'NONE', #63120, #162260, #4435 ) ;
#100506=EDGE_CURVE ( 'NONE', #182918, #34173, #177353, .T. ) ;
#100509=ORIENTED_EDGE ( 'NONE', *, *, #131424, .T. ) ;
#100514=DIRECTION ( 'NONE',  ( 0.000000000000000000, 0.2128009952263601179, -0.9770955615653315052 ) ) ;
#100520=DIRECTION ( 'NONE',  ( -1.000000000000000000, -0.000000000000000000, -0.000000000000000000 ) ) ;
#100549=AXIS2_PLACEMENT_3D ( 'NONE', #253964, #171918, #170650 ) ;
#100558=FACE_OUTER_BOUND ( 'NONE', #82493, .T. ) ;
#100585=DIRECTION ( 'NONE',  ( -0.000000000000000000, 0.07893460099011784248, -0.9968797965484760271 ) ) ;
#100591=CARTESIAN_POINT ( 'NONE',  ( -20.64999999999999858, -4.259020970815408091, -226.0869574510824123 ) ) ;
#100604=DIRECTION ( 'NONE',  ( 0.000000000000000000, -0.2128009952263605897, 0.9770955615653313941 ) ) ;
#100617=AXIS2_PLACEMENT_3D ( 'NONE', #199999, #22664, #21377 ) ;
#100626=VECTOR ( 'NONE', #106489, 1000.000000000000114 ) ;
#100695=CARTESIAN_POINT ( 'NONE',  ( 23.15000000000000213, -6.937571600298355179, -224.3614019333310807 ) ) ;
#100699=ORIENTED_EDGE ( 'NONE', *, *, #87222, .T. ) ;
#100701=DIRECTION ( 'NONE',  ( 0.000000000000000000, -0.9525900758537791946, 0.3042567129660267988 ) ) ;
#100702=APPLICATION_CONTEXT ( 'automotive_design' ) ;
#100725=CARTESIAN_POINT ( 'NONE',  ( -23.15000000000000213, 8.772386841380839684, -220.8375963540301257 ) ) ;
#100766=CIRCLE ( 'NONE', #246554, 0.1000000000000057648 ) ;
#100786=CARTESIAN_POINT ( 'NONE',  ( 21.05000000000000071, 7.128833340094563376, -233.7327013124401276 ) ) ;
#100813=ADVANCED_FACE ( 'NONE', ( #138791 ), #218349, .F. ) ;
#100848=VERTEX_POINT ( 'NONE', #41049 ) ;
#100859=DIRECTION ( 'NONE',  ( -0.000000000000000000, 0.9770955615653313941, 0.2128009952263603954 ) ) ;
#100904=ORIENTED_EDGE ( 'NONE', *, *, #63167, .T. ) ;
#100932=CARTESIAN_POINT ( 'NONE',  ( 23.14999999999999503, 16.02417409648693436, -219.3605785455116006 ) ) ;
#100954=CIRCLE ( 'NONE', #184389, 0.1000000000000128147 ) ;
#100968=ORIENTED_EDGE ( 'NONE', *, *, #148429, .T. ) ;
#100969=LINE ( 'NONE', #24083, #144709 ) ;
#100971=AXIS2_PLACEMENT_3D ( 'NONE', #178241, #199062, #257684 ) ;
#101011=CYLINDRICAL_SURFACE ( 'NONE', #238803, 0.1000000000000035305 ) ;
#101036=CARTESIAN_POINT ( 'NONE',  ( -21.93340585899711215, -1.558585775479259139, -193.8436084524387297 ) ) ;
#101075=DIRECTION ( 'NONE',  ( 1.000000000000000000, 0.000000000000000000, 0.000000000000000000 ) ) ;
#101094=AXIS2_PLACEMENT_3D ( 'NONE', #109199, #191352, #70119 ) ;
#101102=VERTEX_POINT ( 'NONE', #78552 ) ;
#101108=DIRECTION ( 'NONE',  ( -1.000000000000000000, -5.840638543281469327E-15, 6.917008051451466668E-14 ) ) ;
#101204=EDGE_CURVE ( 'NONE', #34477, #212023, #238466, .T. ) ;
#101213=ORIENTED_EDGE ( 'NONE', *, *, #186778, .T. ) ;
#101214=AXIS2_PLACEMENT_3D ( 'NONE', #83976, #81428, #143990 ) ;
#101226=CIRCLE ( 'NONE', #151374, 0.1000000000000055844 ) ;
#101235=CARTESIAN_POINT ( 'NONE',  ( 18.59999999999999432, 2.859758780633683273, -208.6670499591424459 ) ) ;
#101243=ADVANCED_FACE ( 'NONE', ( #143660 ), #181532, .T. ) ;
#101247=ORIENTED_EDGE ( 'NONE', *, *, #204532, .F. ) ;
#101318=ORIENTED_EDGE ( 'NONE', *, *, #58589, .F. ) ;
#101358=EDGE_CURVE ( 'NONE', #168569, #48752, #178151, .T. ) ;
#101360=DIRECTION ( 'NONE',  ( 0.000000000000000000, 0.2128009952263604510, -0.9770955615653315052 ) ) ;
#101406=ORIENTED_EDGE ( 'NONE', *, *, #159960, .F. ) ;
#101421=EDGE_CURVE ( 'NONE', #220753, #89546, #101226, .T. ) ;
#101424=DIRECTION ( 'NONE',  ( 1.000000000000000000, 0.000000000000000000, 0.000000000000000000 ) ) ;
#101451=DIRECTION ( 'NONE',  ( 1.000000000000000000, 0.000000000000000000, 0.000000000000000000 ) ) ;
#101495=VECTOR ( 'NONE', #239307, 1000.000000000000000 ) ;
#101518=EDGE_LOOP ( 'NONE', ( #201140, #204745, #115744, #236727 ) ) ;
#101520=ORIENTED_EDGE ( 'NONE', *, *, #68529, .F. ) ;
#101521=VECTOR ( 'NONE', #244660, 1000.000000000000227 ) ;
#101534=DIRECTION ( 'NONE',  ( 0.000000000000000000, 0.9770955615652963111, 0.2128009952265221549 ) ) ;
#101536=ORIENTED_EDGE ( 'NONE', *, *, #239184, .T. ) ;
#101549=FACE_OUTER_BOUND ( 'NONE', #224639, .T. ) ;
#101551=CIRCLE ( 'NONE', #247310, 0.1000000000000055844 ) ;
#101559=EDGE_CURVE ( 'NONE', #159889, #242169, #93073, .T. ) ;
#101599=DIRECTION ( 'NONE',  ( -0.000000000000000000, 0.7672646620070624479, -0.6413305999523086776 ) ) ;
#101615=CARTESIAN_POINT ( 'NONE',  ( -21.05000000000000071, 1.148907358139439339E-11, -201.0000000000015064 ) ) ;
#101630=EDGE_CURVE ( 'NONE', #253651, #5146, #164011, .T. ) ;
#101648=EDGE_LOOP ( 'NONE', ( #159902, #101895, #233480, #56661 ) ) ;
#101669=CIRCLE ( 'NONE', #176731, 0.1000000000000054040 ) ;
#101685=CIRCLE ( 'NONE', #214152, 0.1000000000000035305 ) ;
#101691=CYLINDRICAL_SURFACE ( 'NONE', #128941, 0.09999999999999939493 ) ;
#101700=AXIS2_PLACEMENT_3D ( 'NONE', #210135, #227100, #151449 ) ;
#101719=CARTESIAN_POINT ( 'NONE',  ( 22.57856590037849287, -2.504457907796295402, -189.5199485407344753 ) ) ;
#101722=EDGE_LOOP ( 'NONE', ( #46912, #82558, #176181, #162650, #72543, #62866 ) ) ;
#101726=CARTESIAN_POINT ( 'NONE',  ( -18.59999999999999787, 8.882751598337863541, -187.0399955572217721 ) ) ;
#101759=DIRECTION ( 'NONE',  ( 0.000000000000000000, 0.2280421351061330537, -0.9736512643735621975 ) ) ;
#101775=ORIENTED_EDGE ( 'NONE', *, *, #220276, .F. ) ;
#101785=EDGE_CURVE ( 'NONE', #81210, #236966, #139015, .T. ) ;
#101799=EDGE_CURVE ( 'NONE', #233023, #94400, #148504, .T. ) ;
#101859=ORIENTED_EDGE ( 'NONE', *, *, #3205, .T. ) ;
#101895=ORIENTED_EDGE ( 'NONE', *, *, #133837, .F. ) ;
#101899=CIRCLE ( 'NONE', #176404, 0.09999999999999810429 ) ;
#101924=AXIS2_PLACEMENT_3D ( 'NONE', #244839, #66220, #200590 ) ;
#101927=AXIS2_PLACEMENT_3D ( 'NONE', #212647, #35320, #215195 ) ;
#101937=DIRECTION ( 'NONE',  ( -1.000000000000000000, 0.000000000000000000, 0.000000000000000000 ) ) ;
#101939=ORIENTED_EDGE ( 'NONE', *, *, #199179, .T. ) ;
#101947=EDGE_CURVE ( 'NONE', #25296, #230954, #187642, .T. ) ;
#101953=DIRECTION ( 'NONE',  ( -0.000000000000000000, 0.9770955615653313941, 0.2128009952263603954 ) ) ;
#101960=ORIENTED_EDGE ( 'NONE', *, *, #43772, .T. ) ;
#102006=LINE ( 'NONE', #241549, #110234 ) ;
#102017=DIRECTION ( 'NONE',  ( 1.000000000000000000, 0.000000000000000000, 0.000000000000000000 ) ) ;
#102025=EDGE_CURVE ( 'NONE', #204167, #200518, #68341, .T. ) ;
#102046=ADVANCED_FACE ( 'NONE', ( #143021 ), #63495, .T. ) ;
#102064=DIRECTION ( 'NONE',  ( 0.000000000000000000, -0.2128009952263604232, 0.9770955615653316162 ) ) ;
#102076=ORIENTED_EDGE ( 'NONE', *, *, #237068, .F. ) ;
#102078=DIRECTION ( 'NONE',  ( 0.000000000000000000, 0.2128009952263605620, -0.9770955615653315052 ) ) ;
#102093=ORIENTED_EDGE ( 'NONE', *, *, #22427, .T. ) ;
#102117=CARTESIAN_POINT ( 'NONE',  ( -20.54999999999999716, -3.770473190032741062, -225.9805569534692324 ) ) ;
#102121=EDGE_CURVE ( 'NONE', #138601, #73041, #240873, .T. ) ;
#102160=CARTESIAN_POINT ( 'NONE',  ( 22.48660254037844197, 11.37252324248628987, -198.4720136275361426 ) ) ;
#102170=ORIENTED_EDGE ( 'NONE', *, *, #220121, .T. ) ;
#102192=DIRECTION ( 'NONE',  ( 0.000000000000000000, 0.2128009952263403282, -0.9770955615653358350 ) ) ;
#102222=SPHERICAL_SURFACE ( 'NONE', #206703, 0.1000000000000000056 ) ;
#102226=CARTESIAN_POINT ( 'NONE',  ( -21.64999999999999858, 9.809744668562228043, -211.5030428704195913 ) ) ;
#102234=AXIS2_PLACEMENT_3D ( 'NONE', #53972, #133514, #168836 ) ;
#102250=CARTESIAN_POINT ( 'NONE',  ( 20.53930447207953236, 10.56810606003652708, -207.3387900815227169 ) ) ;
#102283=CARTESIAN_POINT ( 'NONE',  ( -20.85000000000000142, 17.15380675273576117, -224.5473919504296703 ) ) ;
#102301=VERTEX_POINT ( 'NONE', #209431 ) ;
#102321=EDGE_CURVE ( 'NONE', #75595, #208696, #18440, .T. ) ;
#102326=CARTESIAN_POINT ( 'NONE',  ( -20.07928932188135107, 11.63760776912483763, -211.1049537763353783 ) ) ;
#102368=DIRECTION ( 'NONE',  ( 0.000000000000000000, -0.2128009952263601456, 0.9770955615653316162 ) ) ;
#102372=DIRECTION ( 'NONE',  ( 1.000000000000000000, -0.000000000000000000, -0.000000000000000000 ) ) ;
#102378=CARTESIAN_POINT ( 'NONE',  ( -18.39999999999999858, -7.785976468740645196, -209.8926132507865816 ) ) ;
#102386=VERTEX_POINT ( 'NONE', #95896 ) ;
#102400=ORIENTED_EDGE ( 'NONE', *, *, #101799, .F. ) ;
#102403=ADVANCED_FACE ( 'NONE', ( #54207 ), #21230, .T. ) ;
#102406=ORIENTED_EDGE ( 'NONE', *, *, #81512, .F. ) ;
#102410=VECTOR ( 'NONE', #49820, 1000.000000000000227 ) ;
#102425=CIRCLE ( 'NONE', #56642, 0.1000000000000066946 ) ;
#102456=DIRECTION ( 'NONE',  ( 0.000000000000000000, 0.2128009952263403282, -0.9770955615653358350 ) ) ;
#102482=ORIENTED_EDGE ( 'NONE', *, *, #97703, .T. ) ;
#102493=DIRECTION ( 'NONE',  ( 0.000000000000000000, -0.2128009952263604232, 0.9770955615653316162 ) ) ;
#102495=CARTESIAN_POINT ( 'NONE',  ( -23.15000000000000213, 7.980037321000002848, -237.6410835587014390 ) ) ;
#102506=CARTESIAN_POINT ( 'NONE',  ( -20.64999999999999858, -4.161311414658873886, -226.0656773515597706 ) ) ;
#102510=CARTESIAN_POINT ( 'NONE',  ( -21.56666275994540172, -1.480534921131848813, -194.2019862094511780 ) ) ;
#102520=CARTESIAN_POINT ( 'NONE',  ( -20.85000000000000142, 17.06838326776700399, -224.6250846885016870 ) ) ;
#102523=ADVANCED_FACE ( 'NONE', ( #206258 ), #27655, .F. ) ;
#102543=AXIS2_PLACEMENT_3D ( 'NONE', #225756, #126678, #88809 ) ;
#102550=CARTESIAN_POINT ( 'NONE',  ( -21.07928932188134041, 6.162520550847337297, -199.5566553493351307 ) ) ;
#102565=VERTEX_POINT ( 'NONE', #251794 ) ;
#102569=ORIENTED_EDGE ( 'NONE', *, *, #151110, .T. ) ;
#102619=FACE_OUTER_BOUND ( 'NONE', #50863, .T. ) ;
#102630=ORIENTED_EDGE ( 'NONE', *, *, #207593, .F. ) ;
#102636=CARTESIAN_POINT ( 'NONE',  ( 18.59999999999999432, 0.5876173420563349792, -209.1618981382189588 ) ) ;
#102640=DIRECTION ( 'NONE',  ( 0.000000000000000000, -0.07893460099014820708, 0.9968797965484735846 ) ) ;
#102668=EDGE_CURVE ( 'NONE', #248715, #190923, #40493, .T. ) ;
#102728=CARTESIAN_POINT ( 'NONE',  ( -20.94999999999999929, -4.914013037343267776, -233.1828366659746905 ) ) ;
#102736=AXIS2_PLACEMENT_3D ( 'NONE', #103637, #198907, #39868 ) ;
#102743=CIRCLE ( 'NONE', #77607, 11.70000000000000284 ) ;
#102770=ORIENTED_EDGE ( 'NONE', *, *, #218969, .T. ) ;
#102797=AXIS2_PLACEMENT_3D ( 'NONE', #235918, #61141, #81950 ) ;
#102807=DIRECTION ( 'NONE',  ( -1.000000000000000000, 0.000000000000000000, 0.000000000000000000 ) ) ;
#102811=ADVANCED_FACE ( 'NONE', ( #154035 ), #106264, .T. ) ;
#102834=CARTESIAN_POINT ( 'NONE',  ( 20.85000000000000142, -4.254329952141540971, -236.2118329068272260 ) ) ;
#102842=CARTESIAN_POINT ( 'NONE',  ( -21.13435531349860241, 6.344986029290462959, -199.6181296949467594 ) ) ;
#102873=VERTEX_POINT ( 'NONE', #143401 ) ;
#102913=EDGE_CURVE ( 'NONE', #132241, #216057, #123071, .T. ) ;
#102917=CARTESIAN_POINT ( 'NONE',  ( 21.05000000000000071, 10.45765418377745526, -207.3040725013013912 ) ) ;
#102919=CIRCLE ( 'NONE', #131972, 0.2000000000000100586 ) ;
#102935=VERTEX_POINT ( 'NONE', #61301 ) ;
#102941=EDGE_CURVE ( 'NONE', #142313, #55595, #127134, .T. ) ;
#102962=VERTEX_POINT ( 'NONE', #85962 ) ;
#102965=DIRECTION ( 'NONE',  ( 0.000000000000000000, 0.2128009952263601456, -0.9770955615653316162 ) ) ;
#102985=ORIENTED_EDGE ( 'NONE', *, *, #155266, .T. ) ;
#102989=CYLINDRICAL_SURFACE ( 'NONE', #75573, 4.049999999999995381 ) ;
#103007=CARTESIAN_POINT ( 'NONE',  ( 19.75857864376269291, 16.64998792410003858, -222.7039835543563981 ) ) ;
#103021=ORIENTED_EDGE ( 'NONE', *, *, #12376, .F. ) ;
#103023=VERTEX_POINT ( 'NONE', #127700 ) ;
#103026=ADVANCED_FACE ( 'NONE', ( #248937 ), #205941, .T. ) ;
#103027=DIRECTION ( 'NONE',  ( 0.000000000000000000, 0.3427706569149635007, -0.9394191166662961834 ) ) ;
#103046=AXIS2_PLACEMENT_3D ( 'NONE', #176151, #54876, #77016 ) ;
#103047=AXIS2_PLACEMENT_3D ( 'NONE', #163560, #154926, #183133 ) ;
#103055=CARTESIAN_POINT ( 'NONE',  ( -23.25000000000000000, -4.356730526971936079, -226.1082375506050539 ) ) ;
#103063=EDGE_LOOP ( 'NONE', ( #13177, #115928, #152923, #161536 ) ) ;
#103089=CIRCLE ( 'NONE', #57305, 0.5000000000000007772 ) ;
#103100=DIRECTION ( 'NONE',  ( 0.000000000000000000, 0.9394191166662619885, 0.3427706569150576477 ) ) ;
#103115=ORIENTED_EDGE ( 'NONE', *, *, #102121, .T. ) ;
#103120=ORIENTED_EDGE ( 'NONE', *, *, #177970, .T. ) ;
#103151=CARTESIAN_POINT ( 'NONE',  ( 20.95429693346633471, 11.91077973133057277, -206.1440789982873127 ) ) ;
#103186=LINE ( 'NONE', #219296, #83519 ) ;
#103209=TOROIDAL_SURFACE ( 'NONE', #236498, 0.2000000000000000111, 0.1000000000000000056 ) ;
#103234=EDGE_CURVE ( 'NONE', #31271, #137759, #246437, .T. ) ;
#103242=ORIENTED_EDGE ( 'NONE', *, *, #214338, .F. ) ;
#103243=CARTESIAN_POINT ( 'NONE',  ( -22.39999999999999858, -2.479040261793999722, -189.6172560698084624 ) ) ;
#103247=DIRECTION ( 'NONE',  ( 0.000000000000000000, 0.2128009952263268945, -0.9770955615653388326 ) ) ;
#103280=DIRECTION ( 'NONE',  ( 0.000000000000000000, 0.8267009638119992010, 0.5626415523513276229 ) ) ;
#103288=CARTESIAN_POINT ( 'NONE',  ( -22.39999999999999858, 7.612336166715881092, -199.3421143478784359 ) ) ;
#103293=VECTOR ( 'NONE', #249350, 1000.000000000000000 ) ;
#103327=ORIENTED_EDGE ( 'NONE', *, *, #218201, .T. ) ;
#103329=CIRCLE ( 'NONE', #78395, 4.299999999999966960 ) ;
#103334=CARTESIAN_POINT ( 'NONE',  ( 21.08134388332232234, 6.173453938067205549, -199.5778913402473904 ) ) ;
#103337=ORIENTED_EDGE ( 'NONE', *, *, #102668, .T. ) ;
#103340=CARTESIAN_POINT ( 'NONE',  ( 18.59999999999999432, -0.6576273345615495369, -242.5323337003318898 ) ) ;
#103360=LINE ( 'NONE', #61690, #78605 ) ;
#103368=CIRCLE ( 'NONE', #199076, 11.74999999999999289 ) ;
#103375=VERTEX_POINT ( 'NONE', #141791 ) ;
#103390=AXIS2_PLACEMENT_3D ( 'NONE', #102520, #103818, #183392 ) ;
#103395=CARTESIAN_POINT ( 'NONE',  ( 21.13461538461538325, 12.99955419111918253, -210.8083363671015604 ) ) ;
#103411=ORIENTED_EDGE ( 'NONE', *, *, #140843, .F. ) ;
#103456=CARTESIAN_POINT ( 'NONE',  ( 23.24999999999999289, 17.01923898301590654, -224.3994341343041867 ) ) ;
#103489=EDGE_CURVE ( 'NONE', #16838, #9164, #69994, .T. ) ;
#103547=CARTESIAN_POINT ( 'NONE',  ( 21.53752568622118346, -1.347531963294298585, -194.3475782847248183 ) ) ;
#103553=CARTESIAN_POINT ( 'NONE',  ( 21.09793522318420855, 13.08351628660398980, -210.6767460175381359 ) ) ;
#103554=CARTESIAN_POINT ( 'NONE',  ( 21.14999999999999858, 2.585532092011767702, -212.8717110730202933 ) ) ;
#103565=VERTEX_POINT ( 'NONE', #227751 ) ;
#103583=CARTESIAN_POINT ( 'NONE',  ( -21.44999999999999929, 11.58468387039766512, -220.1227639117171861 ) ) ;
#103590=CIRCLE ( 'NONE', #74439, 0.09999999999999724387 ) ;
#103606=CARTESIAN_POINT ( 'NONE',  ( 18.60000000000000497, 1.148907358139439339E-11, -201.0000000000015064 ) ) ;
#103614=EDGE_CURVE ( 'NONE', #9130, #103755, #44123, .T. ) ;
#103637=CARTESIAN_POINT ( 'NONE',  ( 23.14999999999999858, 7.128833340094563376, -233.7327013124401276 ) ) ;
#103648=AXIS2_PLACEMENT_3D ( 'NONE', #194072, #255247, #54534 ) ;
#103663=EDGE_LOOP ( 'NONE', ( #165980, #30173, #102170, #18478, #66509, #249349, #177914, #226304, #167308, #69537, #82211, #101939, #201170, #43114 ) ) ;
#103698=EDGE_CURVE ( 'NONE', #84780, #55595, #238019, .T. ) ;
#103700=AXIS2_PLACEMENT_3D ( 'NONE', #178618, #177342, #36547 ) ;
#103722=CARTESIAN_POINT ( 'NONE',  ( -21.10257677756355932, 6.246520857501153934, -199.6140387306917603 ) ) ;
#103728=DIRECTION ( 'NONE',  ( 0.000000000000000000, 0.2128009952263485993, -0.9770955615653341697 ) ) ;
#103755=VERTEX_POINT ( 'NONE', #200195 ) ;
#103762=DIRECTION ( 'NONE',  ( 0.000000000000000000, 0.2128009952263602289, -0.9770955615653316162 ) ) ;
#103766=AXIS2_PLACEMENT_3D ( 'NONE', #33965, #53480, #195578 ) ;
#103777=FACE_OUTER_BOUND ( 'NONE', #83427, .T. ) ;
#103778=DIRECTION ( 'NONE',  ( 0.000000000000000000, 0.2128009952263403282, -0.9770955615653358350 ) ) ;
#103783=CARTESIAN_POINT ( 'NONE',  ( 20.94999999999999929, 11.01970663298110154, -220.3481540650095098 ) ) ;
#103818=DIRECTION ( 'NONE',  ( -0.000000000000000000, 0.2128009952263604232, -0.9770955615653316162 ) ) ;
#103849=CARTESIAN_POINT ( 'NONE',  ( -18.59999999999999787, 7.668827189579289438, -241.6142244293585009 ) ) ;
#103851=CARTESIAN_POINT ( 'NONE',  ( 21.04386569057732004, 17.15049515251717338, -224.5321864300209427 ) ) ;
#103858=CARTESIAN_POINT ( 'NONE',  ( -21.05000000000000071, 17.15380675273573985, -224.5473919504296703 ) ) ;
#103864=CARTESIAN_POINT ( 'NONE',  ( -21.14999999999999858, -11.48087284838115707, -203.5004116939112464 ) ) ;
#103879=CARTESIAN_POINT ( 'NONE',  ( 18.59999999999999787, -6.192768117006094641, -227.7812363988097388 ) ) ;
#103880=CARTESIAN_POINT ( 'NONE',  ( -18.59999999999999787, 16.02417409648692725, -219.3605785455116006 ) ) ;
#103882=VERTEX_POINT ( 'NONE', #55199 ) ;
#103889=LINE ( 'NONE', #167769, #93990 ) ;
#103897=CIRCLE ( 'NONE', #16646, 0.09999999999999939493 ) ;
#103906=CARTESIAN_POINT ( 'NONE',  ( -20.64999999999999858, 6.857177884343597540, -212.0437362999421680 ) ) ;
#103922=DIRECTION ( 'NONE',  ( 0.000000000000000000, 0.2128009952263485993, -0.9770955615653341697 ) ) ;
#103924=CARTESIAN_POINT ( 'NONE',  ( -21.05000000000000071, 10.71906255309368383, -222.4921384173655383 ) ) ;
#103946=ADVANCED_FACE ( 'NONE', ( #72243 ), #14852, .F. ) ;
#103958=ORIENTED_EDGE ( 'NONE', *, *, #166570, .T. ) ;
#103993=ORIENTED_EDGE ( 'NONE', *, *, #168405, .F. ) ;
#104033=DIRECTION ( 'NONE',  ( 0.000000000000000000, -0.9550021345545507412, 0.2965989261549202838 ) ) ;
#104034=ORIENTED_EDGE ( 'NONE', *, *, #31191, .T. ) ;
#104036=LINE ( 'NONE', #246147, #36399 ) ;
#104058=ORIENTED_EDGE ( 'NONE', *, *, #147244, .F. ) ;
#104059=DIRECTION ( 'NONE',  ( 1.000000000000000000, 3.190570557967288456E-16, 6.948722487160391713E-17 ) ) ;
#104078=LINE ( 'NONE', #227905, #116950 ) ;
#104081=ADVANCED_FACE ( 'NONE', ( #188686 ), #124872, .F. ) ;
#104101=ORIENTED_EDGE ( 'NONE', *, *, #167040, .F. ) ;
#104113=EDGE_CURVE ( 'NONE', #54081, #98041, #145698, .T. ) ;
#104121=DIRECTION ( 'NONE',  ( -1.000000000000000000, -1.794895427898103559E-16, -3.909090864890002444E-17 ) ) ;
#104135=CIRCLE ( 'NONE', #125019, 0.1000000000000055844 ) ;
#104198=EDGE_CURVE ( 'NONE', #219574, #227124, #110434, .T. ) ;
#104199=ORIENTED_EDGE ( 'NONE', *, *, #123596, .F. ) ;
#104218=CARTESIAN_POINT ( 'NONE',  ( -18.59999999999999787, 14.78417726655519360, -235.8865342417136333 ) ) ;
#104221=CARTESIAN_POINT ( 'NONE',  ( -18.55807992284872299, 18.40923646582965389, -236.9894833875398206 ) ) ;
#104227=FACE_OUTER_BOUND ( 'NONE', #181677, .T. ) ;
#104278=DIRECTION ( 'NONE',  ( 0.000000000000000000, 0.9770955615653316162, 0.2128009952263604232 ) ) ;
#104280=CIRCLE ( 'NONE', #54210, 0.1000000000000009354 ) ;
#104315=EDGE_LOOP ( 'NONE', ( #134554, #32205, #109407 ) ) ;
#104379=CARTESIAN_POINT ( 'NONE',  ( -21.55000000000000071, 9.809744668562228043, -211.5030428704195913 ) ) ;
#104383=CIRCLE ( 'NONE', #12853, 0.2000000000000111688 ) ;
#104406=EDGE_CURVE ( 'NONE', #148114, #80096, #206238, .T. ) ;
#104460=CARTESIAN_POINT ( 'NONE',  ( 21.12230431290520016, -1.369086087588080813, -194.6892316229322262 ) ) ;
#104474=ORIENTED_EDGE ( 'NONE', *, *, #152170, .T. ) ;
#104503=LINE ( 'NONE', #45843, #195264 ) ;
#104511=CARTESIAN_POINT ( 'NONE',  ( -20.54999999999999716, -4.259020970815408091, -226.0869574510824123 ) ) ;
#104559=DIRECTION ( 'NONE',  ( 0.000000000000000000, 0.2128009952263403282, -0.9770955615653358350 ) ) ;
#104585=FACE_OUTER_BOUND ( 'NONE', #87847, .T. ) ;
#104621=CARTESIAN_POINT ( 'NONE',  ( -23.15000000000000213, -3.363022478626109368, -226.2703567425896267 ) ) ;
#104673=CARTESIAN_POINT ( 'NONE',  ( -20.54999999999999716, 4.625797360122408719, -213.1224017332881431 ) ) ;
#104684=ORIENTED_EDGE ( 'NONE', *, *, #30635, .F. ) ;
#104690=ADVANCED_FACE ( 'NONE', ( #79962 ), #134810, .T. ) ;
#104706=SPHERICAL_SURFACE ( 'NONE', #119097, 0.1000000000000000056 ) ;
#104729=ORIENTED_EDGE ( 'NONE', *, *, #130697, .T. ) ;
#104736=CIRCLE ( 'NONE', #17321, 12.77500000000000213 ) ;
#104747=DIRECTION ( 'NONE',  ( 1.000000000000000000, 0.000000000000000000, 0.000000000000000000 ) ) ;
#104757=FACE_OUTER_BOUND ( 'NONE', #217577, .T. ) ;
#104796=ORIENTED_EDGE ( 'NONE', *, *, #219243, .T. ) ;
#104876=DIRECTION ( 'NONE',  ( -4.408576920032447355E-17, 0.3427706569149636118, -0.9394191166662962944 ) ) ;
#104910=ORIENTED_EDGE ( 'NONE', *, *, #14349, .F. ) ;
#104933=EDGE_CURVE ( 'NONE', #156652, #154626, #169034, .T. ) ;
#104939=FACE_OUTER_BOUND ( 'NONE', #31015, .T. ) ;
#104952=CARTESIAN_POINT ( 'NONE',  ( 18.49999999999999289, 8.882751598337870647, -187.0399955572217721 ) ) ;
#104954=EDGE_LOOP ( 'NONE', ( #21918, #158916, #162210, #31276 ) ) ;
#104977=AXIS2_PLACEMENT_3D ( 'NONE', #48042, #31094, #127590 ) ;
#105013=CARTESIAN_POINT ( 'NONE',  ( -21.14999999999999858, 11.50215294792677057, -198.5972978622482970 ) ) ;
#105018=DIRECTION ( 'NONE',  ( -1.000000000000000000, -0.000000000000000000, -0.000000000000000000 ) ) ;
#105023=ADVANCED_FACE ( 'NONE', ( #159247 ), #223330, .T. ) ;
#105042=CARTESIAN_POINT ( 'NONE',  ( 21.05000000000000071, 9.374458193048763377, -220.5475659691911119 ) ) ;
#105048=CARTESIAN_POINT ( 'NONE',  ( 18.59999999999999076, 8.433899723187009201, -209.4150263691077782 ) ) ;
#105067=DIRECTION ( 'NONE',  ( 1.000000000000000000, 7.136802563874199107E-16, 1.554319503706929991E-16 ) ) ;
#105092=AXIS2_PLACEMENT_3D ( 'NONE', #101235, #123425, #85537 ) ;
#105102=DIRECTION ( 'NONE',  ( 0.7071067811865474617, 0.6909108974501236844, 0.1504730267678055788 ) ) ;
#105104=DIRECTION ( 'NONE',  ( 0.000000000000000000, -0.2128009952263604232, 0.9770955615653316162 ) ) ;
#105111=CIRCLE ( 'NONE', #246790, 7.900000000000007461 ) ;
#105129=DIRECTION ( 'NONE',  ( 0.000000000000000000, -0.9394191166662962944, -0.3427706569149635563 ) ) ;
#105149=DIRECTION ( 'NONE',  ( 0.000000000000000000, -0.2128009952263603954, 0.9770955615653315052 ) ) ;
#105152=CARTESIAN_POINT ( 'NONE',  ( 18.59999999999999787, 7.476371755685457643, -241.7308184205399471 ) ) ;
#105172=AXIS2_PLACEMENT_3D ( 'NONE', #53334, #170768, #212424 ) ;
#105204=CARTESIAN_POINT ( 'NONE',  ( 22.39999999999999503, 7.612336166715857111, -199.3421143478784359 ) ) ;
#105246=DIRECTION ( 'NONE',  ( 0.000000000000000000, -0.9770955615653316162, -0.2128009952263604232 ) ) ;
#105247=ORIENTED_EDGE ( 'NONE', *, *, #96218, .T. ) ;
#105248=EDGE_CURVE ( 'NONE', #162643, #71034, #131766, .T. ) ;
#105261=DIRECTION ( 'NONE',  ( 0.000000000000000000, -0.9964539953858893018, -0.08413937888704772772 ) ) ;
#105302=CARTESIAN_POINT ( 'NONE',  ( -20.54999999999999716, -6.980131799343633148, -224.1659828210180194 ) ) ;
#105335=CARTESIAN_POINT ( 'NONE',  ( -23.25000000000000000, -4.352039508298082282, -236.2331130063498676 ) ) ;
#105356=EDGE_CURVE ( 'NONE', #150841, #254455, #77319, .T. ) ;
#105379=DIRECTION ( 'NONE',  ( -1.000000000000000000, -0.000000000000000000, -0.000000000000000000 ) ) ;
#105389=CARTESIAN_POINT ( 'NONE',  ( 23.14999999999999503, 19.68370618165487329, -225.3554403480446240 ) ) ;
#105402=DIRECTION ( 'NONE',  ( 1.000000000000000000, -7.136802563874198121E-16, -1.554319503706931717E-16 ) ) ;
#105409=ADVANCED_FACE ( 'NONE', ( #15588 ), #215157, .T. ) ;
#105418=TOROIDAL_SURFACE ( 'NONE', #201127, 7.800000000000000711, 0.1000000000000000056 ) ;
#105420=CARTESIAN_POINT ( 'NONE',  ( -18.50000000000000000, 16.02417409648692725, -219.3605785455116006 ) ) ;
#105439=CIRCLE ( 'NONE', #9607, 0.1000000000000066946 ) ;
#105442=VECTOR ( 'NONE', #196046, 1000.000000000000114 ) ;
#105447=DIRECTION ( 'NONE',  ( -1.000000000000000000, 0.000000000000000000, 0.000000000000000000 ) ) ;
#105469=AXIS2_PLACEMENT_3D ( 'NONE', #127291, #141708, #23081 ) ;
#105481=AXIS2_PLACEMENT_3D ( 'NONE', #211766, #111373, #162698 ) ;
#105515=DIRECTION ( 'NONE',  ( 0.000000000000000000, -0.2128009952263604232, 0.9770955615653316162 ) ) ;
#105552=ORIENTED_EDGE ( 'NONE', *, *, #39357, .F. ) ;
#105566=DIRECTION ( 'NONE',  ( 0.000000000000000000, 0.2128009952263693327, -0.9770955615653295068 ) ) ;
#105618=CARTESIAN_POINT ( 'NONE',  ( -18.59999999999999787, 14.86477715130881272, -235.7932433709592601 ) ) ;
#105619=ORIENTED_EDGE ( 'NONE', *, *, #65457, .F. ) ;
#105638=CARTESIAN_POINT ( 'NONE',  ( -23.15000000000000213, 17.15380675273576472, -224.5473919504296703 ) ) ;
#105641=CARTESIAN_POINT ( 'NONE',  ( -18.59999999999999787, 0.6713328740235187109, -212.7808875799876205 ) ) ;
#105674=ORIENTED_EDGE ( 'NONE', *, *, #160345, .T. ) ;
#105715=CARTESIAN_POINT ( 'NONE',  ( 21.14999999999999503, 11.40444339177024524, -198.6185779617709670 ) ) ;
#105728=DIRECTION ( 'NONE',  ( 1.000000000000000000, 0.000000000000000000, 0.000000000000000000 ) ) ;
#105731=DIRECTION ( 'NONE',  ( 0.000000000000000000, -0.9770955615653316162, -0.2128009952263604232 ) ) ;
#105740=CARTESIAN_POINT ( 'NONE',  ( 21.08479644141222664, -1.293017255164235157, -194.7878304459186722 ) ) ;
#105753=ORIENTED_EDGE ( 'NONE', *, *, #190594, .F. ) ;
#105760=ORIENTED_EDGE ( 'NONE', *, *, #29746, .T. ) ;
#105768=CARTESIAN_POINT ( 'NONE',  ( 21.05933563467872105, 13.07370587250136040, -210.6321695627368911 ) ) ;
#105847=DIRECTION ( 'NONE',  ( 0.000000000000000000, -0.5626415523513815797, 0.8267009638119623416 ) ) ;
#105852=CARTESIAN_POINT ( 'NONE',  ( -21.07016717456945898, 6.176163237836298059, -199.6548974988868679 ) ) ;
#105879=CARTESIAN_POINT ( 'NONE',  ( 20.85000000000000142, 7.783179459866048866, -245.3643104511423019 ) ) ;
#105890=CARTESIAN_POINT ( 'NONE',  ( 21.08884785362045378, 6.200991531159584902, -199.5985400833362178 ) ) ;
#105906=ORIENTED_EDGE ( 'NONE', *, *, #111253, .F. ) ;
#105907=CARTESIAN_POINT ( 'NONE',  ( 18.59999999999999787, -0.5913595841389442942, -242.4574432119242999 ) ) ;
#105914=ADVANCED_FACE ( 'NONE', ( #48605 ), #105989, .F. ) ;
#105933=ORIENTED_EDGE ( 'NONE', *, *, #32224, .F. ) ;
#105937=AXIS2_PLACEMENT_3D ( 'NONE', #108760, #168791, #171356 ) ;
#105939=DIRECTION ( 'NONE',  ( 1.000000000000000000, 0.000000000000000000, 0.000000000000000000 ) ) ;
#105942=VECTOR ( 'NONE', #90837, 1000.000000000000000 ) ;
#105954=TOROIDAL_SURFACE ( 'NONE', #60184, 11.65000000000000036, 0.1000000000000000056 ) ;
#105955=ORIENTED_EDGE ( 'NONE', *, *, #84103, .F. ) ;
#105961=ORIENTED_EDGE ( 'NONE', *, *, #180597, .F. ) ;
#105989=SPHERICAL_SURFACE ( 'NONE', #207159, 0.1000000000000000056 ) ;
#105994=TOROIDAL_SURFACE ( 'NONE', #43485, 0.2000000000000000111, 0.1000000000000000056 ) ;
#105997=CARTESIAN_POINT ( 'NONE',  ( -20.64999999999999858, 7.533155231024649012, -235.5891828794142384 ) ) ;
#106022=CIRCLE ( 'NONE', #26969, 0.09999999999999553690 ) ;
#106036=VECTOR ( 'NONE', #243907, 1000.000000000000227 ) ;
#106074=VECTOR ( 'NONE', #215242, 1000.000000000000114 ) ;
#106077=ORIENTED_EDGE ( 'NONE', *, *, #19973, .F. ) ;
#106085=DIRECTION ( 'NONE',  ( 6.938893903907223644E-15, -0.9770955615653313941, -0.2128009952263606730 ) ) ;
#106093=CARTESIAN_POINT ( 'NONE',  ( -22.59999999999999787, 1.148907358139439339E-11, -201.0000000000015064 ) ) ;
#106096=VERTEX_POINT ( 'NONE', #190721 ) ;
#106097=CARTESIAN_POINT ( 'NONE',  ( 18.50000000000000000, -7.631834139420993424, -210.1304494778855485 ) ) ;
#106106=ORIENTED_EDGE ( 'NONE', *, *, #219615, .T. ) ;
#106121=DIRECTION ( 'NONE',  ( 0.000000000000000000, 0.7397890806274223241, 0.6728388485993012091 ) ) ;
#106124=FACE_OUTER_BOUND ( 'NONE', #177562, .T. ) ;
#106138=EDGE_CURVE ( 'NONE', #29211, #213820, #116308, .T. ) ;
#106141=CIRCLE ( 'NONE', #64477, 2.100000000000008527 ) ;
#106167=AXIS2_PLACEMENT_3D ( 'NONE', #139890, #18682, #60366 ) ;
#106196=CARTESIAN_POINT ( 'NONE',  ( 20.85000000000000142, 7.128833340094563376, -233.7327013124401276 ) ) ;
#106197=DIRECTION ( 'NONE',  ( -1.000000000000000000, 0.000000000000000000, 0.000000000000000000 ) ) ;
#106221=DIRECTION ( 'NONE',  ( 1.000000000000000000, 2.885090398161910739E-16, 6.283419270304611573E-17 ) ) ;
#106226=AXIS2_PLACEMENT_3D ( 'NONE', #242428, #200749, #222867 ) ;
#106264=TOROIDAL_SURFACE ( 'NONE', #239571, 12.77499999999999858, 0.1000000000000000056 ) ;
#106282=DIRECTION ( 'NONE',  ( -1.836970198721029934E-16, 0.9770955615653316162, 0.2128009952263604232 ) ) ;
#106283=CIRCLE ( 'NONE', #202174, 0.6000000000000064171 ) ;
#106298=DIRECTION ( 'NONE',  ( 0.000000000000000000, -0.9770955615653553750, -0.2128009952262508719 ) ) ;
#106308=VERTEX_POINT ( 'NONE', #106986 ) ;
#106352=DIRECTION ( 'NONE',  ( 0.000000000000000000, -0.9770955615653316162, -0.2128009952263604232 ) ) ;
#106401=ORIENTED_EDGE ( 'NONE', *, *, #85763, .F. ) ;
#106417=DIRECTION ( 'NONE',  ( -1.000000000000000000, 0.000000000000000000, -0.000000000000000000 ) ) ;
#106438=CIRCLE ( 'NONE', #148160, 6.258578643762701788 ) ;
#106446=ADVANCED_FACE ( 'NONE', ( #215086 ), #19462, .T. ) ;
#106489=DIRECTION ( 'NONE',  ( 0.7071067811865486830, -0.1504730267678052180, 0.6909108974501224631 ) ) ;
#106495=CARTESIAN_POINT ( 'NONE',  ( 21.05000000000000071, 2.585532092011767702, -212.8717110730202933 ) ) ;
#106522=AXIS2_PLACEMENT_3D ( 'NONE', #41567, #121111, #71718 ) ;
#106560=EDGE_CURVE ( 'NONE', #196725, #110507, #82396, .T. ) ;
#106579=LINE ( 'NONE', #123605, #222015 ) ;
#106590=FACE_OUTER_BOUND ( 'NONE', #252418, .T. ) ;
#106597=DIRECTION ( 'NONE',  ( 0.000000000000000000, -0.2128009952263603677, 0.9770955615653313941 ) ) ;
#106599=ORIENTED_EDGE ( 'NONE', *, *, #23461, .F. ) ;
#106628=CIRCLE ( 'NONE', #219069, 0.09999999999999130418 ) ;
#106687=ORIENTED_EDGE ( 'NONE', *, *, #175943, .T. ) ;
#106708=ORIENTED_EDGE ( 'NONE', *, *, #248042, .F. ) ;
#106738=VERTEX_POINT ( 'NONE', #173135 ) ;
#106756=DIRECTION ( 'NONE',  ( 0.000000000000000000, -0.2128009952263650861, 0.9770955615653305060 ) ) ;
#106757=LINE ( 'NONE', #165476, #7253 ) ;
#106759=EDGE_CURVE ( 'NONE', #220140, #143709, #120063, .T. ) ;
#106761=FACE_OUTER_BOUND ( 'NONE', #162839, .T. ) ;
#106786=FACE_OUTER_BOUND ( 'NONE', #159767, .T. ) ;
#106795=CARTESIAN_POINT ( 'NONE',  ( -18.51697539158856998, 18.38637412622487588, -236.9471295141160567 ) ) ;
#106805=CARTESIAN_POINT ( 'NONE',  ( 18.41832399655381991, -0.9152169696499932172, -242.2974987189348610 ) ) ;
#106830=ORIENTED_EDGE ( 'NONE', *, *, #18418, .T. ) ;
#106838=DIRECTION ( 'NONE',  ( 0.000000000000000000, -0.2128009952263900384, 0.9770955615653251769 ) ) ;
#106862=VECTOR ( 'NONE', #132821, 1000.000000000000227 ) ;
#106893=ORIENTED_EDGE ( 'NONE', *, *, #110340, .F. ) ;
#106905=EDGE_CURVE ( 'NONE', #31696, #90944, #3485, .T. ) ;
#106923=ORIENTED_EDGE ( 'NONE', *, *, #197644, .F. ) ;
#106929=FACE_OUTER_BOUND ( 'NONE', #175258, .T. ) ;
#106942=CARTESIAN_POINT ( 'NONE',  ( -18.59999999999999787, 12.87592094156238609, -205.3750039893633073 ) ) ;
#106946=ORIENTED_EDGE ( 'NONE', *, *, #27608, .T. ) ;
#106986=CARTESIAN_POINT ( 'NONE',  ( -20.64999999999999858, 8.653397185701672711, -220.7611668973962367 ) ) ;
#106990=DIRECTION ( 'NONE',  ( 0.000000000000000000, -0.08413937888704771384, 0.9964539953858891908 ) ) ;
#107010=CARTESIAN_POINT ( 'NONE',  ( -20.64999999999999858, -6.688413578037177842, -212.5825622730469036 ) ) ;
#107016=DIRECTION ( 'NONE',  ( 0.000000000000000000, -0.2128009952263604232, 0.9770955615653316162 ) ) ;
#107027=ORIENTED_EDGE ( 'NONE', *, *, #157508, .T. ) ;
#107045=EDGE_CURVE ( 'NONE', #241204, #26573, #253468, .T. ) ;
#107054=EDGE_LOOP ( 'NONE', ( #183181, #44720, #131198, #47230, #182714 ) ) ;
#107104=ORIENTED_EDGE ( 'NONE', *, *, #4137, .F. ) ;
#107106=VERTEX_POINT ( 'NONE', #205468 ) ;
#107128=EDGE_LOOP ( 'NONE', ( #8577, #135521, #237425, #171105 ) ) ;
#107139=DIRECTION ( 'NONE',  ( -1.000000000000000000, 0.000000000000000000, 0.000000000000000000 ) ) ;
#107173=ORIENTED_EDGE ( 'NONE', *, *, #90028, .T. ) ;
#107180=DIRECTION ( 'NONE',  ( 0.000000000000000000, 0.8149014228131966631, -0.5795995782408988051 ) ) ;
#107181=DIRECTION ( 'NONE',  ( 0.000000000000000000, -0.08413937888704771384, 0.9964539953858891908 ) ) ;
#107189=EDGE_CURVE ( 'NONE', #220406, #58187, #104280, .T. ) ;
#107205=CARTESIAN_POINT ( 'NONE',  ( 18.39999999999999858, -0.9152171842607033092, -242.2974985173726452 ) ) ;
#107221=CARTESIAN_POINT ( 'NONE',  ( 20.85000000000000142, 7.661991824395936845, -241.5144583139544636 ) ) ;
#107222=VECTOR ( 'NONE', #141727, 999.9999999999998863 ) ;
#107253=ORIENTED_EDGE ( 'NONE', *, *, #58589, .T. ) ;
#107334=VERTEX_POINT ( 'NONE', #64059 ) ;
#107356=CARTESIAN_POINT ( 'NONE',  ( 18.59999999999999787, 7.882824859404637508, -245.3558965132535832 ) ) ;
#107357=EDGE_CURVE ( 'NONE', #192375, #121414, #199986, .T. ) ;
#107374=EDGE_CURVE ( 'NONE', #224443, #190519, #120898, .T. ) ;
#107402=CARTESIAN_POINT ( 'NONE',  ( 18.59999994388910238, -7.620950066970707759, -210.0092139826364814 ) ) ;
#107406=FACE_OUTER_BOUND ( 'NONE', #38728, .T. ) ;
#107474=ORIENTED_EDGE ( 'NONE', *, *, #190594, .T. ) ;
#107485=FACE_OUTER_BOUND ( 'NONE', #254399, .T. ) ;
#107515=AXIS2_PLACEMENT_3D ( 'NONE', #233772, #33042, #53840 ) ;
#107549=ORIENTED_EDGE ( 'NONE', *, *, #199633, .T. ) ;
#107568=DIRECTION ( 'NONE',  ( -0.000000000000000000, 0.07893460099012014619, -0.9968797965484758050 ) ) ;
#107574=FACE_OUTER_BOUND ( 'NONE', #91, .T. ) ;
#107576=DIRECTION ( 'NONE',  ( 0.000000000000000000, 0.2128009952263485993, -0.9770955615653341697 ) ) ;
#107595=EDGE_CURVE ( 'NONE', #114637, #169963, #104078, .T. ) ;
#107614=DIRECTION ( 'NONE',  ( -0.000000000000000000, 0.2128009952263603677, -0.9770955615653313941 ) ) ;
#107626=CARTESIAN_POINT ( 'NONE',  ( -22.50000000000000000, 1.148907358139439339E-11, -201.0000000000015064 ) ) ;
#107628=ORIENTED_EDGE ( 'NONE', *, *, #223705, .T. ) ;
#107715=DIRECTION ( 'NONE',  ( 0.000000000000000000, 0.2128009952263605065, -0.9770955615653315052 ) ) ;
#107749=CIRCLE ( 'NONE', #153607, 0.09999999999999939493 ) ;
#107750=AXIS2_PLACEMENT_3D ( 'NONE', #110707, #130258, #209815 ) ;
#107752=DIRECTION ( 'NONE',  ( 0.000000000000000000, 0.2128009952263403282, -0.9770955615653358350 ) ) ;
#107760=CARTESIAN_POINT ( 'NONE',  ( -20.54999999999999716, 8.751106741858205140, -220.7398867978736234 ) ) ;
#107761=CARTESIAN_POINT ( 'NONE',  ( 21.08804582317334209, 11.30290901145985138, -211.1778474225062894 ) ) ;
#107763=CIRCLE ( 'NONE', #61985, 4.049999999999999822 ) ;
#107768=CIRCLE ( 'NONE', #220219, 0.1000000000000055844 ) ;
#107776=ORIENTED_EDGE ( 'NONE', *, *, #181619, .T. ) ;
#107782=CARTESIAN_POINT ( 'NONE',  ( -18.59999999999999787, 2.923777413779037548, -208.5507632484912222 ) ) ;
#107825=DIRECTION ( 'NONE',  ( -1.000000000000000000, 0.000000000000000000, 0.000000000000000000 ) ) ;
#107843=EDGE_CURVE ( 'NONE', #157474, #184568, #158674, .T. ) ;
#107855=CARTESIAN_POINT ( 'NONE',  ( -23.15000000000000213, 4.554494125284476169, -212.9355439031026265 ) ) ;
#107860=CARTESIAN_POINT ( 'NONE',  ( -20.94999999999999929, 0.6171228861679354250, -203.8335771285409521 ) ) ;
#107880=DIRECTION ( 'NONE',  ( -3.265361837132812600E-16, 0.9770955615653313941, 0.2128009952263603677 ) ) ;
#107891=EDGE_CURVE ( 'NONE', #118478, #70808, #66881, .T. ) ;
#107896=AXIS2_PLACEMENT_3D ( 'NONE', #44488, #124023, #201 ) ;
#107942=DIRECTION ( 'NONE',  ( 0.000000000000000000, -0.07893460099012014619, 0.9968797965484758050 ) ) ;
#107949=CARTESIAN_POINT ( 'NONE',  ( -20.85000000000000142, 7.128833340094563376, -233.7327013124401276 ) ) ;
#108011=AXIS2_PLACEMENT_3D ( 'NONE', #7764, #23506, #122584 ) ;
#108015=TOROIDAL_SURFACE ( 'NONE', #207977, 4.099999999999999645, 0.1000000000000000056 ) ;
#108023=CARTESIAN_POINT ( 'NONE',  ( 21.05000000000000071, 16.98881331171930498, -224.4946931418895417 ) ) ;
#108036=CIRCLE ( 'NONE', #228672, 0.2000000000000111688 ) ;
#108039=EDGE_LOOP ( 'NONE', ( #252157, #107253, #137834, #35614, #139613 ) ) ;
#108049=CARTESIAN_POINT ( 'NONE',  ( -22.39999999999999858, 11.40444339177023814, -198.6185779617709670 ) ) ;
#108052=CARTESIAN_POINT ( 'NONE',  ( 21.00000000000000000, 12.15477401631902232, -210.9923204818763622 ) ) ;
#108070=AXIS2_PLACEMENT_3D ( 'NONE', #30801, #93308, #252366 ) ;
#108108=CARTESIAN_POINT ( 'NONE',  ( -20.64999999999999858, 7.128833340094563376, -233.7327013124401276 ) ) ;
#108113=CARTESIAN_POINT ( 'NONE',  ( 20.94999999999999929, 8.433899723187009201, -209.4150263691077782 ) ) ;
#108134=DIRECTION ( 'NONE',  ( 0.000000000000000000, -0.7397890806274223241, -0.6728388485993012091 ) ) ;
#108182=AXIS2_PLACEMENT_3D ( 'NONE', #110831, #147398, #86102 ) ;
#108187=EDGE_CURVE ( 'NONE', #90864, #182918, #73418, .T. ) ;
#108190=EDGE_LOOP ( 'NONE', ( #59777, #180019, #134180, #24731 ) ) ;
#108191=CARTESIAN_POINT ( 'NONE',  ( 20.94999999999999929, 7.533155231024652565, -235.5891828794142384 ) ) ;
#108193=ADVANCED_FACE ( 'NONE', ( #56613 ), #134879, .F. ) ;
#108199=ORIENTED_EDGE ( 'NONE', *, *, #170464, .F. ) ;
#108219=ORIENTED_EDGE ( 'NONE', *, *, #70443, .F. ) ;
#108246=ORIENTED_EDGE ( 'NONE', *, *, #129665, .F. ) ;
#108249=DIRECTION ( 'NONE',  ( 0.000000000000000000, 0.2128009952263604232, -0.9770955615653316162 ) ) ;
#108254=PLANE ( 'NONE',  #40429 ) ;
#108256=DIRECTION ( 'NONE',  ( 1.000000000000000000, 0.000000000000000000, 0.000000000000000000 ) ) ;
#108263=DIRECTION ( 'NONE',  ( 1.000000000000000000, 0.000000000000000000, 0.000000000000000000 ) ) ;
#108278=DIRECTION ( 'NONE',  ( -1.000000000000000000, -0.000000000000000000, -0.000000000000000000 ) ) ;
#108317=EDGE_CURVE ( 'NONE', #54351, #14295, #224704, .T. ) ;
#108318=DIRECTION ( 'NONE',  ( 0.000000000000000000, 0.2128009952263603677, -0.9770955615653313941 ) ) ;
#108333=CIRCLE ( 'NONE', #254055, 0.1999999999999987899 ) ;
#108344=CARTESIAN_POINT ( 'NONE',  ( -20.54999999999999716, 7.128833340094563376, -233.7327013124401276 ) ) ;
#108366=ORIENTED_EDGE ( 'NONE', *, *, #27844, .F. ) ;
#108377=DIRECTION ( 'NONE',  ( 0.000000000000000000, -0.9770955615653316162, -0.2128009952263604232 ) ) ;
#108417=CIRCLE ( 'NONE', #254136, 11.74999999999999289 ) ;
#108418=CARTESIAN_POINT ( 'NONE',  ( 21.12802099929860944, 11.18586598252357867, -211.0991417416504419 ) ) ;
#108450=CARTESIAN_POINT ( 'NONE',  ( -21.53699400381544748, 6.632243066309741586, -199.5555681750817314 ) ) ;
#108452=ADVANCED_FACE ( 'NONE', ( #211586 ), #91632, .T. ) ;
#108471=CARTESIAN_POINT ( 'NONE',  ( 18.49999999999998934, 15.26077403838592161, -222.9041953915167937 ) ) ;
#108477=ORIENTED_EDGE ( 'NONE', *, *, #115220, .F. ) ;
#108489=CARTESIAN_POINT ( 'NONE',  ( 21.13498764882293557, 6.346487175175731466, -199.6161075385196852 ) ) ;
#108494=AXIS2_PLACEMENT_3D ( 'NONE', #56357, #216730, #77214 ) ;
#108521=CARTESIAN_POINT ( 'NONE',  ( -23.25000000000000000, 1.148907358139439339E-11, -201.0000000000015064 ) ) ;
#108554=EDGE_CURVE ( 'NONE', #102565, #55232, #161252, .T. ) ;
#108575=VECTOR ( 'NONE', #234656, 1000.000000000000227 ) ;
#108577=AXIS2_PLACEMENT_3D ( 'NONE', #80347, #59497, #200331 ) ;
#108596=DIRECTION ( 'NONE',  ( 0.000000000000000000, -0.2128009952263601734, 0.9770955615653315052 ) ) ;
#108602=DIRECTION ( 'NONE',  ( -1.000000000000000000, -1.794895427898103559E-16, -3.909090864890002444E-17 ) ) ;
#108624=DIRECTION ( 'NONE',  ( -1.000000000000000000, 0.000000000000000000, 0.000000000000000000 ) ) ;
#108628=TOROIDAL_SURFACE ( 'NONE', #62843, 11.89999999999999858, 0.1000000000000000056 ) ;
#108648=DIRECTION ( 'NONE',  ( 1.000000000000000000, -0.000000000000000000, -0.000000000000000000 ) ) ;
#108662=CARTESIAN_POINT ( 'NONE',  ( 18.59999999999999076, 15.22030141505243961, -222.9130098973476777 ) ) ;
#108673=EDGE_CURVE ( 'NONE', #13347, #78551, #145827, .T. ) ;
#108702=ORIENTED_EDGE ( 'NONE', *, *, #141937, .T. ) ;
#108717=CARTESIAN_POINT ( 'NONE',  ( 21.06089410995820899, 13.07631742462289282, -210.6405384895012958 ) ) ;
#108719=DIRECTION ( 'NONE',  ( -1.000000000000000000, -0.000000000000000000, -0.000000000000000000 ) ) ;
#108746=DIRECTION ( 'NONE',  ( 0.000000000000000000, -0.9770955615653316162, -0.2128009952263604232 ) ) ;
#108750=CARTESIAN_POINT ( 'NONE',  ( -22.50000000000092371, -2.401771312553021342, -189.4980873520049443 ) ) ;
#108757=ORIENTED_EDGE ( 'NONE', *, *, #58711, .F. ) ;
#108760=CARTESIAN_POINT ( 'NONE',  ( -22.39999999999999858, 11.36188319272496727, -198.4231588494578773 ) ) ;
#108763=( BOUNDED_SURFACE ( )  B_SPLINE_SURFACE ( 3, 2, ( 
 ( #257771, #96168, #54486 ),
 ( #136579, #174501, #117038 ),
 ( #94891, #216122, #214843 ),
 ( #252678, #218681, #119618 ),
 ( #134020, #157482, #75370 ),
 ( #173210, #40099, #37513 ) ),
 .UNSPECIFIED., .F., .F., .F. ) 
 B_SPLINE_SURFACE_WITH_KNOTS ( ( 4, 2, 4 ),
 ( 3, 3 ),
 ( 1.570796326794895448, 2.356194490192343505, 3.141592653589791784 ),
 ( 0.000000000000000000, 1.000000000000000000 ),
 .UNSPECIFIED. ) 
 GEOMETRIC_REPRESENTATION_ITEM ( )  RATIONAL_B_SPLINE_SURFACE ( (
 ( 1.000000000000000000, 0.7071067811865355823, 1.000000000000000000),
 ( 1.000000000000000000, 0.6611148371776521815, 1.000000000000000000),
 ( 1.000000000000000000, 0.6092287576699784157, 1.000000000000000000),
 ( 1.000000000000000000, 0.5278258667053503661, 1.000000000000000000),
 ( 1.000000000000000000, 0.4993418825337702094, 1.000000000000000000),
 ( 1.000000000000000000, 0.4999999999997460920, 1.000000000000000000) ) ) 
 REPRESENTATION_ITEM ( '' )  SURFACE ( )  );
#108770=DIRECTION ( 'NONE',  ( -1.000000000000000000, 0.000000000000000000, 0.000000000000000000 ) ) ;
#108774=CARTESIAN_POINT ( 'NONE',  ( 20.84999999999999787, 17.13730476842946970, -224.4716215546872036 ) ) ;
#108792=ORIENTED_EDGE ( 'NONE', *, *, #14134, .F. ) ;
#108802=CARTESIAN_POINT ( 'NONE',  ( 23.14999999999999503, 15.92646454033040371, -219.3818586450342423 ) ) ;
#108806=EDGE_CURVE ( 'NONE', #208696, #206404, #34920, .T. ) ;
#108812=ADVANCED_FACE ( 'NONE', ( #191422 ), #165332, .T. ) ;
#108818=EDGE_LOOP ( 'NONE', ( #194680, #234437, #194212, #16542 ) ) ;
#108820=LINE ( 'NONE', #226168, #232015 ) ;
#108866=EDGE_CURVE ( 'NONE', #114396, #137793, #38679, .T. ) ;
#108869=CARTESIAN_POINT ( 'NONE',  ( -21.55000000000000071, 9.788464569039593499, -211.4053333142630891 ) ) ;
#108884=LINE ( 'NONE', #226232, #236466 ) ;
#108889=FACE_OUTER_BOUND ( 'NONE', #70485, .T. ) ;
#108931=DIRECTION ( 'NONE',  ( -0.000000000000000000, 0.9770955615653313941, 0.2128009952263603954 ) ) ;
#108936=DIRECTION ( 'NONE',  ( -1.000000000000000000, -0.000000000000000000, -0.000000000000000000 ) ) ;
#108948=AXIS2_PLACEMENT_3D ( 'NONE', #154912, #212306, #230580 ) ;
#108952=ORIENTED_EDGE ( 'NONE', *, *, #152690, .T. ) ;
#108961=CIRCLE ( 'NONE', #113076, 0.6000000000000064171 ) ;
#108996=CIRCLE ( 'NONE', #46453, 0.1000000000000003109 ) ;
#108997=DIRECTION ( 'NONE',  ( -1.000000000000000000, 0.000000000000000000, -0.000000000000000000 ) ) ;
#109011=FACE_OUTER_BOUND ( 'NONE', #66538, .T. ) ;
#109016=CARTESIAN_POINT ( 'NONE',  ( -20.94999999999999929, 0.6869237119019839799, -212.7787591058053067 ) ) ;
#109075=CARTESIAN_POINT ( 'NONE',  ( 23.14999999999999503, 15.92646454033040371, -219.3818586450342423 ) ) ;
#109090=AXIS2_PLACEMENT_3D ( 'NONE', #251715, #215156, #135605 ) ;
#109101=ORIENTED_EDGE ( 'NONE', *, *, #53062, .F. ) ;
#109132=DIRECTION ( 'NONE',  ( -0.000000000000000000, -0.2128009952263604787, 0.9770955615653313941 ) ) ;
#109199=CARTESIAN_POINT ( 'NONE',  ( 20.94999999999999929, 8.629318835500072282, -209.3724661700624949 ) ) ;
#109208=ORIENTED_EDGE ( 'NONE', *, *, #201488, .T. ) ;
#109280=ORIENTED_EDGE ( 'NONE', *, *, #201847, .T. ) ;
#109283=DIRECTION ( 'NONE',  ( 0.000000000000000000, -0.2128009952263403282, 0.9770955615653358350 ) ) ;
#109295=ORIENTED_EDGE ( 'NONE', *, *, #31957, .T. ) ;
#109318=DIRECTION ( 'NONE',  ( 1.000000000000000000, 0.000000000000000000, 0.000000000000000000 ) ) ;
#109322=FACE_OUTER_BOUND ( 'NONE', #101518, .T. ) ;
#109346=CARTESIAN_POINT ( 'NONE',  ( -20.94999999999999929, 16.98881331171929787, -224.4946931418895417 ) ) ;
#109348=AXIS2_PLACEMENT_3D ( 'NONE', #134219, #135499, #215055 ) ;
#109356=CARTESIAN_POINT ( 'NONE',  ( -23.25000000000000000, 6.268811756569107274, -220.3853799378769622 ) ) ;
#109367=VECTOR ( 'NONE', #31305, 1000.000000000000000 ) ;
#109370=DIRECTION ( 'NONE',  ( 0.000000000000000000, -0.2128009952263361926, 0.9770955615653368342 ) ) ;
#109388=CARTESIAN_POINT ( 'NONE',  ( 20.94999999999999929, -3.770473190032740174, -225.9805569534692324 ) ) ;
#109407=ORIENTED_EDGE ( 'NONE', *, *, #118426, .F. ) ;
#109439=ORIENTED_EDGE ( 'NONE', *, *, #234546, .F. ) ;
#109455=ORIENTED_EDGE ( 'NONE', *, *, #35578, .T. ) ;
#109476=EDGE_LOOP ( 'NONE', ( #63851, #120796, #54627, #6113 ) ) ;
#109540=EDGE_CURVE ( 'NONE', #87224, #191212, #70043, .T. ) ;
#109547=DIRECTION ( 'NONE',  ( 1.000000000000000000, 0.000000000000000000, 0.000000000000000000 ) ) ;
#109580=CARTESIAN_POINT ( 'NONE',  ( -21.05000000000000071, -4.871452838297995136, -233.3782557782877518 ) ) ;
#109583=EDGE_CURVE ( 'NONE', #185772, #184179, #178381, .T. ) ;
#109585=CIRCLE ( 'NONE', #59669, 12.87499999999999467 ) ;
#109594=CIRCLE ( 'NONE', #126145, 0.1000000000000054040 ) ;
#109595=EDGE_CURVE ( 'NONE', #175634, #170209, #231201, .T. ) ;
#109615=DIRECTION ( 'NONE',  ( 0.000000000000000000, -0.9525900758537706459, 0.3042567129660534997 ) ) ;
#109616=EDGE_CURVE ( 'NONE', #231419, #127836, #153264, .T. ) ;
#109685=CARTESIAN_POINT ( 'NONE',  ( 20.94999999999999929, -5.637547571910522137, -233.4427589080015650 ) ) ;
#109705=EDGE_LOOP ( 'NONE', ( #131271, #142112, #195531, #207742, #239718 ) ) ;
#109727=DIRECTION ( 'NONE',  ( 1.000000000000000000, 0.000000000000000000, 0.000000000000000000 ) ) ;
#109742=PRODUCT_DEFINITION_SHAPE ( 'NONE', 'NONE',  #228620 ) ;
#109751=EDGE_CURVE ( 'NONE', #127544, #222677, #20334, .T. ) ;
#109779=ORIENTED_EDGE ( 'NONE', *, *, #114504, .T. ) ;
#109781=DIRECTION ( 'NONE',  ( 0.000000000000000000, 0.2128009952263403282, -0.9770955615653358350 ) ) ;
#109793=DIRECTION ( 'NONE',  ( 1.000000000000000000, 0.000000000000000000, 0.000000000000000000 ) ) ;
#109848=VERTEX_POINT ( 'NONE', #185327 ) ;
#109854=VERTEX_POINT ( 'NONE', #5373 ) ;
#109880=DIRECTION ( 'NONE',  ( -1.000000000000000000, 0.000000000000000000, 0.000000000000000000 ) ) ;
#109927=VECTOR ( 'NONE', #204581, 1000.000000000000227 ) ;
#109942=DIRECTION ( 'NONE',  ( 0.000000000000000000, 0.9968797965484755830, 0.07893460099012303277 ) ) ;
#109948=CARTESIAN_POINT ( 'NONE',  ( 20.94999999999999929, 7.128833340094563376, -233.7327013124401276 ) ) ;
#109966=DIRECTION ( 'NONE',  ( -0.000000000000000000, -0.2128009952263603677, 0.9770955615653313941 ) ) ;
#109970=VERTEX_POINT ( 'NONE', #87490 ) ;
#109978=ADVANCED_FACE ( 'NONE', ( #247866 ), #249166, .F. ) ;
#109985=ADVANCED_FACE ( 'NONE', ( #227012 ), #152652, .F. ) ;
#109987=CARTESIAN_POINT ( 'NONE',  ( 22.39999999999999503, 11.48087284840413425, -198.4995883060917947 ) ) ;
#109990=CARTESIAN_POINT ( 'NONE',  ( 22.14074124539698829, 7.199733713072927088, -199.3305999336096761 ) ) ;
#110064=ORIENTED_EDGE ( 'NONE', *, *, #218621, .F. ) ;
#110072=CARTESIAN_POINT ( 'NONE',  ( -23.25000000000000000, 7.128833340094563376, -233.7327013124401276 ) ) ;
#110086=ORIENTED_EDGE ( 'NONE', *, *, #18745, .T. ) ;
#110091=ORIENTED_EDGE ( 'NONE', *, *, #104198, .T. ) ;
#110119=CARTESIAN_POINT ( 'NONE',  ( -18.41799967126737059, -7.785976380097459071, -209.8926136578000126 ) ) ;
#110139=VECTOR ( 'NONE', #144937, 1000.000000000000227 ) ;
#110145=VERTEX_POINT ( 'NONE', #199468 ) ;
#110159=AXIS2_PLACEMENT_3D ( 'NONE', #13135, #172244, #19553 ) ;
#110170=CYLINDRICAL_SURFACE ( 'NONE', #175427, 0.1000000000000055844 ) ;
#110210=CIRCLE ( 'NONE', #77083, 0.09999999999999939493 ) ;
#110234=VECTOR ( 'NONE', #124189, 1000.000000000000227 ) ;
#110244=ADVANCED_FACE ( 'NONE', ( #243707 ), #80760, .T. ) ;
#110308=ADVANCED_FACE ( 'NONE', ( #155867 ), #234082, .T. ) ;
#110340=EDGE_CURVE ( 'NONE', #17245, #130685, #230786, .T. ) ;
#110342=PLANE ( 'NONE',  #195801 ) ;
#110343=ORIENTED_EDGE ( 'NONE', *, *, #134694, .T. ) ;
#110373=EDGE_CURVE ( 'NONE', #119503, #30937, #217074, .T. ) ;
#110374=AXIS2_PLACEMENT_3D ( 'NONE', #251477, #211080, #250206 ) ;
#110407=CARTESIAN_POINT ( 'NONE',  ( 20.85000000000000142, 14.73746888278882849, -235.8584165281851028 ) ) ;
#110410=AXIS2_PLACEMENT_3D ( 'NONE', #173894, #215530, #253375 ) ;
#110414=EDGE_LOOP ( 'NONE', ( #196741, #49111, #128881, #133925 ) ) ;
#110434=LINE ( 'NONE', #129981, #14539 ) ;
#110452=CIRCLE ( 'NONE', #118863, 0.1000000000000054040 ) ;
#110461=ORIENTED_EDGE ( 'NONE', *, *, #170464, .T. ) ;
#110462=CIRCLE ( 'NONE', #251936, 11.70000000000000284 ) ;
#110465=AXIS2_PLACEMENT_3D ( 'NONE', #102834, #100267, #2460 ) ;
#110491=ORIENTED_EDGE ( 'NONE', *, *, #178765, .F. ) ;
#110507=VERTEX_POINT ( 'NONE', #117997 ) ;
#110510=DIRECTION ( 'NONE',  ( 1.000000000000000000, -0.000000000000000000, -0.000000000000000000 ) ) ;
#110519=ORIENTED_EDGE ( 'NONE', *, *, #66839, .F. ) ;
#110523=ORIENTED_EDGE ( 'NONE', *, *, #108806, .F. ) ;
#110528=CIRCLE ( 'NONE', #106226, 0.09999999999999939493 ) ;
#110543=CARTESIAN_POINT ( 'NONE',  ( -18.50000000000000000, 4.064367954407505756, -211.9684786640956418 ) ) ;
#110560=DIRECTION ( 'NONE',  ( 0.000000000000000000, -0.2128009952263606175, 0.9770955615653315052 ) ) ;
#110563=DIRECTION ( 'NONE',  ( 1.000000000000000000, 0.000000000000000000, 0.000000000000000000 ) ) ;
#110599=LINE ( 'NONE', #8941, #257800 ) ;
#110602=DIRECTION ( 'NONE',  ( 1.000000000000000000, 0.000000000000000000, 0.000000000000000000 ) ) ;
#110632=CARTESIAN_POINT ( 'NONE',  ( -23.15000000000000213, 13.96869538424788360, -210.3925794786332233 ) ) ;
#110671=CARTESIAN_POINT ( 'NONE',  ( 18.40000000000000213, -0.6805341177324860658, -242.5179126613615495 ) ) ;
#110675=ORIENTED_EDGE ( 'NONE', *, *, #74926, .T. ) ;
#110682=CARTESIAN_POINT ( 'NONE',  ( -23.25000000000000000, -5.011722593499800205, -233.2041167654973322 ) ) ;
#110687=DIRECTION ( 'NONE',  ( 1.000000000000000000, 0.000000000000000000, 0.000000000000000000 ) ) ;
#110691=B_SPLINE_CURVE_WITH_KNOTS ( 'NONE', 3,
 ( #137021, #216552, #11963, #71924 ),
 .UNSPECIFIED., .F., .F.,
 ( 4, 4 ),
 ( 0.000000000000000000, 0.001767853679387115145 ),
 .UNSPECIFIED. ) ;
#110703=CARTESIAN_POINT ( 'NONE',  ( -22.45372860728439690, -2.464509553302064671, -189.6138598038565419 ) ) ;
#110705=DIRECTION ( 'NONE',  ( -4.391705002472928105E-16, 0.9770955615653315052, 0.2128009952263601179 ) ) ;
#110707=CARTESIAN_POINT ( 'NONE',  ( 23.14999999999999503, 17.01923898301590654, -224.3994341343041867 ) ) ;
#110777=CIRCLE ( 'NONE', #6729, 3.900000000000002132 ) ;
#110784=CIRCLE ( 'NONE', #35968, 4.049999999999995381 ) ;
#110800=AXIS2_PLACEMENT_3D ( 'NONE', #136381, #727, #80256 ) ;
#110801=CARTESIAN_POINT ( 'NONE',  ( 18.59999999999998366, 14.80545736607782814, -235.9842437978701639 ) ) ;
#110807=CARTESIAN_POINT ( 'NONE',  ( 23.15000000000000213, -4.914013037343258894, -233.1828366659746905 ) ) ;
#110810=ORIENTED_EDGE ( 'NONE', *, *, #180597, .T. ) ;
#110825=CARTESIAN_POINT ( 'NONE',  ( -21.13422380239141773, -1.381786344668824107, -194.6553994825906102 ) ) ;
#110826=CARTESIAN_POINT ( 'NONE',  ( -21.14999999999999858, -11.38316329222462464, -203.4791315943886048 ) ) ;
#110831=CARTESIAN_POINT ( 'NONE',  ( 20.94999999999999574, 0.6656436123793491033, -212.6810495496487476 ) ) ;
#110833=CIRCLE ( 'NONE', #56622, 7.899999999999991473 ) ;
#110862=ADVANCED_FACE ( 'NONE', ( #92540 ), #6768, .T. ) ;
#110863=CARTESIAN_POINT ( 'NONE',  ( 18.59999999999999076, 4.252251777740764460, -211.8999245327126744 ) ) ;
#110867=CARTESIAN_POINT ( 'NONE',  ( 18.49999999999999645, 7.783179459866045313, -245.3643104511423303 ) ) ;
#110888=CIRCLE ( 'NONE', #240066, 0.09999999999999939493 ) ;
#110904=ORIENTED_EDGE ( 'NONE', *, *, #222967, .T. ) ;
#110918=CARTESIAN_POINT ( 'NONE',  ( -21.05000000000000071, -10.38870553492056104, -206.3818953267866902 ) ) ;
#110934=CARTESIAN_POINT ( 'NONE',  ( 22.45301702632625762, -2.464224896439110690, -189.6138028341777897 ) ) ;
#110942=CARTESIAN_POINT ( 'NONE',  ( 21.05000000000000071, 8.001317420522640944, -237.7387931148579980 ) ) ;
#110991=CARTESIAN_POINT ( 'NONE',  ( -23.15000000000000213, 1.148907358139439339E-11, -201.0000000000015064 ) ) ;
#111000=ORIENTED_EDGE ( 'NONE', *, *, #245112, .T. ) ;
#111043=LINE ( 'NONE', #228443, #35280 ) ;
#111056=AXIS2_PLACEMENT_3D ( 'NONE', #179504, #809, #80346 ) ;
#111058=VECTOR ( 'NONE', #215855, 1000.000000000000227 ) ;
#111069=EDGE_CURVE ( 'NONE', #227928, #107106, #220021, .T. ) ;
#111075=ORIENTED_EDGE ( 'NONE', *, *, #181322, .F. ) ;
#111083=LINE ( 'NONE', #249328, #196675 ) ;
#111096=CARTESIAN_POINT ( 'NONE',  ( 18.52643265882457868, 18.39335631088233569, -236.9600537807593241 ) ) ;
#111103=ORIENTED_EDGE ( 'NONE', *, *, #234676, .T. ) ;
#111104=ORIENTED_EDGE ( 'NONE', *, *, #18207, .F. ) ;
#111106=LINE ( 'NONE', #169846, #103293 ) ;
#111162=CARTESIAN_POINT ( 'NONE',  ( 21.14999999999999858, -2.479040261793999722, -189.6172560698084624 ) ) ;
#111167=CIRCLE ( 'NONE', #27995, 0.09999999999999942268 ) ;
#111185=CARTESIAN_POINT ( 'NONE',  ( -20.54999999999999716, -4.161311414658873886, -226.0656773515597706 ) ) ;
#111227=DIRECTION ( 'NONE',  ( 0.000000000000000000, 0.2128009952263485993, -0.9770955615653341697 ) ) ;
#111247=DIRECTION ( 'NONE',  ( -1.000000000000000000, -0.000000000000000000, -0.000000000000000000 ) ) ;
#111253=EDGE_CURVE ( 'NONE', #212172, #75051, #111899, .T. ) ;
#111270=DIRECTION ( 'NONE',  ( 0.000000000000000000, -0.2128009952263485993, 0.9770955615653341697 ) ) ;
#111323=CARTESIAN_POINT ( 'NONE',  ( -20.90851465518105812, 18.40294846151842023, -236.9778203247716419 ) ) ;
#111326=DIRECTION ( 'NONE',  ( 0.000000000000000000, -0.7397890806274222131, -0.6728388485993010981 ) ) ;
#111373=DIRECTION ( 'NONE',  ( -1.000000000000000000, 0.000000000000000000, 0.000000000000000000 ) ) ;
#111375=CIRCLE ( 'NONE', #32299, 0.09999999999999939493 ) ;
#111449=VERTEX_POINT ( 'NONE', #92545 ) ;
#111454=ORIENTED_EDGE ( 'NONE', *, *, #193127, .F. ) ;
#111475=CIRCLE ( 'NONE', #144774, 0.1000000000000054040 ) ;
#111497=ORIENTED_EDGE ( 'NONE', *, *, #160759, .T. ) ;
#111556=ORIENTED_EDGE ( 'NONE', *, *, #47488, .T. ) ;
#111580=ADVANCED_FACE ( 'NONE', ( #1129 ), #158980, .T. ) ;
#111632=CARTESIAN_POINT ( 'NONE',  ( 21.05000000000000071, 8.629318835500072282, -209.3724661700624949 ) ) ;
#111641=CARTESIAN_POINT ( 'NONE',  ( 23.15000000000000213, -5.011722593499792211, -233.2041167654973322 ) ) ;
#111664=VECTOR ( 'NONE', #217959, 1000.000000000000227 ) ;
#111695=ADVANCED_FACE ( 'NONE', ( #33272 ), #220413, .F. ) ;
#111730=DIRECTION ( 'NONE',  ( 0.000000000000000000, 0.9770955615653257320, 0.2128009952263869853 ) ) ;
#111775=ORIENTED_EDGE ( 'NONE', *, *, #113879, .F. ) ;
#111838=ORIENTED_EDGE ( 'NONE', *, *, #62711, .F. ) ;
#111884=CARTESIAN_POINT ( 'NONE',  ( 22.39999999999999503, 11.40444339177024524, -198.6185779617709670 ) ) ;
#111895=EDGE_CURVE ( 'NONE', #81634, #9164, #58048, .T. ) ;
#111897=CIRCLE ( 'NONE', #257557, 0.1000000000000055844 ) ;
#111899=CIRCLE ( 'NONE', #108182, 0.1000000000000055844 ) ;
#111900=EDGE_LOOP ( 'NONE', ( #82502, #98740, #79312, #53699 ) ) ;
#111950=VERTEX_POINT ( 'NONE', #228574 ) ;
#111967=CARTESIAN_POINT ( 'NONE',  ( 20.94999999999999929, 6.703231349641842307, -231.7785101893094577 ) ) ;
#111983=DIRECTION ( 'NONE',  ( 0.000000000000000000, 0.2128009952263403282, -0.9770955615653358350 ) ) ;
#112002=CARTESIAN_POINT ( 'NONE',  ( -22.48479450179659977, -2.433215998327764140, -189.6068383706822260 ) ) ;
#112020=DIRECTION ( 'NONE',  ( 0.000000000000000000, 0.2128009952263403282, -0.9770955615653358350 ) ) ;
#112069=VECTOR ( 'NONE', #70286, 1000.000000000000000 ) ;
#112089=ORIENTED_EDGE ( 'NONE', *, *, #193794, .F. ) ;
#112098=DIRECTION ( 'NONE',  ( 0.000000000000000000, 0.2128009952263485993, -0.9770955615653341697 ) ) ;
#112134=DIRECTION ( 'NONE',  ( 0.000000000000000000, 0.08413937888704771384, -0.9964539953858891908 ) ) ;
#112171=CARTESIAN_POINT ( 'NONE',  ( 23.14999999999998792, 11.38316329224760359, -198.5208684056144079 ) ) ;
#112209=CIRCLE ( 'NONE', #62117, 0.1000000000000076938 ) ;
#112219=ORIENTED_EDGE ( 'NONE', *, *, #132391, .F. ) ;
#112242=FACE_OUTER_BOUND ( 'NONE', #251449, .T. ) ;
#112249=CARTESIAN_POINT ( 'NONE',  ( -21.08078803292166725, -1.270299185012213394, -194.7951902842391405 ) ) ;
#112323=FACE_OUTER_BOUND ( 'NONE', #140746, .T. ) ;
#112343=CARTESIAN_POINT ( 'NONE',  ( 20.95539060131842746, 12.00925073368239282, -206.2176608984306938 ) ) ;
#112413=EDGE_LOOP ( 'NONE', ( #69415, #206807, #185151, #239424, #235911 ) ) ;
#112423=AXIS2_PLACEMENT_3D ( 'NONE', #244296, #202615, #102192 ) ;
#112440=CARTESIAN_POINT ( 'NONE',  ( 18.49999999999999289, 13.20456090973765662, -206.4140623547709765 ) ) ;
#112447=EDGE_CURVE ( 'NONE', #189298, #232474, #171, .T. ) ;
#112481=LINE ( 'NONE', #134573, #158126 ) ;
#112483=CARTESIAN_POINT ( 'NONE',  ( -20.64999999999999858, 6.659649981195239654, -220.3002595397864241 ) ) ;
#112503=AXIS2_PLACEMENT_3D ( 'NONE', #162727, #62332, #216252 ) ;
#112504=DIRECTION ( 'NONE',  ( 1.000000000000000000, 0.000000000000000000, 0.000000000000000000 ) ) ;
#112529=CARTESIAN_POINT ( 'NONE',  ( 20.95483826173899899, 10.49151854554416730, -207.4616709084843080 ) ) ;
#112531=CARTESIAN_POINT ( 'NONE',  ( -18.59999999999999787, 7.128833340094563376, -233.7327013124401276 ) ) ;
#112542=ORIENTED_EDGE ( 'NONE', *, *, #57620, .T. ) ;
#112552=DIRECTION ( 'NONE',  ( 1.000000000000000000, 0.000000000000000000, 0.000000000000000000 ) ) ;
#112578=CARTESIAN_POINT ( 'NONE',  ( -21.05000000000000071, 4.193200906077805712, -212.0298262072164164 ) ) ;
#112587=VERTEX_POINT ( 'NONE', #212565 ) ;
#112611=ADVANCED_FACE ( 'NONE', ( #101549 ), #18188, .T. ) ;
#112664=ORIENTED_EDGE ( 'NONE', *, *, #218201, .F. ) ;
#112697=CARTESIAN_POINT ( 'NONE',  ( -18.58693740092158109, -7.674815071417180334, -209.9633246597199445 ) ) ;
#112719=ADVANCED_FACE ( 'NONE', ( #247519 ), #204527, .T. ) ;
#112731=CARTESIAN_POINT ( 'NONE',  ( 20.94999999999999929, 7.128833340094563376, -233.7327013124401276 ) ) ;
#112754=AXIS2_PLACEMENT_3D ( 'NONE', #242692, #105728, #240145 ) ;
#112842=LINE ( 'NONE', #172865, #233608 ) ;
#112868=ADVANCED_FACE ( 'NONE', ( #192688 ), #56983, .F. ) ;
#112882=ORIENTED_EDGE ( 'NONE', *, *, #216611, .F. ) ;
#112889=PLANE ( 'NONE',  #66462 ) ;
#112924=CARTESIAN_POINT ( 'NONE',  ( 20.94999999999999929, 7.554435330547283556, -235.6868924355707691 ) ) ;
#112967=VERTEX_POINT ( 'NONE', #60850 ) ;
#112971=DIRECTION ( 'NONE',  ( -1.000000000000000000, 0.000000000000000000, 0.000000000000000000 ) ) ;
#112989=DIRECTION ( 'NONE',  ( 0.000000000000000000, 0.2128009952263606730, -0.9770955615653313941 ) ) ;
#113028=CARTESIAN_POINT ( 'NONE',  ( 20.94999999999999929, 10.68863688179707694, -222.5873974249509217 ) ) ;
#113041=ORIENTED_EDGE ( 'NONE', *, *, #80232, .F. ) ;
#113076=AXIS2_PLACEMENT_3D ( 'NONE', #143708, #4192, #245395 ) ;
#113094=DIRECTION ( 'NONE',  ( -0.000000000000000000, 0.9770955615653313941, 0.2128009952263603954 ) ) ;
#113101=VERTEX_POINT ( 'NONE', #90682 ) ;
#113108=AXIS2_PLACEMENT_3D ( 'NONE', #142853, #184569, #7206 ) ;
#113116=EDGE_LOOP ( 'NONE', ( #166348, #63058, #134974, #92475 ) ) ;
#113119=AXIS2_PLACEMENT_3D ( 'NONE', #27531, #90016, #144852 ) ;
#113124=CARTESIAN_POINT ( 'NONE',  ( 20.86777300164945004, 18.41441690808118281, -236.9991004306322964 ) ) ;
#113136=CARTESIAN_POINT ( 'NONE',  ( 20.94999999999997442, 7.576017155224048061, -241.7224044826512284 ) ) ;
#113168=CARTESIAN_POINT ( 'NONE',  ( -21.05000000000000071, -4.871452838297995136, -233.3782557782877518 ) ) ;
#113189=CARTESIAN_POINT ( 'NONE',  ( -20.64999999999999858, 6.757359537351773859, -220.2789794402637824 ) ) ;
#113192=DIRECTION ( 'NONE',  ( 0.000000000000000000, -0.2128009952263604232, 0.9770955615653316162 ) ) ;
#113236=DIRECTION ( 'NONE',  ( 3.265361837132812600E-16, -0.9770955615653313941, -0.2128009952263603677 ) ) ;
#113249=EDGE_CURVE ( 'NONE', #102873, #123636, #121210, .T. ) ;
#113273=DIRECTION ( 'NONE',  ( -0.000000000000000000, 0.2128009952263604232, -0.9770955615653316162 ) ) ;
#113277=CIRCLE ( 'NONE', #146569, 0.09999999999999080458 ) ;
#113281=ORIENTED_EDGE ( 'NONE', *, *, #153991, .T. ) ;
#113289=DIRECTION ( 'NONE',  ( 0.000000000000000000, 0.2128009952263605342, -0.9770955615653315052 ) ) ;
#113317=AXIS2_PLACEMENT_3D ( 'NONE', #109075, #9988, #29584 ) ;
#113323=ORIENTED_EDGE ( 'NONE', *, *, #225846, .T. ) ;
#113344=DIRECTION ( 'NONE',  ( 0.000000000000000000, 0.07893460099012300502, -0.9968797965484754720 ) ) ;
#113358=CARTESIAN_POINT ( 'NONE',  ( -18.41418431465368499, -0.7490476236419166822, -242.2033265267436377 ) ) ;
#113389=EDGE_CURVE ( 'NONE', #203210, #68317, #171461, .T. ) ;
#113395=ORIENTED_EDGE ( 'NONE', *, *, #145097, .T. ) ;
#113396=ORIENTED_EDGE ( 'NONE', *, *, #229619, .T. ) ;
#113446=AXIS2_PLACEMENT_3D ( 'NONE', #7027, #202656, #222195 ) ;
#113502=CARTESIAN_POINT ( 'NONE',  ( 22.43288208788031568, -2.474269879911711101, -189.6161341957261470 ) ) ;
#113540=ADVANCED_FACE ( 'NONE', ( #233461 ), #139994, .T. ) ;
#113582=ADVANCED_FACE ( 'NONE', ( #182464 ), #218995, .F. ) ;
#113606=CARTESIAN_POINT ( 'NONE',  ( 18.59999999999999076, 15.51794587355511901, -222.9505302427971003 ) ) ;
#113612=CARTESIAN_POINT ( 'NONE',  ( 20.95378194480896639, 11.90346680009650449, -206.1499410747357786 ) ) ;
#113619=DIRECTION ( 'NONE',  ( -0.000000000000000000, -0.9770955615653316162, -0.2128009952263597848 ) ) ;
#113621=DIRECTION ( 'NONE',  ( 0.000000000000000000, 0.9968797965484670343, 0.07893460099023182075 ) ) ;
#113639=EDGE_LOOP ( 'NONE', ( #29596, #20985, #199317, #2067 ) ) ;
#113717=CYLINDRICAL_SURFACE ( 'NONE', #244625, 0.1000000000000055844 ) ;
#113734=LINE ( 'NONE', #156748, #8140 ) ;
#113764=CARTESIAN_POINT ( 'NONE',  ( 18.54116936837188234, -7.746869717850485948, -209.9009554631552987 ) ) ;
#113803=DIRECTION ( 'NONE',  ( 0.000000000000000000, -0.2128009952263605342, 0.9770955615653315052 ) ) ;
#113826=CARTESIAN_POINT ( 'NONE',  ( 18.46082813848008897, -7.756037395792517053, -209.9396195450558480 ) ) ;
#113832=ORIENTED_EDGE ( 'NONE', *, *, #248219, .F. ) ;
#113838=AXIS2_PLACEMENT_3D ( 'NONE', #100786, #18728, #120437 ) ;
#113839=ADVANCED_FACE ( 'NONE', ( #227994 ), #209019, .F. ) ;
#113846=DIRECTION ( 'NONE',  ( 0.000000000000000000, 0.3427706569149635007, -0.9394191166662961834 ) ) ;
#113851=CARTESIAN_POINT ( 'NONE',  ( 21.30740335185486245, 6.385427988779872166, -199.5080681828139859 ) ) ;
#113873=ORIENTED_EDGE ( 'NONE', *, *, #125494, .F. ) ;
#113879=EDGE_CURVE ( 'NONE', #97885, #27566, #184077, .T. ) ;
#113888=CARTESIAN_POINT ( 'NONE',  ( -22.39999999999999858, -2.479040261794000610, -189.6172560698084624 ) ) ;
#113892=CIRCLE ( 'NONE', #105481, 0.1000000000000054040 ) ;
#113921=ORIENTED_EDGE ( 'NONE', *, *, #199456, .F. ) ;
#113923=DIRECTION ( 'NONE',  ( 1.000000000000000000, 0.000000000000000000, 0.000000000000000000 ) ) ;
#113953=DIRECTION ( 'NONE',  ( 1.000000000000000000, 0.000000000000000000, 0.000000000000000000 ) ) ;
#113970=CARTESIAN_POINT ( 'NONE',  ( -22.49436431346200038, 11.36887822570846041, -198.4555077020579290 ) ) ;
#114006=EDGE_CURVE ( 'NONE', #81280, #173016, #38342, .T. ) ;
#114011=TOROIDAL_SURFACE ( 'NONE', #84958, 11.70000000000000107, 0.1000000000000000056 ) ;
#114170=DIRECTION ( 'NONE',  ( 0.000000000000000000, -0.2128009952263568982, 0.9770955615653323934 ) ) ;
#114175=( BOUNDED_SURFACE ( )  B_SPLINE_SURFACE ( 3, 2, ( 
 ( #5323, #26221, #165737 ),
 ( #142291, #67898, #84852 ),
 ( #186579, #245262, #164445 ),
 ( #87447, #147436, #103151 ),
 ( #226974, #62766, #202278 ),
 ( #221807, #43206, #182729 ) ),
 .UNSPECIFIED., .F., .F., .F. ) 
 B_SPLINE_SURFACE_WITH_KNOTS ( ( 4, 2, 4 ),
 ( 3, 3 ),
 ( 6.719893378902767184E-05, 0.0002757154632485745360, 0.0004842319927081213866 ),
 ( 0.000000000000000000, 1.000000000000000000 ),
 .UNSPECIFIED. ) 
 GEOMETRIC_REPRESENTATION_ITEM ( )  RATIONAL_B_SPLINE_SURFACE ( (
 ( 1.000000000000000000, 0.7250110520819758042, 1.000000000000000000),
 ( 1.000000000000000000, 0.7277932058380147673, 1.000000000000000000),
 ( 1.000000000000000000, 0.7278452872589648015, 1.000000000000000000),
 ( 1.000000000000000000, 0.7221445671577165770, 1.000000000000000000),
 ( 1.000000000000000000, 0.7163662143758368073, 1.000000000000000000),
 ( 1.000000000000000000, 0.7071067811865475727, 1.000000000000000000) ) ) 
 REPRESENTATION_ITEM ( '' )  SURFACE ( )  );
#114192=AXIS2_PLACEMENT_3D ( 'NONE', #32295, #12733, #76517 ) ;
#114197=ORIENTED_EDGE ( 'NONE', *, *, #257807, .F. ) ;
#114203=DIRECTION ( 'NONE',  ( 1.000000000000000000, 0.000000000000000000, 0.000000000000000000 ) ) ;
#114224=EDGE_CURVE ( 'NONE', #95913, #60331, #210681, .T. ) ;
#114304=CYLINDRICAL_SURFACE ( 'NONE', #36823, 0.09999999999999939493 ) ;
#114330=AXIS2_PLACEMENT_3D ( 'NONE', #10583, #130507, #225742 ) ;
#114350=CARTESIAN_POINT ( 'NONE',  ( 21.05000000000000426, 12.09419596560308641, -206.1384538536135267 ) ) ;
#114373=CARTESIAN_POINT ( 'NONE',  ( -20.64999999999999858, -3.685352791942197115, -226.3713951780953550 ) ) ;
#114384=ORIENTED_EDGE ( 'NONE', *, *, #126321, .F. ) ;
#114396=VERTEX_POINT ( 'NONE', #236655 ) ;
#114402=FACE_OUTER_BOUND ( 'NONE', #237748, .T. ) ;
#114403=AXIS2_PLACEMENT_3D ( 'NONE', #30677, #95736, #72364 ) ;
#114406=EDGE_CURVE ( 'NONE', #255134, #183554, #192405, .T. ) ;
#114422=DIRECTION ( 'NONE',  ( 1.000000000000000000, -0.000000000000000000, -0.000000000000000000 ) ) ;
#114429=AXIS2_PLACEMENT_3D ( 'NONE', #8830, #144459, #29705 ) ;
#114484=CARTESIAN_POINT ( 'NONE',  ( -21.52071067811865746, 10.22920135959988563, -211.4116896754832169 ) ) ;
#114493=ADVANCED_FACE ( 'NONE', ( #138805 ), #159706, .T. ) ;
#114501=CARTESIAN_POINT ( 'NONE',  ( 21.05000000000000426, 6.108305422032350052, -199.6352550756156745 ) ) ;
#114504=EDGE_CURVE ( 'NONE', #61748, #90944, #22154, .T. ) ;
#114512=DIRECTION ( 'NONE',  ( 0.000000000000000000, -0.7397890806274223241, -0.6728388485993012091 ) ) ;
#114539=DIRECTION ( 'NONE',  ( 3.469446951953150970E-14, 0.3042567129660163627, 0.9525900758537824142 ) ) ;
#114567=FACE_OUTER_BOUND ( 'NONE', #59069, .T. ) ;
#114572=ORIENTED_EDGE ( 'NONE', *, *, #11974, .T. ) ;
#114582=DIRECTION ( 'NONE',  ( -0.000000000000000000, 0.9770955615653313941, 0.2128009952263603954 ) ) ;
#114595=CARTESIAN_POINT ( 'NONE',  ( -23.25000000000000000, 4.768403829798271154, -213.4961173936592331 ) ) ;
#114624=CARTESIAN_POINT ( 'NONE',  ( -18.50000000000000000, -0.8760381862371811046, -190.6771195118613207 ) ) ;
#114637=VERTEX_POINT ( 'NONE', #152763 ) ;
#114640=ORIENTED_EDGE ( 'NONE', *, *, #164686, .T. ) ;
#114648=ORIENTED_EDGE ( 'NONE', *, *, #77318, .F. ) ;
#114656=DIRECTION ( 'NONE',  ( 0.000000000000000000, 0.2128009952263605897, -0.9770955615653315052 ) ) ;
#114659=CARTESIAN_POINT ( 'NONE',  ( -20.64999999999999858, 6.878457983866232972, -212.1414458560986986 ) ) ;
#114686=CARTESIAN_POINT ( 'NONE',  ( -21.05000000000000071, -1.476139073305543281, -194.6920926048172191 ) ) ;
#114692=ADVANCED_FACE ( 'NONE', ( #221667 ), #256479, .T. ) ;
#114694=ORIENTED_EDGE ( 'NONE', *, *, #80845, .T. ) ;
#114708=CIRCLE ( 'NONE', #147852, 11.90000000000001457 ) ;
#114782=CARTESIAN_POINT ( 'NONE',  ( -18.50000000000000000, 14.76289716703255728, -235.7888246855571026 ) ) ;
#114787=CARTESIAN_POINT ( 'NONE',  ( 21.05000000000000071, -1.489567864901282235, -194.6304332222954372 ) ) ;
#114854=VECTOR ( 'NONE', #169112, 1000.000000000000227 ) ;
#114860=EDGE_LOOP ( 'NONE', ( #28274, #10194, #117993, #94228 ) ) ;
#114863=CARTESIAN_POINT ( 'NONE',  ( 22.60000000000000142, 1.148907358139439339E-11, -201.0000000000015064 ) ) ;
#114868=FACE_OUTER_BOUND ( 'NONE', #70427, .T. ) ;
#114873=CIRCLE ( 'NONE', #231406, 0.9750000000000036415 ) ;
#114880=FACE_OUTER_BOUND ( 'NONE', #29544, .T. ) ;
#114882=SPHERICAL_SURFACE ( 'NONE', #5775, 0.1000000000000000056 ) ;
#114898=CARTESIAN_POINT ( 'NONE',  ( 20.95017935633852346, 11.84804081051113123, -206.1746882498729292 ) ) ;
#114927=CARTESIAN_POINT ( 'NONE',  ( -20.94999999999999929, 1.681127862299736098, -208.7190549363676269 ) ) ;
#114943=EDGE_LOOP ( 'NONE', ( #203118, #209593, #104058, #113921, #10175 ) ) ;
#114950=ORIENTED_EDGE ( 'NONE', *, *, #80276, .T. ) ;
#114971=CIRCLE ( 'NONE', #81610, 0.09999999999999939493 ) ;
#114991=LINE ( 'NONE', #112440, #122233 ) ;
#115003=ADVANCED_FACE ( 'NONE', ( #231980 ), #15500, .T. ) ;
#115049=CARTESIAN_POINT ( 'NONE',  ( -23.25000000000000000, -2.598867842139046314, -189.5410128746472083 ) ) ;
#115054=FILL_AREA_STYLE ('',( #14699 ) ) ;
#115066=CARTESIAN_POINT ( 'NONE',  ( 21.13422380239052600, 6.344600517422461117, -199.6182136553211706 ) ) ;
#115086=CIRCLE ( 'NONE', #194223, 0.2000000000000106137 ) ;
#115088=DIRECTION ( 'NONE',  ( -0.000000000000000000, 0.2128009952263603677, -0.9770955615653313941 ) ) ;
#115105=CARTESIAN_POINT ( 'NONE',  ( 22.48970261584621966, 11.37138061004976386, -198.4667671244310441 ) ) ;
#115133=VERTEX_POINT ( 'NONE', #51357 ) ;
#115135=CARTESIAN_POINT ( 'NONE',  ( -22.47071067811865319, -1.546016791165058635, -193.4356622592196970 ) ) ;
#115142=EDGE_CURVE ( 'NONE', #52138, #51901, #113892, .T. ) ;
#115183=DIRECTION ( 'NONE',  ( 1.000000000000000000, 0.000000000000000000, 0.000000000000000000 ) ) ;
#115210=ORIENTED_EDGE ( 'NONE', *, *, #6684, .T. ) ;
#115220=EDGE_CURVE ( 'NONE', #216057, #109854, #225201, .T. ) ;
#115247=CIRCLE ( 'NONE', #235859, 0.1000000000000035305 ) ;
#115286=CARTESIAN_POINT ( 'NONE',  ( -18.50000000000000000, 15.92646454033039305, -219.3818586450342707 ) ) ;
#115324=DIRECTION ( 'NONE',  ( -1.000000000000000000, 0.000000000000000000, 0.000000000000000000 ) ) ;
#115349=TOROIDAL_SURFACE ( 'NONE', #44059, 0.2000000000000000111, 0.1000000000000000056 ) ;
#115358=DIRECTION ( 'NONE',  ( 0.000000000000000000, -0.9968797965484670343, -0.07893460099023179299 ) ) ;
#115361=VERTEX_POINT ( 'NONE', #82482 ) ;
#115368=DIRECTION ( 'NONE',  ( 0.000000000000000000, -0.9770955615654159931, -0.2128009952259723447 ) ) ;
#115369=CARTESIAN_POINT ( 'NONE',  ( 23.14999999999999858, 7.128833340094563376, -233.7327013124401276 ) ) ;
#115408=LINE ( 'NONE', #94557, #123414 ) ;
#115414=CIRCLE ( 'NONE', #207003, 11.65000000000001457 ) ;
#115452=EDGE_LOOP ( 'NONE', ( #245908, #69176, #18884, #212450 ) ) ;
#115453=CIRCLE ( 'NONE', #232007, 4.150000000000001243 ) ;
#115456=EDGE_CURVE ( 'NONE', #247087, #75163, #59297, .T. ) ;
#115470=EDGE_LOOP ( 'NONE', ( #69305, #189990 ) ) ;
#115478=DIRECTION ( 'NONE',  ( 0.000000000000000000, -0.2128009952263403282, 0.9770955615653358350 ) ) ;
#115522=CARTESIAN_POINT ( 'NONE',  ( 22.60000000000000142, -2.401771312552908544, -189.4980873520049727 ) ) ;
#115537=ORIENTED_EDGE ( 'NONE', *, *, #35578, .F. ) ;
#115575=TOROIDAL_SURFACE ( 'NONE', #219805, 0.2000000000000000111, 0.1000000000000000056 ) ;
#115628=ADVANCED_FACE ( 'NONE', ( #75798 ), #53664, .T. ) ;
#115643=EDGE_LOOP ( 'NONE', ( #42414, #155452, #175192, #140026 ) ) ;
#115683=DIRECTION ( 'NONE',  ( 0.000000000000000000, 0.2128009952263603677, -0.9770955615653315052 ) ) ;
#115737=CARTESIAN_POINT ( 'NONE',  ( 23.14999999999999858, 9.960715529987961503, -220.4198853720552904 ) ) ;
#115744=ORIENTED_EDGE ( 'NONE', *, *, #4137, .T. ) ;
#115745=CARTESIAN_POINT ( 'NONE',  ( 23.14999999999999503, 11.01970663298110154, -220.3481540650095098 ) ) ;
#115746=DIRECTION ( 'NONE',  ( -1.000000000000000000, -0.000000000000000000, -0.000000000000000000 ) ) ;
#115801=CARTESIAN_POINT ( 'NONE',  ( -20.00857864376270001, 13.46244553689443535, -219.8161515769436107 ) ) ;
#115812=CARTESIAN_POINT ( 'NONE',  ( -20.94999999999999929, 0.4810385098657082859, -209.0827657365571213 ) ) ;
#115815=DIRECTION ( 'NONE',  ( 1.000000000000000000, 0.000000000000000000, 0.000000000000000000 ) ) ;
#115823=AXIS2_PLACEMENT_3D ( 'NONE', #51820, #193937, #75290 ) ;
#115849=AXIS2_PLACEMENT_3D ( 'NONE', #13094, #33973, #173495 ) ;
#115877=CARTESIAN_POINT ( 'NONE',  ( 20.94999999999999574, 14.83422855357708414, -203.3235740904736417 ) ) ;
#115880=DIRECTION ( 'NONE',  ( -0.000000000000000000, 0.9770955615653316162, 0.2128009952263604232 ) ) ;
#115886=VERTEX_POINT ( 'NONE', #247704 ) ;
#115893=AXIS2_PLACEMENT_3D ( 'NONE', #116378, #98047, #135908 ) ;
#115916=DIRECTION ( 'NONE',  ( 2.952720810173289112E-16, -0.9770955615653301729, -0.2128009952263660853 ) ) ;
#115928=ORIENTED_EDGE ( 'NONE', *, *, #101785, .F. ) ;
#115945=CARTESIAN_POINT ( 'NONE',  ( -20.64999999999999858, 5.256951610580939516, -213.3897168960460533 ) ) ;
#115976=CARTESIAN_POINT ( 'NONE',  ( -23.25000000000000000, 7.567413955921500346, -241.6205176796878504 ) ) ;
#115998=EDGE_CURVE ( 'NONE', #149075, #9130, #173354, .T. ) ;
#116018=ORIENTED_EDGE ( 'NONE', *, *, #131865, .F. ) ;
#116019=VERTEX_POINT ( 'NONE', #156341 ) ;
#116032=CIRCLE ( 'NONE', #224144, 0.1000000000000054040 ) ;
#116050=DIRECTION ( 'NONE',  ( -0.000000000000000000, 0.2128009952263604232, -0.9770955615653316162 ) ) ;
#116066=AXIS2_PLACEMENT_3D ( 'NONE', #93664, #213602, #174545 ) ;
#116085=CIRCLE ( 'NONE', #257476, 0.1000000000000008937 ) ;
#116088=AXIS2_PLACEMENT_3D ( 'NONE', #175746, #115746, #9262 ) ;
#116134=EDGE_LOOP ( 'NONE', ( #47939, #179716, #49759, #232080 ) ) ;
#116156=AXIS2_PLACEMENT_3D ( 'NONE', #153279, #227630, #192370 ) ;
#116170=SPHERICAL_SURFACE ( 'NONE', #103046, 0.1000000000000000056 ) ;
#116204=CARTESIAN_POINT ( 'NONE',  ( 20.95203847575071521, 11.87081995860093819, -206.1591156951000130 ) ) ;
#116277=EDGE_CURVE ( 'NONE', #65124, #29396, #51303, .T. ) ;
#116308=LINE ( 'NONE', #139683, #190423 ) ;
#116378=CARTESIAN_POINT ( 'NONE',  ( 21.05000000000000071, 10.29970289650803572, -222.9162226222096308 ) ) ;
#116403=ORIENTED_EDGE ( 'NONE', *, *, #103489, .T. ) ;
#116411=CARTESIAN_POINT ( 'NONE',  ( 18.48536876927993688, -7.746817490806097162, -209.9010216391053802 ) ) ;
#116424=DIRECTION ( 'NONE',  ( 0.000000000000000000, 0.2128009952263605897, -0.9770955615653315052 ) ) ;
#116463=ORIENTED_EDGE ( 'NONE', *, *, #72575, .F. ) ;
#116472=EDGE_CURVE ( 'NONE', #234500, #133719, #130446, .T. ) ;
#116493=EDGE_CURVE ( 'NONE', #88973, #103882, #247319, .T. ) ;
#116544=CARTESIAN_POINT ( 'NONE',  ( 21.14999999999999858, 9.083217576421224848, -211.4565844547649931 ) ) ;
#116585=VECTOR ( 'NONE', #257040, 1000.000000000000227 ) ;
#116614=AXIS2_PLACEMENT_3D ( 'NONE', #122867, #245380, #64168 ) ;
#116643=FACE_OUTER_BOUND ( 'NONE', #122670, .T. ) ;
#116649=DIRECTION ( 'NONE',  ( 1.000000000000000000, 2.885090398161910739E-16, 6.283419270304611573E-17 ) ) ;
#116670=EDGE_LOOP ( 'NONE', ( #202224, #162098, #42926, #123478 ) ) ;
#116676=DIRECTION ( 'NONE',  ( 0.000000000000000000, 0.2128009952263601456, -0.9770955615653316162 ) ) ;
#116705=EDGE_LOOP ( 'NONE', ( #41051, #113041, #240944, #102400 ) ) ;
#116714=VERTEX_POINT ( 'NONE', #244510 ) ;
#116716=CARTESIAN_POINT ( 'NONE',  ( 20.97438252431638972, 10.52392060743736835, -207.3789767912604702 ) ) ;
#116723=ORIENTED_EDGE ( 'NONE', *, *, #33293, .F. ) ;
#116770=CYLINDRICAL_SURFACE ( 'NONE', #26734, 11.74999999999999289 ) ;
#116840=CARTESIAN_POINT ( 'NONE',  ( -23.25000000000000000, 7.128833340094563376, -233.7327013124401276 ) ) ;
#116844=EDGE_LOOP ( 'NONE', ( #163386, #68490, #36180, #228892, #175769 ) ) ;
#116885=CARTESIAN_POINT ( 'NONE',  ( 23.14999999999999503, 15.92646454033040371, -219.3818586450342423 ) ) ;
#116941=ORIENTED_EDGE ( 'NONE', *, *, #187033, .F. ) ;
#116950=VECTOR ( 'NONE', #49261, 1000.000000000000227 ) ;
#116953=ORIENTED_EDGE ( 'NONE', *, *, #16731, .F. ) ;
#116960=EDGE_CURVE ( 'NONE', #117463, #7468, #218267, .T. ) ;
#116996=ADVANCED_FACE ( 'NONE', ( #56553 ), #22306, .T. ) ;
#117008=VERTEX_POINT ( 'NONE', #82214 ) ;
#117022=DIRECTION ( 'NONE',  ( 0.000000000000000000, 0.3634403228828347321, -0.9316174814283063599 ) ) ;
#117038=CARTESIAN_POINT ( 'NONE',  ( -21.14999999893415250, 12.93738826932868591, -205.1873143274057441 ) ) ;
#117077=ORIENTED_EDGE ( 'NONE', *, *, #83706, .T. ) ;
#117170=B_SPLINE_CURVE_WITH_KNOTS ( 'NONE', 3,
 ( #115135, #194701, #16065, #215509, #95563, #235091, #56425, #135962, #195971, #36920 ),
 .UNSPECIFIED., .F., .F.,
 ( 4, 3, 3, 4 ),
 ( 4.336808689942017736E-19, 0.0002000000000002811161, 0.001000000000045105867, 0.001967863649472137346 ),
 .UNSPECIFIED. ) ;
#117173=DIRECTION ( 'NONE',  ( 0.000000000000000000, 0.2002428086779743377, -0.9797463026583749235 ) ) ;
#117186=TOROIDAL_SURFACE ( 'NONE', #9040, 11.89999999999999858, 0.1000000000000000056 ) ;
#117212=CIRCLE ( 'NONE', #154649, 6.258578643762700011 ) ;
#117227=DIRECTION ( 'NONE',  ( -1.000000000000000000, 0.000000000000000000, 0.000000000000000000 ) ) ;
#117235=VECTOR ( 'NONE', #256051, 1000.000000000000000 ) ;
#117279=CARTESIAN_POINT ( 'NONE',  ( 23.14999999999999858, 7.128833340094563376, -233.7327013124401276 ) ) ;
#117309=EDGE_LOOP ( 'NONE', ( #831, #177838, #42123, #241457 ) ) ;
#117345=CARTESIAN_POINT ( 'NONE',  ( -23.25000000000000000, 18.60970618848720903, -231.2322896185303875 ) ) ;
#117348=EDGE_LOOP ( 'NONE', ( #89884, #31179, #121059, #49848 ) ) ;
#117350=EDGE_CURVE ( 'NONE', #83634, #176927, #130989, .T. ) ;
#117352=EDGE_CURVE ( 'NONE', #198456, #203538, #55936, .T. ) ;
#117387=VECTOR ( 'NONE', #177522, 1000.000000000000000 ) ;
#117389=LINE ( 'NONE', #136948, #82607 ) ;
#117395=PLANE ( 'NONE',  #137506 ) ;
#117429=EDGE_CURVE ( 'NONE', #134704, #234500, #181081, .T. ) ;
#117444=VECTOR ( 'NONE', #111326, 1000.000000000000114 ) ;
#117453=LINE ( 'NONE', #178740, #8744 ) ;
#117454=ORIENTED_EDGE ( 'NONE', *, *, #102668, .F. ) ;
#117463=VERTEX_POINT ( 'NONE', #165338 ) ;
#117469=EDGE_CURVE ( 'NONE', #123238, #205753, #251795, .T. ) ;
#117480=CARTESIAN_POINT ( 'NONE',  ( 20.94999999999999929, 7.128833340094563376, -233.7327013124401276 ) ) ;
#117533=VERTEX_POINT ( 'NONE', #166652 ) ;
#117617=AXIS2_PLACEMENT_3D ( 'NONE', #91894, #88020, #247108 ) ;
#117634=EDGE_CURVE ( 'NONE', #109854, #192518, #4334, .T. ) ;
#117647=DIRECTION ( 'NONE',  ( 0.000000000000000000, 0.2128009952263403282, -0.9770955615653358350 ) ) ;
#117651=CARTESIAN_POINT ( 'NONE',  ( -20.85000000000000142, 14.61354176542825201, -235.9279552357344016 ) ) ;
#117680=ORIENTED_EDGE ( 'NONE', *, *, #183341, .T. ) ;
#117693=ORIENTED_EDGE ( 'NONE', *, *, #227044, .T. ) ;
#117701=DIRECTION ( 'NONE',  ( -1.000000000000000000, -0.000000000000000000, -0.000000000000000000 ) ) ;
#117702=ADVANCED_FACE ( 'NONE', ( #15260 ), #150127, .F. ) ;
#117725=DIRECTION ( 'NONE',  ( 0.000000000000000000, -0.9770955615653316162, -0.2128009952263604232 ) ) ;
#117750=ORIENTED_EDGE ( 'NONE', *, *, #251888, .T. ) ;
#117857=EDGE_CURVE ( 'NONE', #87436, #76729, #58494, .T. ) ;
#117859=CARTESIAN_POINT ( 'NONE',  ( 20.85000000000000142, 7.783179459866048866, -245.3643104511423303 ) ) ;
#117865=EDGE_LOOP ( 'NONE', ( #62062, #236273, #237416, #164850, #39760 ) ) ;
#117883=DIRECTION ( 'NONE',  ( 0.000000000000000000, 0.2128009952263403282, -0.9770955615653358350 ) ) ;
#117884=VECTOR ( 'NONE', #107181, 1000.000000000000114 ) ;
#117896=SPHERICAL_SURFACE ( 'NONE', #164042, 0.1000000000000000056 ) ;
#117916=DIRECTION ( 'NONE',  ( 0.000000000000000000, -0.08413937888704772772, 0.9964539953858894128 ) ) ;
#117924=EDGE_CURVE ( 'NONE', #68130, #122855, #108036, .T. ) ;
#117938=AXIS2_PLACEMENT_3D ( 'NONE', #130033, #187480, #184889 ) ;
#117948=CARTESIAN_POINT ( 'NONE',  ( 18.59999999999999076, 16.67126802362266247, -222.8016931105129004 ) ) ;
#117977=ORIENTED_EDGE ( 'NONE', *, *, #74160, .T. ) ;
#117978=FACE_OUTER_BOUND ( 'NONE', #77824, .T. ) ;
#117993=ORIENTED_EDGE ( 'NONE', *, *, #121536, .F. ) ;
#117997=CARTESIAN_POINT ( 'NONE',  ( 22.57320508075687115, 11.48087284840413425, -198.4995883060917663 ) ) ;
#117998=CARTESIAN_POINT ( 'NONE',  ( -21.05000000000000071, 10.68863688179707694, -222.5873974249509217 ) ) ;
#118001=CARTESIAN_POINT ( 'NONE',  ( 20.74625933824097146, 10.50000428349506265, -207.4689267983004868 ) ) ;
#118039=AXIS2_PLACEMENT_3D ( 'NONE', #154295, #31763, #111270 ) ;
#118057=EDGE_CURVE ( 'NONE', #148979, #20649, #68053, .T. ) ;
#118059=LINE ( 'NONE', #235425, #111058 ) ;
#118096=EDGE_LOOP ( 'NONE', ( #101213, #59780, #125612, #192634 ) ) ;
#118097=CARTESIAN_POINT ( 'NONE',  ( 22.39999999999999858, 1.148907358139439339E-11, -201.0000000000015064 ) ) ;
#118118=AXIS2_PLACEMENT_3D ( 'NONE', #108049, #110602, #11523 ) ;
#118120=AXIS2_PLACEMENT_3D ( 'NONE', #20016, #79926, #62972 ) ;
#118132=ORIENTED_EDGE ( 'NONE', *, *, #72305, .T. ) ;
#118152=EDGE_LOOP ( 'NONE', ( #16030, #244931, #172984, #38495 ) ) ;
#118165=DIRECTION ( 'NONE',  ( 0.000000000000000000, 0.2128009952263601179, -0.9770955615653315052 ) ) ;
#118189=ORIENTED_EDGE ( 'NONE', *, *, #19973, .T. ) ;
#118205=DIRECTION ( 'NONE',  ( 0.000000000000000000, 0.2128009952263403282, -0.9770955615653358350 ) ) ;
#118234=ORIENTED_EDGE ( 'NONE', *, *, #174697, .F. ) ;
#118263=DIRECTION ( 'NONE',  ( 1.000000000000000000, 0.000000000000000000, 0.000000000000000000 ) ) ;
#118269=CARTESIAN_POINT ( 'NONE',  ( -23.15000000000000213, 0.8618440306782485516, -204.9572370243411115 ) ) ;
#118307=CARTESIAN_POINT ( 'NONE',  ( 20.94999999999999929, 1.148907358139439339E-11, -201.0000000000015064 ) ) ;
#118317=ADVANCED_FACE ( 'NONE', ( #19422 ), #67196, .T. ) ;
#118346=CARTESIAN_POINT ( 'NONE',  ( 18.49505832270841310, -7.690013074335040777, -210.0420179539718504 ) ) ;
#118352=AXIS2_PLACEMENT_3D ( 'NONE', #114927, #174956, #13270 ) ;
#118354=ORIENTED_EDGE ( 'NONE', *, *, #101204, .T. ) ;
#118359=EDGE_CURVE ( 'NONE', #150841, #120381, #241041, .T. ) ;
#118372=ORIENTED_EDGE ( 'NONE', *, *, #34693, .T. ) ;
#118376=DIRECTION ( 'NONE',  ( -1.000000000000000000, -3.190570557967288949E-16, -6.948722487160392945E-17 ) ) ;
#118402=CARTESIAN_POINT ( 'NONE',  ( 21.00000000000000000, 14.04870287383362992, -219.6884709798077893 ) ) ;
#118426=EDGE_CURVE ( 'NONE', #118817, #83582, #62427, .T. ) ;
#118427=CARTESIAN_POINT ( 'NONE',  ( -20.94999999999999929, -4.254329952141550741, -236.2118329068272260 ) ) ;
#118439=ORIENTED_EDGE ( 'NONE', *, *, #45036, .F. ) ;
#118462=CARTESIAN_POINT ( 'NONE',  ( -21.65000000000000213, 12.05403912736948158, -220.1228874760914209 ) ) ;
#118478=VERTEX_POINT ( 'NONE', #228847 ) ;
#118505=CARTESIAN_POINT ( 'NONE',  ( 20.94999999999999574, -10.60885044396467158, -206.2784744251879374 ) ) ;
#118519=EDGE_LOOP ( 'NONE', ( #951, #101859, #159938, #241431 ) ) ;
#118530=EDGE_CURVE ( 'NONE', #98769, #195345, #166498, .T. ) ;
#118534=CARTESIAN_POINT ( 'NONE',  ( -20.85000000000000142, -4.254329952141548965, -236.2118329068272260 ) ) ;
#118537=ORIENTED_EDGE ( 'NONE', *, *, #84302, .T. ) ;
#118540=CIRCLE ( 'NONE', #93573, 1.899999999999997913 ) ;
#118556=EDGE_LOOP ( 'NONE', ( #239927, #140032, #124914 ) ) ;
#118601=CARTESIAN_POINT ( 'NONE',  ( -21.14999999999999858, -11.38316329222462464, -203.4791315943886332 ) ) ;
#118602=DIRECTION ( 'NONE',  ( -0.000000000000000000, -0.2128009952263604232, 0.9770955615653316162 ) ) ;
#118609=EDGE_CURVE ( 'NONE', #63666, #141892, #103897, .T. ) ;
#118646=CARTESIAN_POINT ( 'NONE',  ( 22.45380639571855497, -2.500503674154201939, -189.5187041452655592 ) ) ;
#118668=ORIENTED_EDGE ( 'NONE', *, *, #222046, .T. ) ;
#118670=EDGE_LOOP ( 'NONE', ( #82944, #107104, #106401, #137854 ) ) ;
#118682=ORIENTED_EDGE ( 'NONE', *, *, #229981, .F. ) ;
#118686=DIRECTION ( 'NONE',  ( -1.000000000000000000, -0.000000000000000000, -0.000000000000000000 ) ) ;
#118692=VERTEX_POINT ( 'NONE', #201258 ) ;
#118700=DIRECTION ( 'NONE',  ( 0.000000000000000000, -0.2128009952263604232, 0.9770955615653316162 ) ) ;
#118721=CARTESIAN_POINT ( 'NONE',  ( 18.59999999999999787, -4.317402351199911337, -229.8357552817742260 ) ) ;
#118725=ORIENTED_EDGE ( 'NONE', *, *, #111895, .F. ) ;
#118756=CARTESIAN_POINT ( 'NONE',  ( 20.04142135623731136, 16.72641738073392759, -222.5849938986772258 ) ) ;
#118764=VECTOR ( 'NONE', #167875, 1000.000000000000000 ) ;
#118817=VERTEX_POINT ( 'NONE', #111162 ) ;
#118822=AXIS2_PLACEMENT_3D ( 'NONE', #239051, #185499, #102078 ) ;
#118838=DIRECTION ( 'NONE',  ( -1.000000000000000000, -7.136802563874201079E-16, -1.554319503706925800E-16 ) ) ;
#118846=DIRECTION ( 'NONE',  ( 1.000000000000000000, 0.000000000000000000, 0.000000000000000000 ) ) ;
#118852=ORIENTED_EDGE ( 'NONE', *, *, #138589, .F. ) ;
#118853=CARTESIAN_POINT ( 'NONE',  ( -18.50000000000000000, 1.148907358139439339E-11, -201.0000000000015064 ) ) ;
#118863=AXIS2_PLACEMENT_3D ( 'NONE', #26735, #25439, #65829 ) ;
#118865=DIRECTION ( 'NONE',  ( 0.000000000000000000, -0.2128009952263603677, 0.9770955615653315052 ) ) ;
#118872=ORIENTED_EDGE ( 'NONE', *, *, #179533, .T. ) ;
#118886=EDGE_CURVE ( 'NONE', #55636, #146352, #216679, .T. ) ;
#118887=ORIENTED_EDGE ( 'NONE', *, *, #249637, .T. ) ;
#118934=DIRECTION ( 'NONE',  ( 1.000000000000000000, 2.885090398161910739E-16, 6.283419270304611573E-17 ) ) ;
#118945=ORIENTED_EDGE ( 'NONE', *, *, #58741, .F. ) ;
#118955=DIRECTION ( 'NONE',  ( -0.000000000000000000, -0.9770955615653313941, -0.2128009952263603677 ) ) ;
#118965=DIRECTION ( 'NONE',  ( 0.000000000000000000, 0.2128009952263603677, -0.9770955615653313941 ) ) ;
#118972=ADVANCED_FACE ( 'NONE', ( #197107 ), #19783, .F. ) ;
#118980=VERTEX_POINT ( 'NONE', #253226 ) ;
#118984=ORIENTED_EDGE ( 'NONE', *, *, #89165, .T. ) ;
#118996=AXIS2_PLACEMENT_3D ( 'NONE', #114863, #172319, #171040 ) ;
#118999=CARTESIAN_POINT ( 'NONE',  ( -23.15000000000000213, 6.298909458711757559, -229.9220286223353185 ) ) ;
#119002=FACE_OUTER_BOUND ( 'NONE', #50452, .T. ) ;
#119012=CYLINDRICAL_SURFACE ( 'NONE', #24829, 0.09999999999999939493 ) ;
#119039=AXIS2_PLACEMENT_3D ( 'NONE', #118097, #16456, #133802 ) ;
#119097=AXIS2_PLACEMENT_3D ( 'NONE', #245556, #65615, #66903 ) ;
#119126=ORIENTED_EDGE ( 'NONE', *, *, #34340, .F. ) ;
#119128=ORIENTED_EDGE ( 'NONE', *, *, #238453, .F. ) ;
#119134=ORIENTED_EDGE ( 'NONE', *, *, #43853, .T. ) ;
#119161=ORIENTED_EDGE ( 'NONE', *, *, #51093, .T. ) ;
#119171=EDGE_CURVE ( 'NONE', #237840, #196267, #169599, .T. ) ;
#119309=PLANE ( 'NONE',  #44951 ) ;
#119317=CARTESIAN_POINT ( 'NONE',  ( 21.05000000000000071, 11.40444339177024169, -198.6185779617709670 ) ) ;
#119318=CARTESIAN_POINT ( 'NONE',  ( 23.14999999999999858, 7.128833340094563376, -233.7327013124401276 ) ) ;
#119328=EDGE_CURVE ( 'NONE', #98586, #192518, #32650, .T. ) ;
#119372=DIRECTION ( 'NONE',  ( 0.000000000000000000, -0.2128009952263601734, 0.9770955615653316162 ) ) ;
#119385=CARTESIAN_POINT ( 'NONE',  ( -21.14999999999999858, 11.38316329224760359, -198.5208684056144079 ) ) ;
#119387=CARTESIAN_POINT ( 'NONE',  ( -21.05000000000000071, -10.76604040606818025, -206.3127087229280789 ) ) ;
#119422=CARTESIAN_POINT ( 'NONE',  ( 21.07094088545303734, 6.154362662572053999, -199.5584335273501324 ) ) ;
#119464=AXIS2_PLACEMENT_3D ( 'NONE', #40364, #183694, #143266 ) ;
#119503=VERTEX_POINT ( 'NONE', #110543 ) ;
#119522=EDGE_CURVE ( 'NONE', #19000, #126771, #221163, .T. ) ;
#119560=EDGE_CURVE ( 'NONE', #17786, #112587, #37867, .T. ) ;
#119586=ORIENTED_EDGE ( 'NONE', *, *, #178943, .F. ) ;
#119615=CARTESIAN_POINT ( 'NONE',  ( 20.85000000000000142, -4.969162394454520459, -233.3995358778103935 ) ) ;
#119618=CARTESIAN_POINT ( 'NONE',  ( -21.05439746398122836, 12.96833403348994196, -205.3294046817250660 ) ) ;
#119622=CARTESIAN_POINT ( 'NONE',  ( 21.05000000000000071, 9.863005973831429074, -220.4411654715779321 ) ) ;
#119628=CARTESIAN_POINT ( 'NONE',  ( -18.50000000000000000, 11.72137559264762174, -210.8820217676538391 ) ) ;
#119637=DIRECTION ( 'NONE',  ( -3.265361837132813093E-16, 0.9770955615653316162, 0.2128009952263604232 ) ) ;
#119708=DIRECTION ( 'NONE',  ( 0.000000000000000000, -0.2128009952263900384, 0.9770955615653251769 ) ) ;
#119712=ORIENTED_EDGE ( 'NONE', *, *, #68307, .F. ) ;
#119715=EDGE_LOOP ( 'NONE', ( #102985, #161403, #5856, #150246, #174690 ) ) ;
#119727=ADVANCED_FACE ( 'NONE', ( #114402 ), #246131, .T. ) ;
#119760=EDGE_CURVE ( 'NONE', #46074, #198700, #204414, .T. ) ;
#119774=CYLINDRICAL_SURFACE ( 'NONE', #238615, 0.1000000000000054040 ) ;
#119777=CARTESIAN_POINT ( 'NONE',  ( 20.94999999999999574, 8.494751065780215882, -209.2245083539370114 ) ) ;
#119784=CARTESIAN_POINT ( 'NONE',  ( -22.39999999999999858, -1.657885652111596109, -193.3876638332971254 ) ) ;
#119793=ORIENTED_EDGE ( 'NONE', *, *, #80158, .T. ) ;
#119798=CARTESIAN_POINT ( 'NONE',  ( -18.50000000000000000, 7.661991824395936845, -241.5144583139544636 ) ) ;
#119805=ORIENTED_EDGE ( 'NONE', *, *, #180218, .T. ) ;
#119859=CARTESIAN_POINT ( 'NONE',  ( -18.50000000000000000, 0.5876173420563349792, -209.1618981382189588 ) ) ;
#119872=DIRECTION ( 'NONE',  ( 0.000000000000000000, 0.2128009952263485993, -0.9770955615653341697 ) ) ;
#119873=DIRECTION ( 'NONE',  ( -0.000000000000000000, -0.2128009952263603677, 0.9770955615653313941 ) ) ;
#119897=CARTESIAN_POINT ( 'NONE',  ( -21.05000000000000071, 6.165100388772664530, -199.6791937419174587 ) ) ;
#119931=AXIS2_PLACEMENT_3D ( 'NONE', #9049, #248959, #246382 ) ;
#119955=DIRECTION ( 'NONE',  ( 0.000000000000000000, -0.9770955615653316162, -0.2128009952263604232 ) ) ;
#119977=ADVANCED_FACE ( 'NONE', ( #168977 ), #88076, .T. ) ;
#120023=VERTEX_POINT ( 'NONE', #153256 ) ;
#120063=CIRCLE ( 'NONE', #32582, 0.09999999999999724387 ) ;
#120079=ADVANCED_FACE ( 'NONE', ( #18522 ), #238853, .T. ) ;
#120084=EDGE_CURVE ( 'NONE', #194623, #148114, #50654, .T. ) ;
#120102=TOROIDAL_SURFACE ( 'NONE', #57695, 0.6000000000000017542, 0.1000000000000000056 ) ;
#120116=CARTESIAN_POINT ( 'NONE',  ( 21.14999999999999858, 6.093673009692411213, -199.5727803633481301 ) ) ;
#120148=DIRECTION ( 'NONE',  ( 1.000000000000000000, -0.000000000000000000, -0.000000000000000000 ) ) ;
#120154=CARTESIAN_POINT ( 'NONE',  ( -21.05000000000000071, 1.148907358139439339E-11, -201.0000000000015064 ) ) ;
#120170=CIRCLE ( 'NONE', #95182, 0.1000000000000059591 ) ;
#120207=ADVANCED_FACE ( 'NONE', ( #61504 ), #24964, .T. ) ;
#120219=ORIENTED_EDGE ( 'NONE', *, *, #196779, .T. ) ;
#120229=B_SPLINE_CURVE_WITH_KNOTS ( 'NONE', 3,
 ( #32489, #66445, #225487, #169435, #7761, #209810, #112002, #31212, #166864, #46858, #110703, #246367, #67727, #247645, #147258, #10336 ),
 .UNSPECIFIED., .F., .F.,
 ( 4, 3, 3, 3, 3, 4 ),
 ( 0.000000000000000000, 2.209075297431048351E-05, 5.594258369009902181E-05, 8.979524372342336392E-05, 0.0001236472815274606630, 0.0001574990747609576150 ),
 .UNSPECIFIED. ) ;
#120235=DIRECTION ( 'NONE',  ( -3.265361837132813586E-16, 0.9770955615653313941, 0.2128009952263610893 ) ) ;
#120245=DIRECTION ( 'NONE',  ( -0.000000000000000000, 0.2128009952263603677, -0.9770955615653313941 ) ) ;
#120299=CIRCLE ( 'NONE', #207752, 0.09999999999999691080 ) ;
#120305=STYLED_ITEM ( 'NONE', ( #206186 ), #22252 ) ;
#120327=DIRECTION ( 'NONE',  ( -1.000000000000000000, -0.000000000000000000, -0.000000000000000000 ) ) ;
#120343=AXIS2_PLACEMENT_3D ( 'NONE', #205119, #29124, #164737 ) ;
#120348=CARTESIAN_POINT ( 'NONE',  ( 21.14999999999999858, 9.028068219309963283, -211.6732836666006961 ) ) ;
#120354=AXIS2_PLACEMENT_3D ( 'NONE', #20015, #23878, #22577 ) ;
#120381=VERTEX_POINT ( 'NONE', #156482 ) ;
#120388=DIRECTION ( 'NONE',  ( 1.000000000000000000, 0.000000000000000000, 0.000000000000000000 ) ) ;
#120389=EDGE_CURVE ( 'NONE', #28807, #52494, #217242, .T. ) ;
#120437=DIRECTION ( 'NONE',  ( 0.000000000000000000, 0.2128009952263595073, -0.9770955615653317272 ) ) ;
#120440=CARTESIAN_POINT ( 'NONE',  ( 20.94999999999999929, -3.363022478626109368, -226.2703567425896267 ) ) ;
#120470=AXIS2_PLACEMENT_3D ( 'NONE', #210926, #208380, #131382 ) ;
#120486=FACE_OUTER_BOUND ( 'NONE', #184473, .T. ) ;
#120519=VECTOR ( 'NONE', #221713, 1000.000000000000227 ) ;
#120549=ORIENTED_EDGE ( 'NONE', *, *, #240139, .T. ) ;
#120563=CIRCLE ( 'NONE', #66385, 0.1000000000000054040 ) ;
#120593=CARTESIAN_POINT ( 'NONE',  ( 20.72390388899165714, 11.94582835298777468, -206.0857503901398786 ) ) ;
#120599=ORIENTED_EDGE ( 'NONE', *, *, #104933, .F. ) ;
#120607=DIRECTION ( 'NONE',  ( 0.000000000000000000, 0.2128009952263605342, -0.9770955615653315052 ) ) ;
#120617=CARTESIAN_POINT ( 'NONE',  ( -21.14999999999999858, 12.82677665681128687, -205.1493534351658354 ) ) ;
#120629=EDGE_CURVE ( 'NONE', #68492, #59785, #5221, .T. ) ;
#120637=AXIS2_PLACEMENT_3D ( 'NONE', #52808, #210612, #91945 ) ;
#120642=CIRCLE ( 'NONE', #133106, 0.09999999999999939493 ) ;
#120666=FACE_OUTER_BOUND ( 'NONE', #144615, .T. ) ;
#120687=ADVANCED_FACE ( 'NONE', ( #226675 ), #159214, .F. ) ;
#120724=DIRECTION ( 'NONE',  ( 0.000000000000000000, 0.2128009952263602012, -0.9770955615653315052 ) ) ;
#120741=CIRCLE ( 'NONE', #74950, 0.5000000000000023315 ) ;
#120769=ORIENTED_EDGE ( 'NONE', *, *, #141937, .F. ) ;
#120787=AXIS2_PLACEMENT_3D ( 'NONE', #135543, #97686, #16910 ) ;
#120796=ORIENTED_EDGE ( 'NONE', *, *, #24146, .T. ) ;
#120819=DIRECTION ( 'NONE',  ( -1.000000000000000000, -0.000000000000000000, -0.000000000000000000 ) ) ;
#120861=ORIENTED_EDGE ( 'NONE', *, *, #49561, .F. ) ;
#120880=ORIENTED_EDGE ( 'NONE', *, *, #45433, .T. ) ;
#120898=CIRCLE ( 'NONE', #175081, 0.09999999999999553690 ) ;
#120902=SPHERICAL_SURFACE ( 'NONE', #155221, 0.1000000000000000056 ) ;
#120903=CARTESIAN_POINT ( 'NONE',  ( 20.94560253601876809, 17.12224500340141731, -224.4024732428971731 ) ) ;
#120918=DIRECTION ( 'NONE',  ( 0.000000000000000000, 0.2128009952263678062, -0.9770955615653298398 ) ) ;
#120920=DIRECTION ( 'NONE',  ( 0.000000000000000000, 0.2128009952263603399, -0.9770955615653315052 ) ) ;
#120925=DIRECTION ( 'NONE',  ( 0.000000000000000000, -0.9770955615653551529, -0.2128009952262517601 ) ) ;
#120960=SPHERICAL_SURFACE ( 'NONE', #151643, 0.1000000000000000056 ) ;
#120962=CARTESIAN_POINT ( 'NONE',  ( -20.64999999999999858, -3.444512620907437039, -226.2123967847655592 ) ) ;
#120977=DIRECTION ( 'NONE',  ( 1.000000000000000000, 0.000000000000000000, 0.000000000000000000 ) ) ;
#121018=ADVANCED_FACE ( 'NONE', ( #89421 ), #130319, .F. ) ;
#121032=EDGE_CURVE ( 'NONE', #227071, #109970, #196957, .T. ) ;
#121059=ORIENTED_EDGE ( 'NONE', *, *, #132589, .T. ) ;
#121067=EDGE_CURVE ( 'NONE', #213820, #149564, #154577, .T. ) ;
#121091=FACE_OUTER_BOUND ( 'NONE', #91933, .T. ) ;
#121111=DIRECTION ( 'NONE',  ( 0.000000000000000000, 0.2128009952263604232, -0.9770955615653316162 ) ) ;
#121112=CARTESIAN_POINT ( 'NONE',  ( 23.24999999999999289, 10.74948822439028895, -222.3968794097801549 ) ) ;
#121115=DIRECTION ( 'NONE',  ( 0.000000000000000000, 0.9964539953858966292, 0.08413937888696132461 ) ) ;
#121124=DIRECTION ( 'NONE',  ( 0.000000000000000000, -0.2128009952263734406, 0.9770955615653287296 ) ) ;
#121128=ORIENTED_EDGE ( 'NONE', *, *, #165052, .F. ) ;
#121131=ORIENTED_EDGE ( 'NONE', *, *, #244222, .F. ) ;
#121145=ORIENTED_EDGE ( 'NONE', *, *, #219897, .F. ) ;
#121169=CARTESIAN_POINT ( 'NONE',  ( -23.15000000000000213, 6.757359537351773859, -220.2789794402637824 ) ) ;
#121191=AXIS2_PLACEMENT_3D ( 'NONE', #214555, #17634, #217107 ) ;
#121205=FACE_OUTER_BOUND ( 'NONE', #217832, .T. ) ;
#121207=VECTOR ( 'NONE', #236625, 1000.000000000000000 ) ;
#121210=CIRCLE ( 'NONE', #8745, 12.97499999999999964 ) ;
#121213=VECTOR ( 'NONE', #226311, 1000.000000000000000 ) ;
#121236=EDGE_CURVE ( 'NONE', #204466, #200569, #81384, .T. ) ;
#121315=VERTEX_POINT ( 'NONE', #100932 ) ;
#121328=CIRCLE ( 'NONE', #175470, 0.1000000000000054040 ) ;
#121349=DIRECTION ( 'NONE',  ( -1.000000000000000000, -1.734723475976817507E-14, 0.000000000000000000 ) ) ;
#121365=FACE_OUTER_BOUND ( 'NONE', #212245, .T. ) ;
#121394=CIRCLE ( 'NONE', #179630, 11.65000000000001457 ) ;
#121414=VERTEX_POINT ( 'NONE', #205207 ) ;
#121422=CARTESIAN_POINT ( 'NONE',  ( -18.59999999999999787, 2.859758780633683273, -208.6670499591424459 ) ) ;
#121445=ADVANCED_FACE ( 'NONE', ( #244340 ), #238255, .T. ) ;
#121469=DIRECTION ( 'NONE',  ( 0.000000000000000000, 0.2128009952263485993, -0.9770955615653341697 ) ) ;
#121474=EDGE_CURVE ( 'NONE', #52350, #156064, #1319, .T. ) ;
#121476=EDGE_CURVE ( 'NONE', #229005, #8823, #250768, .T. ) ;
#121486=VECTOR ( 'NONE', #26345, 1000.000000000000000 ) ;
#121491=CIRCLE ( 'NONE', #254517, 0.09999999999999553690 ) ;
#121500=EDGE_CURVE ( 'NONE', #256585, #17954, #172265, .T. ) ;
#121508=ADVANCED_FACE ( 'NONE', ( #70886 ), #95547, .T. ) ;
#121536=EDGE_CURVE ( 'NONE', #93645, #129320, #163845, .T. ) ;
#121569=AXIS2_PLACEMENT_3D ( 'NONE', #18019, #153744, #213661 ) ;
#121588=FACE_OUTER_BOUND ( 'NONE', #224510, .T. ) ;
#121591=CARTESIAN_POINT ( 'NONE',  ( -20.94999999999999929, 0.5876173420563349792, -209.1618981382189588 ) ) ;
#121647=CARTESIAN_POINT ( 'NONE',  ( -20.64999999999999858, 6.703231349641842307, -231.7785101893094577 ) ) ;
#121651=AXIS2_PLACEMENT_3D ( 'NONE', #37914, #157886, #59999 ) ;
#121667=ORIENTED_EDGE ( 'NONE', *, *, #16936, .T. ) ;
#121671=CARTESIAN_POINT ( 'NONE',  ( 21.05000000000000071, 7.128833340094563376, -233.7327013124401276 ) ) ;
#121678=EDGE_CURVE ( 'NONE', #201031, #98769, #55456, .T. ) ;
#121698=AXIS2_PLACEMENT_3D ( 'NONE', #80764, #237304, #57351 ) ;
#121703=ORIENTED_EDGE ( 'NONE', *, *, #154025, .T. ) ;
#121717=VECTOR ( 'NONE', #59807, 1000.000000000000000 ) ;
#121721=CIRCLE ( 'NONE', #105092, 0.1000000000000035305 ) ;
#121763=CARTESIAN_POINT ( 'NONE',  ( 18.55857864376268296, 15.39652800355464279, -222.9769737602899227 ) ) ;
#121812=AXIS2_PLACEMENT_3D ( 'NONE', #187154, #106282, #7190 ) ;
#121832=FACE_OUTER_BOUND ( 'NONE', #138510, .T. ) ;
#121844=DIRECTION ( 'NONE',  ( -1.000000000000000000, 0.000000000000000000, 0.000000000000000000 ) ) ;
#121879=ORIENTED_EDGE ( 'NONE', *, *, #224218, .F. ) ;
#121912=VECTOR ( 'NONE', #106417, 1000.000000000000000 ) ;
#121922=CARTESIAN_POINT ( 'NONE',  ( -22.57320508075686050, 11.48087284840414490, -198.4995883060918231 ) ) ;
#121925=FACE_OUTER_BOUND ( 'NONE', #128045, .T. ) ;
#121938=CARTESIAN_POINT ( 'NONE',  ( -18.59999999999999787, 7.128833340094563376, -233.7327013124401276 ) ) ;
#121941=VERTEX_POINT ( 'NONE', #33115 ) ;
#121943=ADVANCED_FACE ( 'NONE', ( #29261 ), #8292, .T. ) ;
#121978=DIRECTION ( 'NONE',  ( 0.000000000000000000, -0.2128009952265059457, 0.9770955615652998638 ) ) ;
#122001=EDGE_LOOP ( 'NONE', ( #38685, #181338, #245633 ) ) ;
#122053=ORIENTED_EDGE ( 'NONE', *, *, #207633, .F. ) ;
#122060=CARTESIAN_POINT ( 'NONE',  ( -18.59999999999999787, 12.87592094156238609, -205.3750039893633073 ) ) ;
#122112=ADVANCED_FACE ( 'NONE', ( #182874 ), #172442, .T. ) ;
#122116=DIRECTION ( 'NONE',  ( -0.000000000000000000, 0.3427706569149420734, -0.9394191166663041770 ) ) ;
#122142=EDGE_CURVE ( 'NONE', #29396, #25296, #141536, .T. ) ;
#122154=CARTESIAN_POINT ( 'NONE',  ( -23.25000000000000000, 0.8618440306782485516, -204.9572370243411115 ) ) ;
#122162=ADVANCED_FACE ( 'NONE', ( #143713 ), #26349, .T. ) ;
#122164=CARTESIAN_POINT ( 'NONE',  ( 20.85000000000000142, 17.16609282392354174, -224.6038045889790453 ) ) ;
#122191=FACE_OUTER_BOUND ( 'NONE', #199742, .T. ) ;
#122233=VECTOR ( 'NONE', #17197, 1000.000000000000227 ) ;
#122249=ORIENTED_EDGE ( 'NONE', *, *, #257096, .F. ) ;
#122350=ORIENTED_EDGE ( 'NONE', *, *, #132698, .T. ) ;
#122371=CIRCLE ( 'NONE', #184900, 3.999999999999998224 ) ;
#122400=ORIENTED_EDGE ( 'NONE', *, *, #204528, .T. ) ;
#122425=AXIS2_PLACEMENT_3D ( 'NONE', #15279, #227891, #167948 ) ;
#122437=DIRECTION ( 'NONE',  ( 0.000000000000000000, 0.2128009952263485993, -0.9770955615653341697 ) ) ;
#122443=CARTESIAN_POINT ( 'NONE',  ( -21.04999999999959570, 6.351302579977191165, -199.6316406787433664 ) ) ;
#122486=DIRECTION ( 'NONE',  ( 0.000000000000000000, -0.2128009952263601456, 0.9770955615653316162 ) ) ;
#122501=CARTESIAN_POINT ( 'NONE',  ( 18.59999999999999076, 8.366615838327078336, -209.3410474610450365 ) ) ;
#122530=VECTOR ( 'NONE', #145534, 1000.000000000000000 ) ;
#122544=DIRECTION ( 'NONE',  ( 0.000000000000000000, 0.9964539953858966292, 0.08413937888696132461 ) ) ;
#122567=ORIENTED_EDGE ( 'NONE', *, *, #124882, .T. ) ;
#122584=DIRECTION ( 'NONE',  ( 0.000000000000000000, -0.2128009952263485993, 0.9770955615653341697 ) ) ;
#122599=CARTESIAN_POINT ( 'NONE',  ( -23.15000000000000213, 15.92646454033039660, -219.3818586450342707 ) ) ;
#122619=AXIS2_PLACEMENT_3D ( 'NONE', #201289, #44793, #46064 ) ;
#122623=CARTESIAN_POINT ( 'NONE',  ( -20.94999999999999929, -10.60885044396467336, -206.2784744251879090 ) ) ;
#122645=EDGE_LOOP ( 'NONE', ( #213445, #118984, #10135 ) ) ;
#122661=DIRECTION ( 'NONE',  ( 0.000000000000000000, 0.2128009952263604232, -0.9770955615653316162 ) ) ;
#122666=DIRECTION ( 'NONE',  ( -1.000000000000000000, -0.000000000000000000, -0.000000000000000000 ) ) ;
#122668=EDGE_CURVE ( 'NONE', #8823, #59550, #76312, .T. ) ;
#122669=EDGE_CURVE ( 'NONE', #185482, #162306, #120229, .T. ) ;
#122670=EDGE_LOOP ( 'NONE', ( #144748, #30075, #203667, #56405 ) ) ;
#122677=CARTESIAN_POINT ( 'NONE',  ( -21.64999999999999858, 11.58468387039765801, -220.1227639117171861 ) ) ;
#122701=VECTOR ( 'NONE', #127023, 1000.000000000000227 ) ;
#122727=AXIS2_PLACEMENT_3D ( 'NONE', #65871, #129701, #28062 ) ;
#122748=CIRCLE ( 'NONE', #39554, 0.5000000000000076605 ) ;
#122768=DIRECTION ( 'NONE',  ( -3.469446951953679822E-14, -0.9770955615653551529, -0.2128009952262517601 ) ) ;
#122770=VERTEX_POINT ( 'NONE', #75456 ) ;
#122777=VECTOR ( 'NONE', #224853, 1000.000000000000000 ) ;
#122798=ORIENTED_EDGE ( 'NONE', *, *, #80233, .F. ) ;
#122827=FACE_OUTER_BOUND ( 'NONE', #97636, .T. ) ;
#122837=VERTEX_POINT ( 'NONE', #214932 ) ;
#122840=ORIENTED_EDGE ( 'NONE', *, *, #255162, .F. ) ;
#122855=VERTEX_POINT ( 'NONE', #18011 ) ;
#122867=CARTESIAN_POINT ( 'NONE',  ( -21.14999999999999858, -1.236118717437885595, -194.8647072476926496 ) ) ;
#122879=CIRCLE ( 'NONE', #43751, 0.09999999999999897859 ) ;
#122887=CARTESIAN_POINT ( 'NONE',  ( 19.88284271247463053, 16.69046054743353125, -222.6951690485254858 ) ) ;
#122890=EDGE_CURVE ( 'NONE', #115133, #22692, #127068, .T. ) ;
#123017=ORIENTED_EDGE ( 'NONE', *, *, #31919, .F. ) ;
#123035=ORIENTED_EDGE ( 'NONE', *, *, #4536, .F. ) ;
#123068=LINE ( 'NONE', #66934, #150193 ) ;
#123071=CIRCLE ( 'NONE', #173192, 0.1000000000000054040 ) ;
#123072=ADVANCED_FACE ( 'NONE', ( #188321 ), #73543, .T. ) ;
#123172=AXIS2_PLACEMENT_3D ( 'NONE', #150014, #93862, #155163 ) ;
#123197=CYLINDRICAL_SURFACE ( 'NONE', #228106, 0.09999999999999938105 ) ;
#123237=DIRECTION ( 'NONE',  ( 0.7071067811865486830, 0.1504730267678053013, -0.6909108974501224631 ) ) ;
#123238=VERTEX_POINT ( 'NONE', #121647 ) ;
#123243=AXIS2_PLACEMENT_3D ( 'NONE', #205623, #227762, #230328 ) ;
#123246=AXIS2_PLACEMENT_3D ( 'NONE', #56122, #130539, #172292 ) ;
#123289=DIRECTION ( 'NONE',  ( -0.000000000000000000, -0.9770955615653316162, -0.2128009952263604232 ) ) ;
#123341=LINE ( 'NONE', #204137, #241525 ) ;
#123376=DIRECTION ( 'NONE',  ( -1.000000000000000000, -0.000000000000000000, -0.000000000000000000 ) ) ;
#123414=VECTOR ( 'NONE', #210664, 1000.000000000000227 ) ;
#123425=DIRECTION ( 'NONE',  ( 0.000000000000000000, -0.3427706569149662763, 0.9394191166662954062 ) ) ;
#123440=CARTESIAN_POINT ( 'NONE',  ( 21.05000000000000071, 7.128833340094563376, -233.7327013124401276 ) ) ;
#123444=EDGE_CURVE ( 'NONE', #126771, #253449, #249294, .T. ) ;
#123448=AXIS2_PLACEMENT_3D ( 'NONE', #79998, #177866, #239110 ) ;
#123478=ORIENTED_EDGE ( 'NONE', *, *, #145722, .T. ) ;
#123481=CIRCLE ( 'NONE', #252648, 0.1000000000000090955 ) ;
#123488=DIRECTION ( 'NONE',  ( 1.000000000000000000, 0.000000000000000000, 0.000000000000000000 ) ) ;
#123500=DIRECTION ( 'NONE',  ( 0.000000000000000000, 0.2128009952263602844, -0.9770955615653315052 ) ) ;
#123518=FACE_OUTER_BOUND ( 'NONE', #84871, .T. ) ;
#123534=SPHERICAL_SURFACE ( 'NONE', #55148, 0.1000000000000000056 ) ;
#123596=EDGE_CURVE ( 'NONE', #95409, #13934, #6501, .T. ) ;
#123605=CARTESIAN_POINT ( 'NONE',  ( 18.49999999999999289, 14.55853075413893194, -219.6797800383511401 ) ) ;
#123627=ORIENTED_EDGE ( 'NONE', *, *, #132689, .F. ) ;
#123636=VERTEX_POINT ( 'NONE', #225528 ) ;
#123672=ORIENTED_EDGE ( 'NONE', *, *, #172627, .T. ) ;
#123683=AXIS2_PLACEMENT_3D ( 'NONE', #75292, #154826, #231783 ) ;
#123723=CYLINDRICAL_SURFACE ( 'NONE', #137521, 0.09999999999999939493 ) ;
#123732=VECTOR ( 'NONE', #216854, 1000.000000000000000 ) ;
#123752=TOROIDAL_SURFACE ( 'NONE', #11313, 7.800000000000000711, 0.1000000000000000056 ) ;
#123766=DIRECTION ( 'NONE',  ( 0.000000000000000000, 0.2128009952263605065, -0.9770955615653315052 ) ) ;
#123812=CARTESIAN_POINT ( 'NONE',  ( -18.50000972452446035, 18.34807417603271418, -236.8765254748879556 ) ) ;
#123815=VECTOR ( 'NONE', #9059, 1000.000000000000000 ) ;
#123836=AXIS2_PLACEMENT_3D ( 'NONE', #221506, #242366, #122437 ) ;
#123843=EDGE_CURVE ( 'NONE', #21650, #171420, #214267, .T. ) ;
#123860=ADVANCED_FACE ( 'NONE', ( #172043 ), #139210, .T. ) ;
#123897=CIRCLE ( 'NONE', #36620, 0.1000000000000035305 ) ;
#123919=VERTEX_POINT ( 'NONE', #118462 ) ;
#123930=VECTOR ( 'NONE', #157819, 1000.000000000000000 ) ;
#123939=CARTESIAN_POINT ( 'NONE',  ( 18.59999999999999076, 15.51794587355511545, -222.9505302427971003 ) ) ;
#123945=ORIENTED_EDGE ( 'NONE', *, *, #218085, .F. ) ;
#123963=EDGE_CURVE ( 'NONE', #110507, #176941, #22774, .T. ) ;
#123972=EDGE_CURVE ( 'NONE', #36199, #29274, #10261, .T. ) ;
#123997=ORIENTED_EDGE ( 'NONE', *, *, #24359, .T. ) ;
#124023=DIRECTION ( 'NONE',  ( 1.875376730785737719E-16, -0.9770955615653315052, -0.2128009952263603954 ) ) ;
#124057=VECTOR ( 'NONE', #16532, 1000.000000000000000 ) ;
#124060=DIRECTION ( 'NONE',  ( 0.000000000000000000, -0.2128009952263603677, 0.9770955615653313941 ) ) ;
#124096=AXIS2_PLACEMENT_3D ( 'NONE', #118307, #197822, #107715 ) ;
#124097=CIRCLE ( 'NONE', #153164, 0.09999999999999939493 ) ;
#124099=CARTESIAN_POINT ( 'NONE',  ( -23.25000000000000000, 7.882824859404637508, -245.3558965132535832 ) ) ;
#124108=DIRECTION ( 'NONE',  ( 1.000000000000000000, 3.190570557967288949E-16, 6.948722487160392945E-17 ) ) ;
#124116=LINE ( 'NONE', #182813, #220028 ) ;
#124117=ORIENTED_EDGE ( 'NONE', *, *, #25968, .F. ) ;
#124170=VERTEX_POINT ( 'NONE', #12638 ) ;
#124172=EDGE_CURVE ( 'NONE', #137285, #126094, #227802, .T. ) ;
#124176=CARTESIAN_POINT ( 'NONE',  ( -21.93340585971934331, 7.156391548294640970, -199.4414142243538777 ) ) ;
#124186=AXIS2_PLACEMENT_3D ( 'NONE', #153525, #127493, #28435 ) ;
#124189=DIRECTION ( 'NONE',  ( 2.952720810173288126E-16, -0.9770955615653313941, -0.2128009952263603677 ) ) ;
#124216=CARTESIAN_POINT ( 'NONE',  ( 21.08376601933332495, 6.183116931858830156, -199.5881120517869078 ) ) ;
#124225=CARTESIAN_POINT ( 'NONE',  ( 18.58719872626880232, -0.7668622897694893359, -242.4347059258014383 ) ) ;
#124232=CARTESIAN_POINT ( 'NONE',  ( -23.15000000000000213, 7.128833340094563376, -233.7327013124401276 ) ) ;
#124235=ORIENTED_EDGE ( 'NONE', *, *, #57839, .F. ) ;
#124251=ORIENTED_EDGE ( 'NONE', *, *, #138659, .F. ) ;
#124294=CARTESIAN_POINT ( 'NONE',  ( -21.29999999999995808, -0.8618440306552707098, -197.0427629756619297 ) ) ;
#124333=LINE ( 'NONE', #203855, #239304 ) ;
#124361=CIRCLE ( 'NONE', #11954, 0.1000000000000055844 ) ;
#124384=CARTESIAN_POINT ( 'NONE',  ( 21.05000000000000071, -10.86374996222470379, -206.3339888224507206 ) ) ;
#124389=ORIENTED_EDGE ( 'NONE', *, *, #235484, .T. ) ;
#124408=CARTESIAN_POINT ( 'NONE',  ( 23.14999999999999858, 7.128833340094563376, -233.7327013124401276 ) ) ;
#124427=DIRECTION ( 'NONE',  ( -0.000000000000000000, -0.2128009952263603677, 0.9770955615653313941 ) ) ;
#124459=DIRECTION ( 'NONE',  ( -1.000000000000000000, 0.000000000000000000, 0.000000000000000000 ) ) ;
#124463=CARTESIAN_POINT ( 'NONE',  ( 18.59999999999997655, 7.128833340094563376, -233.7327013124401276 ) ) ;
#124495=CARTESIAN_POINT ( 'NONE',  ( 18.59999999999999432, -3.391987963166880338, -191.5331142350599691 ) ) ;
#124530=LINE ( 'NONE', #3265, #1433 ) ;
#124531=EDGE_LOOP ( 'NONE', ( #196459, #237288, #158281, #163369 ) ) ;
#124576=AXIS2_PLACEMENT_3D ( 'NONE', #216527, #75752, #138257 ) ;
#124594=AXIS2_PLACEMENT_3D ( 'NONE', #21003, #122661, #61381 ) ;
#124596=CARTESIAN_POINT ( 'NONE',  ( -21.05000000000000071, 0.5876173420563349792, -209.1618981382189588 ) ) ;
#124598=DIRECTION ( 'NONE',  ( 0.000000000000000000, -0.9770955615653543758, -0.2128009952262553683 ) ) ;
#124613=ORIENTED_EDGE ( 'NONE', *, *, #168405, .T. ) ;
#124631=CYLINDRICAL_SURFACE ( 'NONE', #7418, 0.1000000000000054040 ) ;
#124660=ORIENTED_EDGE ( 'NONE', *, *, #163318, .F. ) ;
#124677=CARTESIAN_POINT ( 'NONE',  ( 21.14999999999999858, 11.40444339177024169, -198.6185779617709670 ) ) ;
#124705=CARTESIAN_POINT ( 'NONE',  ( -20.94999999999999929, 10.68863688179708049, -222.5873974249508933 ) ) ;
#124717=FACE_OUTER_BOUND ( 'NONE', #4101, .T. ) ;
#124724=ORIENTED_EDGE ( 'NONE', *, *, #222046, .F. ) ;
#124737=CARTESIAN_POINT ( 'NONE',  ( -18.39999999999999858, -7.785976468740645196, -209.8926132507865816 ) ) ;
#124744=DIRECTION ( 'NONE',  ( -2.081668171172216981E-13, -0.9742838591452925856, -0.2253241261138180518 ) ) ;
#124758=DIRECTION ( 'NONE',  ( 0.7071067811865476838, -0.6909108974501236844, -0.1504730267678055788 ) ) ;
#124763=DIRECTION ( 'NONE',  ( 0.000000000000000000, 0.2128009952263604232, -0.9770955615653316162 ) ) ;
#124799=CIRCLE ( 'NONE', #166514, 0.2000000000000003997 ) ;
#124808=DIRECTION ( 'NONE',  ( 0.000000000000000000, -0.2128009952263713866, 0.9770955615653290627 ) ) ;
#124828=CARTESIAN_POINT ( 'NONE',  ( -23.15000000000000213, 16.02417409648692725, -219.3605785455116006 ) ) ;
#124856=DIRECTION ( 'NONE',  ( 1.000000000000000000, 0.000000000000000000, 0.000000000000000000 ) ) ;
#124858=AXIS2_PLACEMENT_3D ( 'NONE', #97479, #195358, #158801 ) ;
#124860=EDGE_CURVE ( 'NONE', #203210, #133719, #142205, .T. ) ;
#124864=CARTESIAN_POINT ( 'NONE',  ( -20.54999999999999716, 6.268811756569107274, -220.3853799378769622 ) ) ;
#124872=PLANE ( 'NONE',  #239365 ) ;
#124882=EDGE_CURVE ( 'NONE', #131461, #187418, #106628, .T. ) ;
#124889=EDGE_CURVE ( 'NONE', #202387, #212703, #106438, .T. ) ;
#124914=ORIENTED_EDGE ( 'NONE', *, *, #5285, .F. ) ;
#124982=DIRECTION ( 'NONE',  ( 1.000000000000000000, 0.000000000000000000, 0.000000000000000000 ) ) ;
#125019=AXIS2_PLACEMENT_3D ( 'NONE', #96053, #219858, #41262 ) ;
#125056=EDGE_CURVE ( 'NONE', #200161, #132241, #103889, .T. ) ;
#125065=DIRECTION ( 'NONE',  ( 1.000000000000000000, 0.000000000000000000, 0.000000000000000000 ) ) ;
#125071=DIRECTION ( 'NONE',  ( 0.000000000000000000, 0.2128009952263678062, -0.9770955615653298398 ) ) ;
#125097=ADVANCED_FACE ( 'NONE', ( #145594 ), #43324, .F. ) ;
#125113=DIRECTION ( 'NONE',  ( -3.890533409366484021E-14, 0.08413937888703756918, -0.9964539953858901900 ) ) ;
#125127=DIRECTION ( 'NONE',  ( 0.000000000000000000, 0.2128009952263603954, -0.9770955615653315052 ) ) ;
#125143=ORIENTED_EDGE ( 'NONE', *, *, #72193, .T. ) ;
#125159=ORIENTED_EDGE ( 'NONE', *, *, #18355, .F. ) ;
#125210=EDGE_CURVE ( 'NONE', #226256, #7157, #152474, .T. ) ;
#125227=DIRECTION ( 'NONE',  ( 0.7071067811865476838, -0.6909108974501236844, -0.1504730267678055788 ) ) ;
#125239=ORIENTED_EDGE ( 'NONE', *, *, #94937, .F. ) ;
#125248=FACE_OUTER_BOUND ( 'NONE', #41202, .T. ) ;
#125253=AXIS2_PLACEMENT_3D ( 'NONE', #213964, #195709, #232266 ) ;
#125304=CARTESIAN_POINT ( 'NONE',  ( -21.55000000000000071, 11.50825441376376901, -220.2417535673963300 ) ) ;
#125351=DIRECTION ( 'NONE',  ( -1.000000000000000000, -0.000000000000000000, -0.000000000000000000 ) ) ;
#125372=SURFACE_STYLE_FILL_AREA ( #207486 ) ;
#125374=DIRECTION ( 'NONE',  ( 1.000000000000000000, 0.000000000000000000, 0.000000000000000000 ) ) ;
#125386=B_SPLINE_CURVE_WITH_KNOTS ( 'NONE', 3,
 ( #25907, #164134, #128859, #144542, #184968, #208406, #126266, #169299, #45455, #248805 ),
 .UNSPECIFIED., .F., .F.,
 ( 4, 3, 3, 4 ),
 ( 0.000000000000000000, 0.0002000000000008539272, 0.001000000000082976398, 0.001967863649483329348 ),
 .UNSPECIFIED. ) ;
#125420=VERTEX_POINT ( 'NONE', #5384 ) ;
#125434=EDGE_CURVE ( 'NONE', #221067, #242867, #248303, .T. ) ;
#125437=ORIENTED_EDGE ( 'NONE', *, *, #215289, .F. ) ;
#125463=DIRECTION ( 'NONE',  ( 0.000000000000000000, 0.2128009952263693050, -0.9770955615653296178 ) ) ;
#125478=ORIENTED_EDGE ( 'NONE', *, *, #77318, .T. ) ;
#125494=EDGE_CURVE ( 'NONE', #204482, #22587, #98415, .T. ) ;
#125525=CARTESIAN_POINT ( 'NONE',  ( -20.94999999999999929, 7.633102355717365839, -241.5185714324494484 ) ) ;
#125527=ADVANCED_FACE ( 'NONE', ( #251732 ), #93936, .F. ) ;
#125589=DIRECTION ( 'NONE',  ( -1.000000000000000000, 0.000000000000000000, 0.000000000000000000 ) ) ;
#125612=ORIENTED_EDGE ( 'NONE', *, *, #251888, .F. ) ;
#125624=DIRECTION ( 'NONE',  ( 1.000000000000000000, 0.000000000000000000, 0.000000000000000000 ) ) ;
#125630=AXIS2_PLACEMENT_3D ( 'NONE', #110863, #178573, #101534 ) ;
#125632=CARTESIAN_POINT ( 'NONE',  ( -21.29999999999995808, 1.148907358139439339E-11, -201.0000000000015064 ) ) ;
#125640=LINE ( 'NONE', #63090, #19940 ) ;
#125671=EDGE_CURVE ( 'NONE', #92384, #247087, #56912, .T. ) ;
#125678=VERTEX_POINT ( 'NONE', #238586 ) ;
#125682=DIRECTION ( 'NONE',  ( 0.000000000000000000, 0.2965989261549568656, 0.9550021345545394169 ) ) ;
#125704=CARTESIAN_POINT ( 'NONE',  ( 21.12400247839513767, 13.08273057273256335, -210.6878773030995831 ) ) ;
#125727=CARTESIAN_POINT ( 'NONE',  ( -23.25000000000000000, -4.914013037343267776, -233.1828366659746905 ) ) ;
#125749=FACE_OUTER_BOUND ( 'NONE', #66801, .T. ) ;
#125750=DIRECTION ( 'NONE',  ( 0.000000000000000000, 0.2128009952263607285, -0.9770955615653316162 ) ) ;
#125760=CIRCLE ( 'NONE', #217694, 11.80000000000001670 ) ;
#125875=ORIENTED_EDGE ( 'NONE', *, *, #192442, .F. ) ;
#125892=CIRCLE ( 'NONE', #92584, 0.5999999999999978684 ) ;
#125893=LINE ( 'NONE', #46352, #69357 ) ;
#125916=CIRCLE ( 'NONE', #109348, 0.09999999999999939493 ) ;
#125936=AXIS2_PLACEMENT_3D ( 'NONE', #857, #137811, #180818 ) ;
#125945=DIRECTION ( 'NONE',  ( 0.000000000000000000, 0.2128009952263601734, -0.9770955615653316162 ) ) ;
#125947=ORIENTED_EDGE ( 'NONE', *, *, #49561, .T. ) ;
#125966=EDGE_CURVE ( 'NONE', #66263, #68492, #34642, .T. ) ;
#125991=CIRCLE ( 'NONE', #163424, 0.1000000000000043493 ) ;
#125997=CYLINDRICAL_SURFACE ( 'NONE', #249849, 0.5000000000000007772 ) ;
#125998=DIRECTION ( 'NONE',  ( 0.000000000000000000, -0.2128009952263485993, 0.9770955615653341697 ) ) ;
#126039=CARTESIAN_POINT ( 'NONE',  ( 18.49999999999999645, -1.102499207903926637, -187.8171010361417643 ) ) ;
#126044=CARTESIAN_POINT ( 'NONE',  ( 21.05000000000000071, 1.148907358139439339E-11, -201.0000000000015064 ) ) ;
#126064=CIRCLE ( 'NONE', #34358, 0.4999999999999997780 ) ;
#126073=VERTEX_POINT ( 'NONE', #141416 ) ;
#126081=CARTESIAN_POINT ( 'NONE',  ( -21.05000000000000071, 6.412126976762837494, -199.7058512474018244 ) ) ;
#126090=EDGE_CURVE ( 'NONE', #248650, #202021, #219613, .T. ) ;
#126094=VERTEX_POINT ( 'NONE', #48732 ) ;
#126111=AXIS2_PLACEMENT_3D ( 'NONE', #209199, #227471, #245771 ) ;
#126113=AXIS2_PLACEMENT_3D ( 'NONE', #196723, #216280, #158913 ) ;
#126130=VECTOR ( 'NONE', #52804, 1000.000000000000000 ) ;
#126135=ADVANCED_FACE ( 'NONE', ( #106124 ), #164848, .F. ) ;
#126145=AXIS2_PLACEMENT_3D ( 'NONE', #152963, #156805, #117647 ) ;
#126149=VERTEX_POINT ( 'NONE', #85266 ) ;
#126159=CARTESIAN_POINT ( 'NONE',  ( -23.25000000000000000, -2.576749817950531707, -189.6385361693310756 ) ) ;
#126184=ORIENTED_EDGE ( 'NONE', *, *, #24283, .T. ) ;
#126209=DIRECTION ( 'NONE',  ( 1.000000000000000000, -0.000000000000000000, 0.000000000000000000 ) ) ;
#126220=ORIENTED_EDGE ( 'NONE', *, *, #142926, .F. ) ;
#126238=( BOUNDED_CURVE ( )  B_SPLINE_CURVE ( 3, ( #138191, #220334, #179928, #75694 ),
 .UNSPECIFIED., .F., .T. ) 
 B_SPLINE_CURVE_WITH_KNOTS ( ( 4, 4 ),
 ( 1.570796326794895448, 3.141592653589791784 ),
 .UNSPECIFIED. ) 
 CURVE ( )  GEOMETRIC_REPRESENTATION_ITEM ( )  RATIONAL_B_SPLINE_CURVE ( ( 1.000000000000000000, 0.8047378541243650485, 0.8047378541243650485, 1.000000000000000000 ) ) 
 REPRESENTATION_ITEM ( '' )  );
#126243=DIRECTION ( 'NONE',  ( 1.000000000000000000, 0.000000000000000000, 0.000000000000000000 ) ) ;
#126266=CARTESIAN_POINT ( 'NONE',  ( 21.78635804494511419, -1.400458356024840922, -194.1044180137097044 ) ) ;
#126321=EDGE_CURVE ( 'NONE', #232107, #173153, #86320, .T. ) ;
#126333=PLANE ( 'NONE',  #57858 ) ;
#126336=DIRECTION ( 'NONE',  ( 3.469446951953347238E-14, -0.6413305999522614931, -0.7672646620071019719 ) ) ;
#126390=TOROIDAL_SURFACE ( 'NONE', #143117, 0.2000000000000000111, 0.1000000000000000056 ) ;
#126405=ORIENTED_EDGE ( 'NONE', *, *, #253664, .F. ) ;
#126410=EDGE_CURVE ( 'NONE', #187924, #189298, #46694, .T. ) ;
#126413=ORIENTED_EDGE ( 'NONE', *, *, #164686, .F. ) ;
#126443=AXIS2_PLACEMENT_3D ( 'NONE', #149662, #49251, #170544 ) ;
#126513=ORIENTED_EDGE ( 'NONE', *, *, #87740, .F. ) ;
#126530=DIRECTION ( 'NONE',  ( 0.000000000000000000, 0.7397890806274345366, 0.6728388485992877754 ) ) ;
#126555=EDGE_CURVE ( 'NONE', #194263, #122855, #71869, .T. ) ;
#126564=CARTESIAN_POINT ( 'NONE',  ( 20.94999999999999929, 14.86477715130881272, -235.7932433709592601 ) ) ;
#126580=EDGE_LOOP ( 'NONE', ( #69063, #62887, #98523, #237663, #146033, #149493, #224585, #152901, #98038, #171764, #150974, #197093 ) ) ;
#126584=CARTESIAN_POINT ( 'NONE',  ( 18.49999999999999289, 15.53922597307775000, -223.0482397989536025 ) ) ;
#126640=AXIS2_PLACEMENT_3D ( 'NONE', #71891, #211390, #191857 ) ;
#126668=VECTOR ( 'NONE', #18506, 1000.000000000000000 ) ;
#126678=DIRECTION ( 'NONE',  ( -0.000000000000000000, 0.9770955615653313941, 0.2128009952263603954 ) ) ;
#126716=AXIS2_PLACEMENT_3D ( 'NONE', #203490, #65255, #24877 ) ;
#126721=CARTESIAN_POINT ( 'NONE',  ( -22.39999999999999858, 11.45959274888149970, -198.4018787499352641 ) ) ;
#126727=CARTESIAN_POINT ( 'NONE',  ( -21.14999999999999858, 12.91220014178004050, -205.0716606970938187 ) ) ;
#126771=VERTEX_POINT ( 'NONE', #144647 ) ;
#126787=ORIENTED_EDGE ( 'NONE', *, *, #223318, .F. ) ;
#126792=EDGE_LOOP ( 'NONE', ( #79901, #149665, #38123, #245199 ) ) ;
#126796=AXIS2_PLACEMENT_3D ( 'NONE', #42011, #242742, #82365 ) ;
#126828=EDGE_CURVE ( 'NONE', #83634, #86372, #69001, .T. ) ;
#126831=ORIENTED_EDGE ( 'NONE', *, *, #3417, .F. ) ;
#126890=ORIENTED_EDGE ( 'NONE', *, *, #227664, .T. ) ;
#126912=VERTEX_POINT ( 'NONE', #171971 ) ;
#126919=EDGE_LOOP ( 'NONE', ( #237444, #8788, #258029 ) ) ;
#126970=CYLINDRICAL_SURFACE ( 'NONE', #220388, 0.1000000000000054040 ) ;
#126975=CARTESIAN_POINT ( 'NONE',  ( 18.58703555225022797, -7.674694569411833811, -209.9634296052368256 ) ) ;
#127009=ORIENTED_EDGE ( 'NONE', *, *, #156369, .F. ) ;
#127015=ORIENTED_EDGE ( 'NONE', *, *, #12510, .T. ) ;
#127023=DIRECTION ( 'NONE',  ( -0.000000000000000000, -0.2128009952263603677, 0.9770955615653313941 ) ) ;
#127067=DIRECTION ( 'NONE',  ( 0.000000000000000000, 0.2128009952263618387, -0.9770955615653311721 ) ) ;
#127068=LINE ( 'NONE', #224864, #22193 ) ;
#127107=CARTESIAN_POINT ( 'NONE',  ( -23.15000000000000213, 6.759468328187065111, -212.0650163994647812 ) ) ;
#127134=CIRCLE ( 'NONE', #152103, 0.09999999999999939493 ) ;
#127174=DIRECTION ( 'NONE',  ( 1.296989514748957725E-15, -0.9979305700607959961, -0.06430067914209769420 ) ) ;
#127176=CARTESIAN_POINT ( 'NONE',  ( -21.07928932188134041, 6.162520550847337297, -199.5566553493351307 ) ) ;
#127219=ORIENTED_EDGE ( 'NONE', *, *, #90289, .T. ) ;
#127248=VERTEX_POINT ( 'NONE', #244715 ) ;
#127263=AXIS2_PLACEMENT_3D ( 'NONE', #37740, #217605, #218899 ) ;
#127291=CARTESIAN_POINT ( 'NONE',  ( 21.14999999999999858, 13.96869538424788715, -210.3925794786331949 ) ) ;
#127370=VECTOR ( 'NONE', #33697, 1000.000000000000000 ) ;
#127372=EDGE_CURVE ( 'NONE', #95759, #246109, #124799, .T. ) ;
#127375=DIRECTION ( 'NONE',  ( 0.000000000000000000, 0.2128009952263604232, -0.9770955615653316162 ) ) ;
#127430=CARTESIAN_POINT ( 'NONE',  ( -21.05000000000000071, -4.969162394454528453, -233.3995358778103935 ) ) ;
#127433=CARTESIAN_POINT ( 'NONE',  ( -18.50000000000000000, 0.6656436123793491033, -212.6810495496487476 ) ) ;
#127443=VECTOR ( 'NONE', #156102, 1000.000000000000227 ) ;
#127457=CARTESIAN_POINT ( 'NONE',  ( -21.05000000000000071, 17.01923898301589944, -224.3994341343041867 ) ) ;
#127466=EDGE_LOOP ( 'NONE', ( #173703, #228763, #71612, #144192, #540, #78390, #40176, #118537 ) ) ;
#127474=ORIENTED_EDGE ( 'NONE', *, *, #123963, .T. ) ;
#127482=EDGE_LOOP ( 'NONE', ( #53315, #136127, #200913, #235979 ) ) ;
#127493=DIRECTION ( 'NONE',  ( 0.000000000000000000, 0.2128009952263604232, -0.9770955615653316162 ) ) ;
#127544=VERTEX_POINT ( 'NONE', #249254 ) ;
#127549=DIRECTION ( 'NONE',  ( 0.000000000000000000, 0.2128009952263601456, -0.9770955615653315052 ) ) ;
#127578=ORIENTED_EDGE ( 'NONE', *, *, #108554, .F. ) ;
#127590=DIRECTION ( 'NONE',  ( 0.000000000000000000, 0.2128009952263602844, -0.9770955615653315052 ) ) ;
#127627=CARTESIAN_POINT ( 'NONE',  ( 18.59999999999999076, 10.92199707682457088, -220.3694341645321515 ) ) ;
#127653=EDGE_LOOP ( 'NONE', ( #151346, #214750, #17129, #177435 ) ) ;
#127676=CARTESIAN_POINT ( 'NONE',  ( 18.54271179734046626, -0.8403326744508465840, -242.3672828657570051 ) ) ;
#127680=ORIENTED_EDGE ( 'NONE', *, *, #224203, .T. ) ;
#127688=ADVANCED_FACE ( 'NONE', ( #114868 ), #116170, .T. ) ;
#127699=ORIENTED_EDGE ( 'NONE', *, *, #163470, .F. ) ;
#127700=CARTESIAN_POINT ( 'NONE',  ( 20.94999999999999929, 7.661991824395936845, -241.5144583139544636 ) ) ;
#127730=CIRCLE ( 'NONE', #136055, 0.1000000000000054040 ) ;
#127736=CIRCLE ( 'NONE', #156962, 0.1000000000000055844 ) ;
#127739=DIRECTION ( 'NONE',  ( -0.7071067811865389130, -0.1504730267678074107, 0.6909108974501321221 ) ) ;
#127740=DIRECTION ( 'NONE',  ( 0.000000000000000000, -0.2128009952263636428, 0.9770955615653308390 ) ) ;
#127744=ORIENTED_EDGE ( 'NONE', *, *, #137287, .T. ) ;
#127761=EDGE_CURVE ( 'NONE', #88245, #224443, #256953, .T. ) ;
#127771=AXIS2_PLACEMENT_3D ( 'NONE', #173977, #73571, #153122 ) ;
#127778=DIRECTION ( 'NONE',  ( 0.000000000000000000, -0.2128009952263604232, 0.9770955615653316162 ) ) ;
#127797=AXIS2_PLACEMENT_3D ( 'NONE', #145886, #125065, #84593 ) ;
#127801=CARTESIAN_POINT ( 'NONE',  ( 18.59999999999999432, 0.7653315920341953182, -212.6731560895497353 ) ) ;
#127804=ORIENTED_EDGE ( 'NONE', *, *, #129387, .T. ) ;
#127821=FACE_BOUND ( 'NONE', #152085, .T. ) ;
#127828=CARTESIAN_POINT ( 'NONE',  ( 20.94999999999999929, -6.438379425586758131, -212.1495692908769684 ) ) ;
#127836=VERTEX_POINT ( 'NONE', #45608 ) ;
#127874=DIRECTION ( 'NONE',  ( -1.000000000000000000, -0.000000000000000000, -0.000000000000000000 ) ) ;
#127926=AXIS2_PLACEMENT_3D ( 'NONE', #44455, #60132, #203517 ) ;
#127927=CARTESIAN_POINT ( 'NONE',  ( -20.94999999999999929, 7.128833340094563376, -233.7327013124401276 ) ) ;
#127935=CARTESIAN_POINT ( 'NONE',  ( -18.50000000000000000, 8.006782298343173565, -209.8034900594678618 ) ) ;
#127940=CARTESIAN_POINT ( 'NONE',  ( 21.14999999999999858, 13.09610049681062982, -210.7873096111272844 ) ) ;
#127949=FACE_OUTER_BOUND ( 'NONE', #21923, .T. ) ;
#127959=CIRCLE ( 'NONE', #57179, 0.09999999999999510669 ) ;
#127960=ADVANCED_FACE ( 'NONE', ( #114567 ), #174600, .F. ) ;
#127987=DIRECTION ( 'NONE',  ( 0.000000000000000000, 0.2128009952263601179, -0.9770955615653315052 ) ) ;
#127999=LINE ( 'NONE', #87560, #2244 ) ;
#128010=VECTOR ( 'NONE', #200696, 1000.000000000000000 ) ;
#128026=FACE_OUTER_BOUND ( 'NONE', #34487, .T. ) ;
#128042=CARTESIAN_POINT ( 'NONE',  ( 18.49999999999999289, 15.46667084161607164, -223.0640415323869945 ) ) ;
#128045=EDGE_LOOP ( 'NONE', ( #30203, #227261, #92529, #118852 ) ) ;
#128046=CARTESIAN_POINT ( 'NONE',  ( -23.15000000000000213, -3.281532336344783918, -226.3283167004137226 ) ) ;
#128068=CARTESIAN_POINT ( 'NONE',  ( 18.47149038651510367, -0.9011289498978589663, -242.3107469318997857 ) ) ;
#128069=ORIENTED_EDGE ( 'NONE', *, *, #45744, .F. ) ;
#128109=VERTEX_POINT ( 'NONE', #118427 ) ;
#128144=VECTOR ( 'NONE', #243002, 1000.000000000000114 ) ;
#128171=CARTESIAN_POINT ( 'NONE',  ( 20.94999999999999929, 6.256349259666489360, -229.7266095100222572 ) ) ;
#128195=ORIENTED_EDGE ( 'NONE', *, *, #72698, .F. ) ;
#128199=AXIS2_PLACEMENT_3D ( 'NONE', #33787, #11634, #155000 ) ;
#128217=ADVANCED_FACE ( 'NONE', ( #162681 ), #47833, .T. ) ;
#128218=CARTESIAN_POINT ( 'NONE',  ( 20.94999999999999929, -4.756823075239758225, -233.1486023682345490 ) ) ;
#128237=ADVANCED_FACE ( 'NONE', ( #66139 ), #169938, .T. ) ;
#128249=AXIS2_PLACEMENT_3D ( 'NONE', #76336, #17654, #196297 ) ;
#128267=DIRECTION ( 'NONE',  ( -0.000000000000000000, 0.2128009952263604232, -0.9770955615653316162 ) ) ;
#128288=CARTESIAN_POINT ( 'NONE',  ( 21.06280952165566589, 12.98075861599861724, -210.6630625559073735 ) ) ;
#128298=ADVANCED_FACE ( 'NONE', ( #121832 ), #78812, .T. ) ;
#128318=EDGE_CURVE ( 'NONE', #241890, #57917, #65642, .T. ) ;
#128327=EDGE_CURVE ( 'NONE', #212172, #179904, #61737, .T. ) ;
#128350=AXIS2_PLACEMENT_3D ( 'NONE', #109356, #67683, #24744 ) ;
#128387=EDGE_LOOP ( 'NONE', ( #167633, #20952, #88216, #85425 ) ) ;
#128389=ORIENTED_EDGE ( 'NONE', *, *, #89724, .F. ) ;
#128404=FACE_OUTER_BOUND ( 'NONE', #196348, .T. ) ;
#128413=ORIENTED_EDGE ( 'NONE', *, *, #59279, .F. ) ;
#128428=EDGE_CURVE ( 'NONE', #187418, #88973, #42287, .T. ) ;
#128446=AXIS2_PLACEMENT_3D ( 'NONE', #30290, #211485, #154123 ) ;
#128473=AXIS2_PLACEMENT_3D ( 'NONE', #142604, #52183, #222129 ) ;
#128499=CIRCLE ( 'NONE', #45108, 0.1000000000000055844 ) ;
#128512=CARTESIAN_POINT ( 'NONE',  ( 20.94999999999999574, 2.902497314256400784, -208.4530536923346915 ) ) ;
#128543=CYLINDRICAL_SURFACE ( 'NONE', #116156, 0.09999999999999939493 ) ;
#128578=FACE_OUTER_BOUND ( 'NONE', #178462, .T. ) ;
#128585=EDGE_CURVE ( 'NONE', #66263, #71912, #149242, .T. ) ;
#128589=EDGE_LOOP ( 'NONE', ( #26491, #159968, #64087, #52010 ) ) ;
#128615=EDGE_CURVE ( 'NONE', #38916, #256420, #257309, .T. ) ;
#128620=ADVANCED_FACE ( 'NONE', ( #31743 ), #232499, .F. ) ;
#128649=EDGE_CURVE ( 'NONE', #173153, #122837, #145108, .T. ) ;
#128684=EDGE_CURVE ( 'NONE', #207244, #74308, #34462, .T. ) ;
#128714=ORIENTED_EDGE ( 'NONE', *, *, #81222, .F. ) ;
#128738=PLANE ( 'NONE',  #187683 ) ;
#128756=EDGE_CURVE ( 'NONE', #229898, #29396, #12320, .T. ) ;
#128829=CARTESIAN_POINT ( 'NONE',  ( 21.05000000000000071, -1.489567864901280680, -194.6304332222954372 ) ) ;
#128851=ORIENTED_EDGE ( 'NONE', *, *, #257192, .F. ) ;
#128856=LINE ( 'NONE', #105389, #65464 ) ;
#128859=CARTESIAN_POINT ( 'NONE',  ( 21.17356465864818915, -1.270133162812157934, -194.7032591620159678 ) ) ;
#128881=ORIENTED_EDGE ( 'NONE', *, *, #77576, .T. ) ;
#128909=DIRECTION ( 'NONE',  ( 0.000000000000000000, 0.2128009952263630322, -0.9770955615653309501 ) ) ;
#128923=AXIS2_PLACEMENT_3D ( 'NONE', #117279, #96404, #100244 ) ;
#128936=CARTESIAN_POINT ( 'NONE',  ( -21.51976009735018991, 6.752178271738374704, -199.5294475661460467 ) ) ;
#128937=ORIENTED_EDGE ( 'NONE', *, *, #219703, .F. ) ;
#128941=AXIS2_PLACEMENT_3D ( 'NONE', #161730, #45612, #130264 ) ;
#128948=DIRECTION ( 'NONE',  ( 0.000000000000000000, 0.2128009952263678062, -0.9770955615653298398 ) ) ;
#128957=CARTESIAN_POINT ( 'NONE',  ( 20.12500000000000000, 11.25287472715600146, -206.8511660127314826 ) ) ;
#128963=DIRECTION ( 'NONE',  ( 1.000000000000000000, -0.000000000000000000, -0.000000000000000000 ) ) ;
#128965=EDGE_LOOP ( 'NONE', ( #211408, #86514, #238164, #54363 ) ) ;
#129034=DIRECTION ( 'NONE',  ( 0.000000000000000000, -0.9770955615653312831, -0.2128009952263614224 ) ) ;
#129040=ORIENTED_EDGE ( 'NONE', *, *, #257192, .T. ) ;
#129066=CARTESIAN_POINT ( 'NONE',  ( -23.25000000000000000, -6.388372595096676321, -212.0629706944429813 ) ) ;
#129113=CARTESIAN_POINT ( 'NONE',  ( -20.94999999999999929, 4.193200906077805712, -212.0298262072164164 ) ) ;
#129170=CARTESIAN_POINT ( 'NONE',  ( -23.25000000000000000, 7.128833340094563376, -233.7327013124401276 ) ) ;
#129172=EDGE_CURVE ( 'NONE', #217539, #232829, #151532, .T. ) ;
#129191=DIRECTION ( 'NONE',  ( 1.000000000000000000, 0.000000000000000000, 0.000000000000000000 ) ) ;
#129198=CARTESIAN_POINT ( 'NONE',  ( 21.14999999999999858, -1.391858308744748696, -194.6091531227727955 ) ) ;
#129221=CARTESIAN_POINT ( 'NONE',  ( -18.59999999999999787, 0.5876173420563349792, -209.1618981382189588 ) ) ;
#129247=CARTESIAN_POINT ( 'NONE',  ( -21.00857864376268935, 12.80863705670245878, -205.3010250813005655 ) ) ;
#129264=CARTESIAN_POINT ( 'NONE',  ( 21.14999999999999858, 11.19216743630477673, -211.0996217964688810 ) ) ;
#129278=CARTESIAN_POINT ( 'NONE',  ( -23.15000000000000213, 13.96869538424788360, -210.3925794786332233 ) ) ;
#129288=ORIENTED_EDGE ( 'NONE', *, *, #47488, .F. ) ;
#129320=VERTEX_POINT ( 'NONE', #68768 ) ;
#129323=DIRECTION ( 'NONE',  ( -0.000000000000000000, -0.5795995782408138730, -0.8149014228132570592 ) ) ;
#129335=AXIS2_PLACEMENT_3D ( 'NONE', #120962, #204303, #25689 ) ;
#129338=DIRECTION ( 'NONE',  ( 0.000000000000000000, 0.2128009952263403282, -0.9770955615653358350 ) ) ;
#129340=ORIENTED_EDGE ( 'NONE', *, *, #220276, .T. ) ;
#129350=DIRECTION ( 'NONE',  ( 0.000000000000000000, -0.7489048840758955050, 0.6626775042260523163 ) ) ;
#129363=AXIS2_PLACEMENT_3D ( 'NONE', #81983, #161582, #241116 ) ;
#129378=CARTESIAN_POINT ( 'NONE',  ( 18.50596464788227280, 18.37039103902861470, -236.9176190769589141 ) ) ;
#129387=EDGE_CURVE ( 'NONE', #103375, #83472, #245279, .T. ) ;
#129390=EDGE_CURVE ( 'NONE', #233386, #139309, #33118, .T. ) ;
#129407=ORIENTED_EDGE ( 'NONE', *, *, #12959, .T. ) ;
#129451=ADVANCED_FACE ( 'NONE', ( #56862 ), #75207, .F. ) ;
#129467=CIRCLE ( 'NONE', #62820, 2.000000000000002220 ) ;
#129481=ORIENTED_EDGE ( 'NONE', *, *, #234994, .T. ) ;
#129482=ADVANCED_FACE ( 'NONE', ( #77725 ), #114304, .F. ) ;
#129483=AXIS2_PLACEMENT_3D ( 'NONE', #215155, #36557, #37832 ) ;
#129518=ORIENTED_EDGE ( 'NONE', *, *, #72193, .F. ) ;
#129549=VECTOR ( 'NONE', #90054, 1000.000000000000227 ) ;
#129562=AXIS2_PLACEMENT_3D ( 'NONE', #115369, #17541, #237886 ) ;
#129568=VECTOR ( 'NONE', #184872, 1000.000000000000227 ) ;
#129570=CARTESIAN_POINT ( 'NONE',  ( -21.40925344232282512, 6.484952525504856347, -199.4863767698734307 ) ) ;
#129634=ORIENTED_EDGE ( 'NONE', *, *, #210109, .F. ) ;
#129636=CIRCLE ( 'NONE', #217099, 0.1000000000000055844 ) ;
#129665=EDGE_CURVE ( 'NONE', #154024, #92185, #7556, .T. ) ;
#129674=VECTOR ( 'NONE', #52544, 1000.000000000000227 ) ;
#129697=ADVANCED_FACE ( 'NONE', ( #221097 ), #39933, .F. ) ;
#129699=CIRCLE ( 'NONE', #171435, 0.1000000000000033223 ) ;
#129701=DIRECTION ( 'NONE',  ( -1.000000000000000000, 0.000000000000000000, 0.000000000000000000 ) ) ;
#129728=ORIENTED_EDGE ( 'NONE', *, *, #84987, .F. ) ;
#129735=DIRECTION ( 'NONE',  ( 1.000000000000000000, 0.000000000000000000, 0.000000000000000000 ) ) ;
#129739=ORIENTED_EDGE ( 'NONE', *, *, #192442, .T. ) ;
#129767=DIRECTION ( 'NONE',  ( 1.000000000000000000, 0.000000000000000000, 0.000000000000000000 ) ) ;
#129772=EDGE_CURVE ( 'NONE', #83361, #205893, #116085, .T. ) ;
#129784=LINE ( 'NONE', #51503, #126130 ) ;
#129797=ORIENTED_EDGE ( 'NONE', *, *, #155847, .F. ) ;
#129801=ORIENTED_EDGE ( 'NONE', *, *, #65457, .T. ) ;
#129807=ORIENTED_EDGE ( 'NONE', *, *, #143591, .F. ) ;
#129825=DIRECTION ( 'NONE',  ( 0.000000000000000000, -0.9770955615653313941, -0.2128009952263606730 ) ) ;
#129829=FACE_OUTER_BOUND ( 'NONE', #199074, .T. ) ;
#129903=CARTESIAN_POINT ( 'NONE',  ( -22.50000000000000000, 11.36146383068193622, -198.4232501820394816 ) ) ;
#129906=CARTESIAN_POINT ( 'NONE',  ( 20.94999999999999574, 0.5663372425336981042, -209.0641885820623997 ) ) ;
#129923=VERTEX_POINT ( 'NONE', #232684 ) ;
#129973=DIRECTION ( 'NONE',  ( 1.000000000000000000, 0.000000000000000000, 0.000000000000000000 ) ) ;
#129981=CARTESIAN_POINT ( 'NONE',  ( -23.25000000000000000, 7.788796164756791818, -245.4641525896719543 ) ) ;
#130025=VECTOR ( 'NONE', #214062, 1000.000000000000227 ) ;
#130033=CARTESIAN_POINT ( 'NONE',  ( -22.39999999999999858, 11.36188319272496727, -198.4231588494578773 ) ) ;
#130044=ORIENTED_EDGE ( 'NONE', *, *, #159107, .T. ) ;
#130047=CIRCLE ( 'NONE', #142520, 0.1000000000000054040 ) ;
#130104=CARTESIAN_POINT ( 'NONE',  ( 20.85000000000000142, 7.783179459866048866, -245.3643104511423303 ) ) ;
#130111=ORIENTED_EDGE ( 'NONE', *, *, #132589, .F. ) ;
#130116=DIRECTION ( 'NONE',  ( -0.000000000000000000, 0.7397890806274345366, 0.6728388485992878865 ) ) ;
#130119=CARTESIAN_POINT ( 'NONE',  ( -18.59999999999999787, 1.148907358139439339E-11, -201.0000000000015064 ) ) ;
#130179=CARTESIAN_POINT ( 'NONE',  ( 21.04999999999999716, -1.384190162761350429, -194.8207525781398886 ) ) ;
#130211=DIRECTION ( 'NONE',  ( 0.000000000000000000, -0.2128009952264086346, 0.9770955615653210691 ) ) ;
#130256=CARTESIAN_POINT ( 'NONE',  ( 21.00000000000000000, 14.04870287383362992, -219.6884709798077893 ) ) ;
#130258=DIRECTION ( 'NONE',  ( 0.000000000000000000, 0.9525900758537746427, -0.3042567129660413983 ) ) ;
#130264=DIRECTION ( 'NONE',  ( 1.000000000000000000, 0.000000000000000000, 0.000000000000000000 ) ) ;
#130306=EDGE_LOOP ( 'NONE', ( #215060, #164230, #245871, #15677 ) ) ;
#130319=TOROIDAL_SURFACE ( 'NONE', #155313, 0.9750000000000019762, 0.1000000000000000056 ) ;
#130337=CARTESIAN_POINT ( 'NONE',  ( -18.46907102845854709, -0.7072367829275776341, -242.2718438362406062 ) ) ;
#130338=CIRCLE ( 'NONE', #17913, 0.2000000000000122791 ) ;
#130368=CARTESIAN_POINT ( 'NONE',  ( 21.05000000000000071, 1.148907358139439339E-11, -201.0000000000015064 ) ) ;
#130369=EDGE_CURVE ( 'NONE', #90944, #220406, #99256, .T. ) ;
#130376=EDGE_LOOP ( 'NONE', ( #158789, #141477, #199120, #126413 ) ) ;
#130394=EDGE_CURVE ( 'NONE', #49064, #241890, #228707, .T. ) ;
#130446=CIRCLE ( 'NONE', #18005, 11.80000000000001137 ) ;
#130467=CARTESIAN_POINT ( 'NONE',  ( -23.15000000000000213, 8.653397185701672711, -220.7611668973962367 ) ) ;
#130468=DIRECTION ( 'NONE',  ( 0.000000000000000000, -0.2128009952263603954, 0.9770955615653315052 ) ) ;
#130472=CARTESIAN_POINT ( 'NONE',  ( -20.94999999999999929, 4.158309866074138661, -211.9342015984041439 ) ) ;
#130489=DIRECTION ( 'NONE',  ( 0.000000000000000000, -0.2128009952263601456, 0.9770955615653316162 ) ) ;
#130492=DIRECTION ( 'NONE',  ( -0.000000000000000000, -0.9770955615653315052, -0.2128009952263603954 ) ) ;
#130498=CARTESIAN_POINT ( 'NONE',  ( -21.10320863425827298, -1.337536266937425555, -194.7409926129413122 ) ) ;
#130507=DIRECTION ( 'NONE',  ( -1.000000000000000000, -0.000000000000000000, -0.000000000000000000 ) ) ;
#130539=DIRECTION ( 'NONE',  ( 5.421010862427554711E-16, -0.9770955615653309501, -0.2128009952263636151 ) ) ;
#130569=CYLINDRICAL_SURFACE ( 'NONE', #101700, 0.1000000000000054040 ) ;
#130592=CARTESIAN_POINT ( 'NONE',  ( 19.97071067811864609, 16.69779891432240149, -222.5912266955230621 ) ) ;
#130636=EDGE_LOOP ( 'NONE', ( #96215, #84139, #239520, #181556 ) ) ;
#130640=AXIS2_PLACEMENT_3D ( 'NONE', #211744, #215569, #134735 ) ;
#130647=VERTEX_POINT ( 'NONE', #131676 ) ;
#130657=ORIENTED_EDGE ( 'NONE', *, *, #86631, .T. ) ;
#130685=VERTEX_POINT ( 'NONE', #173430 ) ;
#130697=EDGE_CURVE ( 'NONE', #195345, #184179, #174710, .T. ) ;
#130738=CARTESIAN_POINT ( 'NONE',  ( 22.39999999999999858, 7.591056067193225232, -199.2444047917219052 ) ) ;
#130743=DIRECTION ( 'NONE',  ( 1.000000000000000000, 0.000000000000000000, 0.000000000000000000 ) ) ;
#130761=CIRCLE ( 'NONE', #93156, 0.1000000000000069167 ) ;
#130765=DIRECTION ( 'NONE',  ( 1.000000000000000000, 0.000000000000000000, 0.000000000000000000 ) ) ;
#130799=DIRECTION ( 'NONE',  ( -1.000000000000000000, 0.000000000000000000, 0.000000000000000000 ) ) ;
#130814=CARTESIAN_POINT ( 'NONE',  ( 20.94999999999999929, 7.128833340094563376, -233.7327013124401276 ) ) ;
#130860=CARTESIAN_POINT ( 'NONE',  ( -23.25000000000000000, -10.82118976317943826, -206.5294079347637819 ) ) ;
#130881=ORIENTED_EDGE ( 'NONE', *, *, #61959, .T. ) ;
#130883=AXIS2_PLACEMENT_3D ( 'NONE', #77712, #72621, #153472 ) ;
#130973=DIRECTION ( 'NONE',  ( 0.000000000000000000, 0.1678971852675816834, 0.9858045116447902156 ) ) ;
#130987=EDGE_CURVE ( 'NONE', #248593, #10221, #91904, .T. ) ;
#130989=CIRCLE ( 'NONE', #222546, 0.1000000000000055844 ) ;
#130994=CARTESIAN_POINT ( 'NONE',  ( -20.64999999999999858, 9.593045456726526865, -211.4478935133083439 ) ) ;
#131004=CARTESIAN_POINT ( 'NONE',  ( 20.94999999999999574, 7.939498413483247141, -209.7295111514051200 ) ) ;
#131016=DIRECTION ( 'NONE',  ( 0.000000000000000000, 0.06430067914209719460, -0.9979305700607958851 ) ) ;
#131048=AXIS2_PLACEMENT_3D ( 'NONE', #99723, #137572, #81442 ) ;
#131061=ORIENTED_EDGE ( 'NONE', *, *, #632, .F. ) ;
#131072=FACE_OUTER_BOUND ( 'NONE', #234462, .T. ) ;
#131100=CIRCLE ( 'NONE', #18675, 11.90000000000000213 ) ;
#131119=DIRECTION ( 'NONE',  ( 0.000000000000000000, 0.9770955615653313941, 0.2128009952263603677 ) ) ;
#131125=DIRECTION ( 'NONE',  ( -0.000000000000000000, -0.9770955615653316162, -0.2128009952263604232 ) ) ;
#131160=FACE_OUTER_BOUND ( 'NONE', #1394, .T. ) ;
#131173=CARTESIAN_POINT ( 'NONE',  ( 21.05000000000000782, 11.25362009860280921, -210.9838939269090474 ) ) ;
#131198=ORIENTED_EDGE ( 'NONE', *, *, #245112, .F. ) ;
#131211=EDGE_CURVE ( 'NONE', #141892, #162009, #63044, .T. ) ;
#131216=DIRECTION ( 'NONE',  ( 0.000000000000000000, -0.9770955615653313941, -0.2128009952263603677 ) ) ;
#131226=EDGE_LOOP ( 'NONE', ( #67448, #114197, #248197, #153675 ) ) ;
#131271=ORIENTED_EDGE ( 'NONE', *, *, #165739, .F. ) ;
#131299=AXIS2_PLACEMENT_3D ( 'NONE', #167532, #163658, #85361 ) ;
#131328=ORIENTED_EDGE ( 'NONE', *, *, #226265, .T. ) ;
#131362=CYLINDRICAL_SURFACE ( 'NONE', #114192, 0.09999999999999939493 ) ;
#131366=ADVANCED_FACE ( 'NONE', ( #48623 ), #12101, .F. ) ;
#131382=DIRECTION ( 'NONE',  ( 0.000000000000000000, -0.2128009952263605065, 0.9770955615653315052 ) ) ;
#131400=VERTEX_POINT ( 'NONE', #156753 ) ;
#131405=DIRECTION ( 'NONE',  ( 0.000000000000000000, 0.2128009952263604787, -0.9770955615653315052 ) ) ;
#131406=CYLINDRICAL_SURFACE ( 'NONE', #142501, 0.1000000000000055844 ) ;
#131424=EDGE_CURVE ( 'NONE', #1104, #124170, #52462, .T. ) ;
#131461=VERTEX_POINT ( 'NONE', #13366 ) ;
#131511=AXIS2_PLACEMENT_3D ( 'NONE', #257736, #202628, #4420 ) ;
#131512=FACE_OUTER_BOUND ( 'NONE', #141626, .T. ) ;
#131515=CARTESIAN_POINT ( 'NONE',  ( 18.52326479938708914, -0.8637711017511672251, -242.3455657282801781 ) ) ;
#131544=EDGE_LOOP ( 'NONE', ( #117750, #213066, #38014, #8433 ) ) ;
#131554=DIRECTION ( 'NONE',  ( 0.000000000000000000, 0.9394191166662618775, 0.3427706569150580362 ) ) ;
#131562=CIRCLE ( 'NONE', #19126, 0.09999999999999130418 ) ;
#131566=DIRECTION ( 'NONE',  ( 0.000000000000000000, -0.9770955615653316162, -0.2128009952263604232 ) ) ;
#131572=DIRECTION ( 'NONE',  ( 1.000000000000000000, 0.000000000000000000, 0.000000000000000000 ) ) ;
#131574=EDGE_LOOP ( 'NONE', ( #1137, #40497, #87773, #29699 ) ) ;
#131593=VECTOR ( 'NONE', #164353, 1000.000000000000000 ) ;
#131619=CIRCLE ( 'NONE', #123243, 0.09999999999999939493 ) ;
#131660=DIRECTION ( 'NONE',  ( 0.000000000000000000, -0.9797463026583741463, -0.2002428086779789451 ) ) ;
#131676=CARTESIAN_POINT ( 'NONE',  ( -23.25000000000000000, 5.354661166737471056, -213.3684367965233832 ) ) ;
#131677=CARTESIAN_POINT ( 'NONE',  ( -21.05000000000000071, 0.5876173420563349792, -209.1618981382189588 ) ) ;
#131684=AXIS2_PLACEMENT_3D ( 'NONE', #3610, #6173, #83112 ) ;
#131766=CIRCLE ( 'NONE', #177598, 0.09999999999999939493 ) ;
#131778=DIRECTION ( 'NONE',  ( 0.000000000000000000, 0.2128009952263585081, -0.9770955615653320603 ) ) ;
#131781=FACE_OUTER_BOUND ( 'NONE', #184110, .T. ) ;
#131794=CARTESIAN_POINT ( 'NONE',  ( -18.50000000000000000, 4.324939842317335525, -212.0862480289983409 ) ) ;
#131798=CARTESIAN_POINT ( 'NONE',  ( 21.14999999999999858, 6.390846877240206503, -199.6081416912452653 ) ) ;
#131825=ORIENTED_EDGE ( 'NONE', *, *, #116472, .F. ) ;
#131865=EDGE_CURVE ( 'NONE', #212805, #63849, #29533, .T. ) ;
#131871=DIRECTION ( 'NONE',  ( 1.000000000000000000, 0.000000000000000000, 0.000000000000000000 ) ) ;
#131886=CARTESIAN_POINT ( 'NONE',  ( 18.49999999999999289, 15.53922597307774822, -223.0482397989536310 ) ) ;
#131891=AXIS2_PLACEMENT_3D ( 'NONE', #204579, #66366, #5069 ) ;
#131913=ORIENTED_EDGE ( 'NONE', *, *, #75022, .T. ) ;
#131919=CARTESIAN_POINT ( 'NONE',  ( 21.14999999999999858, 11.21344753582741127, -211.1973313526253833 ) ) ;
#131945=DIRECTION ( 'NONE',  ( 1.000000000000000000, 0.000000000000000000, 0.000000000000000000 ) ) ;
#131951=VERTEX_POINT ( 'NONE', #100269 ) ;
#131956=DIRECTION ( 'NONE',  ( 0.000000000000000000, 0.2128009952263602289, -0.9770955615653316162 ) ) ;
#131972=AXIS2_PLACEMENT_3D ( 'NONE', #60843, #98655, #62148 ) ;
#131973=DIRECTION ( 'NONE',  ( 1.000000000000000000, 0.000000000000000000, 0.000000000000000000 ) ) ;
#131995=VECTOR ( 'NONE', #115183, 1000.000000000000000 ) ;
#132024=EDGE_CURVE ( 'NONE', #633, #70740, #207110, .T. ) ;
#132045=SHAPE_REPRESENTATION_RELATIONSHIP ( 'NONE' , 'NONE' ,  #53611, #241103 ) ;
#132052=EDGE_CURVE ( 'NONE', #17019, #192537, #244936, .T. ) ;
#132081=DIRECTION ( 'NONE',  ( -1.000000000000000000, 0.000000000000000000, 0.000000000000000000 ) ) ;
#132085=CARTESIAN_POINT ( 'NONE',  ( 20.95289811251229750, 10.49866850695357989, -207.4146053197192998 ) ) ;
#132094=AXIS2_PLACEMENT_3D ( 'NONE', #39549, #74827, #78621 ) ;
#132105=CARTESIAN_POINT ( 'NONE',  ( -18.54270223418607699, -0.8403597433258389593, -242.3672582601704164 ) ) ;
#132107=EDGE_CURVE ( 'NONE', #175179, #173016, #125386, .T. ) ;
#132116=DIRECTION ( 'NONE',  ( -0.000000000000000000, -0.9770955615653310611, -0.2128009952263620608 ) ) ;
#132202=EDGE_CURVE ( 'NONE', #148979, #206404, #129636, .T. ) ;
#132220=VERTEX_POINT ( 'NONE', #150530 ) ;
#132221=AXIS2_PLACEMENT_3D ( 'NONE', #185483, #207632, #70700 ) ;
#132223=ORIENTED_EDGE ( 'NONE', *, *, #24345, .F. ) ;
#132241=VERTEX_POINT ( 'NONE', #90532 ) ;
#132291=ORIENTED_EDGE ( 'NONE', *, *, #234994, .F. ) ;
#132302=EDGE_LOOP ( 'NONE', ( #232830, #182642, #52058, #190209 ) ) ;
#132314=ORIENTED_EDGE ( 'NONE', *, *, #42884, .T. ) ;
#132318=DIRECTION ( 'NONE',  ( 0.000000000000000000, -0.2128009952263485993, 0.9770955615653341697 ) ) ;
#132329=CIRCLE ( 'NONE', #28320, 0.1000000000000055844 ) ;
#132334=LINE ( 'NONE', #216689, #156114 ) ;
#132355=DIRECTION ( 'NONE',  ( 0.000000000000000000, -0.9964539953858966292, -0.08413937888696096379 ) ) ;
#132358=DIRECTION ( 'NONE',  ( -1.000000000000000000, 0.000000000000000000, 0.000000000000000000 ) ) ;
#132366=DIRECTION ( 'NONE',  ( 0.000000000000000000, -0.2128009952263613669, 0.9770955615653312831 ) ) ;
#132391=EDGE_CURVE ( 'NONE', #232370, #90864, #50514, .T. ) ;
#132414=AXIS2_PLACEMENT_3D ( 'NONE', #132584, #238082, #36057 ) ;
#132476=CIRCLE ( 'NONE', #20068, 0.09999999999999939493 ) ;
#132553=DIRECTION ( 'NONE',  ( 0.000000000000000000, 0.9770955615653313941, 0.2128009952263606452 ) ) ;
#132576=TOROIDAL_SURFACE ( 'NONE', #74166, 0.4000000000000012990, 0.1000000000000000056 ) ;
#132584=CARTESIAN_POINT ( 'NONE',  ( -20.54999999999999716, 7.128833340094563376, -233.7327013124401276 ) ) ;
#132589=EDGE_CURVE ( 'NONE', #141892, #126094, #254643, .T. ) ;
#132592=ORIENTED_EDGE ( 'NONE', *, *, #237275, .F. ) ;
#132593=ORIENTED_EDGE ( 'NONE', *, *, #257364, .F. ) ;
#132599=DIRECTION ( 'NONE',  ( 0.000000000000000000, -0.2128009952263604510, 0.9770955615653315052 ) ) ;
#132621=ORIENTED_EDGE ( 'NONE', *, *, #84103, .T. ) ;
#132643=EDGE_CURVE ( 'NONE', #220753, #208402, #204825, .T. ) ;
#132650=CARTESIAN_POINT ( 'NONE',  ( 18.59999999999996945, 18.41524492703432614, -237.0006385043383546 ) ) ;
#132657=DIRECTION ( 'NONE',  ( 1.000000000000000000, 0.000000000000000000, 0.000000000000000000 ) ) ;
#132687=EDGE_CURVE ( 'NONE', #235411, #112587, #84993, .T. ) ;
#132689=EDGE_CURVE ( 'NONE', #209650, #5593, #154795, .T. ) ;
#132698=EDGE_CURVE ( 'NONE', #154024, #24047, #208932, .T. ) ;
#132699=CARTESIAN_POINT ( 'NONE',  ( 20.93975676684922504, 18.37846419038447010, -236.9325101954432853 ) ) ;
#132726=EDGE_CURVE ( 'NONE', #55232, #162084, #108961, .T. ) ;
#132729=CARTESIAN_POINT ( 'NONE',  ( 20.94999999999999929, 8.985508020264692419, -211.4778645542876347 ) ) ;
#132733=DIRECTION ( 'NONE',  ( 0.000000000000000000, 0.9316174814283056937, 0.3634403228828368970 ) ) ;
#132815=DIRECTION ( 'NONE',  ( 0.000000000000000000, 0.2128009952263602844, -0.9770955615653315052 ) ) ;
#132821=DIRECTION ( 'NONE',  ( -0.000000000000000000, 0.07893460099012301889, -0.9968797965484754720 ) ) ;
#132865=CARTESIAN_POINT ( 'NONE',  ( -23.15000000000000213, -6.438379425586759908, -212.1495692908769684 ) ) ;
#132883=CIRCLE ( 'NONE', #53757, 0.1000000000000055844 ) ;
#132912=ADVANCED_FACE ( 'NONE', ( #97828 ), #171729, .T. ) ;
#132922=AXIS2_PLACEMENT_3D ( 'NONE', #166682, #164088, #25870 ) ;
#132945=ORIENTED_EDGE ( 'NONE', *, *, #174829, .T. ) ;
#132982=CARTESIAN_POINT ( 'NONE',  ( -21.07928932188134397, -1.250084634896337921, -194.7953894783290423 ) ) ;
#133012=ADVANCED_FACE ( 'NONE', ( #63871 ), #185102, .T. ) ;
#133015=DIRECTION ( 'NONE',  ( -0.000000000000000000, 0.9770955615653313941, 0.2128009952263603954 ) ) ;
#133093=AXIS2_PLACEMENT_3D ( 'NONE', #107010, #86146, #250388 ) ;
#133106=AXIS2_PLACEMENT_3D ( 'NONE', #180925, #2260, #55799 ) ;
#133109=VECTOR ( 'NONE', #17810, 1000.000000000000000 ) ;
#133123=ORIENTED_EDGE ( 'NONE', *, *, #240391, .T. ) ;
#133124=DIRECTION ( 'NONE',  ( -0.000000000000000000, -0.3427706569149662763, 0.9394191166662954062 ) ) ;
#133143=DIRECTION ( 'NONE',  ( 1.000000000000000000, 2.885090398161910739E-16, 6.283419270304611573E-17 ) ) ;
#133159=ORIENTED_EDGE ( 'NONE', *, *, #214338, .T. ) ;
#133211=DIRECTION ( 'NONE',  ( -2.915501640297154283E-16, 0.9770955615653317272, 0.2128009952263596460 ) ) ;
#133219=ORIENTED_EDGE ( 'NONE', *, *, #220810, .F. ) ;
#133228=ADVANCED_FACE ( 'NONE', ( #212381 ), #72889, .T. ) ;
#133259=CIRCLE ( 'NONE', #112423, 0.1000000000000054040 ) ;
#133275=ADVANCED_FACE ( 'NONE', ( #28650 ), #192811, .T. ) ;
#133292=ORIENTED_EDGE ( 'NONE', *, *, #8430, .T. ) ;
#133296=DIRECTION ( 'NONE',  ( 7.304098846218135653E-16, -0.9770955615653315052, -0.2128009952263603954 ) ) ;
#133317=SPHERICAL_SURFACE ( 'NONE', #44408, 0.1000000000000000056 ) ;
#133337=( LENGTH_UNIT ( ) NAMED_UNIT ( * ) SI_UNIT ( .MILLI., .METRE. ) );
#133364=AXIS2_PLACEMENT_3D ( 'NONE', #27382, #243812, #65170 ) ;
#133369=CYLINDRICAL_SURFACE ( 'NONE', #115893, 0.09999999999999939493 ) ;
#133370=EDGE_CURVE ( 'NONE', #286, #30493, #246703, .T. ) ;
#133377=DIRECTION ( 'NONE',  ( 0.000000000000000000, 0.9770955615653551529, 0.2128009952262517601 ) ) ;
#133412=EDGE_LOOP ( 'NONE', ( #181122, #801, #63210, #235764 ) ) ;
#133428=ORIENTED_EDGE ( 'NONE', *, *, #55774, .T. ) ;
#133436=ORIENTED_EDGE ( 'NONE', *, *, #16199, .F. ) ;
#133446=CARTESIAN_POINT ( 'NONE',  ( -20.94403535211772294, 18.37039103902859694, -236.9176190769588857 ) ) ;
#133456=ADVANCED_FACE ( 'NONE', ( #140507 ), #123534, .T. ) ;
#133488=EDGE_CURVE ( 'NONE', #246033, #217539, #184777, .T. ) ;
#133494=FACE_OUTER_BOUND ( 'NONE', #13066, .T. ) ;
#133498=ORIENTED_EDGE ( 'NONE', *, *, #100459, .F. ) ;
#133514=DIRECTION ( 'NONE',  ( 1.000000000000000000, 0.000000000000000000, 0.000000000000000000 ) ) ;
#133525=CARTESIAN_POINT ( 'NONE',  ( 20.94999999999999929, -7.176961358819842651, -212.6889627706600834 ) ) ;
#133531=EDGE_CURVE ( 'NONE', #9423, #98837, #163508, .T. ) ;
#133538=CARTESIAN_POINT ( 'NONE',  ( -18.40000000000000213, -7.817436562502988906, -209.8389866834999111 ) ) ;
#133584=DIRECTION ( 'NONE',  ( 1.000000000000000000, 0.000000000000000000, 0.000000000000000000 ) ) ;
#133623=ORIENTED_EDGE ( 'NONE', *, *, #192373, .T. ) ;
#133664=DIRECTION ( 'NONE',  ( -1.000000000000000000, 0.000000000000000000, 0.000000000000000000 ) ) ;
#133719=VERTEX_POINT ( 'NONE', #252445 ) ;
#133724=FACE_OUTER_BOUND ( 'NONE', #126580, .T. ) ;
#133732=FACE_OUTER_BOUND ( 'NONE', #174675, .T. ) ;
#133766=FACE_OUTER_BOUND ( 'NONE', #136112, .T. ) ;
#133774=VECTOR ( 'NONE', #32167, 1000.000000000000227 ) ;
#133783=CARTESIAN_POINT ( 'NONE',  ( 21.05000000000000071, 6.093673009692411213, -199.5727803633481301 ) ) ;
#133789=DIRECTION ( 'NONE',  ( -0.7071067811865474617, -0.6909108974501236844, -0.1504730267678055788 ) ) ;
#133802=DIRECTION ( 'NONE',  ( 0.000000000000000000, 0.2128009952263603677, -0.9770955615653315052 ) ) ;
#133814=EDGE_LOOP ( 'NONE', ( #163274, #231514, #16847 ) ) ;
#133824=EDGE_CURVE ( 'NONE', #22410, #17786, #209474, .T. ) ;
#133837=EDGE_CURVE ( 'NONE', #17786, #183689, #81490, .T. ) ;
#133854=ADVANCED_FACE ( 'NONE', ( #227129 ), #80204, .T. ) ;
#133858=ADVANCED_FACE ( 'NONE', ( #68067 ), #217835, .F. ) ;
#133889=CIRCLE ( 'NONE', #108948, 0.5999999999999987566 ) ;
#133891=EDGE_LOOP ( 'NONE', ( #39291, #124251, #36676, #184642 ) ) ;
#133925=ORIENTED_EDGE ( 'NONE', *, *, #108673, .T. ) ;
#133942=AXIS2_PLACEMENT_3D ( 'NONE', #182016, #109793, #32881 ) ;
#133959=CIRCLE ( 'NONE', #46460, 0.1000000000000133560 ) ;
#133979=AXIS2_PLACEMENT_3D ( 'NONE', #38860, #120977, #200489 ) ;
#134020=CARTESIAN_POINT ( 'NONE',  ( -20.97625342178429975, 12.80863705740234693, -205.3010250806640329 ) ) ;
#134037=DIRECTION ( 'NONE',  ( 0.000000000000000000, 0.2128009952263485993, -0.9770955615653341697 ) ) ;
#134041=ORIENTED_EDGE ( 'NONE', *, *, #178943, .T. ) ;
#134053=AXIS2_PLACEMENT_3D ( 'NONE', #74377, #116050, #174772 ) ;
#134055=TOROIDAL_SURFACE ( 'NONE', #171514, 7.800000000000000711, 0.1000000000000000056 ) ;
#134076=DIRECTION ( 'NONE',  ( -0.000000000000000000, 0.9770955615653316162, 0.2128009952263604232 ) ) ;
#134090=AXIS2_PLACEMENT_3D ( 'NONE', #240495, #46139, #121844 ) ;
#134110=CARTESIAN_POINT ( 'NONE',  ( 18.59999999999999076, 7.675662554762638479, -241.7139905447625381 ) ) ;
#134180=ORIENTED_EDGE ( 'NONE', *, *, #187735, .T. ) ;
#134181=ORIENTED_EDGE ( 'NONE', *, *, #185522, .T. ) ;
#134202=DIRECTION ( 'NONE',  ( -1.000000000000000000, 0.000000000000000000, -0.000000000000000000 ) ) ;
#134204=CARTESIAN_POINT ( 'NONE',  ( 21.30000000000002558, 1.148907358139439339E-11, -201.0000000000015064 ) ) ;
#134219=CARTESIAN_POINT ( 'NONE',  ( -18.59999999999999787, 18.51199663233067483, -231.2535697180530292 ) ) ;
#134223=DIRECTION ( 'NONE',  ( 1.000000000000000000, 0.000000000000000000, 0.000000000000000000 ) ) ;
#134227=CARTESIAN_POINT ( 'NONE',  ( 18.50000000000000000, -7.785976468740638090, -209.8926132507865816 ) ) ;
#134232=CARTESIAN_POINT ( 'NONE',  ( -21.05000000000000071, -1.300857950936794571, -194.8777500463866659 ) ) ;
#134242=EDGE_LOOP ( 'NONE', ( #185466, #185808, #243710, #56881 ) ) ;
#134249=EDGE_LOOP ( 'NONE', ( #68895, #38348, #62952, #96531 ) ) ;
#134251=ORIENTED_EDGE ( 'NONE', *, *, #182471, .F. ) ;
#134279=CYLINDRICAL_SURFACE ( 'NONE', #103766, 0.1000000000000001305 ) ;
#134303=AXIS2_PLACEMENT_3D ( 'NONE', #67172, #107568, #149299 ) ;
#134330=CIRCLE ( 'NONE', #50935, 0.09999999999999939493 ) ;
#134384=EDGE_CURVE ( 'NONE', #126771, #176941, #171713, .T. ) ;
#134386=CARTESIAN_POINT ( 'NONE',  ( -23.15000000000000213, 1.148907358139439339E-11, -201.0000000000015064 ) ) ;
#134411=ORIENTED_EDGE ( 'NONE', *, *, #53113, .T. ) ;
#134433=ORIENTED_EDGE ( 'NONE', *, *, #165233, .T. ) ;
#134434=CARTESIAN_POINT ( 'NONE',  ( 20.95052659398289308, 11.85180822207893669, -206.1716151108944644 ) ) ;
#134438=EDGE_CURVE ( 'NONE', #7468, #247780, #71929, .T. ) ;
#134485=EDGE_CURVE ( 'NONE', #102962, #148888, #26132, .T. ) ;
#134488=CARTESIAN_POINT ( 'NONE',  ( 18.51024323315077069, 18.37846419038448431, -236.9325101954433137 ) ) ;
#134517=VECTOR ( 'NONE', #123237, 1000.000000000000114 ) ;
#134541=EDGE_LOOP ( 'NONE', ( #200621, #211275, #83483, #168685 ) ) ;
#134554=ORIENTED_EDGE ( 'NONE', *, *, #20944, .T. ) ;
#134573=CARTESIAN_POINT ( 'NONE',  ( 23.25000000000000000, -11.88052908492543480, -191.5620167057819287 ) ) ;
#134594=CARTESIAN_POINT ( 'NONE',  ( 18.52130828395272033, -7.769407441232962341, -209.8812647411876071 ) ) ;
#134625=CIRCLE ( 'NONE', #26339, 11.80000000000000959 ) ;
#134636=EDGE_CURVE ( 'NONE', #65554, #187942, #88450, .T. ) ;
#134641=FACE_OUTER_BOUND ( 'NONE', #158270, .T. ) ;
#134651=DIRECTION ( 'NONE',  ( 1.000000000000000000, 2.885090398161910739E-16, 6.283419270304611573E-17 ) ) ;
#134694=EDGE_CURVE ( 'NONE', #71034, #53701, #38587, .T. ) ;
#134704=VERTEX_POINT ( 'NONE', #85686 ) ;
#134735=DIRECTION ( 'NONE',  ( 1.000000000000000000, 0.000000000000000000, 0.000000000000000000 ) ) ;
#134763=EDGE_LOOP ( 'NONE', ( #195563, #221757, #164714, #252753 ) ) ;
#134794=ORIENTED_EDGE ( 'NONE', *, *, #15980, .F. ) ;
#134810=CYLINDRICAL_SURFACE ( 'NONE', #243999, 0.1000000000000055705 ) ;
#134849=DIRECTION ( 'NONE',  ( 0.000000000000000000, -0.2128009952263645033, 0.9770955615653306170 ) ) ;
#134855=TOROIDAL_SURFACE ( 'NONE', #22497, 0.2000000000000000111, 0.1000000000000000056 ) ;
#134861=CARTESIAN_POINT ( 'NONE',  ( -22.50000000000000000, 11.48087284840413425, -198.4995883060917947 ) ) ;
#134879=PLANE ( 'NONE',  #152719 ) ;
#134884=EDGE_CURVE ( 'NONE', #115886, #227071, #155340, .T. ) ;
#134916=CARTESIAN_POINT ( 'NONE',  ( -18.46154800491008174, -0.7175219691130436672, -242.2550643080716668 ) ) ;
#134928=AXIS2_PLACEMENT_3D ( 'NONE', #209973, #189116, #67876 ) ;
#134941=CARTESIAN_POINT ( 'NONE',  ( -18.59999999999999787, 2.859758780633683273, -208.6670499591424459 ) ) ;
#134959=AXIS2_PLACEMENT_3D ( 'NONE', #155556, #255853, #56399 ) ;
#134974=ORIENTED_EDGE ( 'NONE', *, *, #225914, .F. ) ;
#134975=DIRECTION ( 'NONE',  ( 0.000000000000000000, 0.2128009952263485993, -0.9770955615653341697 ) ) ;
#134985=EDGE_CURVE ( 'NONE', #6661, #286, #153454, .T. ) ;
#135009=ADVANCED_FACE ( 'NONE', ( #197651 ), #137723, .F. ) ;
#135016=ORIENTED_EDGE ( 'NONE', *, *, #216881, .F. ) ;
#135018=CARTESIAN_POINT ( 'NONE',  ( -23.15000000000000213, 1.148907358139439339E-11, -201.0000000000015064 ) ) ;
#135022=CARTESIAN_POINT ( 'NONE',  ( -20.85000000000000142, 14.70949956575304185, -235.9560995168023112 ) ) ;
#135033=PLANE ( 'NONE',  #44441 ) ;
#135046=DIRECTION ( 'NONE',  ( -1.000000000000000000, 0.000000000000000000, 0.000000000000000000 ) ) ;
#135106=VECTOR ( 'NONE', #100071, 1000.000000000000000 ) ;
#135125=AXIS2_PLACEMENT_3D ( 'NONE', #199406, #40354, #119872 ) ;
#135145=VERTEX_POINT ( 'NONE', #50135 ) ;
#135157=CIRCLE ( 'NONE', #168557, 0.1000000000000054040 ) ;
#135160=DIRECTION ( 'NONE',  ( 0.000000000000000000, 0.000000000000000000, 1.000000000000000000 ) ) ;
#135258=ADVANCED_FACE ( 'NONE', ( #136074 ), #55477, .T. ) ;
#135281=DIRECTION ( 'NONE',  ( 0.000000000000000000, 0.2128009952263485993, -0.9770955615653340587 ) ) ;
#135305=DIRECTION ( 'NONE',  ( 0.000000000000000000, 0.9968797965484670343, 0.07893460099023182075 ) ) ;
#135312=PLANE ( 'NONE',  #103047 ) ;
#135336=DIRECTION ( 'NONE',  ( 0.000000000000000000, 0.2128009952263604232, -0.9770955615653316162 ) ) ;
#135343=DIRECTION ( 'NONE',  ( 1.000000000000000000, 0.000000000000000000, 0.000000000000000000 ) ) ;
#135363=FACE_OUTER_BOUND ( 'NONE', #78585, .T. ) ;
#135405=AXIS2_PLACEMENT_3D ( 'NONE', #144539, #63729, #168010 ) ;
#135412=ORIENTED_EDGE ( 'NONE', *, *, #124882, .F. ) ;
#135441=CIRCLE ( 'NONE', #81261, 0.1000000000000057648 ) ;
#135499=DIRECTION ( 'NONE',  ( 0.000000000000000000, 0.2128009952263604232, -0.9770955615653316162 ) ) ;
#135507=CARTESIAN_POINT ( 'NONE',  ( 18.59999999999999432, 0.5663372425336981042, -209.0641885820623997 ) ) ;
#135521=ORIENTED_EDGE ( 'NONE', *, *, #34603, .F. ) ;
#135525=CARTESIAN_POINT ( 'NONE',  ( -21.05000000000000071, -1.489567864901279792, -194.6304332222954372 ) ) ;
#135527=EDGE_CURVE ( 'NONE', #173624, #38916, #228496, .T. ) ;
#135543=CARTESIAN_POINT ( 'NONE',  ( 23.14999999999999858, 5.076932660807364606, -234.1795834024154885 ) ) ;
#135562=LINE ( 'NONE', #239827, #183206 ) ;
#135568=ORIENTED_EDGE ( 'NONE', *, *, #119760, .T. ) ;
#135584=EDGE_CURVE ( 'NONE', #229705, #64043, #89009, .T. ) ;
#135605=DIRECTION ( 'NONE',  ( 0.000000000000000000, -0.2128009952267955196, 0.9770955615652368031 ) ) ;
#135661=DIRECTION ( 'NONE',  ( 0.000000000000000000, 0.9394191166662618775, 0.3427706569150580362 ) ) ;
#135690=CARTESIAN_POINT ( 'NONE',  ( 20.02499999999999858, 14.02742277431099538, -219.5907614236512870 ) ) ;
#135756=VERTEX_POINT ( 'NONE', #183592 ) ;
#135817=DIRECTION ( 'NONE',  ( 0.000000000000000000, -0.2128009952263601456, 0.9770955615653316162 ) ) ;
#135867=ORIENTED_EDGE ( 'NONE', *, *, #127372, .T. ) ;
#135872=DIRECTION ( 'NONE',  ( 1.000000000000000000, 0.000000000000000000, 0.000000000000000000 ) ) ;
#135899=ORIENTED_EDGE ( 'NONE', *, *, #87112, .F. ) ;
#135908=DIRECTION ( 'NONE',  ( 1.000000000000000000, 0.000000000000000000, 0.000000000000000000 ) ) ;
#135942=VERTEX_POINT ( 'NONE', #103583 ) ;
#135948=AXIS2_PLACEMENT_3D ( 'NONE', #42747, #124856, #45315 ) ;
#135955=ORIENTED_EDGE ( 'NONE', *, *, #226370, .T. ) ;
#135962=CARTESIAN_POINT ( 'NONE',  ( -21.53551880898957549, -1.347108827648217044, -194.3495433631890705 ) ) ;
#135965=DIRECTION ( 'NONE',  ( 0.000000000000000000, -0.9394191166662962944, -0.3427706569149635563 ) ) ;
#135987=AXIS2_PLACEMENT_3D ( 'NONE', #59194, #149071, #5654 ) ;
#136007=DIRECTION ( 'NONE',  ( -0.000000000000000000, -0.9770955615653313941, -0.2128009952263606730 ) ) ;
#136050=EDGE_CURVE ( 'NONE', #21586, #237840, #205907, .T. ) ;
#136051=ORIENTED_EDGE ( 'NONE', *, *, #107843, .F. ) ;
#136055=AXIS2_PLACEMENT_3D ( 'NONE', #16150, #235172, #14860 ) ;
#136074=FACE_OUTER_BOUND ( 'NONE', #20743, .T. ) ;
#136112=EDGE_LOOP ( 'NONE', ( #33501, #227256, #71441, #228191 ) ) ;
#136115=ORIENTED_EDGE ( 'NONE', *, *, #38007, .F. ) ;
#136127=ORIENTED_EDGE ( 'NONE', *, *, #98211, .F. ) ;
#136149=AXIS2_PLACEMENT_3D ( 'NONE', #167342, #169933, #108624 ) ;
#136176=CARTESIAN_POINT ( 'NONE',  ( 23.14999999999999858, 7.128833340094563376, -233.7327013124401276 ) ) ;
#136215=AXIS2_PLACEMENT_3D ( 'NONE', #41557, #78077, #101451 ) ;
#136226=CARTESIAN_POINT ( 'NONE',  ( -21.14999999999999858, 6.412126976762837494, -199.7058512474018244 ) ) ;
#136233=ADVANCED_FACE ( 'NONE', ( #242451 ), #235148, .F. ) ;
#136243=DIRECTION ( 'NONE',  ( 0.000000000000000000, -0.2128009952264117433, 0.9770955615653204029 ) ) ;
#136275=CARTESIAN_POINT ( 'NONE',  ( -21.05000000000000071, 8.001317420522642720, -237.7387931148579980 ) ) ;
#136292=EDGE_CURVE ( 'NONE', #80924, #88973, #17921, .T. ) ;
#136309=CARTESIAN_POINT ( 'NONE',  ( 20.02499999999999858, 14.04870287383362992, -219.6884709798078177 ) ) ;
#136327=ADVANCED_FACE ( 'NONE', ( #187653, #186360 ), #7721, .T. ) ;
#136330=VERTEX_POINT ( 'NONE', #48111 ) ;
#136334=CARTESIAN_POINT ( 'NONE',  ( -21.07094088545368038, -1.248309276978958104, -194.8035479807908530 ) ) ;
#136344=AXIS2_PLACEMENT_3D ( 'NONE', #238668, #39210, #3912 ) ;
#136367=EDGE_LOOP ( 'NONE', ( #52407, #98403, #244655, #42385 ) ) ;
#136369=VERTEX_POINT ( 'NONE', #153696 ) ;
#136381=CARTESIAN_POINT ( 'NONE',  ( 20.94999999999999929, 0.5450571430110628945, -208.9664790259058691 ) ) ;
#136386=DIRECTION ( 'NONE',  ( -1.000000000000000000, 0.000000000000000000, 0.000000000000000000 ) ) ;
#136409=CARTESIAN_POINT ( 'NONE',  ( 21.14999999999999858, -1.236118717437887371, -194.8647072476926212 ) ) ;
#136427=AXIS2_PLACEMENT_3D ( 'NONE', #156307, #57142, #78005 ) ;
#136429=ADVANCED_FACE ( 'NONE', ( #170685 ), #171956, .T. ) ;
#136448=DIRECTION ( 'NONE',  ( 0.000000000000000000, 0.2128009952263605620, -0.9770955615653315052 ) ) ;
#136449=VERTEX_POINT ( 'NONE', #15427 ) ;
#136491=DIRECTION ( 'NONE',  ( -1.000000000000000000, -0.000000000000000000, -0.000000000000000000 ) ) ;
#136512=DIRECTION ( 'NONE',  ( 0.000000000000000000, 0.2128009952263604787, -0.9770955615653315052 ) ) ;
#136532=VECTOR ( 'NONE', #233143, 1000.000000000000114 ) ;
#136536=EDGE_CURVE ( 'NONE', #200569, #235587, #135157, .T. ) ;
#136579=CARTESIAN_POINT ( 'NONE',  ( -21.05000000000000071, 12.82201439108308527, -205.1891724321641277 ) ) ;
#136589=CARTESIAN_POINT ( 'NONE',  ( -20.94999999999999929, -4.756823075239758225, -233.1486023682345490 ) ) ;
#136591=LINE ( 'NONE', #216136, #225560 ) ;
#136612=DIRECTION ( 'NONE',  ( -1.000000000000000000, -0.000000000000000000, -0.000000000000000000 ) ) ;
#136619=AXIS2_PLACEMENT_3D ( 'NONE', #217496, #38897, #182250 ) ;
#136625=FACE_OUTER_BOUND ( 'NONE', #127466, .T. ) ;
#136648=CARTESIAN_POINT ( 'NONE',  ( 20.84999999999998721, 18.41524492703432614, -237.0006385043383546 ) ) ;
#136671=CARTESIAN_POINT ( 'NONE',  ( -21.14999999999999858, -10.86374996222471268, -206.3339888224507206 ) ) ;
#136681=EDGE_CURVE ( 'NONE', #183742, #58187, #165185, .T. ) ;
#136689=CARTESIAN_POINT ( 'NONE',  ( -22.45305610364635740, -2.598867842139048534, -189.5410128746471798 ) ) ;
#136704=ORIENTED_EDGE ( 'NONE', *, *, #81865, .T. ) ;
#136721=AXIS2_PLACEMENT_3D ( 'NONE', #90688, #9874, #73728 ) ;
#136750=DIRECTION ( 'NONE',  ( 0.000000000000000000, 0.2128009952263568982, -0.9770955615653323934 ) ) ;
#136812=TOROIDAL_SURFACE ( 'NONE', #207577, 11.65000000000000036, 0.1000000000000000056 ) ;
#136823=AXIS2_PLACEMENT_3D ( 'NONE', #124596, #241955, #183277 ) ;
#136830=EDGE_LOOP ( 'NONE', ( #177990, #77310 ) ) ;
#136894=AXIS2_PLACEMENT_3D ( 'NONE', #238299, #118376, #2243 ) ;
#136920=TOROIDAL_SURFACE ( 'NONE', #199487, 11.65000000000000036, 0.1000000000000000056 ) ;
#136930=DIRECTION ( 'NONE',  ( -0.000000000000000000, 0.9770955615653315052, 0.2128009952263602844 ) ) ;
#136931=EDGE_CURVE ( 'NONE', #250321, #250869, #64189, .T. ) ;
#136932=CARTESIAN_POINT ( 'NONE',  ( 20.94999999999999929, 8.001317420522637391, -237.7387931148579980 ) ) ;
#136948=CARTESIAN_POINT ( 'NONE',  ( -20.54999999999999716, 6.757359537351773859, -220.2789794402637824 ) ) ;
#136978=ORIENTED_EDGE ( 'NONE', *, *, #68579, .T. ) ;
#136981=CIRCLE ( 'NONE', #107750, 0.1000000000000133560 ) ;
#136982=VERTEX_POINT ( 'NONE', #120348 ) ;
#137012=CARTESIAN_POINT ( 'NONE',  ( -21.05000000000000071, 12.82677665681128332, -205.1493534351658354 ) ) ;
#137021=CARTESIAN_POINT ( 'NONE',  ( 22.39999999999999503, -1.657885652111590780, -193.3876638332971538 ) ) ;
#137029=CARTESIAN_POINT ( 'NONE',  ( 20.95556889135987788, 12.00496303110825025, -206.2069893072027469 ) ) ;
#137041=VECTOR ( 'NONE', #164150, 1000.000000000000227 ) ;
#137059=ORIENTED_EDGE ( 'NONE', *, *, #131865, .T. ) ;
#137061=AXIS2_PLACEMENT_3D ( 'NONE', #235195, #76109, #33181 ) ;
#137067=ADVANCED_FACE ( 'NONE', ( #150160 ), #198092, .T. ) ;
#137077=DIRECTION ( 'NONE',  ( 0.000000000000000000, -0.2965989261549410450, -0.9550021345545443019 ) ) ;
#137108=ORIENTED_EDGE ( 'NONE', *, *, #114504, .F. ) ;
#137180=CIRCLE ( 'NONE', #53796, 0.1000000000000066946 ) ;
#137183=ADVANCED_FACE ( 'NONE', ( #53609 ), #19009, .T. ) ;
#137213=AXIS2_PLACEMENT_3D ( 'NONE', #9038, #192823, #110705 ) ;
#137256=DIRECTION ( 'NONE',  ( 0.000000000000000000, 0.3427706569149635007, -0.9394191166662961834 ) ) ;
#137285=VERTEX_POINT ( 'NONE', #216525 ) ;
#137287=EDGE_CURVE ( 'NONE', #66263, #83634, #6547, .T. ) ;
#137382=DIRECTION ( 'NONE',  ( -1.000000000000000000, -0.000000000000000000, -0.000000000000000000 ) ) ;
#137407=AXIS2_PLACEMENT_3D ( 'NONE', #168230, #247721, #7844 ) ;
#137414=DIRECTION ( 'NONE',  ( -0.7071067811865475727, -0.6909108974501237954, -0.1504730267678056066 ) ) ;
#137457=ORIENTED_EDGE ( 'NONE', *, *, #223352, .T. ) ;
#137506=AXIS2_PLACEMENT_3D ( 'NONE', #255567, #57401, #239923 ) ;
#137521=AXIS2_PLACEMENT_3D ( 'NONE', #118601, #139405, #81984 ) ;
#137535=AXIS2_PLACEMENT_3D ( 'NONE', #184130, #144994, #82439 ) ;
#137550=DIRECTION ( 'NONE',  ( 0.000000000000000000, 0.08413937888704771384, -0.9964539953858891908 ) ) ;
#137572=DIRECTION ( 'NONE',  ( 0.000000000000000000, 0.2128009952263604232, -0.9770955615653316162 ) ) ;
#137604=FACE_OUTER_BOUND ( 'NONE', #214471, .T. ) ;
#137633=CARTESIAN_POINT ( 'NONE',  ( -23.25000000000000000, 7.668827189579289438, -241.6142244293585009 ) ) ;
#137648=EDGE_CURVE ( 'NONE', #30937, #38453, #255071, .T. ) ;
#137654=CARTESIAN_POINT ( 'NONE',  ( -20.00857864376270001, 11.56851667937982775, -211.1200010790121553 ) ) ;
#137723=( BOUNDED_SURFACE ( )  B_SPLINE_SURFACE ( 3, 2, ( 
 ( #94703, #178122, #59395 ),
 ( #138934, #15191, #218483 ),
 ( #39903, #195124, #174303 ),
 ( #119422, #198938, #253768 ) ),
 .UNSPECIFIED., .F., .F., .F. ) 
 B_SPLINE_SURFACE_WITH_KNOTS ( ( 4, 4 ),
 ( 3, 3 ),
 ( 0.04058434257139474644, 0.04256401539001600925 ),
 ( 0.000000000000000000, 1.000000000000000000 ),
 .UNSPECIFIED. ) 
 GEOMETRIC_REPRESENTATION_ITEM ( )  RATIONAL_B_SPLINE_SURFACE ( (
 ( 1.000000000000000000, 0.7103081912008574195, 1.000000000000000000),
 ( 1.000000000000000000, 0.7104998333553186329, 1.000000000000000000),
 ( 1.000000000000000000, 0.7107238315756846392, 1.000000000000000000),
 ( 1.000000000000000000, 0.7110073749539638222, 1.000000000000000000) ) ) 
 REPRESENTATION_ITEM ( '' )  SURFACE ( )  );
#137738=LINE ( 'NONE', #79038, #180861 ) ;
#137755=EDGE_CURVE ( 'NONE', #44901, #139739, #143078, .T. ) ;
#137758=ORIENTED_EDGE ( 'NONE', *, *, #63158, .F. ) ;
#137759=VERTEX_POINT ( 'NONE', #105204 ) ;
#137761=ORIENTED_EDGE ( 'NONE', *, *, #132052, .T. ) ;
#137781=CARTESIAN_POINT ( 'NONE',  ( -20.94999999999999929, 14.80545736607782814, -235.9842437978701639 ) ) ;
#137793=VERTEX_POINT ( 'NONE', #126081 ) ;
#137807=ORIENTED_EDGE ( 'NONE', *, *, #80232, .T. ) ;
#137811=DIRECTION ( 'NONE',  ( 1.000000000000000000, 3.190570557967288949E-16, 6.948722487160392945E-17 ) ) ;
#137834=ORIENTED_EDGE ( 'NONE', *, *, #190932, .T. ) ;
#137845=FACE_OUTER_BOUND ( 'NONE', #114860, .T. ) ;
#137852=CARTESIAN_POINT ( 'NONE',  ( 21.05000000000000071, 10.68863688179707694, -222.5873974249509217 ) ) ;
#137854=ORIENTED_EDGE ( 'NONE', *, *, #8706, .F. ) ;
#137971=CARTESIAN_POINT ( 'NONE',  ( 23.24999999999999645, 7.187745831299792165, -211.5611048126997389 ) ) ;
#137972=ORIENTED_EDGE ( 'NONE', *, *, #32224, .T. ) ;
#137980=ORIENTED_EDGE ( 'NONE', *, *, #89213, .F. ) ;
#138032=ADVANCED_FACE ( 'NONE', ( #200202 ), #172827, .F. ) ;
#138123=FACE_OUTER_BOUND ( 'NONE', #194583, .T. ) ;
#138161=CARTESIAN_POINT ( 'NONE',  ( 22.59999999999999432, -2.401771312552908544, -189.4980873520049727 ) ) ;
#138191=CARTESIAN_POINT ( 'NONE',  ( -21.14999999999999858, 12.92448621296781930, -205.1280733356431938 ) ) ;
#138200=CARTESIAN_POINT ( 'NONE',  ( -23.15000000000000213, 6.835897784820962109, -211.9460267437856373 ) ) ;
#138241=FACE_OUTER_BOUND ( 'NONE', #92334, .T. ) ;
#138257=DIRECTION ( 'NONE',  ( 0.000000000000000000, 0.2128009952263602289, -0.9770955615653316162 ) ) ;
#138321=AXIS2_PLACEMENT_3D ( 'NONE', #234787, #40481, #56129 ) ;
#138327=ORIENTED_EDGE ( 'NONE', *, *, #133370, .T. ) ;
#138332=CARTESIAN_POINT ( 'NONE',  ( -20.85000000000000142, 14.86477715130881272, -235.7932433709592601 ) ) ;
#138338=EDGE_CURVE ( 'NONE', #211554, #31271, #19989, .T. ) ;
#138357=ORIENTED_EDGE ( 'NONE', *, *, #91740, .T. ) ;
#138360=ADVANCED_FACE ( 'NONE', ( #57788 ), #156938, .T. ) ;
#138363=VERTEX_POINT ( 'NONE', #214321 ) ;
#138407=DIRECTION ( 'NONE',  ( 2.659396599871503240E-15, 0.7672646620070624479, -0.6413305999523086776 ) ) ;
#138415=CARTESIAN_POINT ( 'NONE',  ( 21.05000000000000071, 0.5450571430110628945, -208.9664790259058691 ) ) ;
#138434=AXIS2_PLACEMENT_3D ( 'NONE', #149333, #170211, #153198 ) ;
#138451=( BOUNDED_CURVE ( )  B_SPLINE_CURVE ( 3, ( #218306, #59213, #18843, #177938 ),
 .UNSPECIFIED., .F., .F. ) 
 B_SPLINE_CURVE_WITH_KNOTS ( ( 4, 4 ),
 ( 0.000000000000000000, 1.570796326794908992 ),
 .UNSPECIFIED. ) 
 CURVE ( )  GEOMETRIC_REPRESENTATION_ITEM ( )  RATIONAL_B_SPLINE_CURVE ( ( 1.000000000000000000, 0.8047378541243619399, 0.8047378541243619399, 1.000000000000000000 ) ) 
 REPRESENTATION_ITEM ( '' )  );
#138481=ORIENTED_EDGE ( 'NONE', *, *, #220093, .F. ) ;
#138505=AXIS2_PLACEMENT_3D ( 'NONE', #45575, #125127, #63853 ) ;
#138510=EDGE_LOOP ( 'NONE', ( #64669, #128195, #179463, #5951 ) ) ;
#138528=ORIENTED_EDGE ( 'NONE', *, *, #202750, .T. ) ;
#138589=EDGE_CURVE ( 'NONE', #64043, #74308, #30672, .T. ) ;
#138591=CARTESIAN_POINT ( 'NONE',  ( -21.05000000000000071, 1.148907358139439339E-11, -201.0000000000015064 ) ) ;
#138601=VERTEX_POINT ( 'NONE', #212428 ) ;
#138621=DIRECTION ( 'NONE',  ( -1.000000000000000000, -5.840638543281469327E-15, 6.917008051451466668E-14 ) ) ;
#138636=CIRCLE ( 'NONE', #125630, 0.1000000000000014766 ) ;
#138650=CARTESIAN_POINT ( 'NONE',  ( 21.14999999999999858, 0.02128009953412425548, -201.0977095561580370 ) ) ;
#138657=AXIS2_PLACEMENT_3D ( 'NONE', #104511, #180243, #185363 ) ;
#138659=EDGE_CURVE ( 'NONE', #129923, #211815, #72937, .T. ) ;
#138679=DIRECTION ( 'NONE',  ( 0.000000000000000000, 0.2128009952263604232, -0.9770955615653316162 ) ) ;
#138683=CARTESIAN_POINT ( 'NONE',  ( 21.05000000000000071, 7.916168987336737572, -211.9720049928963874 ) ) ;
#138695=ORIENTED_EDGE ( 'NONE', *, *, #117350, .F. ) ;
#138740=LINE ( 'NONE', #43548, #162608 ) ;
#138741=CARTESIAN_POINT ( 'NONE',  ( -21.05000000000000071, 6.256349259666485807, -229.7266095100222572 ) ) ;
#138758=CARTESIAN_POINT ( 'NONE',  ( -18.48408745364677586, -0.8919672813139534195, -242.3192850797796325 ) ) ;
#138776=DIRECTION ( 'NONE',  ( 0.000000000000000000, 0.2128009952263603677, -0.9770955615653313941 ) ) ;
#138791=FACE_OUTER_BOUND ( 'NONE', #11835, .T. ) ;
#138805=FACE_OUTER_BOUND ( 'NONE', #160973, .T. ) ;
#138806=CARTESIAN_POINT ( 'NONE',  ( 20.41140022480414018, 11.79246562616856941, -206.2252339310995524 ) ) ;
#138822=DIRECTION ( 'NONE',  ( 0.000000000000000000, -0.2128009952263601456, 0.9770955615653316162 ) ) ;
#138831=DIRECTION ( 'NONE',  ( 0.000000000000000000, 0.9770955615653316162, 0.2128009952263605342 ) ) ;
#138862=CARTESIAN_POINT ( 'NONE',  ( 20.94999999999999574, 0.4879293624014888198, -209.1697915983179428 ) ) ;
#138889=EDGE_CURVE ( 'NONE', #145985, #98647, #248656, .T. ) ;
#138890=ORIENTED_EDGE ( 'NONE', *, *, #54708, .T. ) ;
#138928=EDGE_CURVE ( 'NONE', #254124, #183349, #184958, .T. ) ;
#138934=CARTESIAN_POINT ( 'NONE',  ( 22.00411653962172664, 7.066231425286733092, -199.3596904452042793 ) ) ;
#138982=EDGE_LOOP ( 'NONE', ( #24585, #242604, #201301, #25115 ) ) ;
#139007=DIRECTION ( 'NONE',  ( -1.000000000000000000, 0.000000000000000000, 0.000000000000000000 ) ) ;
#139010=DIRECTION ( 'NONE',  ( -0.000000000000000000, -0.9770955615653315052, -0.2128009952263603954 ) ) ;
#139015=CIRCLE ( 'NONE', #88970, 0.8750000000000007772 ) ;
#139057=DIRECTION ( 'NONE',  ( 0.000000000000000000, 0.9987946567507913764, -0.04908394489106009811 ) ) ;
#139077=CARTESIAN_POINT ( 'NONE',  ( -20.85000000000000142, -4.352039508298082282, -236.2331130063498676 ) ) ;
#139079=AXIS2_PLACEMENT_3D ( 'NONE', #219111, #20957, #183850 ) ;
#139086=ORIENTED_EDGE ( 'NONE', *, *, #128318, .F. ) ;
#139087=VERTEX_POINT ( 'NONE', #75181 ) ;
#139111=CIRCLE ( 'NONE', #26738, 0.3999999999999994671 ) ;
#139144=EDGE_CURVE ( 'NONE', #205893, #126912, #191283, .T. ) ;
#139158=EDGE_CURVE ( 'NONE', #114637, #183877, #22911, .T. ) ;
#139165=DIRECTION ( 'NONE',  ( 0.000000000000000000, 0.9788861828082167094, 0.2044060691544132835 ) ) ;
#139169=EDGE_CURVE ( 'NONE', #121414, #173153, #201699, .T. ) ;
#139179=FACE_OUTER_BOUND ( 'NONE', #159498, .T. ) ;
#139184=CARTESIAN_POINT ( 'NONE',  ( -21.05000000000000071, 2.859758780633683273, -208.6670499591424459 ) ) ;
#139202=CARTESIAN_POINT ( 'NONE',  ( 23.14999999999999858, 9.083024463225227052, -233.3070993219874083 ) ) ;
#139210=TOROIDAL_SURFACE ( 'NONE', #235118, 0.2000000000000000111, 0.1000000000000000056 ) ;
#139272=ORIENTED_EDGE ( 'NONE', *, *, #90325, .T. ) ;
#139299=DIRECTION ( 'NONE',  ( 0.000000000000000000, -0.9770955615653551529, -0.2128009952262517601 ) ) ;
#139305=AXIS2_PLACEMENT_3D ( 'NONE', #23002, #64659, #145474 ) ;
#139309=VERTEX_POINT ( 'NONE', #257578 ) ;
#139338=LINE ( 'NONE', #199351, #139426 ) ;
#139351=DIRECTION ( 'NONE',  ( 1.000000000000000000, 0.000000000000000000, 0.000000000000000000 ) ) ;
#139387=DIRECTION ( 'NONE',  ( -2.952720810173287633E-16, 0.9770955615653312831, 0.2128009952263610616 ) ) ;
#139390=CARTESIAN_POINT ( 'NONE',  ( 18.49999999999998934, 9.125777775466493935, -211.6520035670780544 ) ) ;
#139405=DIRECTION ( 'NONE',  ( 0.000000000000000000, -0.2128009952263604232, 0.9770955615653316162 ) ) ;
#139406=CARTESIAN_POINT ( 'NONE',  ( 18.39999999999999858, -7.785976468740638090, -209.8926132507865816 ) ) ;
#139412=AXIS2_PLACEMENT_3D ( 'NONE', #168979, #69854, #225028 ) ;
#139426=VECTOR ( 'NONE', #78090, 1000.000000000000227 ) ;
#139446=AXIS2_PLACEMENT_3D ( 'NONE', #87225, #49405, #147216 ) ;
#139468=CARTESIAN_POINT ( 'NONE',  ( 20.94999999999999929, 4.252251777740766236, -211.8999245327126744 ) ) ;
#139481=CARTESIAN_POINT ( 'NONE',  ( -23.25000000000000000, 7.128833340094563376, -233.7327013124401276 ) ) ;
#139510=DIRECTION ( 'NONE',  ( 0.000000000000000000, 0.2128009952263403282, -0.9770955615653358350 ) ) ;
#139566=CARTESIAN_POINT ( 'NONE',  ( 21.05000000000000071, 0.5876173420563349792, -209.1618981382189588 ) ) ;
#139569=ORIENTED_EDGE ( 'NONE', *, *, #93935, .T. ) ;
#139613=ORIENTED_EDGE ( 'NONE', *, *, #33811, .F. ) ;
#139620=CARTESIAN_POINT ( 'NONE',  ( 18.59117750673696179, 18.41524492703433324, -237.0006385043383546 ) ) ;
#139622=ORIENTED_EDGE ( 'NONE', *, *, #8854, .T. ) ;
#139627=EDGE_LOOP ( 'NONE', ( #167518, #181389, #184486 ) ) ;
#139628=EDGE_LOOP ( 'NONE', ( #216317, #237379, #62907, #111838 ) ) ;
#139640=EDGE_CURVE ( 'NONE', #236182, #27566, #234643, .T. ) ;
#139666=CIRCLE ( 'NONE', #27299, 0.5000000000000007772 ) ;
#139677=ORIENTED_EDGE ( 'NONE', *, *, #194540, .T. ) ;
#139678=DIRECTION ( 'NONE',  ( 0.000000000000000000, -0.07893460099012301889, 0.9968797965484754720 ) ) ;
#139683=CARTESIAN_POINT ( 'NONE',  ( -20.54999999999999716, 8.772386841380839684, -220.8375963540301257 ) ) ;
#139712=LINE ( 'NONE', #64047, #111664 ) ;
#139739=VERTEX_POINT ( 'NONE', #91415 ) ;
#139757=DIRECTION ( 'NONE',  ( 0.000000000000000000, -0.9595780032479205301, 0.2814428106787130734 ) ) ;
#139784=DIRECTION ( 'NONE',  ( 0.000000000000000000, -0.2128009952263601456, 0.9770955615653316162 ) ) ;
#139788=CARTESIAN_POINT ( 'NONE',  ( -21.59142135623730852, 10.27701234982225920, -211.2989328166499092 ) ) ;
#139795=DIRECTION ( 'NONE',  ( -0.000000000000000000, 0.2128009952263604232, -0.9770955615653316162 ) ) ;
#139801=EDGE_CURVE ( 'NONE', #205753, #131400, #173565, .T. ) ;
#139830=CARTESIAN_POINT ( 'NONE',  ( -20.94999999999999929, 1.148907358139439339E-11, -201.0000000000015064 ) ) ;
#139874=CARTESIAN_POINT ( 'NONE',  ( -23.15000000000000213, 15.92646454033039660, -219.3818586450342423 ) ) ;
#139877=AXIS2_PLACEMENT_3D ( 'NONE', #211633, #16015, #33036 ) ;
#139878=PLANE ( 'NONE',  #60166 ) ;
#139890=CARTESIAN_POINT ( 'NONE',  ( 20.94999999999999929, 7.525330762710603416, -212.0571253909869256 ) ) ;
#139932=CARTESIAN_POINT ( 'NONE',  ( -18.59999999999999787, 7.804459559388684298, -245.4620200072988325 ) ) ;
#139971=LINE ( 'NONE', #3036, #198968 ) ;
#139994=( BOUNDED_SURFACE ( )  B_SPLINE_SURFACE ( 3, 2, ( 
 ( #213869, #255509, #138161 ),
 ( #216429, #59905, #14417 ),
 ( #99025, #118646, #173518 ),
 ( #258080, #93918, #252987 ) ),
 .UNSPECIFIED., .F., .F., .F. ) 
 B_SPLINE_SURFACE_WITH_KNOTS ( ( 4, 4 ),
 ( 3, 3 ),
 ( -2.141299290658871257E-18, 0.0003124336600439480273 ),
 ( 0.000000000000000000, 1.000000000000000000 ),
 .UNSPECIFIED. ) 
 GEOMETRIC_REPRESENTATION_ITEM ( )  RATIONAL_B_SPLINE_SURFACE ( (
 ( 1.000000000000000000, 0.7071067811865472397, 1.000000000000000000),
 ( 1.000000000000000000, 0.7089187706049221438, 1.000000000000000000),
 ( 1.000000000000000000, 0.7039288185052831048, 1.000000000000000000),
 ( 1.000000000000000000, 0.7040654476016580121, 1.000000000000000000) ) ) 
 REPRESENTATION_ITEM ( '' )  SURFACE ( )  );
#139995=ADVANCED_FACE ( 'NONE', ( #128026 ), #147333, .T. ) ;
#140026=ORIENTED_EDGE ( 'NONE', *, *, #142987, .F. ) ;
#140032=ORIENTED_EDGE ( 'NONE', *, *, #174697, .T. ) ;
#140066=ADVANCED_FACE ( 'NONE', ( #253083 ), #130569, .T. ) ;
#140111=CARTESIAN_POINT ( 'NONE',  ( 20.97565083910961192, 11.84729602164285112, -206.1753656360330069 ) ) ;
#140118=ORIENTED_EDGE ( 'NONE', *, *, #167121, .F. ) ;
#140129=DIRECTION ( 'NONE',  ( 0.000000000000000000, -0.2128009952263403282, 0.9770955615653358350 ) ) ;
#140143=MECHANICAL_DESIGN_GEOMETRIC_PRESENTATION_REPRESENTATION('',(#169247),#85969);
#140148=LINE ( 'NONE', #80154, #217375 ) ;
#140180=AXIS2_PLACEMENT_3D ( 'NONE', #171218, #70814, #228586 ) ;
#140195=CARTESIAN_POINT ( 'NONE',  ( -21.46681500597999914, -1.459285199490397256, -194.2995562827408662 ) ) ;
#140238=DIRECTION ( 'NONE',  ( 0.000000000000000000, 0.2128009952263485993, -0.9770955615653341697 ) ) ;
#140253=EDGE_LOOP ( 'NONE', ( #220507, #36047, #131913, #121879 ) ) ;
#140258=CIRCLE ( 'NONE', #244321, 11.65000000000001457 ) ;
#140314=DIRECTION ( 'NONE',  ( 0.000000000000000000, -0.05689261644169250898, 0.9983803033886528011 ) ) ;
#140331=ORIENTED_EDGE ( 'NONE', *, *, #109595, .T. ) ;
#140339=CARTESIAN_POINT ( 'NONE',  ( -18.54118089899634114, -7.746836289017205779, -209.9009841126467109 ) ) ;
#140340=DIRECTION ( 'NONE',  ( 1.000000000000000000, 0.000000000000000000, 0.000000000000000000 ) ) ;
#140374=CARTESIAN_POINT ( 'NONE',  ( -20.94999999999999929, 4.252251777740766236, -211.8999245327126744 ) ) ;
#140421=CARTESIAN_POINT ( 'NONE',  ( 21.05315837326108763, 17.15379753644537786, -224.5473496284387238 ) ) ;
#140426=AXIS2_PLACEMENT_3D ( 'NONE', #223821, #201708, #163877 ) ;
#140452=CIRCLE ( 'NONE', #132094, 0.1000000000000023231 ) ;
#140461=ORIENTED_EDGE ( 'NONE', *, *, #250588, .F. ) ;
#140504=VECTOR ( 'NONE', #131216, 1000.000000000000227 ) ;
#140507=FACE_OUTER_BOUND ( 'NONE', #176986, .T. ) ;
#140554=ORIENTED_EDGE ( 'NONE', *, *, #18745, .F. ) ;
#140579=CARTESIAN_POINT ( 'NONE',  ( 21.87500000000000355, 12.15477401631902588, -210.9923204818763622 ) ) ;
#140597=CARTESIAN_POINT ( 'NONE',  ( 20.94999999999999574, 1.148907358139439339E-11, -201.0000000000015064 ) ) ;
#140605=VERTEX_POINT ( 'NONE', #188333 ) ;
#140619=ORIENTED_EDGE ( 'NONE', *, *, #81253, .F. ) ;
#140622=ADVANCED_FACE ( 'NONE', ( #184467 ), #243163, .F. ) ;
#140670=CIRCLE ( 'NONE', #178299, 0.09999999999999939493 ) ;
#140671=ORIENTED_EDGE ( 'NONE', *, *, #202883, .F. ) ;
#140672=ORIENTED_EDGE ( 'NONE', *, *, #167771, .F. ) ;
#140709=ADVANCED_FACE ( 'NONE', ( #209174 ), #30566, .T. ) ;
#140717=LINE ( 'NONE', #199434, #137041 ) ;
#140719=ADVANCED_FACE ( 'NONE', ( #192203 ), #230024, .T. ) ;
#140723=DIRECTION ( 'NONE',  ( 0.000000000000000000, 0.9983803033886529121, 0.05689261644169053833 ) ) ;
#140725=ORIENTED_EDGE ( 'NONE', *, *, #5642, .F. ) ;
#140740=ORIENTED_EDGE ( 'NONE', *, *, #149458, .T. ) ;
#140746=EDGE_LOOP ( 'NONE', ( #128389, #36023, #146514, #192490 ) ) ;
#140758=DIRECTION ( 'NONE',  ( 1.000000000000000000, 0.000000000000000000, 0.000000000000000000 ) ) ;
#140769=ADVANCED_FACE ( 'NONE', ( #133494 ), #43654, .F. ) ;
#140819=DIRECTION ( 'NONE',  ( -0.000000000000000000, -0.9770955615653316162, -0.2128009952263604232 ) ) ;
#140827=CARTESIAN_POINT ( 'NONE',  ( -21.14999999999999858, 11.40444339177023814, -198.6185779617709670 ) ) ;
#140843=EDGE_CURVE ( 'NONE', #247087, #208402, #110462, .T. ) ;
#140875=CARTESIAN_POINT ( 'NONE',  ( 19.99999999999999645, 16.72641738073392403, -222.5849938986771974 ) ) ;
#140876=ADVANCED_FACE ( 'NONE', ( #239016 ), #1669, .F. ) ;
#140901=EDGE_CURVE ( 'NONE', #36199, #98560, #85311, .T. ) ;
#140924=CARTESIAN_POINT ( 'NONE',  ( -20.94999999999999929, -10.86374996222471090, -206.3339888224507206 ) ) ;
#140938=VECTOR ( 'NONE', #101937, 1000.000000000000000 ) ;
#140960=DIRECTION ( 'NONE',  ( 1.301042606982683418E-14, -0.9525900758537759749, 0.3042567129660372904 ) ) ;
#140962=DIRECTION ( 'NONE',  ( 0.000000000000000000, -0.9595780032479205301, 0.2814428106787130734 ) ) ;
#140979=EDGE_CURVE ( 'NONE', #5593, #44687, #27711, .T. ) ;
#140982=DIRECTION ( 'NONE',  ( 0.000000000000000000, -0.2128009952263602012, 0.9770955615653315052 ) ) ;
#141015=CARTESIAN_POINT ( 'NONE',  ( -20.64999999999999858, 6.353932154659650777, -220.7762181625030848 ) ) ;
#141016=ORIENTED_EDGE ( 'NONE', *, *, #211342, .T. ) ;
#141028=CARTESIAN_POINT ( 'NONE',  ( -20.64999999999999858, 1.148907358139439339E-11, -201.0000000000015064 ) ) ;
#141057=CARTESIAN_POINT ( 'NONE',  ( -18.59999999999999787, 13.96869538424787649, -210.3925794786331949 ) ) ;
#141080=EDGE_CURVE ( 'NONE', #31271, #160183, #160180, .T. ) ;
#141153=DIRECTION ( 'NONE',  ( 0.000000000000000000, -0.2128009952263609783, 0.9770955615653315052 ) ) ;
#141171=ORIENTED_EDGE ( 'NONE', *, *, #117429, .T. ) ;
#141174=DIRECTION ( 'NONE',  ( -1.000000000000000000, 0.000000000000000000, 0.000000000000000000 ) ) ;
#141196=DIRECTION ( 'NONE',  ( 0.000000000000000000, 0.2128009952263403282, -0.9770955615653358350 ) ) ;
#141202=TOROIDAL_SURFACE ( 'NONE', #53710, 11.65000000000000036, 0.1000000000000000056 ) ;
#141203=DIRECTION ( 'NONE',  ( 0.000000000000000000, -0.9752329468386645717, -0.2211802418851520069 ) ) ;
#141312=CIRCLE ( 'NONE', #124576, 7.720710678118687831 ) ;
#141317=CARTESIAN_POINT ( 'NONE',  ( 18.59999999999999076, 4.193200906077805712, -212.0298262072164164 ) ) ;
#141323=DIRECTION ( 'NONE',  ( 1.000000000000000000, 0.000000000000000000, 0.000000000000000000 ) ) ;
#141365=EDGE_LOOP ( 'NONE', ( #124613, #49280, #236146, #163504 ) ) ;
#141373=DIRECTION ( 'NONE',  ( 0.000000000000000000, 0.2128009952263485993, -0.9770955615653341697 ) ) ;
#141407=LINE ( 'NONE', #98386, #180664 ) ;
#141410=DIRECTION ( 'NONE',  ( 0.000000000000000000, 0.2128009952263485993, -0.9770955615653341697 ) ) ;
#141411=CARTESIAN_POINT ( 'NONE',  ( 20.87631937322879239, 11.84462878906222727, -206.1777914865159005 ) ) ;
#141416=CARTESIAN_POINT ( 'NONE',  ( 21.30000000000002558, 0.8618440306782485516, -204.9572370243411115 ) ) ;
#141417=FACE_OUTER_BOUND ( 'NONE', #248139, .T. ) ;
#141477=ORIENTED_EDGE ( 'NONE', *, *, #115456, .T. ) ;
#141485=DIRECTION ( 'NONE',  ( -1.000000000000000000, -3.190570557967288949E-16, -6.948722487160392945E-17 ) ) ;
#141497=CARTESIAN_POINT ( 'NONE',  ( -22.47071067811865319, -1.546016791165058413, -193.4356622592196970 ) ) ;
#141523=DIRECTION ( 'NONE',  ( -4.448008912761042820E-16, 0.9770955615653312831, 0.2128009952263615334 ) ) ;
#141529=DIRECTION ( 'NONE',  ( 0.000000000000000000, -0.2128009952263650861, 0.9770955615653305060 ) ) ;
#141536=( BOUNDED_CURVE ( )  B_SPLINE_CURVE ( 3, ( #163295, #204956, #122887, #165872 ),
 .UNSPECIFIED., .F., .F. ) 
 B_SPLINE_CURVE_WITH_KNOTS ( ( 4, 4 ),
 ( -1.092459456231154036E-13, 1.570796326794918985 ),
 .UNSPECIFIED. ) 
 CURVE ( )  GEOMETRIC_REPRESENTATION_ITEM ( )  RATIONAL_B_SPLINE_CURVE ( ( 1.000000000000000000, 0.8047378541243339622, 0.8047378541243339622, 1.000000000000000000 ) ) 
 REPRESENTATION_ITEM ( '' )  );
#141537=CARTESIAN_POINT ( 'NONE',  ( -23.25000000000000000, -11.48087284838115885, -203.5004116939112464 ) ) ;
#141555=AXIS2_PLACEMENT_3D ( 'NONE', #56427, #135965, #137256 ) ;
#141559=ORIENTED_EDGE ( 'NONE', *, *, #54259, .F. ) ;
#141599=EDGE_LOOP ( 'NONE', ( #28547, #135867, #13894, #8776 ) ) ;
#141626=EDGE_LOOP ( 'NONE', ( #56218, #116953, #200965, #219143, #114648 ) ) ;
#141633=CARTESIAN_POINT ( 'NONE',  ( 21.14999999999999858, -8.874060656858240748, -215.4698323230865640 ) ) ;
#141661=FACE_OUTER_BOUND ( 'NONE', #247504, .T. ) ;
#141674=AXIS2_PLACEMENT_3D ( 'NONE', #21275, #23841, #141196 ) ;
#141692=ADVANCED_FACE ( 'NONE', ( #197981 ), #35840, .T. ) ;
#141708=DIRECTION ( 'NONE',  ( -0.000000000000000000, 0.9770955615653313941, 0.2128009952263603954 ) ) ;
#141709=CARTESIAN_POINT ( 'NONE',  ( 21.02374657821566828, 16.98881331262128214, -224.4946931421776810 ) ) ;
#141727=DIRECTION ( 'NONE',  ( 0.7071067811865475727, 0.6909108974501237954, 0.1504730267678056066 ) ) ;
#141761=UNCERTAINTY_MEASURE_WITH_UNIT (LENGTH_MEASURE( 1.000000000000000082E-05 ), #133337, 'distance_accuracy_value', 'NONE');
#141791=CARTESIAN_POINT ( 'NONE',  ( 20.94999999999999574, -10.47749788991998088, -206.4278944321438587 ) ) ;
#141835=DIRECTION ( 'NONE',  ( 0.000000000000000000, 0.2128009952264214300, -0.9770955615653181825 ) ) ;
#141892=VERTEX_POINT ( 'NONE', #220127 ) ;
#141902=VERTEX_POINT ( 'NONE', #249957 ) ;
#141936=ORIENTED_EDGE ( 'NONE', *, *, #121474, .T. ) ;
#141937=EDGE_CURVE ( 'NONE', #72705, #190923, #248222, .T. ) ;
#142029=ORIENTED_EDGE ( 'NONE', *, *, #142347, .F. ) ;
#142040=CARTESIAN_POINT ( 'NONE',  ( 20.94999999999999929, 7.128833340094563376, -233.7327013124401276 ) ) ;
#142095=DIRECTION ( 'NONE',  ( 0.000000000000000000, 0.2128009952263485993, -0.9770955615653341697 ) ) ;
#142112=ORIENTED_EDGE ( 'NONE', *, *, #193185, .F. ) ;
#142145=CARTESIAN_POINT ( 'NONE',  ( 19.75857864376269291, 16.74769748025657279, -222.6827034548337849 ) ) ;
#142205=LINE ( 'NONE', #183904, #131593 ) ;
#142210=ORIENTED_EDGE ( 'NONE', *, *, #173329, .T. ) ;
#142228=VERTEX_POINT ( 'NONE', #171126 ) ;
#142235=ADVANCED_FACE ( 'NONE', ( #190666 ), #252468, .T. ) ;
#142275=VECTOR ( 'NONE', #244992, 1000.000000000000227 ) ;
#142291=CARTESIAN_POINT ( 'NONE',  ( 21.05000000000000071, 12.09419181799517062, -206.1384361755945918 ) ) ;
#142297=CARTESIAN_POINT ( 'NONE',  ( 20.94999999999999929, 7.675662554762638479, -241.7139905447625381 ) ) ;
#142306=EDGE_CURVE ( 'NONE', #22873, #92979, #253168, .T. ) ;
#142313=VERTEX_POINT ( 'NONE', #214053 ) ;
#142320=AXIS2_PLACEMENT_3D ( 'NONE', #88474, #28101, #106298 ) ;
#142343=CIRCLE ( 'NONE', #29958, 0.09999999999999939493 ) ;
#142347=EDGE_CURVE ( 'NONE', #241890, #183380, #11063, .T. ) ;
#142349=( NAMED_UNIT ( * ) PLANE_ANGLE_UNIT ( ) SI_UNIT ( $, .RADIAN. ) );
#142352=DIRECTION ( 'NONE',  ( -1.000000000000000000, -0.000000000000000000, -0.000000000000000000 ) ) ;
#142395=CARTESIAN_POINT ( 'NONE',  ( 18.59999999999999076, 8.882751598337870647, -187.0399955572217721 ) ) ;
#142410=CARTESIAN_POINT ( 'NONE',  ( 23.15000000000000213, -3.770473190032740174, -225.9805569534692324 ) ) ;
#142431=DIRECTION ( 'NONE',  ( -0.000000000000000000, 0.2128009952263603677, -0.9770955615653313941 ) ) ;
#142446=CARTESIAN_POINT ( 'NONE',  ( -20.85000000000000142, 7.668827189579289438, -241.6142244293585009 ) ) ;
#142458=EDGE_LOOP ( 'NONE', ( #60800, #145656, #40316, #8510 ) ) ;
#142462=ORIENTED_EDGE ( 'NONE', *, *, #193185, .T. ) ;
#142466=CARTESIAN_POINT ( 'NONE',  ( 18.59999999999999076, 7.668827189579289438, -241.6142244293585009 ) ) ;
#142476=FACE_OUTER_BOUND ( 'NONE', #198729, .T. ) ;
#142488=CARTESIAN_POINT ( 'NONE',  ( -23.25000000000000000, 13.96869538424788360, -210.3925794786332233 ) ) ;
#142501=AXIS2_PLACEMENT_3D ( 'NONE', #209670, #110563, #36186 ) ;
#142520=AXIS2_PLACEMENT_3D ( 'NONE', #63380, #182070, #103778 ) ;
#142529=VERTEX_POINT ( 'NONE', #127801 ) ;
#142533=ORIENTED_EDGE ( 'NONE', *, *, #97982, .F. ) ;
#142545=DIRECTION ( 'NONE',  ( -1.000000000000000000, 0.000000000000000000, 0.000000000000000000 ) ) ;
#142575=DIRECTION ( 'NONE',  ( -0.000000000000000000, 0.2128009952263603677, -0.9770955615653313941 ) ) ;
#142594=ADVANCED_FACE ( 'NONE', ( #106929 ), #43128, .F. ) ;
#142603=DIRECTION ( 'NONE',  ( 0.000000000000000000, 0.8267009638119717785, 0.5626415523513675909 ) ) ;
#142604=CARTESIAN_POINT ( 'NONE',  ( 22.50000000000000000, 1.148907358139439339E-11, -201.0000000000015064 ) ) ;
#142626=ORIENTED_EDGE ( 'NONE', *, *, #151633, .T. ) ;
#142656=DIRECTION ( 'NONE',  ( 0.000000000000000000, 0.2128009952263621718, -0.9770955615653310611 ) ) ;
#142694=ORIENTED_EDGE ( 'NONE', *, *, #165653, .T. ) ;
#142712=ADVANCED_FACE ( 'NONE', ( #194207 ), #15573, .F. ) ;
#142726=AXIS2_PLACEMENT_3D ( 'NONE', #81406, #61885, #141410 ) ;
#142804=DIRECTION ( 'NONE',  ( -1.000000000000000000, -3.190570557967288949E-16, -6.948722487160392945E-17 ) ) ;
#142823=B_SPLINE_CURVE_WITH_KNOTS ( 'NONE', 3,
 ( #185893, #86775, #200330, #166372, #140339, #219886, #21701, #150626 ),
 .UNSPECIFIED., .F., .F.,
 ( 4, 2, 2, 4 ),
 ( 0.000000000000000000, 0.0001049670497869903125, 0.0002099340995739806251, 0.0004198681991480121534 ),
 .UNSPECIFIED. ) ;
#142827=CARTESIAN_POINT ( 'NONE',  ( -22.57320508075687115, 11.38316329224760892, -198.5208684056144364 ) ) ;
#142853=CARTESIAN_POINT ( 'NONE',  ( -21.44999999999999929, 9.788464569039593499, -211.4053333142630891 ) ) ;
#142867=DIRECTION ( 'NONE',  ( 1.000000000000000000, 0.000000000000000000, 0.000000000000000000 ) ) ;
#142872=CARTESIAN_POINT ( 'NONE',  ( -18.59999999999999787, 0.6770221356676882074, -212.8807256103264649 ) ) ;
#142874=ORIENTED_EDGE ( 'NONE', *, *, #146384, .F. ) ;
#142888=CIRCLE ( 'NONE', #59492, 4.000000000000006217 ) ;
#142926=EDGE_CURVE ( 'NONE', #78551, #86393, #104036, .T. ) ;
#142928=DIRECTION ( 'NONE',  ( -7.304098846218419643E-16, 0.9770955615653543758, 0.2128009952262553683 ) ) ;
#142935=DIRECTION ( 'NONE',  ( 0.000000000000000000, 0.9987946567507778317, -0.04908394489133698774 ) ) ;
#142955=DIRECTION ( 'NONE',  ( -0.4999999999999799050, 0.1842910678166416460, -0.8461895782406104738 ) ) ;
#142973=FACE_OUTER_BOUND ( 'NONE', #243828, .T. ) ;
#142987=EDGE_CURVE ( 'NONE', #86372, #196267, #57191, .T. ) ;
#143000=CYLINDRICAL_SURFACE ( 'NONE', #189046, 0.09999999999999810429 ) ;
#143018=AXIS2_PLACEMENT_3D ( 'NONE', #98094, #22471, #78559 ) ;
#143021=FACE_OUTER_BOUND ( 'NONE', #156393, .T. ) ;
#143023=AXIS2_PLACEMENT_3D ( 'NONE', #224185, #6424, #203354 ) ;
#143040=DIRECTION ( 'NONE',  ( -0.000000000000000000, 0.9770955615653313941, 0.2128009952263603954 ) ) ;
#143049=ORIENTED_EDGE ( 'NONE', *, *, #14349, .T. ) ;
#143078=LINE ( 'NONE', #247322, #226068 ) ;
#143082=ORIENTED_EDGE ( 'NONE', *, *, #16731, .T. ) ;
#143084=ORIENTED_EDGE ( 'NONE', *, *, #53905, .F. ) ;
#143086=CARTESIAN_POINT ( 'NONE',  ( -20.85000000000000142, 18.41524492703433680, -237.0006385043383830 ) ) ;
#143117=AXIS2_PLACEMENT_3D ( 'NONE', #30195, #169727, #92703 ) ;
#143124=ADVANCED_FACE ( 'NONE', ( #150892 ), #148326, .T. ) ;
#143148=DIRECTION ( 'NONE',  ( 0.000000000000000000, 0.9770955615653548199, 0.2128009952262535920 ) ) ;
#143157=ORIENTED_EDGE ( 'NONE', *, *, #230940, .F. ) ;
#143164=ORIENTED_EDGE ( 'NONE', *, *, #137287, .F. ) ;
#143199=ORIENTED_EDGE ( 'NONE', *, *, #235590, .T. ) ;
#143236=FACE_OUTER_BOUND ( 'NONE', #78861, .T. ) ;
#143237=EDGE_CURVE ( 'NONE', #162306, #222722, #79023, .T. ) ;
#143240=CARTESIAN_POINT ( 'NONE',  ( 20.94999999999999929, 7.128833340094563376, -233.7327013124401276 ) ) ;
#143254=CIRCLE ( 'NONE', #226426, 0.1000000000000055844 ) ;
#143266=DIRECTION ( 'NONE',  ( -2.940209281316620030E-16, 0.9770955615653310611, 0.2128009952263628379 ) ) ;
#143267=CARTESIAN_POINT ( 'NONE',  ( -20.94999999999999929, 7.476371755685461196, -241.7308184205399471 ) ) ;
#143274=CARTESIAN_POINT ( 'NONE',  ( -21.05000000000094218, 6.196269102992084221, -199.6354557928876829 ) ) ;
#143297=AXIS2_PLACEMENT_3D ( 'NONE', #207985, #170173, #50159 ) ;
#143303=EDGE_LOOP ( 'NONE', ( #189889, #82747, #151631, #233621 ) ) ;
#143317=B_SPLINE_CURVE_WITH_KNOTS ( 'NONE', 3,
 ( #187919, #53528, #208767, #169675, #113502, #9265, #110934, #151367, #69259, #50932, #148791, #13133, #193053, #210054, #31437, #93934 ),
 .UNSPECIFIED., .F., .F.,
 ( 4, 3, 3, 3, 3, 4 ),
 ( 0.000000000000000000, 2.209833635978128636E-05, 5.595056164119354553E-05, 8.979992002655480337E-05, 0.0001236482757198921142, 0.0001574984039363022149 ),
 .UNSPECIFIED. ) ;
#143323=DIRECTION ( 'NONE',  ( -0.7071067811865475727, -0.6909108974501237954, -0.1504730267678056066 ) ) ;
#143356=EDGE_CURVE ( 'NONE', #102386, #5593, #257263, .T. ) ;
#143357=AXIS2_PLACEMENT_3D ( 'NONE', #75783, #57473, #94042 ) ;
#143368=DIRECTION ( 'NONE',  ( 1.000000000000000000, 0.000000000000000000, 0.000000000000000000 ) ) ;
#143378=AXIS2_PLACEMENT_3D ( 'NONE', #9675, #150489, #211747 ) ;
#143396=AXIS2_PLACEMENT_3D ( 'NONE', #255204, #216124, #120918 ) ;
#143399=ORIENTED_EDGE ( 'NONE', *, *, #240139, .F. ) ;
#143400=ORIENTED_EDGE ( 'NONE', *, *, #174180, .F. ) ;
#143401=CARTESIAN_POINT ( 'NONE',  ( 20.94999999999999929, 2.761092913073515120, -213.6778149113116854 ) ) ;
#143403=DIRECTION ( 'NONE',  ( -0.000000000000000000, 0.9770955615653313941, 0.2128009952263603954 ) ) ;
#143489=EDGE_CURVE ( 'NONE', #226256, #91428, #108884, .T. ) ;
#143502=EDGE_LOOP ( 'NONE', ( #40910, #85256, #140461, #116723 ) ) ;
#143520=LINE ( 'NONE', #223055, #167649 ) ;
#143541=EDGE_CURVE ( 'NONE', #3257, #199490, #49026, .T. ) ;
#143564=ORIENTED_EDGE ( 'NONE', *, *, #149184, .F. ) ;
#143589=DIRECTION ( 'NONE',  ( 1.000000000000000000, 0.000000000000000000, 0.000000000000000000 ) ) ;
#143591=EDGE_CURVE ( 'NONE', #176555, #17833, #81839, .T. ) ;
#143605=LINE ( 'NONE', #44520, #44617 ) ;
#143651=LINE ( 'NONE', #178976, #76718 ) ;
#143653=CARTESIAN_POINT ( 'NONE',  ( -23.25000000000000000, 6.835897784820962109, -211.9460267437856373 ) ) ;
#143660=FACE_OUTER_BOUND ( 'NONE', #71804, .T. ) ;
#143667=AXIS2_PLACEMENT_3D ( 'NONE', #72820, #195333, #251426 ) ;
#143696=ADVANCED_FACE ( 'NONE', ( #16824 ), #240757, .T. ) ;
#143708=CARTESIAN_POINT ( 'NONE',  ( -23.25000000000000000, 6.268811756569107274, -220.3853799378769622 ) ) ;
#143709=VERTEX_POINT ( 'NONE', #255357 ) ;
#143713=FACE_OUTER_BOUND ( 'NONE', #245182, .T. ) ;
#143724=CIRCLE ( 'NONE', #160509, 11.75000000000000355 ) ;
#143735=CARTESIAN_POINT ( 'NONE',  ( 21.30000000000002558, 1.148907358139439339E-11, -201.0000000000015064 ) ) ;
#143758=EDGE_LOOP ( 'NONE', ( #175149, #81472, #164065, #161805 ) ) ;
#143790=AXIS2_PLACEMENT_3D ( 'NONE', #12095, #92877, #31664 ) ;
#143813=ORIENTED_EDGE ( 'NONE', *, *, #116960, .F. ) ;
#143815=VERTEX_POINT ( 'NONE', #1062 ) ;
#143844=VERTEX_POINT ( 'NONE', #119784 ) ;
#143902=AXIS2_PLACEMENT_3D ( 'NONE', #234491, #96256, #54572 ) ;
#143906=CIRCLE ( 'NONE', #43952, 0.09999999999999939493 ) ;
#143953=DIRECTION ( 'NONE',  ( -1.000000000000000000, -0.000000000000000000, -0.000000000000000000 ) ) ;
#143971=AXIS2_PLACEMENT_3D ( 'NONE', #10460, #108278, #195206 ) ;
#143990=DIRECTION ( 'NONE',  ( 0.000000000000000000, 0.2128009952263605897, -0.9770955615653315052 ) ) ;
#143991=EDGE_CURVE ( 'NONE', #215393, #47690, #173789, .T. ) ;
#143996=CYLINDRICAL_SURFACE ( 'NONE', #27557, 0.09999999999999724387 ) ;
#144022=EDGE_CURVE ( 'NONE', #106738, #14516, #115453, .T. ) ;
#144043=CARTESIAN_POINT ( 'NONE',  ( 21.04999999999782645, 10.49705515483494267, -207.3998863419698182 ) ) ;
#144057=ORIENTED_EDGE ( 'NONE', *, *, #212022, .T. ) ;
#144078=CYLINDRICAL_SURFACE ( 'NONE', #173019, 0.5000000000000007772 ) ;
#144154=CYLINDRICAL_SURFACE ( 'NONE', #85131, 0.09999999999999939493 ) ;
#144178=CARTESIAN_POINT ( 'NONE',  ( -18.50000000000000000, 7.675662554762638479, -241.7139905447625381 ) ) ;
#144192=ORIENTED_EDGE ( 'NONE', *, *, #134884, .T. ) ;
#144196=DIRECTION ( 'NONE',  ( 1.000000000000000000, 0.000000000000000000, 0.000000000000000000 ) ) ;
#144219=FACE_OUTER_BOUND ( 'NONE', #243481, .T. ) ;
#144222=CARTESIAN_POINT ( 'NONE',  ( -21.14999999999999858, -1.391858308744747807, -194.6091531227727955 ) ) ;
#144235=EDGE_CURVE ( 'NONE', #193505, #34155, #28007, .T. ) ;
#144238=DIRECTION ( 'NONE',  ( 0.000000000000000000, -0.2128009952263403282, 0.9770955615653358350 ) ) ;
#144245=CYLINDRICAL_SURFACE ( 'NONE', #32208, 0.1000000000000001305 ) ;
#144276=CARTESIAN_POINT ( 'NONE',  ( 18.39999999999999858, -11.68510997261236106, -191.5194565067366455 ) ) ;
#144369=EDGE_LOOP ( 'NONE', ( #31952, #64164, #118354, #149236, #113281, #6280 ) ) ;
#144372=ORIENTED_EDGE ( 'NONE', *, *, #149064, .T. ) ;
#144451=ORIENTED_EDGE ( 'NONE', *, *, #77324, .T. ) ;
#144459=DIRECTION ( 'NONE',  ( 1.000000000000000000, 0.000000000000000000, 0.000000000000000000 ) ) ;
#144461=EDGE_CURVE ( 'NONE', #172105, #1731, #15733, .T. ) ;
#144508=LINE ( 'NONE', #66284, #3189 ) ;
#144525=CARTESIAN_POINT ( 'NONE',  ( 22.50000000000000000, 1.148907358139439339E-11, -201.0000000000015064 ) ) ;
#144535=ORIENTED_EDGE ( 'NONE', *, *, #154330, .F. ) ;
#144539=CARTESIAN_POINT ( 'NONE',  ( -20.94999999999999929, 0.5876173420563349792, -209.1618981382189588 ) ) ;
#144542=CARTESIAN_POINT ( 'NONE',  ( 21.22070241538126467, -1.280157660226128646, -194.6571941450697807 ) ) ;
#144552=VECTOR ( 'NONE', #24673, 1000.000000000000000 ) ;
#144585=LINE ( 'NONE', #224128, #13151 ) ;
#144592=CARTESIAN_POINT ( 'NONE',  ( 20.94999999999999929, 7.525330762710603416, -212.0571253909869256 ) ) ;
#144601=CARTESIAN_POINT ( 'NONE',  ( -23.15000000000000213, 4.590145742703442444, -213.0289728181953706 ) ) ;
#144608=AXIS2_PLACEMENT_3D ( 'NONE', #216006, #139010, #99891 ) ;
#144615=EDGE_LOOP ( 'NONE', ( #256444, #196033, #84781, #119128 ) ) ;
#144637=CARTESIAN_POINT ( 'NONE',  ( -18.50000324121759121, 18.34775554461856473, -236.8759397601555179 ) ) ;
#144647=CARTESIAN_POINT ( 'NONE',  ( 22.50000000000000000, 11.36146383068193444, -198.4232501820394816 ) ) ;
#144682=VERTEX_POINT ( 'NONE', #202532 ) ;
#144709=VECTOR ( 'NONE', #181851, 1000.000000000000227 ) ;
#144713=DIRECTION ( 'NONE',  ( 0.000000000000000000, -0.9770955615653316162, -0.2128009952263604232 ) ) ;
#144748=ORIENTED_EDGE ( 'NONE', *, *, #92632, .T. ) ;
#144774=AXIS2_PLACEMENT_3D ( 'NONE', #102226, #219637, #1859 ) ;
#144782=VECTOR ( 'NONE', #211372, 1000.000000000000227 ) ;
#144786=AXIS2_PLACEMENT_3D ( 'NONE', #121938, #39851, #119372 ) ;
#144805=CARTESIAN_POINT ( 'NONE',  ( 21.05000000000000071, -4.756823075239758225, -233.1486023682345490 ) ) ;
#144852=DIRECTION ( 'NONE',  ( 2.715809747126116015E-16, -0.9770955615653313941, -0.2128009952263606730 ) ) ;
#144902=CARTESIAN_POINT ( 'NONE',  ( 21.05000000000000071, 13.06600978423091242, -210.6006273873371129 ) ) ;
#144906=SURFACE_SIDE_STYLE ('',( #125372 ) ) ;
#144930=AXIS2_PLACEMENT_3D ( 'NONE', #155542, #111247, #10867 ) ;
#144935=( BOUNDED_SURFACE ( )  B_SPLINE_SURFACE ( 3, 2, ( 
 ( #52325, #108471, #212720 ),
 ( #231009, #88884, #148894 ),
 ( #28982, #49776, #188017 ),
 ( #48489, #34111, #73230 ),
 ( #32830, #9356, #128042 ),
 ( #113606, #92744, #131886 ) ),
 .UNSPECIFIED., .F., .F., .T. ) 
 B_SPLINE_SURFACE_WITH_KNOTS ( ( 4, 2, 4 ),
 ( 3, 3 ),
 ( 3.141592653589852180, 3.926990816987266264, 4.712388980384680792 ),
 ( 0.000000000000000000, 1.000000000000000000 ),
 .UNSPECIFIED. ) 
 GEOMETRIC_REPRESENTATION_ITEM ( )  RATIONAL_B_SPLINE_SURFACE ( (
 ( 1.000000000000000000, 0.9238795325112717505, 1.000000000000000000),
 ( 1.000000000000000000, 0.9240297172246723090, 1.000000000000000000),
 ( 1.000000000000000000, 0.9038128468035413476, 1.000000000000000000),
 ( 1.000000000000000000, 0.8282379607653282960, 1.000000000000000000),
 ( 1.000000000000000000, 0.7727932973488256252, 1.000000000000000000),
 ( 1.000000000000000000, 0.7071067811865475727, 1.000000000000000000) ) ) 
 REPRESENTATION_ITEM ( '' )  SURFACE ( )  );
#144937=DIRECTION ( 'NONE',  ( -0.000000000000000000, -0.2128009952263603677, 0.9770955615653313941 ) ) ;
#144957=ORIENTED_EDGE ( 'NONE', *, *, #237406, .F. ) ;
#144990=AXIS2_PLACEMENT_3D ( 'NONE', #250606, #212787, #71993 ) ;
#144994=DIRECTION ( 'NONE',  ( -1.000000000000000000, -2.885090398161910739E-16, -6.283419270304611573E-17 ) ) ;
#145005=DIRECTION ( 'NONE',  ( -1.000000000000000000, -0.000000000000000000, -0.000000000000000000 ) ) ;
#145097=EDGE_CURVE ( 'NONE', #89128, #246033, #185239, .T. ) ;
#145108=CIRCLE ( 'NONE', #144930, 0.5000000000000007772 ) ;
#145160=VECTOR ( 'NONE', #35294, 1000.000000000000000 ) ;
#145178=LINE ( 'NONE', #46083, #242670 ) ;
#145213=FACE_OUTER_BOUND ( 'NONE', #12712, .T. ) ;
#145229=LINE ( 'NONE', #206501, #231668 ) ;
#145238=VECTOR ( 'NONE', #224738, 1000.000000000000227 ) ;
#145242=CIRCLE ( 'NONE', #137061, 0.5000000000000007772 ) ;
#145252=EDGE_LOOP ( 'NONE', ( #133623, #44842, #5525, #149884 ) ) ;
#145277=VERTEX_POINT ( 'NONE', #49581 ) ;
#145285=ORIENTED_EDGE ( 'NONE', *, *, #96218, .F. ) ;
#145300=EDGE_CURVE ( 'NONE', #32779, #250321, #226930, .T. ) ;
#145348=DIRECTION ( 'NONE',  ( 1.000000000000000000, 0.000000000000000000, 0.000000000000000000 ) ) ;
#145361=VERTEX_POINT ( 'NONE', #224982 ) ;
#145371=CIRCLE ( 'NONE', #187099, 6.329289321881355512 ) ;
#145377=VERTEX_POINT ( 'NONE', #45090 ) ;
#145403=CARTESIAN_POINT ( 'NONE',  ( 21.14999999999999858, -1.391858308744748696, -194.6091531227727955 ) ) ;
#145421=CARTESIAN_POINT ( 'NONE',  ( -22.39999999999999858, -2.576749817950531707, -189.6385361693310756 ) ) ;
#145429=ORIENTED_EDGE ( 'NONE', *, *, #202996, .F. ) ;
#145438=CARTESIAN_POINT ( 'NONE',  ( -21.14999999999999858, 6.390846877240202950, -199.6081416912452653 ) ) ;
#145474=DIRECTION ( 'NONE',  ( 0.000000000000000000, -0.2128009952263485993, 0.9770955615653341697 ) ) ;
#145476=DIRECTION ( 'NONE',  ( -0.000000000000000000, -0.2128009952263603677, 0.9770955615653313941 ) ) ;
#145507=CARTESIAN_POINT ( 'NONE',  ( 18.52928932188133970, 14.58714922055045626, -219.6735472415052755 ) ) ;
#145534=DIRECTION ( 'NONE',  ( -1.000000000000000000, -0.000000000000000000, -0.000000000000000000 ) ) ;
#145545=EDGE_CURVE ( 'NONE', #100848, #112967, #52773, .T. ) ;
#145556=DIRECTION ( 'NONE',  ( 1.000000000000000000, 0.000000000000000000, 0.000000000000000000 ) ) ;
#145565=CARTESIAN_POINT ( 'NONE',  ( -21.05000000000000071, 16.98881331171929787, -224.4946931418895701 ) ) ;
#145574=CARTESIAN_POINT ( 'NONE',  ( 20.94999999999999574, 1.148907358139439339E-11, -201.0000000000015064 ) ) ;
#145594=FACE_OUTER_BOUND ( 'NONE', #28754, .T. ) ;
#145595=CIRCLE ( 'NONE', #195716, 0.1000000000000069861 ) ;
#145627=DIRECTION ( 'NONE',  ( -1.000000000000000000, -0.000000000000000000, -0.000000000000000000 ) ) ;
#145642=VECTOR ( 'NONE', #227927, 1000.000000000000227 ) ;
#145648=AXIS2_PLACEMENT_3D ( 'NONE', #207454, #87474, #31407 ) ;
#145656=ORIENTED_EDGE ( 'NONE', *, *, #1005, .T. ) ;
#145661=DIRECTION ( 'NONE',  ( -1.000000000000000000, -2.885090398161910739E-16, -6.283419270304611573E-17 ) ) ;
#145678=EDGE_CURVE ( 'NONE', #26573, #53843, #3068, .T. ) ;
#145681=VERTEX_POINT ( 'NONE', #160900 ) ;
#145690=DIRECTION ( 'NONE',  ( 0.000000000000000000, 0.2128009952263588966, -0.9770955615653318382 ) ) ;
#145698=LINE ( 'NONE', #186125, #118764 ) ;
#145720=FACE_OUTER_BOUND ( 'NONE', #152491, .T. ) ;
#145722=EDGE_CURVE ( 'NONE', #143709, #68824, #61778, .T. ) ;
#145731=CIRCLE ( 'NONE', #233074, 0.5000000000000007772 ) ;
#145755=CARTESIAN_POINT ( 'NONE',  ( 21.05000000000000071, 4.252251777740766236, -211.8999245327126744 ) ) ;
#145771=CARTESIAN_POINT ( 'NONE',  ( -20.94999999999999929, 0.5450571430110628945, -208.9664790259058691 ) ) ;
#145801=DIRECTION ( 'NONE',  ( -2.827886303505248766E-16, 0.7397890806274223241, 0.6728388485993012091 ) ) ;
#145811=ORIENTED_EDGE ( 'NONE', *, *, #81952, .T. ) ;
#145814=CYLINDRICAL_SURFACE ( 'NONE', #183537, 0.1000000000000055844 ) ;
#145827=LINE ( 'NONE', #44191, #57158 ) ;
#145833=CARTESIAN_POINT ( 'NONE',  ( -18.50000000000000000, 13.96869538424788004, -210.3925794786332233 ) ) ;
#145845=ADVANCED_FACE ( 'NONE', ( #47331 ), #168643, .F. ) ;
#145874=VECTOR ( 'NONE', #136007, 1000.000000000000114 ) ;
#145886=CARTESIAN_POINT ( 'NONE',  ( 21.05000000000000071, 1.148907358139439339E-11, -201.0000000000015064 ) ) ;
#145907=CARTESIAN_POINT ( 'NONE',  ( -21.93642651522410247, 7.159341611308074782, -199.4407717320839879 ) ) ;
#145921=ORIENTED_EDGE ( 'NONE', *, *, #106560, .F. ) ;
#145945=EDGE_CURVE ( 'NONE', #113101, #96338, #112481, .T. ) ;
#145985=VERTEX_POINT ( 'NONE', #111185 ) ;
#145992=FACE_OUTER_BOUND ( 'NONE', #115452, .T. ) ;
#146023=CIRCLE ( 'NONE', #91861, 7.800000000000002487 ) ;
#146033=ORIENTED_EDGE ( 'NONE', *, *, #234202, .T. ) ;
#146048=DIRECTION ( 'NONE',  ( 4.026293107431335996E-15, -0.9550021345545530727, 0.2965989261549131228 ) ) ;
#146078=DIRECTION ( 'NONE',  ( 0.000000000000000000, 0.2128009952263601179, -0.9770955615653315052 ) ) ;
#146131=CARTESIAN_POINT ( 'NONE',  ( 18.59999999999999076, 18.51199663233068193, -231.2535697180530292 ) ) ;
#146151=AXIS2_PLACEMENT_3D ( 'NONE', #116544, #38292, #39607 ) ;
#146195=CARTESIAN_POINT ( 'NONE',  ( 21.05563370358598263, 13.07117173248338560, -210.6219170696655283 ) ) ;
#146233=CARTESIAN_POINT ( 'NONE',  ( -18.59999999999999787, 2.838478681111047841, -208.5693404029859437 ) ) ;
#146280=CARTESIAN_POINT ( 'NONE',  ( -22.00356870143295041, 7.088088014903060063, -199.4562900056665455 ) ) ;
#146332=ORIENTED_EDGE ( 'NONE', *, *, #199109, .T. ) ;
#146334=ORIENTED_EDGE ( 'NONE', *, *, #170199, .F. ) ;
#146352=VERTEX_POINT ( 'NONE', #30090 ) ;
#146384=EDGE_CURVE ( 'NONE', #117008, #89222, #79126, .T. ) ;
#146389=CARTESIAN_POINT ( 'NONE',  ( -20.54999999999999716, -6.688413578037177842, -212.5825622730469036 ) ) ;
#146398=CIRCLE ( 'NONE', #113108, 0.2000000000000003997 ) ;
#146422=DIRECTION ( 'NONE',  ( -1.836970198721029934E-16, 0.9770955615653315052, 0.2128009952263603954 ) ) ;
#146452=ORIENTED_EDGE ( 'NONE', *, *, #92597, .F. ) ;
#146485=CARTESIAN_POINT ( 'NONE',  ( -18.41809261886926308, -0.9152170315146264112, -242.2974986608316499 ) ) ;
#146487=VERTEX_POINT ( 'NONE', #139406 ) ;
#146514=ORIENTED_EDGE ( 'NONE', *, *, #254001, .T. ) ;
#146532=CARTESIAN_POINT ( 'NONE',  ( -21.12642695952773764, 6.208582294788165257, -199.5466152643390387 ) ) ;
#146545=EDGE_LOOP ( 'NONE', ( #190906, #21169 ) ) ;
#146546=B_SPLINE_CURVE_WITH_KNOTS ( 'NONE', 3,
 ( #34166, #229758, #51084, #193217, #14591, #233625, #129378, #134488, #15880, #111096, #171122, #250597, #248035, #208911, #32890, #13288, #92802, #139620, #57521 ),
 .UNSPECIFIED., .F., .F.,
 ( 4, 3, 3, 3, 3, 3, 4 ),
 ( -2.000416914655141542E-06, 0.000000000000000000, 4.714008503747371182E-05, 9.979203887777928774E-05, 0.0001372215519229508436, 0.0001635031576221009011, 0.0001900083748504142458 ),
 .UNSPECIFIED. ) ;
#146564=EDGE_CURVE ( 'NONE', #245093, #1731, #135562, .T. ) ;
#146567=ADVANCED_FACE ( 'NONE', ( #138123 ), #16627, .T. ) ;
#146569=AXIS2_PLACEMENT_3D ( 'NONE', #97111, #256160, #39784 ) ;
#146572=EDGE_CURVE ( 'NONE', #17833, #69101, #228998, .T. ) ;
#146612=ORIENTED_EDGE ( 'NONE', *, *, #151876, .F. ) ;
#146634=AXIS2_PLACEMENT_3D ( 'NONE', #194021, #15379, #156183 ) ;
#146764=EDGE_CURVE ( 'NONE', #103375, #75051, #191794, .T. ) ;
#146769=VECTOR ( 'NONE', #38743, 1000.000000000000227 ) ;
#146838=CARTESIAN_POINT ( 'NONE',  ( -20.94999999999999929, 17.04749343158673014, -224.5908524457887268 ) ) ;
#146883=CARTESIAN_POINT ( 'NONE',  ( 20.94999999999999574, 2.817198581588411077, -208.4716308468294130 ) ) ;
#146905=CYLINDRICAL_SURFACE ( 'NONE', #46663, 0.1000000000000055844 ) ;
#146922=CARTESIAN_POINT ( 'NONE',  ( -21.05000000000000071, 1.148907358139439339E-11, -201.0000000000015064 ) ) ;
#146961=CIRCLE ( 'NONE', #117938, 0.09999999999999939493 ) ;
#146962=CYLINDRICAL_SURFACE ( 'NONE', #135948, 7.900000000000007461 ) ;
#146977=CARTESIAN_POINT ( 'NONE',  ( -23.25000000000000000, 7.567413955921500346, -241.6205176796878504 ) ) ;
#147002=CARTESIAN_POINT ( 'NONE',  ( -23.15000000000000213, 6.780748427709700543, -212.1627259556213403 ) ) ;
#147023=DIRECTION ( 'NONE',  ( 0.000000000000000000, -0.9964539953858966292, -0.08413937888696132461 ) ) ;
#147027=CARTESIAN_POINT ( 'NONE',  ( 23.14999999999998437, 1.148907358139439339E-11, -201.0000000000015064 ) ) ;
#147028=ORIENTED_EDGE ( 'NONE', *, *, #72688, .F. ) ;
#147049=ORIENTED_EDGE ( 'NONE', *, *, #68782, .F. ) ;
#147111=DIRECTION ( 'NONE',  ( -0.000000000000000000, 0.2128009952263603677, -0.9770955615653313941 ) ) ;
#147128=ADVANCED_FACE ( 'NONE', ( #48851 ), #225230, .F. ) ;
#147172=ORIENTED_EDGE ( 'NONE', *, *, #191280, .T. ) ;
#147205=ORIENTED_EDGE ( 'NONE', *, *, #207387, .T. ) ;
#147215=VERTEX_POINT ( 'NONE', #81236 ) ;
#147216=DIRECTION ( 'NONE',  ( 0.000000000000000000, 0.2128009952263603677, -0.9770955615653313941 ) ) ;
#147244=EDGE_CURVE ( 'NONE', #97897, #235714, #8781, .T. ) ;
#147255=TOROIDAL_SURFACE ( 'NONE', #26464, 1.900000000000002576, 0.1000000000000000056 ) ;
#147258=CARTESIAN_POINT ( 'NONE',  ( -22.41119224318417125, -2.479040261793999722, -189.6172560698084624 ) ) ;
#147302=ORIENTED_EDGE ( 'NONE', *, *, #68307, .T. ) ;
#147333=TOROIDAL_SURFACE ( 'NONE', #209705, 0.2000000000000000111, 0.1000000000000000056 ) ;
#147369=CARTESIAN_POINT ( 'NONE',  ( 21.13461538461538325, 11.30999384151886211, -211.1763045966511640 ) ) ;
#147398=DIRECTION ( 'NONE',  ( -1.000000000000000000, 0.000000000000000000, 0.000000000000000000 ) ) ;
#147399=AXIS2_PLACEMENT_3D ( 'NONE', #73532, #35691, #74824 ) ;
#147428=EDGE_LOOP ( 'NONE', ( #166718, #28069, #137108, #245348 ) ) ;
#147436=CARTESIAN_POINT ( 'NONE',  ( 21.04999999999902371, 11.91025941954771739, -206.1395922244702490 ) ) ;
#147505=CARTESIAN_POINT ( 'NONE',  ( -21.08198257630413508, -1.277454622087745850, -194.7930808841681198 ) ) ;
#147536=DIRECTION ( 'NONE',  ( -1.040834085586103947E-13, 0.9770955615653551529, 0.2128009952262517601 ) ) ;
#147598=EDGE_LOOP ( 'NONE', ( #27788, #95080, #215708, #88628 ) ) ;
#147609=ADVANCED_FACE ( 'NONE', ( #229382 ), #98800, .F. ) ;
#147628=CARTESIAN_POINT ( 'NONE',  ( 20.94999999999999574, 0.6656436123793491033, -212.6810495496487476 ) ) ;
#147633=ORIENTED_EDGE ( 'NONE', *, *, #6655, .T. ) ;
#147636=DIRECTION ( 'NONE',  ( 1.000000000000000000, 0.000000000000000000, 0.000000000000000000 ) ) ;
#147654=CIRCLE ( 'NONE', #31556, 1.899999999999995914 ) ;
#147685=( BOUNDED_SURFACE ( )  B_SPLINE_SURFACE ( 3, 2, ( 
 ( #236603, #37154, #78801 ),
 ( #17553, #215753, #15021 ),
 ( #97060, #57957, #95800 ),
 ( #217033, #59216, #154549 ),
 ( #134916, #38419, #235324 ),
 ( #35871, #175393, #138758 ),
 ( #218312, #39732, #20151 ),
 ( #179239, #555, #159657 ),
 ( #26578, #61840, #146485 ),
 ( #244306, #44838, #4413 ) ),
 .UNSPECIFIED., .F., .F., .F. ) 
 B_SPLINE_SURFACE_WITH_KNOTS ( ( 4, 2, 2, 2, 4 ),
 ( 3, 3 ),
 ( 0.0001836757140119173052, 0.0004000170051583524936, 0.0005081876507315700878, 0.0005622729735181788849, 0.0006163582963047876820 ),
 ( 0.000000000000000000, 1.000000000000000000 ),
 .UNSPECIFIED. ) 
 GEOMETRIC_REPRESENTATION_ITEM ( )  RATIONAL_B_SPLINE_SURFACE ( (
 ( 1.000000000000000000, 0.7071067811865414665, 1.000000000000000000),
 ( 1.000000000000000000, 0.6461995200012695673, 1.000000000000000000),
 ( 1.000000000000000000, 0.5776453529573633006, 1.000000000000000000),
 ( 1.000000000000000000, 0.4585233068339978346, 1.000000000000000000),
 ( 1.000000000000000000, 0.4154092989970996630, 1.000000000000000000),
 ( 1.000000000000000000, 0.3550093145823429164, 1.000000000000000000),
 ( 1.000000000000000000, 0.3354498651681590560, 1.000000000000000000),
 ( 1.000000000000000000, 0.3060347992261199246, 1.000000000000000000),
 ( 1.000000000000000000, 0.2963555829624707760, 1.000000000000000000),
 ( 1.000000000000000000, 0.2966190024559251515, 1.000000000000000000) ) ) 
 REPRESENTATION_ITEM ( '' )  SURFACE ( )  );
#147767=VERTEX_POINT ( 'NONE', #124828 ) ;
#147807=LINE ( 'NONE', #164798, #198153 ) ;
#147821=CARTESIAN_POINT ( 'NONE',  ( 20.94999999999999574, 17.02177226667169663, -224.5487030889150901 ) ) ;
#147852=AXIS2_PLACEMENT_3D ( 'NONE', #155714, #202509, #47263 ) ;
#147873=CARTESIAN_POINT ( 'NONE',  ( 23.14999999999999858, 1.148907358139439339E-11, -201.0000000000015064 ) ) ;
#147919=EDGE_CURVE ( 'NONE', #185124, #58187, #131619, .T. ) ;
#147986=CARTESIAN_POINT ( 'NONE',  ( -23.15000000000000213, 5.256951610580939516, -213.3897168960460533 ) ) ;
#148003=LINE ( 'NONE', #108869, #232540 ) ;
#148014=CARTESIAN_POINT ( 'NONE',  ( 21.13461538461538325, 11.30999384151886211, -211.1763045966511640 ) ) ;
#148019=ORIENTED_EDGE ( 'NONE', *, *, #95349, .F. ) ;
#148022=DIRECTION ( 'NONE',  ( 0.000000000000000000, 0.2128009952263485993, -0.9770955615653341697 ) ) ;
#148023=EDGE_CURVE ( 'NONE', #156064, #163980, #253735, .T. ) ;
#148032=EDGE_CURVE ( 'NONE', #87352, #201117, #35957, .T. ) ;
#148059=CARTESIAN_POINT ( 'NONE',  ( -20.64999999999999858, 9.614325556249161409, -211.5456030694648746 ) ) ;
#148073=VERTEX_POINT ( 'NONE', #119385 ) ;
#148080=DIRECTION ( 'NONE',  ( 0.000000000000000000, 0.2128009952263601456, -0.9770955615653315052 ) ) ;
#148092=ADVANCED_FACE ( 'NONE', ( #200205 ), #223370, .F. ) ;
#148097=CYLINDRICAL_SURFACE ( 'NONE', #227589, 0.09999999999999810429 ) ;
#148106=EDGE_CURVE ( 'NONE', #32893, #236679, #23691, .T. ) ;
#148114=VERTEX_POINT ( 'NONE', #181922 ) ;
#148121=CARTESIAN_POINT ( 'NONE',  ( -23.25000000000000000, 6.738188228664430568, -211.9673068433082790 ) ) ;
#148126=DIRECTION ( 'NONE',  ( -0.7071067811865302533, 0.6909108974501196876, 0.1504730267679053324 ) ) ;
#148139=DIRECTION ( 'NONE',  ( 1.000000000000000000, 0.000000000000000000, 0.000000000000000000 ) ) ;
#148141=DIRECTION ( 'NONE',  ( -0.000000000000000000, -0.9770955615653313941, -0.2128009952263603677 ) ) ;
#148160=AXIS2_PLACEMENT_3D ( 'NONE', #225569, #122666, #46936 ) ;
#148168=ORIENTED_EDGE ( 'NONE', *, *, #65801, .F. ) ;
#148191=CIRCLE ( 'NONE', #252234, 2.000000000000003109 ) ;
#148206=ORIENTED_EDGE ( 'NONE', *, *, #244222, .T. ) ;
#148216=CIRCLE ( 'NONE', #85636, 6.329289321881352848 ) ;
#148235=LINE ( 'NONE', #206932, #21767 ) ;
#148255=EDGE_CURVE ( 'NONE', #182409, #245093, #235846, .T. ) ;
#148269=DIRECTION ( 'NONE',  ( 0.000000000000000000, 0.2128009952263605342, -0.9770955615653315052 ) ) ;
#148287=DIRECTION ( 'NONE',  ( -1.000000000000000000, -3.190570557967288949E-16, -6.948722487160392945E-17 ) ) ;
#148297=EDGE_CURVE ( 'NONE', #236905, #167762, #127730, .T. ) ;
#148300=EDGE_CURVE ( 'NONE', #97885, #239248, #2792, .T. ) ;
#148322=ORIENTED_EDGE ( 'NONE', *, *, #45596, .T. ) ;
#148326=CYLINDRICAL_SURFACE ( 'NONE', #186424, 0.1000000000000055844 ) ;
#148385=DIRECTION ( 'NONE',  ( -0.000000000000000000, -0.2128009952263603677, 0.9770955615653313941 ) ) ;
#148390=( BOUNDED_SURFACE ( )  B_SPLINE_SURFACE ( 3, 2, ( 
 ( #203955, #4465, #202670 ),
 ( #185688, #227373, #164846 ),
 ( #48730, #128288, #108717 ),
 ( #3171, #24064, #103553 ),
 ( #7039, #82691, #125704 ),
 ( #183128, #162285, #205225 ) ),
 .UNSPECIFIED., .F., .F., .F. ) 
 B_SPLINE_SURFACE_WITH_KNOTS ( ( 4, 2, 4 ),
 ( 3, 3 ),
 ( 0.0001342700090130058096, 0.0002909192928057405345, 0.0004475685765984752595 ),
 ( 0.000000000000000000, 1.000000000000000000 ),
 .UNSPECIFIED. ) 
 GEOMETRIC_REPRESENTATION_ITEM ( )  RATIONAL_B_SPLINE_SURFACE ( (
 ( 1.000000000000000000, 0.7250110520819763593, 1.000000000000000000),
 ( 1.000000000000000000, 0.7257599279143153170, 1.000000000000000000),
 ( 1.000000000000000000, 0.7137594617271856290, 1.000000000000000000),
 ( 1.000000000000000000, 0.6959270178822787312, 1.000000000000000000),
 ( 1.000000000000000000, 0.6919879549328636914, 1.000000000000000000),
 ( 1.000000000000000000, 0.7071067811866138531, 1.000000000000000000) ) ) 
 REPRESENTATION_ITEM ( '' )  SURFACE ( )  );
#148425=ORIENTED_EDGE ( 'NONE', *, *, #7318, .T. ) ;
#148429=EDGE_CURVE ( 'NONE', #142529, #93777, #169264, .T. ) ;
#148434=DIRECTION ( 'NONE',  ( -0.000000000000000000, 0.9770955615653316162, 0.2128009952263604232 ) ) ;
#148465=DIRECTION ( 'NONE',  ( 1.000000000000000000, 0.000000000000000000, 0.000000000000000000 ) ) ;
#148474=FACE_OUTER_BOUND ( 'NONE', #60417, .T. ) ;
#148487=ORIENTED_EDGE ( 'NONE', *, *, #35859, .F. ) ;
#148499=ORIENTED_EDGE ( 'NONE', *, *, #33260, .F. ) ;
#148504=LINE ( 'NONE', #109346, #97327 ) ;
#148510=CARTESIAN_POINT ( 'NONE',  ( -18.57399277249657032, 18.41291479239798434, -236.9963116028434058 ) ) ;
#148515=CARTESIAN_POINT ( 'NONE',  ( 20.94999999999999929, 7.980037321000004624, -237.6410835587014390 ) ) ;
#148522=CARTESIAN_POINT ( 'NONE',  ( 18.48413544395651442, -0.8919438430603255918, -242.3193070551389496 ) ) ;
#148550=ORIENTED_EDGE ( 'NONE', *, *, #163318, .T. ) ;
#148592=CARTESIAN_POINT ( 'NONE',  ( 21.05000000000000071, 7.980037321000004624, -237.6410835587014390 ) ) ;
#148593=ADVANCED_FACE ( 'NONE', ( #205001 ), #26409, .F. ) ;
#148651=AXIS2_PLACEMENT_3D ( 'NONE', #142040, #217713, #36570 ) ;
#148688=DIRECTION ( 'NONE',  ( 0.000000000000000000, 0.3427706569149635563, -0.9394191166662964054 ) ) ;
#148702=VERTEX_POINT ( 'NONE', #24500 ) ;
#148722=CARTESIAN_POINT ( 'NONE',  ( -23.15000000000000213, -4.892732937820631456, -233.2805462221312496 ) ) ;
#148751=EDGE_CURVE ( 'NONE', #93645, #64897, #198619, .T. ) ;
#148754=ADVANCED_FACE ( 'NONE', ( #246104 ), #10046, .F. ) ;
#148760=CARTESIAN_POINT ( 'NONE',  ( -18.59999999999999787, 7.128833340094563376, -233.7327013124401276 ) ) ;
#148767=CARTESIAN_POINT ( 'NONE',  ( 21.13614978966382196, -1.383015948619066959, -194.6497536416913761 ) ) ;
#148788=DIRECTION ( 'NONE',  ( 0.000000000000000000, -0.9770955615653316162, -0.2128009952263604232 ) ) ;
#148791=CARTESIAN_POINT ( 'NONE',  ( 22.48508240969612615, -2.433917398835509616, -189.6069785549278208 ) ) ;
#148793=DIRECTION ( 'NONE',  ( 0.000000000000000000, 0.2128009952263603677, -0.9770955615653313941 ) ) ;
#148800=CARTESIAN_POINT ( 'NONE',  ( -21.08884785362073089, -1.304174234192418069, -194.7778206845017337 ) ) ;
#148802=CARTESIAN_POINT ( 'NONE',  ( 21.05000000000000071, -5.637547571910522137, -233.4427589080015650 ) ) ;
#148817=EDGE_CURVE ( 'NONE', #109970, #633, #115414, .T. ) ;
#148842=FACE_OUTER_BOUND ( 'NONE', #220176, .T. ) ;
#148865=AXIS2_PLACEMENT_3D ( 'NONE', #177315, #20794, #181145 ) ;
#148888=VERTEX_POINT ( 'NONE', #93423 ) ;
#148894=CARTESIAN_POINT ( 'NONE',  ( 18.49999999999999289, 15.23147493058208113, -222.9643141222125848 ) ) ;
#148898=AXIS2_PLACEMENT_3D ( 'NONE', #196795, #18169, #36480 ) ;
#148914=CIRCLE ( 'NONE', #253120, 7.900000000000011013 ) ;
#148938=LINE ( 'NONE', #188057, #165560 ) ;
#148957=CARTESIAN_POINT ( 'NONE',  ( 23.14999999999999147, 1.148907358139439339E-11, -201.0000000000015064 ) ) ;
#148967=CIRCLE ( 'NONE', #28177, 0.1000000000000054040 ) ;
#148978=DIRECTION ( 'NONE',  ( -1.000000000000000000, -0.000000000000000000, -0.000000000000000000 ) ) ;
#148979=VERTEX_POINT ( 'NONE', #65861 ) ;
#148995=CARTESIAN_POINT ( 'NONE',  ( -21.59142135623730852, 12.17094120733686680, -219.9950833145813363 ) ) ;
#149013=ORIENTED_EDGE ( 'NONE', *, *, #58330, .F. ) ;
#149019=ORIENTED_EDGE ( 'NONE', *, *, #160345, .F. ) ;
#149036=DIRECTION ( 'NONE',  ( 2.259780016855444678E-14, 0.9984213852963244040, 0.05616704890742149625 ) ) ;
#149041=CARTESIAN_POINT ( 'NONE',  ( 18.59999999999999076, 16.67126802362266247, -222.8016931105129004 ) ) ;
#149042=FACE_OUTER_BOUND ( 'NONE', #236121, .T. ) ;
#149064=EDGE_CURVE ( 'NONE', #170209, #2973, #164966, .T. ) ;
#149071=DIRECTION ( 'NONE',  ( -1.000000000000000000, -3.190570557967288949E-16, -6.948722487160392945E-17 ) ) ;
#149075=VERTEX_POINT ( 'NONE', #162416 ) ;
#149138=DIRECTION ( 'NONE',  ( 1.000000000000000000, -7.136802563874199107E-16, -1.554319503706929991E-16 ) ) ;
#149139=CIRCLE ( 'NONE', #3336, 0.1000000000000054040 ) ;
#149147=CARTESIAN_POINT ( 'NONE',  ( -22.24259225415828567, 7.299257922272452959, -199.3089113299467954 ) ) ;
#149175=DIRECTION ( 'NONE',  ( 1.000000000000000000, 3.190570557967288949E-16, 6.948722487160392945E-17 ) ) ;
#149177=ORIENTED_EDGE ( 'NONE', *, *, #524, .F. ) ;
#149181=CARTESIAN_POINT ( 'NONE',  ( -20.91682497891423154, 18.39833411442327105, -236.9692678682430085 ) ) ;
#149184=EDGE_CURVE ( 'NONE', #75595, #218226, #61445, .T. ) ;
#149211=CARTESIAN_POINT ( 'NONE',  ( 20.93284271247462414, 17.11694853917244075, -224.3781540347815735 ) ) ;
#149218=DIRECTION ( 'NONE',  ( 0.000000000000000000, 0.2128009952263601456, -0.9770955615653316162 ) ) ;
#149221=ORIENTED_EDGE ( 'NONE', *, *, #251364, .F. ) ;
#149236=ORIENTED_EDGE ( 'NONE', *, *, #191646, .T. ) ;
#149242=CIRCLE ( 'NONE', #107515, 0.2000000000000111688 ) ;
#149247=ORIENTED_EDGE ( 'NONE', *, *, #221157, .T. ) ;
#149256=CARTESIAN_POINT ( 'NONE',  ( 23.15000000000000213, -3.664072692419559907, -226.4691047342518857 ) ) ;
#149272=CARTESIAN_POINT ( 'NONE',  ( -18.50000000000000355, -7.567701079425762423, -210.0537230116848377 ) ) ;
#149299=DIRECTION ( 'NONE',  ( 0.000000000000000000, -0.9968797965484670343, -0.07893460099023182075 ) ) ;
#149304=CARTESIAN_POINT ( 'NONE',  ( -20.94999999999999929, 0.6656436123793491033, -212.6810495496487476 ) ) ;
#149332=CARTESIAN_POINT ( 'NONE',  ( 23.24999999999999289, 9.083217576421224848, -211.4565844547649931 ) ) ;
#149333=CARTESIAN_POINT ( 'NONE',  ( 23.24999999999999645, 9.374458193048763377, -220.5475659691911119 ) ) ;
#149358=VECTOR ( 'NONE', #48293, 1000.000000000000227 ) ;
#149382=EDGE_CURVE ( 'NONE', #92185, #166165, #60745, .T. ) ;
#149415=AXIS2_PLACEMENT_3D ( 'NONE', #29179, #89100, #133377 ) ;
#149433=AXIS2_PLACEMENT_3D ( 'NONE', #31352, #109547, #151277 ) ;
#149438=EDGE_CURVE ( 'NONE', #227124, #21586, #219828, .T. ) ;
#149458=EDGE_CURVE ( 'NONE', #232107, #225466, #61714, .T. ) ;
#149473=VECTOR ( 'NONE', #108318, 1000.000000000000227 ) ;
#149483=ORIENTED_EDGE ( 'NONE', *, *, #109540, .F. ) ;
#149493=ORIENTED_EDGE ( 'NONE', *, *, #198651, .T. ) ;
#149526=LINE ( 'NONE', #106495, #140504 ) ;
#149527=CIRCLE ( 'NONE', #78747, 0.2000000000000122791 ) ;
#149564=VERTEX_POINT ( 'NONE', #49843 ) ;
#149571=ADVANCED_FACE ( 'NONE', ( #227197 ), #168571, .F. ) ;
#149572=ORIENTED_EDGE ( 'NONE', *, *, #114224, .T. ) ;
#149607=ORIENTED_EDGE ( 'NONE', *, *, #181322, .T. ) ;
#149616=CARTESIAN_POINT ( 'NONE',  ( -23.25000000000000000, 1.148907358139439339E-11, -201.0000000000015064 ) ) ;
#149662=CARTESIAN_POINT ( 'NONE',  ( 21.00000000000000000, 12.15477401631902232, -210.9923204818763622 ) ) ;
#149665=ORIENTED_EDGE ( 'NONE', *, *, #239184, .F. ) ;
#149673=FACE_OUTER_BOUND ( 'NONE', #90749, .T. ) ;
#149677=EDGE_CURVE ( 'NONE', #115886, #154024, #111106, .T. ) ;
#149681=CIRCLE ( 'NONE', #120470, 11.74999999999999289 ) ;
#149700=ORIENTED_EDGE ( 'NONE', *, *, #161726, .T. ) ;
#149776=DIRECTION ( 'NONE',  ( 1.000000000000000000, 0.000000000000000000, 0.000000000000000000 ) ) ;
#149791=ORIENTED_EDGE ( 'NONE', *, *, #122890, .T. ) ;
#149796=CIRCLE ( 'NONE', #187200, 0.1000000000000054040 ) ;
#149800=EDGE_CURVE ( 'NONE', #26422, #114396, #99194, .T. ) ;
#149804=CIRCLE ( 'NONE', #74971, 11.65000000000001457 ) ;
#149834=DIRECTION ( 'NONE',  ( 0.000000000000000000, 0.2128009952263603677, -0.9770955615653313941 ) ) ;
#149845=ORIENTED_EDGE ( 'NONE', *, *, #109616, .T. ) ;
#149884=ORIENTED_EDGE ( 'NONE', *, *, #43772, .F. ) ;
#149984=CARTESIAN_POINT ( 'NONE',  ( 23.25000000000000355, -20.49622690151871396, -212.4170162771926016 ) ) ;
#150014=CARTESIAN_POINT ( 'NONE',  ( -20.64999999999999858, 4.625797360122408719, -213.1224017332881431 ) ) ;
#150127=TOROIDAL_SURFACE ( 'NONE', #12570, 0.2000000000000000111, 0.1000000000000000056 ) ;
#150143=DIRECTION ( 'NONE',  ( 0.000000000000000000, 0.9770955615653551529, 0.2128009952262517601 ) ) ;
#150160=FACE_OUTER_BOUND ( 'NONE', #153388, .T. ) ;
#150193=VECTOR ( 'NONE', #125624, 1000.000000000000000 ) ;
#150214=ADVANCED_FACE ( 'NONE', ( #239739 ), #218865, .F. ) ;
#150232=DIRECTION ( 'NONE',  ( 0.7071359030027619674, 0.6908824414808002468, 0.1504668293611484409 ) ) ;
#150246=ORIENTED_EDGE ( 'NONE', *, *, #119760, .F. ) ;
#150248=ORIENTED_EDGE ( 'NONE', *, *, #145945, .T. ) ;
#150264=ORIENTED_EDGE ( 'NONE', *, *, #148297, .F. ) ;
#150278=AXIS2_PLACEMENT_3D ( 'NONE', #240072, #40623, #100514 ) ;
#150299=EDGE_LOOP ( 'NONE', ( #250619, #64658, #182283, #164887 ) ) ;
#150313=DIRECTION ( 'NONE',  ( 0.000000000000000000, -0.9550021345545530727, 0.2965989261549131228 ) ) ;
#150371=EDGE_CURVE ( 'NONE', #11889, #145377, #157119, .T. ) ;
#150395=CARTESIAN_POINT ( 'NONE',  ( 20.94999999999999929, 17.06838326776701109, -224.6250846885016870 ) ) ;
#150402=DIRECTION ( 'NONE',  ( 2.952720810173289112E-16, -0.9770955615653318382, -0.2128009952263588411 ) ) ;
#150411=CARTESIAN_POINT ( 'NONE',  ( 18.54147908293611735, -7.746487623352177110, -209.9012881796168983 ) ) ;
#150413=ORIENTED_EDGE ( 'NONE', *, *, #76968, .F. ) ;
#150443=CARTESIAN_POINT ( 'NONE',  ( 18.59999999999999076, 7.128833340094563376, -233.7327013124401276 ) ) ;
#150489=DIRECTION ( 'NONE',  ( 0.000000000000000000, 0.2128009952263604232, -0.9770955615653316162 ) ) ;
#150499=CARTESIAN_POINT ( 'NONE',  ( -18.59999999999999787, 11.74265569217025629, -210.9797313238103698 ) ) ;
#150530=CARTESIAN_POINT ( 'NONE',  ( -23.15000000000000213, 14.06640494040441602, -210.3712993791105532 ) ) ;
#150543=CARTESIAN_POINT ( 'NONE',  ( -18.43473496883412466, -7.778107375242646171, -209.9050251632729100 ) ) ;
#150544=VERTEX_POINT ( 'NONE', #176579 ) ;
#150547=ORIENTED_EDGE ( 'NONE', *, *, #135527, .T. ) ;
#150560=ADVANCED_FACE ( 'NONE', ( #233961 ), #232701, .T. ) ;
#150573=DIRECTION ( 'NONE',  ( -1.000000000000000000, -0.000000000000000000, -0.000000000000000000 ) ) ;
#150575=CARTESIAN_POINT ( 'NONE',  ( 23.14999999999999503, 10.80300742114540391, -220.2930047078982625 ) ) ;
#150626=CARTESIAN_POINT ( 'NONE',  ( -18.59999999999999787, -7.567701079425722455, -210.0537230116848662 ) ) ;
#150628=ORIENTED_EDGE ( 'NONE', *, *, #39161, .F. ) ;
#150674=VECTOR ( 'NONE', #26928, 999.9999999999998863 ) ;
#150697=EDGE_CURVE ( 'NONE', #122837, #207244, #139971, .T. ) ;
#150709=CARTESIAN_POINT ( 'NONE',  ( 18.46905048506371116, -0.7072635980893239305, -242.2718000941648882 ) ) ;
#150754=ORIENTED_EDGE ( 'NONE', *, *, #28656, .T. ) ;
#150841=VERTEX_POINT ( 'NONE', #206398 ) ;
#150855=ORIENTED_EDGE ( 'NONE', *, *, #85206, .T. ) ;
#150892=FACE_OUTER_BOUND ( 'NONE', #14885, .T. ) ;
#150908=CARTESIAN_POINT ( 'NONE',  ( -22.59999999999999787, 1.148907358139439339E-11, -201.0000000000015064 ) ) ;
#150925=DIRECTION ( 'NONE',  ( 0.000000000000000000, 0.2128009952263603122, -0.9770955615653315052 ) ) ;
#150939=CIRCLE ( 'NONE', #138434, 0.5999999999999987566 ) ;
#150972=CARTESIAN_POINT ( 'NONE',  ( 20.87600722750343252, 18.41291479239798079, -236.9963116028434058 ) ) ;
#150974=ORIENTED_EDGE ( 'NONE', *, *, #71168, .F. ) ;
#150982=FACE_OUTER_BOUND ( 'NONE', #235913, .T. ) ;
#151045=CIRCLE ( 'NONE', #217652, 0.5000000000000007772 ) ;
#151057=ORIENTED_EDGE ( 'NONE', *, *, #253196, .T. ) ;
#151108=DIRECTION ( 'NONE',  ( 2.952720810173288126E-16, -0.9770955615653313941, -0.2128009952263603677 ) ) ;
#151110=EDGE_CURVE ( 'NONE', #110145, #6661, #236559, .T. ) ;
#151121=CIRCLE ( 'NONE', #255104, 0.1000000000000048489 ) ;
#151170=ORIENTED_EDGE ( 'NONE', *, *, #179533, .F. ) ;
#151189=CARTESIAN_POINT ( 'NONE',  ( 23.24999999999999645, 9.180734019381761257, -233.2858192224647382 ) ) ;
#151261=CARTESIAN_POINT ( 'NONE',  ( -21.05000000000000426, -1.387982811671854444, -194.7102154522737578 ) ) ;
#151277=DIRECTION ( 'NONE',  ( 0.000000000000000000, 0.2128009952263601456, -0.9770955615653316162 ) ) ;
#151301=CARTESIAN_POINT ( 'NONE',  ( 18.49999999999999289, 15.22030141505243961, -222.9130098973476777 ) ) ;
#151325=EDGE_CURVE ( 'NONE', #245608, #125678, #79492, .T. ) ;
#151327=FACE_OUTER_BOUND ( 'NONE', #104954, .T. ) ;
#151336=CARTESIAN_POINT ( 'NONE',  ( -21.05000000000000071, 4.158309866074138661, -211.9342015984041439 ) ) ;
#151346=ORIENTED_EDGE ( 'NONE', *, *, #24146, .F. ) ;
#151350=ADVANCED_FACE ( 'NONE', ( #173532 ), #81344, .T. ) ;
#151356=EDGE_CURVE ( 'NONE', #167415, #206865, #61975, .T. ) ;
#151357=AXIS2_PLACEMENT_3D ( 'NONE', #79849, #216810, #36940 ) ;
#151358=DIRECTION ( 'NONE',  ( 0.000000000000000000, 0.2128009952263403282, -0.9770955615653358350 ) ) ;
#151367=CARTESIAN_POINT ( 'NONE',  ( 22.46250603428203618, -2.458442580695145985, -189.6124709730212032 ) ) ;
#151374=AXIS2_PLACEMENT_3D ( 'NONE', #191815, #50960, #28909 ) ;
#151388=ORIENTED_EDGE ( 'NONE', *, *, #199456, .T. ) ;
#151403=DIRECTION ( 'NONE',  ( 0.000000000000000000, 0.2128009952263601179, -0.9770955615653315052 ) ) ;
#151409=CARTESIAN_POINT ( 'NONE',  ( -23.25000000000000000, 8.576967729067776602, -220.8801565530754090 ) ) ;
#151433=DIRECTION ( 'NONE',  ( 1.000000000000000000, 8.034189347746079853E-16, -2.566115377699052699E-16 ) ) ;
#151439=DIRECTION ( 'NONE',  ( 0.000000000000000000, -0.2128009952263403282, 0.9770955615653358350 ) ) ;
#151445=VECTOR ( 'NONE', #85592, 1000.000000000000000 ) ;
#151449=DIRECTION ( 'NONE',  ( 0.000000000000000000, 0.2128009952263403282, -0.9770955615653358350 ) ) ;
#151516=DIRECTION ( 'NONE',  ( 0.000000000000000000, -0.9770955615653316162, -0.2128009952263604232 ) ) ;
#151523=DIRECTION ( 'NONE',  ( 0.7070776581709139474, -0.6909393522474895910, -0.1504792239193035175 ) ) ;
#151532=LINE ( 'NONE', #119777, #16341 ) ;
#151535=VERTEX_POINT ( 'NONE', #191482 ) ;
#151554=ORIENTED_EDGE ( 'NONE', *, *, #175832, .F. ) ;
#151572=ORIENTED_EDGE ( 'NONE', *, *, #219243, .F. ) ;
#151599=VECTOR ( 'NONE', #105939, 1000.000000000000000 ) ;
#151608=CARTESIAN_POINT ( 'NONE',  ( 21.05000000000000071, 8.592460621936744758, -209.2032282544143698 ) ) ;
#151619=CARTESIAN_POINT ( 'NONE',  ( -23.15000000000000213, 4.662003332185090443, -213.0075696128765514 ) ) ;
#151624=DIRECTION ( 'NONE',  ( 5.603264701231743991E-32, -0.2128009952263605620, 0.9770955615653313941 ) ) ;
#151629=DIRECTION ( 'NONE',  ( 1.000000000000000000, 0.000000000000000000, 0.000000000000000000 ) ) ;
#151631=ORIENTED_EDGE ( 'NONE', *, *, #254001, .F. ) ;
#151633=EDGE_CURVE ( 'NONE', #94400, #163287, #176581, .T. ) ;
#151637=ORIENTED_EDGE ( 'NONE', *, *, #170446, .F. ) ;
#151643=AXIS2_PLACEMENT_3D ( 'NONE', #199192, #143040, #242154 ) ;
#151649=DIRECTION ( 'NONE',  ( 0.000000000000000000, -0.9770955615653315052, -0.2128009952263603954 ) ) ;
#151661=CARTESIAN_POINT ( 'NONE',  ( 23.15000000000000213, -4.914013037343258894, -233.1828366659746905 ) ) ;
#151697=VECTOR ( 'NONE', #198809, 1000.000000000000227 ) ;
#151731=DIRECTION ( 'NONE',  ( 0.000000000000000000, -0.2128009952263734406, 0.9770955615653287296 ) ) ;
#151766=CIRCLE ( 'NONE', #89187, 0.1000000000000055844 ) ;
#151789=ADVANCED_FACE ( 'NONE', ( #9608 ), #183130, .T. ) ;
#151807=ORIENTED_EDGE ( 'NONE', *, *, #229619, .F. ) ;
#151822=ORIENTED_EDGE ( 'NONE', *, *, #240275, .T. ) ;
#151823=AXIS2_PLACEMENT_3D ( 'NONE', #94353, #213026, #154384 ) ;
#151845=CARTESIAN_POINT ( 'NONE',  ( -18.51555513499438987, -7.607300382162530461, -210.0206232990065587 ) ) ;
#151876=EDGE_CURVE ( 'NONE', #57651, #160183, #96679, .T. ) ;
#151945=CIRCLE ( 'NONE', #122727, 7.900000000000007461 ) ;
#151950=CARTESIAN_POINT ( 'NONE',  ( -18.59999999999999787, 3.132039894996829776, -190.2813437854022993 ) ) ;
#151963=DIRECTION ( 'NONE',  ( 0.000000000000000000, -0.2128009952263485993, 0.9770955615653341697 ) ) ;
#151986=ADVANCED_FACE ( 'NONE', ( #119002 ), #82962, .T. ) ;
#151988=CARTESIAN_POINT ( 'NONE',  ( 20.12500000000000000, 11.25287472715600146, -206.8511660127314826 ) ) ;
#152004=DIRECTION ( 'NONE',  ( 0.000000000000000000, -0.9770955615653316162, -0.2128009952263604232 ) ) ;
#152019=DIRECTION ( 'NONE',  ( 1.000000000000000000, -0.000000000000000000, -0.000000000000000000 ) ) ;
#152085=EDGE_LOOP ( 'NONE', ( #193886, #149845 ) ) ;
#152094=EDGE_CURVE ( 'NONE', #21586, #27420, #257911, .T. ) ;
#152103=AXIS2_PLACEMENT_3D ( 'NONE', #220387, #24772, #200816 ) ;
#152131=DIRECTION ( 'NONE',  ( -0.000000000000000000, -0.2128009952263603677, 0.9770955615653313941 ) ) ;
#152133=LINE ( 'NONE', #110407, #105942 ) ;
#152142=ADVANCED_FACE ( 'NONE', ( #245365 ), #65427, .T. ) ;
#152170=EDGE_CURVE ( 'NONE', #164707, #16838, #83668, .T. ) ;
#152191=DIRECTION ( 'NONE',  ( 0.000000000000000000, 0.2128009952263485993, -0.9770955615653341697 ) ) ;
#152214=ORIENTED_EDGE ( 'NONE', *, *, #168839, .F. ) ;
#152216=FACE_OUTER_BOUND ( 'NONE', #28560, .T. ) ;
#152218=CARTESIAN_POINT ( 'NONE',  ( -21.45000000000000284, 10.16011026985487398, -211.4267369781599939 ) ) ;
#152225=CARTESIAN_POINT ( 'NONE',  ( -22.39999999999999858, 11.48087284840413425, -198.4995883060917947 ) ) ;
#152231=ORIENTED_EDGE ( 'NONE', *, *, #60314, .T. ) ;
#152232=CARTESIAN_POINT ( 'NONE',  ( -23.15000000000000213, 6.857177884343597540, -212.0437362999421680 ) ) ;
#152254=ORIENTED_EDGE ( 'NONE', *, *, #221556, .T. ) ;
#152257=DIRECTION ( 'NONE',  ( -0.000000000000000000, -0.7397890806274223241, -0.6728388485993012091 ) ) ;
#152268=ORIENTED_EDGE ( 'NONE', *, *, #69677, .F. ) ;
#152287=CARTESIAN_POINT ( 'NONE',  ( -21.05000000000000071, 6.119053122312926973, -199.6316501170689719 ) ) ;
#152302=( BOUNDED_CURVE ( )  B_SPLINE_CURVE ( 3, ( #196962, #108774, #149211, #195723 ),
 .UNSPECIFIED., .F., .T. ) 
 B_SPLINE_CURVE_WITH_KNOTS ( ( 4, 4 ),
 ( 4.712388980384690562, 6.283185307179586232 ),
 .UNSPECIFIED. ) 
 CURVE ( )  GEOMETRIC_REPRESENTATION_ITEM ( )  RATIONAL_B_SPLINE_CURVE ( ( 1.000000000000000000, 0.8047378541243652705, 0.8047378541243652705, 1.000000000000000000 ) ) 
 REPRESENTATION_ITEM ( '' )  );
#152308=DIRECTION ( 'NONE',  ( 0.000000000000000000, -0.9968797965484670343, -0.07893460099023182075 ) ) ;
#152384=AXIS2_PLACEMENT_3D ( 'NONE', #40633, #21053, #254466 ) ;
#152385=DIRECTION ( 'NONE',  ( 0.000000000000000000, 0.6728388485993177515, -0.7397890806274072251 ) ) ;
#152424=ORIENTED_EDGE ( 'NONE', *, *, #6445, .F. ) ;
#152455=EDGE_LOOP ( 'NONE', ( #91842, #185749 ) ) ;
#152462=DIRECTION ( 'NONE',  ( 0.000000000000000000, 0.9752329468386375932, 0.2211802418852714114 ) ) ;
#152473=ORIENTED_EDGE ( 'NONE', *, *, #159107, .F. ) ;
#152474=CIRCLE ( 'NONE', #185760, 0.1000000000000055844 ) ;
#152479=ADVANCED_FACE ( 'NONE', ( #195678 ), #117395, .F. ) ;
#152491=EDGE_LOOP ( 'NONE', ( #251387, #56846, #397, #56812 ) ) ;
#152533=DIRECTION ( 'NONE',  ( 0.000000000000000000, -0.2128009952263485993, 0.9770955615653341697 ) ) ;
#152555=CARTESIAN_POINT ( 'NONE',  ( -20.64999999999999858, -7.079251802663312887, -212.6676826711374417 ) ) ;
#152563=LINE ( 'NONE', #234630, #24068 ) ;
#152565=AXIS2_PLACEMENT_3D ( 'NONE', #134110, #192831, #72908 ) ;
#152586=TOROIDAL_SURFACE ( 'NONE', #85877, 3.899999999999999467, 0.1000000000000000056 ) ;
#152616=CIRCLE ( 'NONE', #198359, 0.1000000000000073330 ) ;
#152647=EDGE_CURVE ( 'NONE', #98041, #248715, #99898, .T. ) ;
#152652=CYLINDRICAL_SURFACE ( 'NONE', #3555, 11.80000000000000959 ) ;
#152655=AXIS2_PLACEMENT_3D ( 'NONE', #138741, #179224, #81343 ) ;
#152690=EDGE_CURVE ( 'NONE', #120381, #174683, #54723, .T. ) ;
#152702=DIRECTION ( 'NONE',  ( 1.000000000000000000, 0.000000000000000000, 0.000000000000000000 ) ) ;
#152706=DIRECTION ( 'NONE',  ( 1.000000000000000000, 2.885090398161910739E-16, 6.283419270304611573E-17 ) ) ;
#152716=CIRCLE ( 'NONE', #169474, 0.3999999999999952482 ) ;
#152719=AXIS2_PLACEMENT_3D ( 'NONE', #39693, #35828, #234003 ) ;
#152736=CARTESIAN_POINT ( 'NONE',  ( -23.15000000000000213, -4.259020970815408091, -226.0869574510824123 ) ) ;
#152743=AXIS2_PLACEMENT_3D ( 'NONE', #116840, #196367, #17717 ) ;
#152753=DIRECTION ( 'NONE',  ( 0.000000000000000000, -0.9770955615653315052, -0.2128009952263603954 ) ) ;
#152763=CARTESIAN_POINT ( 'NONE',  ( 21.14999999999998082, -11.48087284838115885, -203.5004116939112464 ) ) ;
#152777=CYLINDRICAL_SURFACE ( 'NONE', #143357, 0.1000000000000054040 ) ;
#152789=CARTESIAN_POINT ( 'NONE',  ( 21.08035267497491105, 6.169086428650065734, -199.5718117947534438 ) ) ;
#152801=DIRECTION ( 'NONE',  ( -1.000000000000000000, 0.000000000000000000, 0.000000000000000000 ) ) ;
#152858=ORIENTED_EDGE ( 'NONE', *, *, #88771, .T. ) ;
#152878=AXIS2_PLACEMENT_3D ( 'NONE', #30931, #248659, #129973 ) ;
#152901=ORIENTED_EDGE ( 'NONE', *, *, #229902, .T. ) ;
#152923=ORIENTED_EDGE ( 'NONE', *, *, #197415, .T. ) ;
#152951=EDGE_CURVE ( 'NONE', #212023, #227433, #237497, .T. ) ;
#152961=ORIENTED_EDGE ( 'NONE', *, *, #75333, .T. ) ;
#152963=CARTESIAN_POINT ( 'NONE',  ( -23.15000000000000213, 7.958757221477368304, -237.5433740025449083 ) ) ;
#152966=DIRECTION ( 'NONE',  ( -7.304098846218132695E-16, 0.9770955615653315052, 0.2128009952263603954 ) ) ;
#152977=LINE ( 'NONE', #124099, #206033 ) ;
#152983=DIRECTION ( 'NONE',  ( 0.000000000000000000, 0.2128009952263604510, -0.9770955615653315052 ) ) ;
#152994=CARTESIAN_POINT ( 'NONE',  ( 22.39999999999999858, 7.591056067193225232, -199.2444047917219052 ) ) ;
#153012=ORIENTED_EDGE ( 'NONE', *, *, #13618, .F. ) ;
#153019=CARTESIAN_POINT ( 'NONE',  ( -21.59780538579341069, 6.669199007058423057, -199.4462207020707751 ) ) ;
#153032=DIRECTION ( 'NONE',  ( -3.265361837132813586E-16, 0.9770955615653315052, 0.2128009952263600901 ) ) ;
#153063=CARTESIAN_POINT ( 'NONE',  ( -22.60000000000094289, -2.401771312553118598, -189.4980873520050011 ) ) ;
#153066=VECTOR ( 'NONE', #149776, 1000.000000000000000 ) ;
#153067=AXIS2_PLACEMENT_3D ( 'NONE', #241923, #142804, #31908 ) ;
#153069=CARTESIAN_POINT ( 'NONE',  ( 20.94999999999999929, -4.735542975717121905, -233.2463119243910796 ) ) ;
#153086=ORIENTED_EDGE ( 'NONE', *, *, #31191, .F. ) ;
#153092=DIRECTION ( 'NONE',  ( 1.000000000000000000, 0.000000000000000000, 0.000000000000000000 ) ) ;
#153122=DIRECTION ( 'NONE',  ( 0.000000000000000000, -0.2128009952263678062, 0.9770955615653298398 ) ) ;
#153126=DIRECTION ( 'NONE',  ( 1.000000000000000000, -0.000000000000000000, -0.000000000000000000 ) ) ;
#153133=ORIENTED_EDGE ( 'NONE', *, *, #256490, .F. ) ;
#153152=CARTESIAN_POINT ( 'NONE',  ( -22.48660254037843487, 11.37252324248628632, -198.4720136275361710 ) ) ;
#153164=AXIS2_PLACEMENT_3D ( 'NONE', #117948, #77511, #194944 ) ;
#153198=DIRECTION ( 'NONE',  ( 0.000000000000000000, -0.9770955615653357240, -0.2128009952263406890 ) ) ;
#153199=LINE ( 'NONE', #208020, #16168 ) ;
#153226=FACE_OUTER_BOUND ( 'NONE', #170623, .T. ) ;
#153249=CARTESIAN_POINT ( 'NONE',  ( -18.59999999999999787, 13.56015509305096778, -219.7948714774209691 ) ) ;
#153256=CARTESIAN_POINT ( 'NONE',  ( 23.24999999999999289, 11.38316329224760892, -198.5208684056144079 ) ) ;
#153264=CIRCLE ( 'NONE', #219847, 4.300000000000024691 ) ;
#153270=DIRECTION ( 'NONE',  ( -1.000000000000000000, -1.794895427898103559E-16, -3.909090864890002444E-17 ) ) ;
#153279=CARTESIAN_POINT ( 'NONE',  ( 23.14999999999999858, 9.960715529987961503, -220.4198853720552904 ) ) ;
#153285=ORIENTED_EDGE ( 'NONE', *, *, #70913, .T. ) ;
#153297=ORIENTED_EDGE ( 'NONE', *, *, #188089, .F. ) ;
#153304=CARTESIAN_POINT ( 'NONE',  ( -20.85000000000000142, 7.804459559388684298, -245.4620200072988325 ) ) ;
#153322=CIRCLE ( 'NONE', #186624, 11.74999999999999289 ) ;
#153388=EDGE_LOOP ( 'NONE', ( #203212, #108219, #149177, #32824 ) ) ;
#153403=ORIENTED_EDGE ( 'NONE', *, *, #33293, .T. ) ;
#153424=ORIENTED_EDGE ( 'NONE', *, *, #168538, .F. ) ;
#153433=ORIENTED_EDGE ( 'NONE', *, *, #225038, .F. ) ;
#153441=EDGE_LOOP ( 'NONE', ( #23949, #95435, #83488, #170057 ) ) ;
#153454=LINE ( 'NONE', #97233, #80237 ) ;
#153472=DIRECTION ( 'NONE',  ( -1.000000000000000000, 0.000000000000000000, 0.000000000000000000 ) ) ;
#153490=AXIS2_PLACEMENT_3D ( 'NONE', #178921, #217981, #120235 ) ;
#153499=AXIS2_PLACEMENT_3D ( 'NONE', #175907, #54637, #115916 ) ;
#153513=CARTESIAN_POINT ( 'NONE',  ( 0.000000000000000000, 0.000000000000000000, 0.000000000000000000 ) ) ;
#153523=DIRECTION ( 'NONE',  ( 0.000000000000000000, 0.9770955615653313941, 0.2128009952263606452 ) ) ;
#153525=CARTESIAN_POINT ( 'NONE',  ( -21.14999999999999858, 11.40444339177023814, -198.6185779617709670 ) ) ;
#153566=CARTESIAN_POINT ( 'NONE',  ( -23.25000000000000000, -4.356730526971941408, -226.1082375506050539 ) ) ;
#153571=DIRECTION ( 'NONE',  ( 1.000000000000000000, -0.000000000000000000, -0.000000000000000000 ) ) ;
#153587=CARTESIAN_POINT ( 'NONE',  ( 20.90851465518105812, 18.40294846151842023, -236.9778203247716419 ) ) ;
#153603=CARTESIAN_POINT ( 'NONE',  ( -20.94999999999999929, 7.661991824395936845, -241.5144583139544636 ) ) ;
#153607=AXIS2_PLACEMENT_3D ( 'NONE', #109580, #209990, #86145 ) ;
#153625=CARTESIAN_POINT ( 'NONE',  ( 20.94999999999999929, 8.788681102860177674, -241.3540466926497174 ) ) ;
#153661=CARTESIAN_POINT ( 'NONE',  ( -20.85000000000000142, 7.661991824395936845, -241.5144583139544636 ) ) ;
#153675=ORIENTED_EDGE ( 'NONE', *, *, #28609, .F. ) ;
#153690=DIRECTION ( 'NONE',  ( 0.000000000000000000, 0.2128009952263603122, -0.9770955615653315052 ) ) ;
#153696=CARTESIAN_POINT ( 'NONE',  ( 20.94999999999999929, -7.079251802663310222, -212.6676826711374417 ) ) ;
#153698=ADVANCED_FACE ( 'NONE', ( #23510 ), #102989, .F. ) ;
#153716=ORIENTED_EDGE ( 'NONE', *, *, #241530, .F. ) ;
#153732=EDGE_LOOP ( 'NONE', ( #135016, #32177, #114384, #180076 ) ) ;
#153744=DIRECTION ( 'NONE',  ( -1.000000000000000000, 0.000000000000000000, -0.000000000000000000 ) ) ;
#153748=CIRCLE ( 'NONE', #195230, 0.1000000000000053069 ) ;
#153762=DIRECTION ( 'NONE',  ( 1.000000000000000000, 0.000000000000000000, 0.000000000000000000 ) ) ;
#153776=CARTESIAN_POINT ( 'NONE',  ( 23.15000000000000213, -6.688413578037176066, -212.5825622730469036 ) ) ;
#153800=CARTESIAN_POINT ( 'NONE',  ( -20.94999999999999929, 8.001317420522642720, -237.7387931148579980 ) ) ;
#153826=DIRECTION ( 'NONE',  ( -1.000000000000000000, 0.000000000000000000, 0.000000000000000000 ) ) ;
#153899=ORIENTED_EDGE ( 'NONE', *, *, #68217, .T. ) ;
#153902=EDGE_CURVE ( 'NONE', #127248, #139087, #242122, .T. ) ;
#153938=CARTESIAN_POINT ( 'NONE',  ( -21.44999999999999929, 9.593045456726526865, -211.4478935133083439 ) ) ;
#153961=DIRECTION ( 'NONE',  ( 0.000000000000000000, -0.2128009952263604232, 0.9770955615653316162 ) ) ;
#153991=EDGE_CURVE ( 'NONE', #70808, #165685, #8914, .T. ) ;
#154024=VERTEX_POINT ( 'NONE', #19310 ) ;
#154025=EDGE_CURVE ( 'NONE', #188047, #89128, #92465, .T. ) ;
#154030=CARTESIAN_POINT ( 'NONE',  ( 21.05000000000000071, -3.444512620907433487, -226.2123967847655308 ) ) ;
#154032=CARTESIAN_POINT ( 'NONE',  ( -23.15000000000000213, -4.660452010345190743, -233.2299579127752054 ) ) ;
#154035=FACE_OUTER_BOUND ( 'NONE', #251463, .T. ) ;
#154040=LINE ( 'NONE', #56150, #159428 ) ;
#154057=DIRECTION ( 'NONE',  ( 0.000000000000000000, -0.9770955615653313941, -0.2128009952263603677 ) ) ;
#154074=CARTESIAN_POINT ( 'NONE',  ( 20.95568717954149562, 11.97698268079552797, -206.1722622973479702 ) ) ;
#154113=DIRECTION ( 'NONE',  ( 1.000000000000000000, 7.136802563874199107E-16, 1.554319503706929991E-16 ) ) ;
#154122=DIRECTION ( 'NONE',  ( 0.000000000000000000, 0.3634403228828347321, -0.9316174814283063599 ) ) ;
#154123=DIRECTION ( 'NONE',  ( 0.000000000000000000, 0.2128009952263403282, -0.9770955615653358350 ) ) ;
#154129=VERTEX_POINT ( 'NONE', #23187 ) ;
#154134=LINE ( 'NONE', #96644, #130025 ) ;
#154141=EDGE_LOOP ( 'NONE', ( #48215, #178004, #66467, #237490 ) ) ;
#154143=AXIS2_PLACEMENT_3D ( 'NONE', #101615, #2541, #82059 ) ;
#154175=ORIENTED_EDGE ( 'NONE', *, *, #113249, .F. ) ;
#154209=FACE_OUTER_BOUND ( 'NONE', #46300, .T. ) ;
#154241=CARTESIAN_POINT ( 'NONE',  ( 21.05000000000000071, 6.412126976762839270, -199.7058512474018244 ) ) ;
#154288=VERTEX_POINT ( 'NONE', #115522 ) ;
#154295=CARTESIAN_POINT ( 'NONE',  ( -18.59999999999999787, 7.675662554762638479, -241.7139905447625381 ) ) ;
#154313=LINE ( 'NONE', #57710, #211670 ) ;
#154330=EDGE_CURVE ( 'NONE', #88245, #75640, #242310, .T. ) ;
#154362=CARTESIAN_POINT ( 'NONE',  ( -18.59999999999999787, 11.64494613601372386, -211.0010114233329830 ) ) ;
#154383=AXIS2_PLACEMENT_3D ( 'NONE', #197347, #16178, #20027 ) ;
#154384=DIRECTION ( 'NONE',  ( 0.000000000000000000, 0.9770955615653313941, 0.2128009952263606452 ) ) ;
#154426=DIRECTION ( 'NONE',  ( -1.000000000000000000, -2.885090398161910739E-16, -6.283419270304611573E-17 ) ) ;
#154508=ORIENTED_EDGE ( 'NONE', *, *, #119171, .F. ) ;
#154537=DIRECTION ( 'NONE',  ( 0.000000000000000000, -0.2128009952262926163, 0.9770955615653463822 ) ) ;
#154539=EDGE_LOOP ( 'NONE', ( #243884, #56512, #256136, #136051, #81597 ) ) ;
#154549=CARTESIAN_POINT ( 'NONE',  ( -18.54260524012582323, -0.8405054967425236168, -242.3671242014665097 ) ) ;
#154574=DIRECTION ( 'NONE',  ( -1.000000000000000000, 0.000000000000000000, 0.000000000000000000 ) ) ;
#154577=LINE ( 'NONE', #77542, #88612 ) ;
#154584=AXIS2_PLACEMENT_3D ( 'NONE', #166339, #171477, #134849 ) ;
#154626=VERTEX_POINT ( 'NONE', #187227 ) ;
#154649=AXIS2_PLACEMENT_3D ( 'NONE', #214209, #233776, #152983 ) ;
#154672=ORIENTED_EDGE ( 'NONE', *, *, #170446, .T. ) ;
#154698=AXIS2_PLACEMENT_3D ( 'NONE', #122599, #92425, #250229 ) ;
#154717=ORIENTED_EDGE ( 'NONE', *, *, #65637, .F. ) ;
#154795=CIRCLE ( 'NONE', #4887, 0.09999999999998969435 ) ;
#154826=DIRECTION ( 'NONE',  ( -1.000000000000000000, -0.000000000000000000, -0.000000000000000000 ) ) ;
#154841=CARTESIAN_POINT ( 'NONE',  ( 23.14999999999998437, -3.957237024328102759, -201.8618440306682658 ) ) ;
#154845=CARTESIAN_POINT ( 'NONE',  ( 20.85882249326303040, 18.41524492703433324, -237.0006385043383546 ) ) ;
#154866=AXIS2_PLACEMENT_3D ( 'NONE', #40188, #179681, #119708 ) ;
#154883=LINE ( 'NONE', #16644, #226689 ) ;
#154887=AXIS2_PLACEMENT_3D ( 'NONE', #108052, #247556, #148465 ) ;
#154892=EDGE_CURVE ( 'NONE', #164555, #75163, #43547, .T. ) ;
#154894=ORIENTED_EDGE ( 'NONE', *, *, #139169, .F. ) ;
#154898=CARTESIAN_POINT ( 'NONE',  ( -18.59999999999999787, 15.90518444080775851, -219.2841490888777116 ) ) ;
#154912=CARTESIAN_POINT ( 'NONE',  ( 23.24999999999999645, 7.525330762710603416, -212.0571253909869256 ) ) ;
#154918=DIRECTION ( 'NONE',  ( 0.000000000000000000, 0.07893460099012303277, -0.9968797965484756940 ) ) ;
#154926=DIRECTION ( 'NONE',  ( 0.000000000000000000, -0.9770955615653315052, -0.2128009952263605897 ) ) ;
#154960=CARTESIAN_POINT ( 'NONE',  ( 18.50000000000000355, -0.5913595841389387431, -242.4574432119242999 ) ) ;
#154970=CARTESIAN_POINT ( 'NONE',  ( -20.54999999999999716, -6.688413578037177842, -212.5825622730469036 ) ) ;
#154976=AXIS2_PLACEMENT_3D ( 'NONE', #27357, #143403, #164269 ) ;
#155000=DIRECTION ( 'NONE',  ( 0.000000000000000000, -0.2128009952263602289, 0.9770955615653315052 ) ) ;
#155007=DIRECTION ( 'NONE',  ( 1.000000000000000000, 0.000000000000000000, 0.000000000000000000 ) ) ;
#155008=ORIENTED_EDGE ( 'NONE', *, *, #189412, .F. ) ;
#155015=ADVANCED_FACE ( 'NONE', ( #38111 ), #71506, .T. ) ;
#155035=DIRECTION ( 'NONE',  ( 0.000000000000000000, -0.9770955615653320603, -0.2128009952263585081 ) ) ;
#155052=ORIENTED_EDGE ( 'NONE', *, *, #206142, .T. ) ;
#155073=ORIENTED_EDGE ( 'NONE', *, *, #175938, .F. ) ;
#155084=DIRECTION ( 'NONE',  ( 2.694716079187273439E-16, -0.9770955615653316162, -0.2128009952263598958 ) ) ;
#155116=B_SPLINE_CURVE_WITH_KNOTS ( 'NONE', 3,
 ( #187620, #29841, #50635, #130179, #171931, #88472, #27282, #168084 ),
 .UNSPECIFIED., .F., .F.,
 ( 4, 2, 2, 4 ),
 ( 0.000000000000000000, 0.0001881495939909207983, 0.0002822243909863812110, 0.0003762991879818415966 ),
 .UNSPECIFIED. ) ;
#155126=LINE ( 'NONE', #221450, #160755 ) ;
#155163=DIRECTION ( 'NONE',  ( 0.000000000000000000, 0.3565161741896938907, -0.9342891509276685102 ) ) ;
#155180=DIRECTION ( 'NONE',  ( 1.000000000000000000, 0.000000000000000000, 0.000000000000000000 ) ) ;
#155184=FACE_OUTER_BOUND ( 'NONE', #215014, .T. ) ;
#155191=DIRECTION ( 'NONE',  ( 0.000000000000000000, 0.2128009952263603677, -0.9770955615653313941 ) ) ;
#155204=CARTESIAN_POINT ( 'NONE',  ( -20.64999999999999858, 6.757359537351773859, -220.2789794402637824 ) ) ;
#155216=AXIS2_PLACEMENT_3D ( 'NONE', #72922, #188989, #70356 ) ;
#155217=ORIENTED_EDGE ( 'NONE', *, *, #247552, .T. ) ;
#155221=AXIS2_PLACEMENT_3D ( 'NONE', #255184, #200408, #21785 ) ;
#155225=ORIENTED_EDGE ( 'NONE', *, *, #51093, .F. ) ;
#155230=AXIS2_PLACEMENT_3D ( 'NONE', #34611, #8938, #174145 ) ;
#155235=CARTESIAN_POINT ( 'NONE',  ( -20.64999999999999858, 6.780748427709700543, -212.1627259556213403 ) ) ;
#155259=DIRECTION ( 'NONE',  ( 1.000000000000000000, 0.000000000000000000, 0.000000000000000000 ) ) ;
#155266=EDGE_CURVE ( 'NONE', #250869, #43729, #133959, .T. ) ;
#155279=CARTESIAN_POINT ( 'NONE',  ( 18.59999999999999076, 14.73746888278883560, -235.8584165281851028 ) ) ;
#155313=AXIS2_PLACEMENT_3D ( 'NONE', #205516, #105104, #69894 ) ;
#155340=CIRCLE ( 'NONE', #167795, 11.74999999999999289 ) ;
#155374=EDGE_CURVE ( 'NONE', #16906, #175179, #12402, .T. ) ;
#155393=CARTESIAN_POINT ( 'NONE',  ( -21.05000000000000071, 0.5663372425336981042, -209.0641885820623997 ) ) ;
#155405=VERTEX_POINT ( 'NONE', #130467 ) ;
#155452=ORIENTED_EDGE ( 'NONE', *, *, #159960, .T. ) ;
#155474=VECTOR ( 'NONE', #76305, 1000.000000000000000 ) ;
#155477=DIRECTION ( 'NONE',  ( 0.000000000000000000, 0.2128009952263603677, -0.9770955615653313941 ) ) ;
#155500=SURFACE_STYLE_USAGE ( .BOTH. , #254530 ) ;
#155505=CARTESIAN_POINT ( 'NONE',  ( 18.46921299892754575, -7.804820308205004942, -209.8501601876789948 ) ) ;
#155512=CARTESIAN_POINT ( 'NONE',  ( 21.04999999999999716, 6.195883767078806059, -199.6353987068638105 ) ) ;
#155542=CARTESIAN_POINT ( 'NONE',  ( 21.05000000000000071, -3.770473190032740174, -225.9805569534692324 ) ) ;
#155545=ORIENTED_EDGE ( 'NONE', *, *, #36171, .F. ) ;
#155550=CARTESIAN_POINT ( 'NONE',  ( 22.49806830649814060, 11.36657099087203093, -198.4452018475131183 ) ) ;
#155551=DIRECTION ( 'NONE',  ( -1.000000000000000000, 0.000000000000000000, 0.000000000000000000 ) ) ;
#155556=CARTESIAN_POINT ( 'NONE',  ( 20.94999999999999929, 9.863005973831429074, -220.4411654715779321 ) ) ;
#155560=DIRECTION ( 'NONE',  ( -2.978066053179066765E-16, 0.9770955615653311721, 0.2128009952263619775 ) ) ;
#155561=CARTESIAN_POINT ( 'NONE',  ( -20.64999999999999858, -3.664072692419557242, -226.4691047342518857 ) ) ;
#155572=AXIS2_PLACEMENT_3D ( 'NONE', #121591, #240236, #103247 ) ;
#155586=CIRCLE ( 'NONE', #21707, 11.70000000000000284 ) ;
#155603=DIRECTION ( 'NONE',  ( -0.000000000000000000, 0.9770955615653313941, 0.2128009952263603954 ) ) ;
#155630=LINE ( 'NONE', #153069, #131995 ) ;
#155661=CARTESIAN_POINT ( 'NONE',  ( -20.54999999999999716, 7.128833340094563376, -233.7327013124401276 ) ) ;
#155676=ORIENTED_EDGE ( 'NONE', *, *, #214708, .T. ) ;
#155714=CARTESIAN_POINT ( 'NONE',  ( -18.50000000000000000, 1.148907358139439339E-11, -201.0000000000015064 ) ) ;
#155740=CIRCLE ( 'NONE', #247267, 0.1999999999999987899 ) ;
#155741=CARTESIAN_POINT ( 'NONE',  ( 18.49999999999998934, 15.26077403838592339, -222.9041953915167369 ) ) ;
#155759=EDGE_LOOP ( 'NONE', ( #169439, #233515, #92004, #180702 ) ) ;
#155784=CYLINDRICAL_SURFACE ( 'NONE', #93122, 11.80000000000000959 ) ;
#155844=CARTESIAN_POINT ( 'NONE',  ( -18.50000000000000000, 0.6770221356676882074, -212.8807256103264649 ) ) ;
#155847=EDGE_CURVE ( 'NONE', #44396, #137285, #196682, .T. ) ;
#155857=DIRECTION ( 'NONE',  ( 0.000000000000000000, 0.9770955615653317272, 0.2128009952263598126 ) ) ;
#155863=CARTESIAN_POINT ( 'NONE',  ( 22.00356870067119175, -1.543709994167115740, -193.9119119857884073 ) ) ;
#155867=FACE_OUTER_BOUND ( 'NONE', #254798, .T. ) ;
#155873=CARTESIAN_POINT ( 'NONE',  ( 20.58091095332355280, 10.60340429618756275, -207.3066863033071456 ) ) ;
#155879=ORIENTED_EDGE ( 'NONE', *, *, #51935, .F. ) ;
#155880=DIRECTION ( 'NONE',  ( 1.000000000000000000, 0.000000000000000000, 0.000000000000000000 ) ) ;
#155894=EDGE_CURVE ( 'NONE', #23148, #116019, #63592, .T. ) ;
#155898=VERTEX_POINT ( 'NONE', #91041 ) ;
#155908=ORIENTED_EDGE ( 'NONE', *, *, #107045, .F. ) ;
#155963=ORIENTED_EDGE ( 'NONE', *, *, #80897, .F. ) ;
#156011=CARTESIAN_POINT ( 'NONE',  ( 21.05000000000000071, 8.299331953467152800, -209.2670685529822663 ) ) ;
#156038=ADVANCED_FACE ( 'NONE', ( #889 ), #120902, .T. ) ;
#156043=DIRECTION ( 'NONE',  ( -1.000000000000000000, -7.136802563874199107E-16, -1.554319503706929991E-16 ) ) ;
#156047=EDGE_LOOP ( 'NONE', ( #122053, #117693, #178767, #53747 ) ) ;
#156064=VERTEX_POINT ( 'NONE', #103849 ) ;
#156069=CARTESIAN_POINT ( 'NONE',  ( 23.14999999999999503, 13.96869538424789070, -210.3925794786331949 ) ) ;
#156089=CARTESIAN_POINT ( 'NONE',  ( 20.94999999999999929, 9.006788119787323410, -211.5755741104441654 ) ) ;
#156102=DIRECTION ( 'NONE',  ( -0.000000000000000000, 0.9770955615653313941, 0.2128009952263603677 ) ) ;
#156114=VECTOR ( 'NONE', #129767, 1000.000000000000000 ) ;
#156128=AXIS2_PLACEMENT_3D ( 'NONE', #223390, #44775, #125589 ) ;
#156145=FACE_OUTER_BOUND ( 'NONE', #33924, .T. ) ;
#156149=ADVANCED_FACE ( 'NONE', ( #247224 ), #217520, .F. ) ;
#156159=CYLINDRICAL_SURFACE ( 'NONE', #131511, 0.09999999999999939493 ) ;
#156183=DIRECTION ( 'NONE',  ( 0.7071359030027473125, 0.1504668293610846030, -0.6908824414808292236 ) ) ;
#156237=AXIS2_PLACEMENT_3D ( 'NONE', #6758, #240253, #82414 ) ;
#156307=CARTESIAN_POINT ( 'NONE',  ( 23.15000000000000213, -5.658827671433157569, -233.3450493518450344 ) ) ;
#156329=ADVANCED_FACE ( 'NONE', ( #194681 ), #235067, .F. ) ;
#156341=CARTESIAN_POINT ( 'NONE',  ( 18.59999999999998721, 14.70949956575304185, -235.9560995168023112 ) ) ;
#156342=VERTEX_POINT ( 'NONE', #139788 ) ;
#156355=DIRECTION ( 'NONE',  ( 1.000000000000000000, 0.000000000000000000, 0.000000000000000000 ) ) ;
#156356=EDGE_LOOP ( 'NONE', ( #184453, #257593, #13155, #110064 ) ) ;
#156369=EDGE_CURVE ( 'NONE', #175321, #133719, #43409, .T. ) ;
#156388=DIRECTION ( 'NONE',  ( 1.000000000000000000, 0.000000000000000000, 0.000000000000000000 ) ) ;
#156392=EDGE_CURVE ( 'NONE', #210485, #229898, #143651, .T. ) ;
#156393=EDGE_LOOP ( 'NONE', ( #198525, #96234, #171068, #188092 ) ) ;
#156415=CYLINDRICAL_SURFACE ( 'NONE', #127263, 0.09999999999999939493 ) ;
#156448=DIRECTION ( 'NONE',  ( 0.000000000000000000, -0.2128009952263485993, 0.9770955615653341697 ) ) ;
#156469=DIRECTION ( 'NONE',  ( 0.000000000000000000, 0.9770955615653548199, 0.2128009952262535920 ) ) ;
#156482=CARTESIAN_POINT ( 'NONE',  ( 20.95512820512820440, 10.49413282287806481, -207.4737445703522383 ) ) ;
#156491=FACE_OUTER_BOUND ( 'NONE', #163905, .T. ) ;
#156512=CIRCLE ( 'NONE', #81425, 0.09999999999999939493 ) ;
#156524=LINE ( 'NONE', #78222, #123930 ) ;
#156559=CYLINDRICAL_SURFACE ( 'NONE', #16951, 0.09999999999999939493 ) ;
#156593=VERTEX_POINT ( 'NONE', #131794 ) ;
#156627=DIRECTION ( 'NONE',  ( 0.000000000000000000, 0.2128009952263601456, -0.9770955615653316162 ) ) ;
#156652=VERTEX_POINT ( 'NONE', #176090 ) ;
#156691=CIRCLE ( 'NONE', #81593, 0.1000000000000054040 ) ;
#156702=AXIS2_PLACEMENT_3D ( 'NONE', #151950, #117916, #132355 ) ;
#156709=DIRECTION ( 'NONE',  ( 0.000000000000000000, -0.2128009952263604232, 0.9770955615653316162 ) ) ;
#156741=CARTESIAN_POINT ( 'NONE',  ( 20.94999999999999929, 6.511710453938116316, -230.8991241839006534 ) ) ;
#156748=CARTESIAN_POINT ( 'NONE',  ( -20.54999999999999716, -7.176961358819843539, -212.6889627706600834 ) ) ;
#156753=CARTESIAN_POINT ( 'NONE',  ( -23.15000000000000213, 7.554435330547284444, -235.6868924355707691 ) ) ;
#156770=LINE ( 'NONE', #115049, #202816 ) ;
#156786=ORIENTED_EDGE ( 'NONE', *, *, #135584, .T. ) ;
#156793=VECTOR ( 'NONE', #60647, 1000.000000000000227 ) ;
#156805=DIRECTION ( 'NONE',  ( 0.000000000000000000, -0.9770955615653315052, -0.2128009952263603954 ) ) ;
#156818=CARTESIAN_POINT ( 'NONE',  ( 21.07928932188134397, -1.250084634896337255, -194.7953894783290423 ) ) ;
#156879=ORIENTED_EDGE ( 'NONE', *, *, #210933, .T. ) ;
#156903=AXIS2_PLACEMENT_3D ( 'NONE', #11478, #90994, #48012 ) ;
#156922=CARTESIAN_POINT ( 'NONE',  ( -20.54999999999999716, 5.256951610580939516, -213.3897168960460533 ) ) ;
#156924=AXIS2_PLACEMENT_3D ( 'NONE', #37715, #254150, #255394 ) ;
#156938=CYLINDRICAL_SURFACE ( 'NONE', #84775, 0.09999999999999810429 ) ;
#156944=CIRCLE ( 'NONE', #86160, 0.1000000000000003525 ) ;
#156962=AXIS2_PLACEMENT_3D ( 'NONE', #33756, #134076, #72869 ) ;
#157018=ORIENTED_EDGE ( 'NONE', *, *, #27936, .F. ) ;
#157035=ORIENTED_EDGE ( 'NONE', *, *, #173549, .T. ) ;
#157052=AXIS2_PLACEMENT_3D ( 'NONE', #204833, #226982, #90026 ) ;
#157062=ORIENTED_EDGE ( 'NONE', *, *, #118609, .F. ) ;
#157074=FACE_OUTER_BOUND ( 'NONE', #97954, .T. ) ;
#157119=CIRCLE ( 'NONE', #190453, 4.050000000000001599 ) ;
#157154=CARTESIAN_POINT ( 'NONE',  ( 20.19326291202132495, 11.57517403174952619, -206.4228608358838244 ) ) ;
#157197=VECTOR ( 'NONE', #35449, 1000.000000000000000 ) ;
#157242=ORIENTED_EDGE ( 'NONE', *, *, #134636, .T. ) ;
#157309=DIRECTION ( 'NONE',  ( 0.000000000000000000, -0.2128009952263664739, 0.9770955615653302839 ) ) ;
#157315=DIRECTION ( 'NONE',  ( 1.000000000000000000, 0.000000000000000000, 0.000000000000000000 ) ) ;
#157338=EDGE_LOOP ( 'NONE', ( #151057, #109779, #51244, #200292 ) ) ;
#157347=ORIENTED_EDGE ( 'NONE', *, *, #248054, .T. ) ;
#157357=ORIENTED_EDGE ( 'NONE', *, *, #136681, .F. ) ;
#157366=AXIS2_PLACEMENT_3D ( 'NONE', #78122, #201942, #102807 ) ;
#157383=CARTESIAN_POINT ( 'NONE',  ( 18.59999999999999076, 0.4810385098657082859, -209.0827657365571213 ) ) ;
#157389=CARTESIAN_POINT ( 'NONE',  ( -23.15000000000000213, 7.128833340094563376, -233.7327013124401276 ) ) ;
#157398=AXIS2_PLACEMENT_3D ( 'NONE', #202845, #183293, #24238 ) ;
#157418=ORIENTED_EDGE ( 'NONE', *, *, #97523, .F. ) ;
#157420=CARTESIAN_POINT ( 'NONE',  ( 20.94999999999999929, 7.128833340094563376, -233.7327013124401276 ) ) ;
#157434=DIRECTION ( 'NONE',  ( -1.000000000000000000, -0.000000000000000000, -0.000000000000000000 ) ) ;
#157474=VERTEX_POINT ( 'NONE', #169060 ) ;
#157482=CARTESIAN_POINT ( 'NONE',  ( -20.94684162810195005, 12.93678149440677494, -205.1845283066507761 ) ) ;
#157495=CARTESIAN_POINT ( 'NONE',  ( 18.46858270002953617, -7.745884046994173211, -209.9554738686949520 ) ) ;
#157504=LINE ( 'NONE', #199160, #162059 ) ;
#157508=EDGE_CURVE ( 'NONE', #132241, #2617, #231033, .T. ) ;
#157520=ORIENTED_EDGE ( 'NONE', *, *, #232673, .T. ) ;
#157528=DIRECTION ( 'NONE',  ( -1.000000000000000000, 0.000000000000000000, 0.000000000000000000 ) ) ;
#157575=EDGE_CURVE ( 'NONE', #98560, #30925, #42352, .T. ) ;
#157650=ORIENTED_EDGE ( 'NONE', *, *, #133488, .T. ) ;
#157654=CARTESIAN_POINT ( 'NONE',  ( -20.64999999999999858, 7.128833340094563376, -233.7327013124401276 ) ) ;
#157669=VECTOR ( 'NONE', #217863, 1000.000000000000227 ) ;
#157690=CARTESIAN_POINT ( 'NONE',  ( 20.85000000000000142, 6.803341081522319200, -233.7601854879220298 ) ) ;
#157702=ORIENTED_EDGE ( 'NONE', *, *, #248648, .F. ) ;
#157715=AXIS2_PLACEMENT_3D ( 'NONE', #10600, #152702, #151403 ) ;
#157721=ORIENTED_EDGE ( 'NONE', *, *, #71168, .T. ) ;
#157746=EDGE_CURVE ( 'NONE', #182918, #117533, #226095, .T. ) ;
#157765=CARTESIAN_POINT ( 'NONE',  ( 21.00000000000000000, 12.13349391679638778, -210.8946109257198032 ) ) ;
#157768=DIRECTION ( 'NONE',  ( 1.000000000000000000, 0.000000000000000000, 0.000000000000000000 ) ) ;
#157819=DIRECTION ( 'NONE',  ( 1.000000000000000000, 1.794895427898103559E-16, 3.909090864890002444E-17 ) ) ;
#157841=CARTESIAN_POINT ( 'NONE',  ( -18.59999999999999787, 4.288595810029049993, -211.9930862808554934 ) ) ;
#157859=VERTEX_POINT ( 'NONE', #31811 ) ;
#157886=DIRECTION ( 'NONE',  ( -1.000000000000000000, -2.885090398161910739E-16, -6.283419270304611573E-17 ) ) ;
#157894=AXIS2_PLACEMENT_3D ( 'NONE', #30377, #109880, #189443 ) ;
#157917=CARTESIAN_POINT ( 'NONE',  ( 19.86930884467578196, 16.68375915355484196, -222.6855985437128140 ) ) ;
#157968=DIRECTION ( 'NONE',  ( 0.000000000000000000, 0.9736512643735623085, 0.2280421351061316382 ) ) ;
#158006=ORIENTED_EDGE ( 'NONE', *, *, #127372, .F. ) ;
#158039=CARTESIAN_POINT ( 'NONE',  ( -21.05000000000000071, -1.236118717437885595, -194.8647072476926496 ) ) ;
#158047=ADVANCED_FACE ( 'NONE', ( #70497 ), #251662, .F. ) ;
#158094=SPHERICAL_SURFACE ( 'NONE', #71217, 0.1000000000000000056 ) ;
#158102=VERTEX_POINT ( 'NONE', #110867 ) ;
#158113=CARTESIAN_POINT ( 'NONE',  ( -18.50000000000000000, 13.58143519257360232, -219.8925810335774997 ) ) ;
#158126=VECTOR ( 'NONE', #151624, 1000.000000000000227 ) ;
#158139=DIRECTION ( 'NONE',  ( 0.000000000000000000, -0.2128009952263154869, 0.9770955615653412751 ) ) ;
#158168=B_SPLINE_CURVE_WITH_KNOTS ( 'NONE', 3,
 ( #193381, #216765, #231223, #52549, #132105, #13448, #172567, #211657 ),
 .UNSPECIFIED., .F., .F.,
 ( 4, 2, 2, 4 ),
 ( 0.000000000000000000, 0.0001094981963948483559, 0.0002189963927896967119, 0.0004379927855793889243 ),
 .UNSPECIFIED. ) ;
#158179=FACE_OUTER_BOUND ( 'NONE', #173341, .T. ) ;
#158187=VECTOR ( 'NONE', #106121, 999.9999999999998863 ) ;
#158222=ORIENTED_EDGE ( 'NONE', *, *, #163929, .T. ) ;
#158270=EDGE_LOOP ( 'NONE', ( #182369, #209633, #195102, #182322 ) ) ;
#158272=FACE_OUTER_BOUND ( 'NONE', #78576, .T. ) ;
#158281=ORIENTED_EDGE ( 'NONE', *, *, #66062, .F. ) ;
#158296=EDGE_CURVE ( 'NONE', #126073, #248782, #93995, .T. ) ;
#158327=VECTOR ( 'NONE', #62915, 1000.000000000000227 ) ;
#158446=CARTESIAN_POINT ( 'NONE',  ( 20.30531438145591139, 11.52463756055922417, -206.4688238028691671 ) ) ;
#158457=DIRECTION ( 'NONE',  ( -1.000000000000000000, 0.000000000000000000, 0.000000000000000000 ) ) ;
#158480=ADVANCED_FACE ( 'NONE', ( #228162 ), #181512, .F. ) ;
#158483=ORIENTED_EDGE ( 'NONE', *, *, #21809, .T. ) ;
#158515=FACE_OUTER_BOUND ( 'NONE', #131544, .T. ) ;
#158549=CARTESIAN_POINT ( 'NONE',  ( -23.15000000000000213, -11.48087284838115885, -203.5004116939112464 ) ) ;
#158596=CARTESIAN_POINT ( 'NONE',  ( -2.995603634470829482E-16, -8.874060656858240748, -215.4698323230865640 ) ) ;
#158636=DIRECTION ( 'NONE',  ( 2.840903330521632269E-16, -0.9550021345545507412, 0.2965989261549202838 ) ) ;
#158660=DIRECTION ( 'NONE',  ( 4.408576920032446123E-17, 0.07893460099012301889, -0.9968797965484754720 ) ) ;
#158674=CIRCLE ( 'NONE', #108577, 3.999999999999998224 ) ;
#158686=CARTESIAN_POINT ( 'NONE',  ( 18.59999999999999076, 4.252251777740764460, -211.8999245327126744 ) ) ;
#158714=CIRCLE ( 'NONE', #246167, 4.049999999999995381 ) ;
#158745=DIRECTION ( 'NONE',  ( 1.000000000000000000, 0.000000000000000000, 0.000000000000000000 ) ) ;
#158789=ORIENTED_EDGE ( 'NONE', *, *, #125671, .T. ) ;
#158801=DIRECTION ( 'NONE',  ( 0.000000000000000000, -0.2128009952263678062, 0.9770955615653298398 ) ) ;
#158818=ORIENTED_EDGE ( 'NONE', *, *, #8854, .F. ) ;
#158837=DIRECTION ( 'NONE',  ( 0.000000000000000000, -0.9394191166662618775, -0.3427706569150580362 ) ) ;
#158854=CARTESIAN_POINT ( 'NONE',  ( -21.14999999999999858, -11.48087284838115885, -203.5004116939112464 ) ) ;
#158870=ORIENTED_EDGE ( 'NONE', *, *, #47098, .T. ) ;
#158880=CARTESIAN_POINT ( 'NONE',  ( 22.60000000000000142, 11.45898712536580177, -198.4011321578509808 ) ) ;
#158888=DIRECTION ( 'NONE',  ( 0.000000000000000000, -0.8659859643398405415, 0.5000683049008369796 ) ) ;
#158913=DIRECTION ( 'NONE',  ( 0.000000000000000000, -0.2128009952261912530, 0.9770955615653682536 ) ) ;
#158916=ORIENTED_EDGE ( 'NONE', *, *, #235593, .T. ) ;
#158945=EDGE_CURVE ( 'NONE', #164707, #14295, #161020, .T. ) ;
#158980=CYLINDRICAL_SURFACE ( 'NONE', #95318, 4.000000000000006217 ) ;
#159016=FACE_OUTER_BOUND ( 'NONE', #23744, .T. ) ;
#159039=DIRECTION ( 'NONE',  ( -3.265361837132813586E-16, 0.9770955615653313941, 0.2128009952263609783 ) ) ;
#159056=ORIENTED_EDGE ( 'NONE', *, *, #250987, .F. ) ;
#159068=DIRECTION ( 'NONE',  ( 1.000000000000000000, 0.000000000000000000, 0.000000000000000000 ) ) ;
#159076=CARTESIAN_POINT ( 'NONE',  ( -20.94999999999999929, 4.617781596423509605, -222.2029736859691980 ) ) ;
#159077=TOROIDAL_SURFACE ( 'NONE', #213196, 0.4000000000000009104, 0.1000000000000000056 ) ;
#159099=EDGE_CURVE ( 'NONE', #135145, #17786, #194362, .T. ) ;
#159106=VERTEX_POINT ( 'NONE', #46313 ) ;
#159107=EDGE_CURVE ( 'NONE', #59070, #17019, #248494, .T. ) ;
#159128=ORIENTED_EDGE ( 'NONE', *, *, #249335, .F. ) ;
#159170=AXIS2_PLACEMENT_3D ( 'NONE', #226084, #29245, #209113 ) ;
#159185=EDGE_CURVE ( 'NONE', #172105, #182409, #12366, .T. ) ;
#159214=TOROIDAL_SURFACE ( 'NONE', #104977, 12.97499999999999609, 0.1000000000000000056 ) ;
#159223=LINE ( 'NONE', #256964, #157669 ) ;
#159235=CARTESIAN_POINT ( 'NONE',  ( -18.39999999999999858, -0.9152171842607024210, -242.2974985173726452 ) ) ;
#159236=DIRECTION ( 'NONE',  ( 0.000000000000000000, 0.2128009952263485993, -0.9770955615653341697 ) ) ;
#159242=VERTEX_POINT ( 'NONE', #115286 ) ;
#159247=FACE_OUTER_BOUND ( 'NONE', #66515, .T. ) ;
#159271=FACE_OUTER_BOUND ( 'NONE', #142458, .T. ) ;
#159329=CIRCLE ( 'NONE', #192628, 0.09999999999999939493 ) ;
#159340=AXIS2_PLACEMENT_3D ( 'NONE', #247177, #105067, #142928 ) ;
#159381=CARTESIAN_POINT ( 'NONE',  ( 22.49999999999999645, 11.36403278914770176, -198.4341430231427807 ) ) ;
#159410=DIRECTION ( 'NONE',  ( -0.000000000000000000, 0.9770955615653315052, 0.2128009952263602844 ) ) ;
#159428=VECTOR ( 'NONE', #254347, 1000.000000000000227 ) ;
#159492=VECTOR ( 'NONE', #15538, 999.9999999999998863 ) ;
#159497=ORIENTED_EDGE ( 'NONE', *, *, #173420, .T. ) ;
#159498=EDGE_LOOP ( 'NONE', ( #55537, #121667, #138695, #143164 ) ) ;
#159516=ORIENTED_EDGE ( 'NONE', *, *, #201907, .F. ) ;
#159522=CARTESIAN_POINT ( 'NONE',  ( 21.05000000000000071, -4.161311414658873886, -226.0656773515597706 ) ) ;
#159542=CARTESIAN_POINT ( 'NONE',  ( -22.39999999999999858, -1.560176095955062348, -193.3663837337744837 ) ) ;
#159575=FACE_OUTER_BOUND ( 'NONE', #99523, .T. ) ;
#159650=CIRCLE ( 'NONE', #72767, 0.3999999999999948597 ) ;
#159657=CARTESIAN_POINT ( 'NONE',  ( -18.43634282235123578, -0.9118504197709764725, -242.3006630565730006 ) ) ;
#159668=DIRECTION ( 'NONE',  ( 0.000000000000000000, 0.2128009952263603954, -0.9770955615653315052 ) ) ;
#159696=AXIS2_PLACEMENT_3D ( 'NONE', #108802, #247024, #89238 ) ;
#159706=CYLINDRICAL_SURFACE ( 'NONE', #255116, 0.09999999999999939493 ) ;
#159707=CARTESIAN_POINT ( 'NONE',  ( 20.97107704358301916, 10.49354833045136637, -207.4742241701343062 ) ) ;
#159709=CARTESIAN_POINT ( 'NONE',  ( -20.94999999999999574, 17.02177226667168597, -224.5487030889150901 ) ) ;
#159767=EDGE_LOOP ( 'NONE', ( #114640, #8453, #84410, #129634 ) ) ;
#159795=DIRECTION ( 'NONE',  ( 0.000000000000000000, 0.07893460099012301889, -0.9968797965484755830 ) ) ;
#159816=CIRCLE ( 'NONE', #76595, 0.09999999999999895084 ) ;
#159843=ORIENTED_EDGE ( 'NONE', *, *, #72076, .F. ) ;
#159858=EDGE_CURVE ( 'NONE', #233386, #23148, #93505, .T. ) ;
#159876=DIRECTION ( 'NONE',  ( 1.000000000000000000, 0.000000000000000000, 0.000000000000000000 ) ) ;
#159888=ORIENTED_EDGE ( 'NONE', *, *, #186580, .F. ) ;
#159889=VERTEX_POINT ( 'NONE', #152232 ) ;
#159902=ORIENTED_EDGE ( 'NONE', *, *, #24959, .T. ) ;
#159929=AXIS2_PLACEMENT_3D ( 'NONE', #2232, #182187, #200457 ) ;
#159938=ORIENTED_EDGE ( 'NONE', *, *, #173329, .F. ) ;
#159957=PLANE ( 'NONE',  #82129 ) ;
#159960=EDGE_CURVE ( 'NONE', #52350, #212886, #169789, .T. ) ;
#159968=ORIENTED_EDGE ( 'NONE', *, *, #13314, .T. ) ;
#160014=CARTESIAN_POINT ( 'NONE',  ( 23.24999999999999289, 8.930358663153430854, -211.6945637661233377 ) ) ;
#160019=CARTESIAN_POINT ( 'NONE',  ( 21.05000000000000071, 1.148907358139439339E-11, -201.0000000000015064 ) ) ;
#160027=AXIS2_PLACEMENT_3D ( 'NONE', #117998, #197524, #18891 ) ;
#160031=CARTESIAN_POINT ( 'NONE',  ( 23.14999999999999858, 7.128833340094563376, -233.7327013124401276 ) ) ;
#160048=DIRECTION ( 'NONE',  ( -1.000000000000000000, -7.136802563874199107E-16, -1.554319503706929991E-16 ) ) ;
#160053=CARTESIAN_POINT ( 'NONE',  ( -18.50000000000000000, 2.859758780633683273, -208.6670499591424459 ) ) ;
#160064=ORIENTED_EDGE ( 'NONE', *, *, #24345, .T. ) ;
#160098=ADVANCED_FACE ( 'NONE', ( #22991 ), #124631, .T. ) ;
#160111=EDGE_CURVE ( 'NONE', #98224, #192518, #232316, .T. ) ;
#160114=CARTESIAN_POINT ( 'NONE',  ( 18.59999999999999432, 2.859758780633683273, -208.6670499591424459 ) ) ;
#160180=B_SPLINE_CURVE_WITH_KNOTS ( 'NONE', 3,
 ( #29000, #83746, #108489, #44676, #188037, #45946, #162064, #204997, #241578, #105890, #23848, #124216, #64227, #103334, #247992, #152789, #13255, #10682, #69383 ),
 .UNSPECIFIED., .F., .F.,
 ( 4, 3, 3, 3, 3, 3, 4 ),
 ( 0.000000000000000000, 7.110282409889723450E-05, 0.0001508797727291417718, 0.0002027344179858366850, 0.0002343294522349049320, 0.0002454816334821112531, 0.0002619873080085701302 ),
 .UNSPECIFIED. ) ;
#160183=VERTEX_POINT ( 'NONE', #31969 ) ;
#160201=CARTESIAN_POINT ( 'NONE',  ( 23.14999999999999858, 1.148907358139439339E-11, -201.0000000000015064 ) ) ;
#160228=DIRECTION ( 'NONE',  ( 0.000000000000000000, -0.2128009952262243931, 0.9770955615653611481 ) ) ;
#160254=ORIENTED_EDGE ( 'NONE', *, *, #196399, .T. ) ;
#160273=CARTESIAN_POINT ( 'NONE',  ( -18.49499033040907392, -7.690199103985159823, -210.0417310202402632 ) ) ;
#160289=DIRECTION ( 'NONE',  ( 1.000000000000000000, 3.190570557967288949E-16, 6.948722487160392945E-17 ) ) ;
#160291=AXIS2_PLACEMENT_3D ( 'NONE', #95633, #74837, #194773 ) ;
#160323=DIRECTION ( 'NONE',  ( -0.000000000000000000, 0.08413937888706959911, -0.9964539953858875254 ) ) ;
#160345=EDGE_CURVE ( 'NONE', #25296, #77581, #240662, .T. ) ;
#160349=CARTESIAN_POINT ( 'NONE',  ( -23.15000000000000213, 7.128833340094563376, -233.7327013124401276 ) ) ;
#160392=ORIENTED_EDGE ( 'NONE', *, *, #207044, .T. ) ;
#160404=AXIS2_PLACEMENT_3D ( 'NONE', #7799, #202140, #105566 ) ;
#160450=AXIS2_PLACEMENT_3D ( 'NONE', #165029, #224975, #240719 ) ;
#160461=FACE_OUTER_BOUND ( 'NONE', #83414, .T. ) ;
#160479=CYLINDRICAL_SURFACE ( 'NONE', #218188, 0.09999999999999939493 ) ;
#160506=ADVANCED_FACE ( 'NONE', ( #86442 ), #206424, .T. ) ;
#160509=AXIS2_PLACEMENT_3D ( 'NONE', #198018, #18107, #33871 ) ;
#160516=CARTESIAN_POINT ( 'NONE',  ( 20.94999999999999929, 7.476371755685457643, -241.7308184205399471 ) ) ;
#160528=TOROIDAL_SURFACE ( 'NONE', #118822, 11.65000000000000036, 0.1000000000000000056 ) ;
#160533=ORIENTED_EDGE ( 'NONE', *, *, #38458, .F. ) ;
#160535=ORIENTED_EDGE ( 'NONE', *, *, #217838, .T. ) ;
#160604=DIRECTION ( 'NONE',  ( 0.000000000000000000, -0.2128009952263485993, 0.9770955615653341697 ) ) ;
#160637=AXIS2_PLACEMENT_3D ( 'NONE', #204270, #124758, #227689 ) ;
#160642=FACE_OUTER_BOUND ( 'NONE', #251955, .T. ) ;
#160660=DIRECTION ( 'NONE',  ( 0.000000000000000000, 0.2128009952263603677, -0.9770955615653313941 ) ) ;
#160708=FACE_OUTER_BOUND ( 'NONE', #140253, .T. ) ;
#160755=VECTOR ( 'NONE', #239766, 1000.000000000000227 ) ;
#160757=DIRECTION ( 'NONE',  ( -1.000000000000000000, -3.190570557967288949E-16, -6.948722487160392945E-17 ) ) ;
#160759=EDGE_CURVE ( 'NONE', #236966, #174683, #139712, .T. ) ;
#160765=CARTESIAN_POINT ( 'NONE',  ( 20.94999999999999574, -10.58757034444203704, -206.3761839813444396 ) ) ;
#160778=EDGE_CURVE ( 'NONE', #220140, #256420, #41940, .T. ) ;
#160779=FACE_OUTER_BOUND ( 'NONE', #153441, .T. ) ;
#160784=ADVANCED_FACE ( 'NONE', ( #24947 ), #211640, .F. ) ;
#160802=ORIENTED_EDGE ( 'NONE', *, *, #232926, .T. ) ;
#160835=ORIENTED_EDGE ( 'NONE', *, *, #133531, .F. ) ;
#160841=ORIENTED_EDGE ( 'NONE', *, *, #189132, .T. ) ;
#160872=EDGE_CURVE ( 'NONE', #144682, #129320, #107749, .T. ) ;
#160900=CARTESIAN_POINT ( 'NONE',  ( -21.05000000000000071, -4.656943609564678788, -233.1535107627236414 ) ) ;
#160936=EDGE_CURVE ( 'NONE', #121315, #201117, #28825, .T. ) ;
#160973=EDGE_LOOP ( 'NONE', ( #216354, #119126, #98785, #167645 ) ) ;
#160990=ORIENTED_EDGE ( 'NONE', *, *, #134985, .T. ) ;
#160994=CARTESIAN_POINT ( 'NONE',  ( -21.05000000000000071, 16.98881331171929787, -224.4946931418895417 ) ) ;
#161019=AXIS2_PLACEMENT_3D ( 'NONE', #198353, #120148, #19737 ) ;
#161020=CIRCLE ( 'NONE', #2780, 0.1000000000000057648 ) ;
#161037=VECTOR ( 'NONE', #91906, 1000.000000000000000 ) ;
#161047=CARTESIAN_POINT ( 'NONE',  ( -22.59999985501179154, 11.46678616150632379, -198.4355198451642366 ) ) ;
#161075=AXIS2_PLACEMENT_3D ( 'NONE', #136409, #97271, #98553 ) ;
#161092=DIRECTION ( 'NONE',  ( 0.000000000000000000, 0.9770955615653316162, 0.2128009952263604232 ) ) ;
#161103=ORIENTED_EDGE ( 'NONE', *, *, #190660, .T. ) ;
#161111=VECTOR ( 'NONE', #143323, 999.9999999999998863 ) ;
#161115=DIRECTION ( 'NONE',  ( -1.000000000000000000, 0.000000000000000000, 0.000000000000000000 ) ) ;
#161121=DIRECTION ( 'NONE',  ( 1.000000000000000000, 0.000000000000000000, 0.000000000000000000 ) ) ;
#161160=ORIENTED_EDGE ( 'NONE', *, *, #121500, .T. ) ;
#161170=ORIENTED_EDGE ( 'NONE', *, *, #65579, .F. ) ;
#161198=CIRCLE ( 'NONE', #65500, 0.1000000000000006717 ) ;
#161211=AXIS2_PLACEMENT_3D ( 'NONE', #250076, #130116, #173157 ) ;
#161252=CIRCLE ( 'NONE', #123836, 0.1000000000000055844 ) ;
#161302=CARTESIAN_POINT ( 'NONE',  ( 21.05000000000000071, 16.98881331171930498, -224.4946931418895701 ) ) ;
#161328=VECTOR ( 'NONE', #203276, 1000.000000000000000 ) ;
#161383=ORIENTED_EDGE ( 'NONE', *, *, #199109, .F. ) ;
#161396=CIRCLE ( 'NONE', #194734, 0.09999999999999979738 ) ;
#161403=ORIENTED_EDGE ( 'NONE', *, *, #63547, .F. ) ;
#161456=EDGE_LOOP ( 'NONE', ( #100968, #92797, #65251, #94644 ) ) ;
#161490=VECTOR ( 'NONE', #183146, 1000.000000000000227 ) ;
#161534=DIRECTION ( 'NONE',  ( 0.000000000000000000, -0.2128009952263601456, 0.9770955615653316162 ) ) ;
#161536=ORIENTED_EDGE ( 'NONE', *, *, #120389, .F. ) ;
#161537=AXIS2_PLACEMENT_3D ( 'NONE', #195981, #52587, #151731 ) ;
#161547=CARTESIAN_POINT ( 'NONE',  ( -18.46856557590794168, -7.745904572654687570, -209.9554418084320560 ) ) ;
#161576=CARTESIAN_POINT ( 'NONE',  ( 23.24999999999999289, 10.80300742114540391, -220.2930047078982625 ) ) ;
#161582=DIRECTION ( 'NONE',  ( 1.000000000000000000, 0.000000000000000000, 0.000000000000000000 ) ) ;
#161584=DIRECTION ( 'NONE',  ( 0.000000000000000000, 0.2128009952263603122, -0.9770955615653315052 ) ) ;
#161585=CARTESIAN_POINT ( 'NONE',  ( -21.05000000000000071, 6.093673009697585741, -199.5727803633465385 ) ) ;
#161664=AXIS2_PLACEMENT_3D ( 'NONE', #16614, #58268, #231808 ) ;
#161725=VECTOR ( 'NONE', #13175, 1000.000000000000000 ) ;
#161726=EDGE_CURVE ( 'NONE', #10248, #97608, #57469, .T. ) ;
#161730=CARTESIAN_POINT ( 'NONE',  ( 18.59999999999999076, 10.82428752066803845, -220.3907142640547931 ) ) ;
#161735=LINE ( 'NONE', #199578, #100298 ) ;
#161743=CARTESIAN_POINT ( 'NONE',  ( 19.94784844284960101, 16.70146065711004724, -222.6438515326542813 ) ) ;
#161744=ADVANCED_FACE ( 'NONE', ( #82035 ), #99159, .T. ) ;
#161756=ORIENTED_EDGE ( 'NONE', *, *, #132024, .F. ) ;
#161805=ORIENTED_EDGE ( 'NONE', *, *, #98706, .F. ) ;
#161821=EDGE_CURVE ( 'NONE', #5146, #97897, #70245, .T. ) ;
#161901=ORIENTED_EDGE ( 'NONE', *, *, #60149, .T. ) ;
#161932=CARTESIAN_POINT ( 'NONE',  ( -22.50000000000000000, -1.330006220153263641, -194.8931527402181700 ) ) ;
#161966=CARTESIAN_POINT ( 'NONE',  ( -20.54999999999999716, -6.794814075650357665, -212.0940144922642219 ) ) ;
#161968=AXIS2_PLACEMENT_3D ( 'NONE', #253544, #115324, #16262 ) ;
#162009=VERTEX_POINT ( 'NONE', #119622 ) ;
#162056=DIRECTION ( 'NONE',  ( -1.000000000000000000, 0.000000000000000000, 0.000000000000000000 ) ) ;
#162059=VECTOR ( 'NONE', #196582, 1000.000000000000000 ) ;
#162064=CARTESIAN_POINT ( 'NONE',  ( 21.10320863425824811, 6.248357867143764288, -199.6135654718238186 ) ) ;
#162076=ADVANCED_FACE ( 'NONE', ( #204260 ), #6061, .F. ) ;
#162084=VERTEX_POINT ( 'NONE', #85567 ) ;
#162085=AXIS2_PLACEMENT_3D ( 'NONE', #214586, #217137, #16420 ) ;
#162098=ORIENTED_EDGE ( 'NONE', *, *, #123596, .T. ) ;
#162105=ADVANCED_FACE ( 'NONE', ( #66042 ), #178498, .F. ) ;
#162131=ADVANCED_FACE ( 'NONE', ( #109011 ), #232663, .T. ) ;
#162150=CONICAL_SURFACE ( 'NONE', #187092, 4.049999999999995381, 0.7853981633974604915 ) ;
#162194=CARTESIAN_POINT ( 'NONE',  ( 23.15000000000000213, -4.756823075239757337, -233.1486023682345490 ) ) ;
#162210=ORIENTED_EDGE ( 'NONE', *, *, #74999, .F. ) ;
#162233=ADVANCED_FACE ( 'NONE', ( #121588 ), #35932, .T. ) ;
#162260=DIRECTION ( 'NONE',  ( 0.000000000000000000, 0.2128009952263604232, -0.9770955615653316162 ) ) ;
#162285=CARTESIAN_POINT ( 'NONE',  ( 21.13461538461539035, 12.97827409159657464, -210.7106268109450298 ) ) ;
#162301=CARTESIAN_POINT ( 'NONE',  ( 23.14999999999999503, 16.00289399696429271, -219.2628689893550700 ) ) ;
#162306=VERTEX_POINT ( 'NONE', #103243 ) ;
#162325=TOROIDAL_SURFACE ( 'NONE', #120637, 0.6000000000000015321, 0.1000000000000000056 ) ;
#162326=CIRCLE ( 'NONE', #208128, 0.2000000000000111688 ) ;
#162328=ORIENTED_EDGE ( 'NONE', *, *, #131211, .F. ) ;
#162379=CIRCLE ( 'NONE', #237387, 12.87499999999999467 ) ;
#162386=AXIS2_PLACEMENT_3D ( 'NONE', #157690, #217588, #121115 ) ;
#162398=ORIENTED_EDGE ( 'NONE', *, *, #130697, .F. ) ;
#162416=CARTESIAN_POINT ( 'NONE',  ( -21.59142135623730852, 12.19222130685950312, -220.0927928707378669 ) ) ;
#162450=FACE_OUTER_BOUND ( 'NONE', #256402, .T. ) ;
#162591=ORIENTED_EDGE ( 'NONE', *, *, #148255, .T. ) ;
#162608=VECTOR ( 'NONE', #184318, 1000.000000000000000 ) ;
#162618=CARTESIAN_POINT ( 'NONE',  ( 21.09787244211748103, 11.17890107025148261, -211.0915125386900968 ) ) ;
#162624=CARTESIAN_POINT ( 'NONE',  ( -23.25000000000000000, -0.8618440306552699326, -197.0427629756619297 ) ) ;
#162643=VERTEX_POINT ( 'NONE', #96514 ) ;
#162650=ORIENTED_EDGE ( 'NONE', *, *, #121474, .F. ) ;
#162652=CARTESIAN_POINT ( 'NONE',  ( -23.25000000000000000, 18.41524492703432614, -237.0006385043383546 ) ) ;
#162666=DIRECTION ( 'NONE',  ( 1.000000000000000000, 0.000000000000000000, 0.000000000000000000 ) ) ;
#162681=FACE_OUTER_BOUND ( 'NONE', #44820, .T. ) ;
#162698=DIRECTION ( 'NONE',  ( 0.000000000000000000, -0.2128009952263403282, 0.9770955615653358350 ) ) ;
#162706=CIRCLE ( 'NONE', #196032, 0.2000000000000104194 ) ;
#162707=EDGE_CURVE ( 'NONE', #41827, #28455, #132883, .T. ) ;
#162711=CARTESIAN_POINT ( 'NONE',  ( 21.14999999999999858, 13.98997548377052524, -210.4902890347897255 ) ) ;
#162727=CARTESIAN_POINT ( 'NONE',  ( 20.94999999999999929, -3.770473190032740174, -225.9805569534692324 ) ) ;
#162774=ORIENTED_EDGE ( 'NONE', *, *, #66657, .F. ) ;
#162788=DIRECTION ( 'NONE',  ( 0.000000000000000000, 0.2128009952263609783, -0.9770955615653315052 ) ) ;
#162802=CARTESIAN_POINT ( 'NONE',  ( -20.54999999999999716, 9.614325556249161409, -211.5456030694648746 ) ) ;
#162839=EDGE_LOOP ( 'NONE', ( #9194, #168556, #89445, #60424 ) ) ;
#162854=FACE_OUTER_BOUND ( 'NONE', #256537, .T. ) ;
#162871=CARTESIAN_POINT ( 'NONE',  ( -21.05000000000000071, 6.390846877240203838, -199.6081416912452937 ) ) ;
#162924=CARTESIAN_POINT ( 'NONE',  ( 21.07928932188134041, -1.250084634897252522, -194.7953894783236990 ) ) ;
#162960=CARTESIAN_POINT ( 'NONE',  ( -18.59999999999999787, 13.67914474873013475, -219.8713009340548865 ) ) ;
#163019=CARTESIAN_POINT ( 'NONE',  ( 19.83283456528358002, 16.76897757965512881, -222.7804130104206592 ) ) ;
#163083=ADVANCED_FACE ( 'NONE', ( #139179 ), #220719, .T. ) ;
#163137=DIRECTION ( 'NONE',  ( 1.000000000000000000, 0.000000000000000000, 0.000000000000000000 ) ) ;
#163163=CARTESIAN_POINT ( 'NONE',  ( -21.05000000000000071, 4.273531877263400780, -211.9976340888692050 ) ) ;
#163231=DIRECTION ( 'NONE',  ( -2.952720810173287633E-16, 0.9770955615653312831, 0.2128009952263610616 ) ) ;
#163266=CARTESIAN_POINT ( 'NONE',  ( 21.07199075132372101, 11.17301161084810168, -211.0664710372803938 ) ) ;
#163274=ORIENTED_EDGE ( 'NONE', *, *, #136050, .F. ) ;
#163281=ADVANCED_FACE ( 'NONE', ( #170375 ), #110342, .F. ) ;
#163287=VERTEX_POINT ( 'NONE', #167786 ) ;
#163295=CARTESIAN_POINT ( 'NONE',  ( 19.97071067811864609, 16.69779891432240149, -222.5912266955230621 ) ) ;
#163310=CARTESIAN_POINT ( 'NONE',  ( 21.05000000000000071, 10.39655183198268418, -207.4949966697317620 ) ) ;
#163312=VERTEX_POINT ( 'NONE', #111632 ) ;
#163318=EDGE_CURVE ( 'NONE', #121941, #21979, #224793, .T. ) ;
#163328=ORIENTED_EDGE ( 'NONE', *, *, #38561, .T. ) ;
#163369=ORIENTED_EDGE ( 'NONE', *, *, #155374, .T. ) ;
#163376=EDGE_LOOP ( 'NONE', ( #37209, #17150, #106106, #229418, #176127, #49910, #88841 ) ) ;
#163386=ORIENTED_EDGE ( 'NONE', *, *, #71757, .T. ) ;
#163413=DIRECTION ( 'NONE',  ( -0.000000000000000000, 0.2128009952263603677, -0.9770955615653313941 ) ) ;
#163424=AXIS2_PLACEMENT_3D ( 'NONE', #140374, #122116, #227617 ) ;
#163434=CARTESIAN_POINT ( 'NONE',  ( 21.05000000000000071, 8.433899723187009201, -209.4150263691077782 ) ) ;
#163456=DIRECTION ( 'NONE',  ( 0.000000000000000000, 0.2128009952263403282, -0.9770955615653358350 ) ) ;
#163470=EDGE_CURVE ( 'NONE', #365, #43729, #174217, .T. ) ;
#163474=CIRCLE ( 'NONE', #138321, 0.09999999999999942268 ) ;
#163475=CARTESIAN_POINT ( 'NONE',  ( -20.54999999999999716, 13.63658454968486389, -219.6758818217417968 ) ) ;
#163504=ORIENTED_EDGE ( 'NONE', *, *, #227044, .F. ) ;
#163508=CIRCLE ( 'NONE', #51043, 4.299999999999969624 ) ;
#163516=EDGE_CURVE ( 'NONE', #44981, #245138, #58184, .T. ) ;
#163521=CARTESIAN_POINT ( 'NONE',  ( -21.64999999999999858, 9.690755012883050412, -211.4266134137857023 ) ) ;
#163526=DIRECTION ( 'NONE',  ( 0.000000000000000000, 0.2128009952263601179, -0.9770955615653315052 ) ) ;
#163542=DIRECTION ( 'NONE',  ( 0.000000000000000000, -0.2128009952263604232, 0.9770955615653316162 ) ) ;
#163554=FACE_OUTER_BOUND ( 'NONE', #32870, .T. ) ;
#163560=CARTESIAN_POINT ( 'NONE',  ( 20.94999999999999929, -4.259020970815407203, -226.0869574510824123 ) ) ;
#163582=ORIENTED_EDGE ( 'NONE', *, *, #43507, .T. ) ;
#163588=AXIS2_PLACEMENT_3D ( 'NONE', #134941, #179265, #35898 ) ;
#163658=DIRECTION ( 'NONE',  ( 1.000000000000000000, -0.000000000000000000, -0.000000000000000000 ) ) ;
#163750=CARTESIAN_POINT ( 'NONE',  ( -20.64999999999999858, 6.878457983866232972, -212.1414458560986986 ) ) ;
#163753=AXIS2_PLACEMENT_3D ( 'NONE', #89059, #112504, #192050 ) ;
#163754=FACE_OUTER_BOUND ( 'NONE', #201224, .T. ) ;
#163761=VERTEX_POINT ( 'NONE', #246981 ) ;
#163763=CARTESIAN_POINT ( 'NONE',  ( 23.14999999999999503, 13.96869538424789070, -210.3925794786331949 ) ) ;
#163773=DIRECTION ( 'NONE',  ( 0.000000000000000000, -0.2128009952272136851, 0.9770955615651456538 ) ) ;
#163782=EDGE_LOOP ( 'NONE', ( #106830, #63611 ) ) ;
#163794=SPHERICAL_SURFACE ( 'NONE', #61655, 0.1000000000000000056 ) ;
#163827=DIRECTION ( 'NONE',  ( 0.000000000000000000, 0.2128009952263403282, -0.9770955615653358350 ) ) ;
#163834=ORIENTED_EDGE ( 'NONE', *, *, #64624, .F. ) ;
#163845=CIRCLE ( 'NONE', #180411, 0.09999999999999939493 ) ;
#163858=EDGE_CURVE ( 'NONE', #243059, #21979, #77326, .T. ) ;
#163877=DIRECTION ( 'NONE',  ( 1.000000000000000000, 0.000000000000000000, 0.000000000000000000 ) ) ;
#163883=FACE_OUTER_BOUND ( 'NONE', #71711, .T. ) ;
#163889=DIRECTION ( 'NONE',  ( -1.000000000000000000, 0.000000000000000000, 0.000000000000000000 ) ) ;
#163905=EDGE_LOOP ( 'NONE', ( #234555, #162398, #133436, #240028 ) ) ;
#163929=EDGE_CURVE ( 'NONE', #192537, #162084, #21015, .T. ) ;
#163980=VERTEX_POINT ( 'NONE', #142446 ) ;
#164004=ORIENTED_EDGE ( 'NONE', *, *, #256442, .T. ) ;
#164011=CIRCLE ( 'NONE', #193062, 0.5000000000000007772 ) ;
#164041=DIRECTION ( 'NONE',  ( 0.000000000000000000, -0.2965989261549489275, -0.9550021345545417484 ) ) ;
#164042=AXIS2_PLACEMENT_3D ( 'NONE', #162194, #100859, #141323 ) ;
#164065=ORIENTED_EDGE ( 'NONE', *, *, #177727, .T. ) ;
#164068=TOROIDAL_SURFACE ( 'NONE', #72491, 4.099999999999999645, 0.1000000000000000056 ) ;
#164088=DIRECTION ( 'NONE',  ( -1.000000000000000000, 0.000000000000000000, 0.000000000000000000 ) ) ;
#164103=CARTESIAN_POINT ( 'NONE',  ( -18.50000000000000000, 13.96869538424787649, -210.3925794786331949 ) ) ;
#164105=CYLINDRICAL_SURFACE ( 'NONE', #234191, 0.09999999999999691080 ) ;
#164106=CARTESIAN_POINT ( 'NONE',  ( -18.59999999999999787, 7.783179459866045313, -245.3643104511423303 ) ) ;
#164130=VERTEX_POINT ( 'NONE', #136671 ) ;
#164134=CARTESIAN_POINT ( 'NONE',  ( 21.12642695952774119, -1.260108817593847519, -194.7493242710371248 ) ) ;
#164142=CARTESIAN_POINT ( 'NONE',  ( -21.05000000000000071, 6.412126976762841046, -199.7058512474018244 ) ) ;
#164150=DIRECTION ( 'NONE',  ( 0.000000000000000000, 0.2128009952263603677, -0.9770955615653313941 ) ) ;
#164174=DIRECTION ( 'NONE',  ( 0.000000000000000000, -0.2128009952263585913, 0.9770955615653319493 ) ) ;
#164183=VECTOR ( 'NONE', #28635, 1000.000000000000000 ) ;
#164195=CARTESIAN_POINT ( 'NONE',  ( 21.05000000000000071, -1.300607522999445820, -194.8777000085252666 ) ) ;
#164196=CARTESIAN_POINT ( 'NONE',  ( 20.94999999999999574, 10.52493806863738079, -207.3780514093641330 ) ) ;
#164198=DIRECTION ( 'NONE',  ( 1.000000000000000000, 0.000000000000000000, 0.000000000000000000 ) ) ;
#164205=AXIS2_PLACEMENT_3D ( 'NONE', #105152, #85597, #253685 ) ;
#164230=ORIENTED_EDGE ( 'NONE', *, *, #186124, .T. ) ;
#164260=CYLINDRICAL_SURFACE ( 'NONE', #98352, 0.09999999999999895084 ) ;
#164269=DIRECTION ( 'NONE',  ( 1.000000000000000000, 0.000000000000000000, 0.000000000000000000 ) ) ;
#164299=CIRCLE ( 'NONE', #160027, 0.1000000000000128147 ) ;
#164312=ORIENTED_EDGE ( 'NONE', *, *, #175032, .F. ) ;
#164339=EDGE_CURVE ( 'NONE', #245998, #79677, #15153, .T. ) ;
#164341=ORIENTED_EDGE ( 'NONE', *, *, #124172, .T. ) ;
#164348=CIRCLE ( 'NONE', #22887, 0.09999999999999767408 ) ;
#164353=DIRECTION ( 'NONE',  ( 1.000000000000000000, 0.000000000000000000, 0.000000000000000000 ) ) ;
#164376=DIRECTION ( 'NONE',  ( 0.000000000000000000, -0.2128009952263603954, 0.9770955615653315052 ) ) ;
#164431=EDGE_CURVE ( 'NONE', #217380, #109970, #232935, .T. ) ;
#164433=CARTESIAN_POINT ( 'NONE',  ( -20.94999999999999929, 7.939498413483247141, -209.7295111514051200 ) ) ;
#164445=CARTESIAN_POINT ( 'NONE',  ( 20.95595012432479365, 11.97768371613162586, -206.1652126091303785 ) ) ;
#164453=ORIENTED_EDGE ( 'NONE', *, *, #72698, .T. ) ;
#164473=CARTESIAN_POINT ( 'NONE',  ( 21.10257677756355932, -1.337202735977050638, -194.7428600538324019 ) ) ;
#164492=ADVANCED_FACE ( 'NONE', ( #252451 ), #21373, .F. ) ;
#164546=DIRECTION ( 'NONE',  ( 0.000000000000000000, 0.2128009952263485993, -0.9770955615653341697 ) ) ;
#164555=VERTEX_POINT ( 'NONE', #119387 ) ;
#164568=VECTOR ( 'NONE', #7475, 1000.000000000000227 ) ;
#164582=CARTESIAN_POINT ( 'NONE',  ( -22.47071067811865674, 7.522163794833024220, -199.2603376134759117 ) ) ;
#164629=EDGE_LOOP ( 'NONE', ( #177591, #49515, #91766, #93389 ) ) ;
#164661=VERTEX_POINT ( 'NONE', #61982 ) ;
#164670=CARTESIAN_POINT ( 'NONE',  ( -21.05000000000000071, 4.252251777740764460, -211.8999245327126744 ) ) ;
#164686=EDGE_CURVE ( 'NONE', #92384, #229005, #213062, .T. ) ;
#164707=VERTEX_POINT ( 'NONE', #247015 ) ;
#164714=ORIENTED_EDGE ( 'NONE', *, *, #241162, .F. ) ;
#164737=DIRECTION ( 'NONE',  ( 0.000000000000000000, 0.2128009952263485993, -0.9770955615653341697 ) ) ;
#164798=CARTESIAN_POINT ( 'NONE',  ( -20.64999999999999858, 9.690755012883057518, -211.4266134137857023 ) ) ;
#164817=DIRECTION ( 'NONE',  ( 1.000000000000000000, 0.000000000000000000, 0.000000000000000000 ) ) ;
#164831=FACE_OUTER_BOUND ( 'NONE', #153732, .T. ) ;
#164846=CARTESIAN_POINT ( 'NONE',  ( 21.05000000000000071, 13.06921230367881037, -210.6153319958218617 ) ) ;
#164847=DIRECTION ( 'NONE',  ( 0.000000000000000000, 0.2128009952263485993, -0.9770955615653341697 ) ) ;
#164848=CYLINDRICAL_SURFACE ( 'NONE', #28118, 11.80000000000000959 ) ;
#164850=ORIENTED_EDGE ( 'NONE', *, *, #121678, .T. ) ;
#164853=ORIENTED_EDGE ( 'NONE', *, *, #144022, .T. ) ;
#164857=DIRECTION ( 'NONE',  ( 1.000000000000000000, 0.000000000000000000, 0.000000000000000000 ) ) ;
#164877=ORIENTED_EDGE ( 'NONE', *, *, #237068, .T. ) ;
#164887=ORIENTED_EDGE ( 'NONE', *, *, #19330, .T. ) ;
#164894=LINE ( 'NONE', #167485, #135106 ) ;
#164923=DIRECTION ( 'NONE',  ( 0.000000000000000000, -0.2128009952263604232, 0.9770955615653316162 ) ) ;
#164953=CYLINDRICAL_SURFACE ( 'NONE', #42767, 0.1000000000000055844 ) ;
#164966=LINE ( 'NONE', #104952, #86348 ) ;
#164975=AXIS2_PLACEMENT_3D ( 'NONE', #1398, #240039, #13941 ) ;
#165008=ORIENTED_EDGE ( 'NONE', *, *, #106759, .F. ) ;
#165011=ORIENTED_EDGE ( 'NONE', *, *, #70471, .T. ) ;
#165014=VERTEX_POINT ( 'NONE', #114782 ) ;
#165018=CARTESIAN_POINT ( 'NONE',  ( -23.25000000000000000, 8.751106741858205140, -220.7398867978735950 ) ) ;
#165029=CARTESIAN_POINT ( 'NONE',  ( -23.25000000000000000, -2.576749817950531707, -189.6385361693310756 ) ) ;
#165052=EDGE_CURVE ( 'NONE', #130647, #17019, #192589, .T. ) ;
#165061=ORIENTED_EDGE ( 'NONE', *, *, #107189, .F. ) ;
#165070=DIRECTION ( 'NONE',  ( 1.000000000000000000, 0.000000000000000000, 0.000000000000000000 ) ) ;
#165078=DIRECTION ( 'NONE',  ( 1.000000000000000000, 0.000000000000000000, 0.000000000000000000 ) ) ;
#165087=CARTESIAN_POINT ( 'NONE',  ( 20.85000000000000142, 7.128833340094563376, -233.7327013124401276 ) ) ;
#165110=CARTESIAN_POINT ( 'NONE',  ( -18.59999999999999787, 2.953700692300310848, -208.6327728934509764 ) ) ;
#165116=EDGE_CURVE ( 'NONE', #241204, #114637, #250841, .T. ) ;
#165142=AXIS2_PLACEMENT_3D ( 'NONE', #51446, #213119, #34510 ) ;
#165151=DIRECTION ( 'NONE',  ( -0.000000000000000000, 0.2253241261139106999, -0.9742838591452712693 ) ) ;
#165154=CARTESIAN_POINT ( 'NONE',  ( -21.65000000000000213, 10.16011026985487398, -211.4267369781599939 ) ) ;
#165166=DIRECTION ( 'NONE',  ( -1.000000000000000000, 0.000000000000000000, 0.000000000000000000 ) ) ;
#165173=CARTESIAN_POINT ( 'NONE',  ( 21.13461538461538680, 11.30999384151885856, -211.1763045966511356 ) ) ;
#165182=ADVANCED_FACE ( 'NONE', ( #256799 ), #16984, .F. ) ;
#165185=LINE ( 'NONE', #126039, #22959 ) ;
#165189=AXIS2_PLACEMENT_3D ( 'NONE', #184284, #185574, #89033 ) ;
#165216=VERTEX_POINT ( 'NONE', #176068 ) ;
#165220=CIRCLE ( 'NONE', #136149, 0.09999999999999939493 ) ;
#165223=DIRECTION ( 'NONE',  ( 1.000000000000000000, 0.000000000000000000, 0.000000000000000000 ) ) ;
#165233=EDGE_CURVE ( 'NONE', #102935, #174819, #205038, .T. ) ;
#165239=ORIENTED_EDGE ( 'NONE', *, *, #117924, .F. ) ;
#165274=DIRECTION ( 'NONE',  ( 1.000000000000000000, -0.000000000000000000, -0.000000000000000000 ) ) ;
#165286=ADVANCED_FACE ( 'NONE', ( #95374 ), #175863, .T. ) ;
#165292=EDGE_CURVE ( 'NONE', #31563, #121315, #111083, .T. ) ;
#165317=PLANE ( 'NONE',  #101924 ) ;
#165332=TOROIDAL_SURFACE ( 'NONE', #165536, 12.77499999999999858, 0.1000000000000000056 ) ;
#165334=ORIENTED_EDGE ( 'NONE', *, *, #252105, .F. ) ;
#165338=CARTESIAN_POINT ( 'NONE',  ( 21.05000000000000071, -4.892732937820623462, -233.2805462221312496 ) ) ;
#165363=ORIENTED_EDGE ( 'NONE', *, *, #92768, .F. ) ;
#165370=TOROIDAL_SURFACE ( 'NONE', #127771, 0.2000000000000000111, 0.1000000000000000056 ) ;
#165415=CARTESIAN_POINT ( 'NONE',  ( -23.25000000000000000, 8.882751598337867094, -187.0399955572217721 ) ) ;
#165476=CARTESIAN_POINT ( 'NONE',  ( -23.25000000000000000, 7.804459559388685186, -245.4620200072988325 ) ) ;
#165499=ADVANCED_FACE ( 'NONE', ( #170806 ), #171970, .T. ) ;
#165501=CARTESIAN_POINT ( 'NONE',  ( -21.33487959338958362, 6.571513019293445446, -199.5687945318220500 ) ) ;
#165505=DIRECTION ( 'NONE',  ( 1.000000000000000000, 0.000000000000000000, 0.000000000000000000 ) ) ;
#165513=ORIENTED_EDGE ( 'NONE', *, *, #25968, .T. ) ;
#165519=DIRECTION ( 'NONE',  ( -1.000000000000000000, 0.000000000000000000, 0.000000000000000000 ) ) ;
#165525=CARTESIAN_POINT ( 'NONE',  ( 18.50000000000000000, -0.6242021414292636683, -242.4056766684517186 ) ) ;
#165536=AXIS2_PLACEMENT_3D ( 'NONE', #192684, #55684, #131405 ) ;
#165560=VECTOR ( 'NONE', #147636, 1000.000000000000000 ) ;
#165574=DIRECTION ( 'NONE',  ( 0.000000000000000000, -0.2128009952263602012, 0.9770955615653315052 ) ) ;
#165581=CARTESIAN_POINT ( 'NONE',  ( 18.59999999999999787, 1.148907358139439339E-11, -201.0000000000015064 ) ) ;
#165631=DIRECTION ( 'NONE',  ( 0.000000000000000000, 0.2128009952263604510, -0.9770955615653315052 ) ) ;
#165653=EDGE_CURVE ( 'NONE', #187418, #165014, #238567, .T. ) ;
#165685=VERTEX_POINT ( 'NONE', #36402 ) ;
#165688=AXIS2_PLACEMENT_3D ( 'NONE', #231483, #52815, #132366 ) ;
#165693=LINE ( 'NONE', #129113, #93599 ) ;
#165695=EDGE_CURVE ( 'NONE', #61015, #117533, #193332, .T. ) ;
#165737=CARTESIAN_POINT ( 'NONE',  ( 20.95512820512820085, 12.01161663143393454, -206.2285874551107554 ) ) ;
#165739=EDGE_CURVE ( 'NONE', #32893, #56802, #63584, .T. ) ;
#165747=DIRECTION ( 'NONE',  ( -1.000000000000000000, 3.389981217840264988E-14, 7.383017642607961770E-15 ) ) ;
#165751=EDGE_CURVE ( 'NONE', #38916, #217539, #17777, .T. ) ;
#165760=ORIENTED_EDGE ( 'NONE', *, *, #187616, .F. ) ;
#165811=DIRECTION ( 'NONE',  ( -0.000000000000000000, 0.9770955615653313941, 0.2128009952263603677 ) ) ;
#165816=DIRECTION ( 'NONE',  ( -1.000000000000000000, 0.000000000000000000, 0.000000000000000000 ) ) ;
#165838=DIRECTION ( 'NONE',  ( -1.000000000000000000, 0.000000000000000000, 0.000000000000000000 ) ) ;
#165839=CARTESIAN_POINT ( 'NONE',  ( 21.13920837816993270, 11.18888390033836266, -211.1003369155923224 ) ) ;
#165872=CARTESIAN_POINT ( 'NONE',  ( 19.75857864376268935, 16.64998792410002793, -222.7039835543563981 ) ) ;
#165890=ADVANCED_FACE ( 'NONE', ( #230091 ), #241000, .F. ) ;
#165895=CARTESIAN_POINT ( 'NONE',  ( -23.25000000000000000, 7.668827189579289438, -241.6142244293585009 ) ) ;
#165908=DIRECTION ( 'NONE',  ( 0.000000000000000000, 0.9964539953858966292, 0.08413937888696132461 ) ) ;
#165947=ORIENTED_EDGE ( 'NONE', *, *, #54977, .T. ) ;
#165980=ORIENTED_EDGE ( 'NONE', *, *, #245685, .F. ) ;
#165996=EDGE_LOOP ( 'NONE', ( #206823, #155963, #173143, #38850 ) ) ;
#166004=CARTESIAN_POINT ( 'NONE',  ( 23.24999999999999645, 2.971323450867608518, -188.3274415783412508 ) ) ;
#166016=CIRCLE ( 'NONE', #53561, 0.1000000000000099282 ) ;
#166070=CARTESIAN_POINT ( 'NONE',  ( 20.94999999999999929, -3.444512620907435263, -226.2123967847655308 ) ) ;
#166100=VECTOR ( 'NONE', #171417, 1000.000000000000227 ) ;
#166121=CARTESIAN_POINT ( 'NONE',  ( 20.94999999999999574, 4.288595810029049993, -211.9930862808554934 ) ) ;
#166141=TOROIDAL_SURFACE ( 'NONE', #57753, 0.2000000000000000111, 0.1000000000000000056 ) ;
#166143=CARTESIAN_POINT ( 'NONE',  ( -20.85000000000000142, 18.60970618848720903, -231.2322896185303875 ) ) ;
#166163=EDGE_LOOP ( 'NONE', ( #42438, #155676, #212607, #92512, #203078, #104474, #116403, #177091, #199059, #9824, #34802, #148425 ) ) ;
#166165=VERTEX_POINT ( 'NONE', #167278 ) ;
#166166=ORIENTED_EDGE ( 'NONE', *, *, #38869, .T. ) ;
#166215=CARTESIAN_POINT ( 'NONE',  ( 23.15000000000000213, -6.688413578037176066, -212.5825622730469036 ) ) ;
#166227=CARTESIAN_POINT ( 'NONE',  ( -20.64999999999999858, -3.770473190032741062, -225.9805569534692324 ) ) ;
#166274=CYLINDRICAL_SURFACE ( 'NONE', #201346, 0.5000000000000007772 ) ;
#166290=ORIENTED_EDGE ( 'NONE', *, *, #252110, .T. ) ;
#166295=CIRCLE ( 'NONE', #108011, 0.1000000000000055844 ) ;
#166296=ORIENTED_EDGE ( 'NONE', *, *, #239586, .F. ) ;
#166317=CARTESIAN_POINT ( 'NONE',  ( -23.15000000000000213, 4.768403829798271154, -213.4961173936592331 ) ) ;
#166339=CARTESIAN_POINT ( 'NONE',  ( -20.94999999999999929, 7.128833340094563376, -233.7327013124401276 ) ) ;
#166348=ORIENTED_EDGE ( 'NONE', *, *, #123972, .F. ) ;
#166372=CARTESIAN_POINT ( 'NONE',  ( -18.52139480978223318, -7.769361016604765524, -209.8813056420265752 ) ) ;
#166419=DIRECTION ( 'NONE',  ( 0.000000000000000000, 0.2128009952263601734, -0.9770955615653316162 ) ) ;
#166422=ORIENTED_EDGE ( 'NONE', *, *, #137755, .T. ) ;
#166432=EDGE_CURVE ( 'NONE', #211815, #68317, #155586, .T. ) ;
#166449=VERTEX_POINT ( 'NONE', #1436 ) ;
#166491=CIRCLE ( 'NONE', #137407, 0.09999999999999641120 ) ;
#166498=CIRCLE ( 'NONE', #208178, 0.1000000000000054040 ) ;
#166514=AXIS2_PLACEMENT_3D ( 'NONE', #94636, #160757, #235422 ) ;
#166570=EDGE_CURVE ( 'NONE', #111449, #64043, #243901, .T. ) ;
#166603=DIRECTION ( 'NONE',  ( 0.000000000000000000, 0.2128009952263603677, -0.9770955615653313941 ) ) ;
#166652=CARTESIAN_POINT ( 'NONE',  ( -20.85000000000000142, 17.16609282392353819, -224.6038045889790453 ) ) ;
#166679=ORIENTED_EDGE ( 'NONE', *, *, #212022, .F. ) ;
#166682=CARTESIAN_POINT ( 'NONE',  ( -21.05000000000000071, 7.128833340094563376, -233.7327013124401276 ) ) ;
#166687=EDGE_CURVE ( 'NONE', #235587, #191384, #143520, .T. ) ;
#166718=ORIENTED_EDGE ( 'NONE', *, *, #244057, .T. ) ;
#166729=CARTESIAN_POINT ( 'NONE',  ( 20.94999999999999574, 1.148907358139439339E-11, -201.0000000000015064 ) ) ;
#166746=CARTESIAN_POINT ( 'NONE',  ( -20.85000000000000142, 7.788796164756791818, -245.4641525896719543 ) ) ;
#166779=LINE ( 'NONE', #65072, #142275 ) ;
#166804=CARTESIAN_POINT ( 'NONE',  ( -22.39999999999999858, 7.612336166715881092, -199.3421143478784359 ) ) ;
#166810=EDGE_CURVE ( 'NONE', #34173, #103882, #125916, .T. ) ;
#166816=AXIS2_PLACEMENT_3D ( 'NONE', #10507, #88719, #54745 ) ;
#166833=ORIENTED_EDGE ( 'NONE', *, *, #124172, .F. ) ;
#166844=CARTESIAN_POINT ( 'NONE',  ( -22.57320508075687115, 11.48087284840413425, -198.4995883060917663 ) ) ;
#166851=DIRECTION ( 'NONE',  ( 1.000000000000000000, 2.885090398161910739E-16, 6.283419270304611573E-17 ) ) ;
#166864=CARTESIAN_POINT ( 'NONE',  ( -22.47120815636973745, -2.450875325420101447, -189.6107523991855146 ) ) ;
#166899=DIRECTION ( 'NONE',  ( 0.000000000000000000, 0.2128009952263403282, -0.9770955615653358350 ) ) ;
#166916=EDGE_CURVE ( 'NONE', #158102, #235411, #42729, .T. ) ;
#167010=ORIENTED_EDGE ( 'NONE', *, *, #170635, .T. ) ;
#167024=DIRECTION ( 'NONE',  ( -1.000000000000000000, 0.000000000000000000, 0.000000000000000000 ) ) ;
#167040=EDGE_CURVE ( 'NONE', #87043, #193316, #247377, .T. ) ;
#167042=CYLINDRICAL_SURFACE ( 'NONE', #7955, 7.900000000000007461 ) ;
#167053=AXIS2_PLACEMENT_3D ( 'NONE', #191405, #92257, #231798 ) ;
#167064=DIRECTION ( 'NONE',  ( 1.000000000000000000, 0.000000000000000000, 0.000000000000000000 ) ) ;
#167121=EDGE_CURVE ( 'NONE', #145277, #77509, #25854, .T. ) ;
#167148=VECTOR ( 'NONE', #218292, 1000.000000000000227 ) ;
#167220=ORIENTED_EDGE ( 'NONE', *, *, #87222, .F. ) ;
#167227=DIRECTION ( 'NONE',  ( 1.713247197920696616E-14, 0.9983803033886531342, 0.05689261644169053833 ) ) ;
#167231=CARTESIAN_POINT ( 'NONE',  ( 21.05000000000000071, 7.128833340094563376, -233.7327013124401276 ) ) ;
#167278=CARTESIAN_POINT ( 'NONE',  ( -22.50000000000000000, 11.36146383068193444, -198.4232501820394816 ) ) ;
#167284=CARTESIAN_POINT ( 'NONE',  ( 23.14999999999999858, 3.220451093833237355, -234.5839052933455378 ) ) ;
#167293=CARTESIAN_POINT ( 'NONE',  ( 18.59999999999999787, 0.6656436123793491033, -212.6810495496487476 ) ) ;
#167308=ORIENTED_EDGE ( 'NONE', *, *, #148300, .T. ) ;
#167342=CARTESIAN_POINT ( 'NONE',  ( 21.14999999999999858, -1.489567864901280680, -194.6304332222954372 ) ) ;
#167345=AXIS2_PLACEMENT_3D ( 'NONE', #241557, #206288, #66778 ) ;
#167380=CARTESIAN_POINT ( 'NONE',  ( 20.85000000000000142, 14.80545736607782814, -235.9842437978701639 ) ) ;
#167388=CARTESIAN_POINT ( 'NONE',  ( 23.24999999999999289, 9.125777775466493935, -211.6520035670780544 ) ) ;
#167403=FACE_OUTER_BOUND ( 'NONE', #154539, .T. ) ;
#167412=DIRECTION ( 'NONE',  ( 0.000000000000000000, 0.2128009952263604232, -0.9770955615653316162 ) ) ;
#167415=VERTEX_POINT ( 'NONE', #77784 ) ;
#167419=AXIS2_PLACEMENT_3D ( 'NONE', #93012, #170035, #34355 ) ;
#167468=ORIENTED_EDGE ( 'NONE', *, *, #207983, .F. ) ;
#167477=ORIENTED_EDGE ( 'NONE', *, *, #65801, .T. ) ;
#167482=ORIENTED_EDGE ( 'NONE', *, *, #217162, .F. ) ;
#167485=CARTESIAN_POINT ( 'NONE',  ( -22.50000000000000000, -2.479040261793999722, -189.6172560698084624 ) ) ;
#167496=AXIS2_PLACEMENT_3D ( 'NONE', #22120, #159068, #174807 ) ;
#167518=ORIENTED_EDGE ( 'NONE', *, *, #53905, .T. ) ;
#167532=CARTESIAN_POINT ( 'NONE',  ( -20.94999999999999929, 7.128833340094563376, -233.7327013124401276 ) ) ;
#167539=ORIENTED_EDGE ( 'NONE', *, *, #206142, .F. ) ;
#167582=DIRECTION ( 'NONE',  ( 0.000000000000000000, 0.9968797965484670343, 0.07893460099023182075 ) ) ;
#167633=ORIENTED_EDGE ( 'NONE', *, *, #232511, .T. ) ;
#167645=ORIENTED_EDGE ( 'NONE', *, *, #83706, .F. ) ;
#167649=VECTOR ( 'NONE', #44444, 1000.000000000000000 ) ;
#167677=CIRCLE ( 'NONE', #88513, 0.1000000000000054040 ) ;
#167701=CARTESIAN_POINT ( 'NONE',  ( -18.39999999999999858, -7.792952876741447987, -209.8605804245960655 ) ) ;
#167724=ORIENTED_EDGE ( 'NONE', *, *, #177675, .T. ) ;
#167735=CARTESIAN_POINT ( 'NONE',  ( -20.94999999999999929, 2.923777413779037548, -208.5507632484912222 ) ) ;
#167762=VERTEX_POINT ( 'NONE', #148722 ) ;
#167769=CARTESIAN_POINT ( 'NONE',  ( 21.05000000000000071, 11.38316329224760892, -198.5208684056144079 ) ) ;
#167771=EDGE_CURVE ( 'NONE', #2973, #44901, #58970, .T. ) ;
#167786=CARTESIAN_POINT ( 'NONE',  ( -20.94999999999999929, 17.06838326776700399, -224.6250846885016870 ) ) ;
#167795=AXIS2_PLACEMENT_3D ( 'NONE', #68738, #72604, #148269 ) ;
#167810=DIRECTION ( 'NONE',  ( -1.000000000000000000, 0.000000000000000000, 0.000000000000000000 ) ) ;
#167869=DIRECTION ( 'NONE',  ( 1.836970198721029934E-16, -0.9770955615653316162, -0.2128009952263604232 ) ) ;
#167875=DIRECTION ( 'NONE',  ( -1.000000000000000000, -0.000000000000000000, -0.000000000000000000 ) ) ;
#167887=CARTESIAN_POINT ( 'NONE',  ( -20.54999999999999716, -3.770473190032741062, -225.9805569534692324 ) ) ;
#167945=DIRECTION ( 'NONE',  ( -1.000000000000000000, 0.000000000000000000, 0.000000000000000000 ) ) ;
#167948=DIRECTION ( 'NONE',  ( 0.000000000000000000, -0.2128009952263403282, 0.9770955615653358350 ) ) ;
#167956=DIRECTION ( 'NONE',  ( -1.000000000000000000, -2.885090398161910739E-16, -6.283419270304611573E-17 ) ) ;
#168010=DIRECTION ( 'NONE',  ( 0.000000000000000000, 0.2128009952263678062, -0.9770955615653298398 ) ) ;
#168013=EDGE_CURVE ( 'NONE', #173624, #220140, #138636, .T. ) ;
#168037=ORIENTED_EDGE ( 'NONE', *, *, #185984, .F. ) ;
#168077=CARTESIAN_POINT ( 'NONE',  ( -23.25000000000000000, 14.70949956575304185, -235.9560995168023112 ) ) ;
#168080=DIRECTION ( 'NONE',  ( 0.000000000000000000, 0.2128009952263485993, -0.9770955615653341697 ) ) ;
#168084=CARTESIAN_POINT ( 'NONE',  ( 21.05000000000000071, -1.236118717437887371, -194.8647072476926212 ) ) ;
#168097=AXIS2_PLACEMENT_3D ( 'NONE', #200409, #37500, #117022 ) ;
#168106=ORIENTED_EDGE ( 'NONE', *, *, #105248, .T. ) ;
#168110=AXIS2_PLACEMENT_3D ( 'NONE', #103606, #22841, #241855 ) ;
#168119=ADVANCED_FACE ( 'NONE', ( #162854 ), #42887, .F. ) ;
#168123=CARTESIAN_POINT ( 'NONE',  ( 20.94999999999999929, 7.128833340094563376, -233.7327013124401276 ) ) ;
#168127=CARTESIAN_POINT ( 'NONE',  ( 18.41815437325345073, -0.7469876510888040499, -242.2067223904661830 ) ) ;
#168150=VECTOR ( 'NONE', #88491, 1000.000000000000000 ) ;
#168184=CARTESIAN_POINT ( 'NONE',  ( -18.59999999999999787, 1.148907358139439339E-11, -201.0000000000015064 ) ) ;
#168191=CARTESIAN_POINT ( 'NONE',  ( 23.15000000000000213, -7.176961358819842651, -212.6889627706600834 ) ) ;
#168230=CARTESIAN_POINT ( 'NONE',  ( 23.14999999999999858, 17.01923898301590654, -224.3994341343041867 ) ) ;
#168288=CYLINDRICAL_SURFACE ( 'NONE', #169660, 0.1000000000000055844 ) ;
#168300=ORIENTED_EDGE ( 'NONE', *, *, #168839, .T. ) ;
#168340=VECTOR ( 'NONE', #103027, 1000.000000000000227 ) ;
#168398=DIRECTION ( 'NONE',  ( 0.1538461538461468048, 0.9654630569144685426, 0.2102675597426226228 ) ) ;
#168405=EDGE_CURVE ( 'NONE', #32735, #183554, #220940, .T. ) ;
#168406=CARTESIAN_POINT ( 'NONE',  ( -21.12757541349819590, -1.372498826969863917, -194.6737902636474757 ) ) ;
#168413=DIRECTION ( 'NONE',  ( 0.000000000000000000, 0.2128009952263604232, -0.9770955615653316162 ) ) ;
#168440=AXIS2_PLACEMENT_3D ( 'NONE', #144276, #223824, #45204 ) ;
#168475=CARTESIAN_POINT ( 'NONE',  ( -22.47007471830798409, 7.543872110139036025, -199.3570250894167941 ) ) ;
#168492=ORIENTED_EDGE ( 'NONE', *, *, #255519, .T. ) ;
#168493=CARTESIAN_POINT ( 'NONE',  ( -18.59999999999999787, 7.654382455240002159, -241.6162809886059790 ) ) ;
#168538=EDGE_CURVE ( 'NONE', #30421, #214314, #192646, .T. ) ;
#168556=ORIENTED_EDGE ( 'NONE', *, *, #139640, .F. ) ;
#168557=AXIS2_PLACEMENT_3D ( 'NONE', #96216, #157528, #62237 ) ;
#168569=VERTEX_POINT ( 'NONE', #38730 ) ;
#168571=CYLINDRICAL_SURFACE ( 'NONE', #94925, 0.1000000000000055844 ) ;
#168603=EDGE_CURVE ( 'NONE', #38009, #211815, #125991, .T. ) ;
#168608=EDGE_LOOP ( 'NONE', ( #51327, #163582, #52311, #250191 ) ) ;
#168610=EDGE_CURVE ( 'NONE', #46709, #148979, #105111, .T. ) ;
#168616=VERTEX_POINT ( 'NONE', #64699 ) ;
#168629=ADVANCED_FACE ( 'NONE', ( #144219 ), #68563, .T. ) ;
#168632=ORIENTED_EDGE ( 'NONE', *, *, #154892, .T. ) ;
#168636=DIRECTION ( 'NONE',  ( 0.000000000000000000, -0.05616704890742720696, 0.9984213852963240710 ) ) ;
#168643=CYLINDRICAL_SURFACE ( 'NONE', #120343, 0.1000000000000055844 ) ;
#168666=DIRECTION ( 'NONE',  ( -1.000000000000000000, 7.136802563874201079E-16, 1.554319503706925800E-16 ) ) ;
#168685=ORIENTED_EDGE ( 'NONE', *, *, #85763, .T. ) ;
#168718=DIRECTION ( 'NONE',  ( 0.000000000000000000, 0.2128009952263403282, -0.9770955615653358350 ) ) ;
#168725=EDGE_LOOP ( 'NONE', ( #45237, #195098, #192908, #37749, #212247, #186780, #122350, #248558, #74347 ) ) ;
#168767=AXIS2_PLACEMENT_3D ( 'NONE', #118402, #195385, #16739 ) ;
#168783=ORIENTED_EDGE ( 'NONE', *, *, #136292, .F. ) ;
#168791=DIRECTION ( 'NONE',  ( -7.304098846218132695E-16, -0.9770955615653315052, -0.2128009952263603954 ) ) ;
#168817=CIRCLE ( 'NONE', #251977, 0.09999999999999939493 ) ;
#168832=ORIENTED_EDGE ( 'NONE', *, *, #195440, .F. ) ;
#168836=DIRECTION ( 'NONE',  ( 0.000000000000000000, 0.2128009952263485993, -0.9770955615653341697 ) ) ;
#168838=ORIENTED_EDGE ( 'NONE', *, *, #64309, .F. ) ;
#168839=EDGE_CURVE ( 'NONE', #65124, #77581, #138451, .T. ) ;
#168941=VERTEX_POINT ( 'NONE', #153800 ) ;
#168977=FACE_OUTER_BOUND ( 'NONE', #173206, .T. ) ;
#168979=CARTESIAN_POINT ( 'NONE',  ( -18.59999999999999787, -4.375386779258390924, -188.8379487402709742 ) ) ;
#169005=ADVANCED_FACE ( 'NONE', ( #173358 ), #213711, .F. ) ;
#169034=CIRCLE ( 'NONE', #231728, 3.900000000000000799 ) ;
#169043=CARTESIAN_POINT ( 'NONE',  ( -18.50000000000000000, 7.476371755685454090, -241.7308184205399471 ) ) ;
#169047=ORIENTED_EDGE ( 'NONE', *, *, #245359, .F. ) ;
#169053=ADVANCED_FACE ( 'NONE', ( #61047 ), #119774, .F. ) ;
#169060=CARTESIAN_POINT ( 'NONE',  ( 23.14999999999999858, 7.980037321000002848, -237.6410835587014390 ) ) ;
#169066=CARTESIAN_POINT ( 'NONE',  ( 21.06086055315972416, 11.17039406559869619, -211.0555683265898210 ) ) ;
#169079=DIRECTION ( 'NONE',  ( 0.000000000000000000, -0.2128009952263403282, 0.9770955615653358350 ) ) ;
#169080=VERTEX_POINT ( 'NONE', #255348 ) ;
#169108=DIRECTION ( 'NONE',  ( 0.000000000000000000, -0.2128009952264065807, 0.9770955615653215132 ) ) ;
#169112=DIRECTION ( 'NONE',  ( 0.000000000000000000, 0.9770955615653313941, 0.2128009952263603677 ) ) ;
#169239=EDGE_CURVE ( 'NONE', #95759, #195345, #106579, .T. ) ;
#169247=STYLED_ITEM ( 'NONE', ( #36835 ), #241103 ) ;
#169264=CIRCLE ( 'NONE', #194380, 0.09999999999999767408 ) ;
#169272=CARTESIAN_POINT ( 'NONE',  ( -20.85000000000000142, 7.783179459866048866, -245.3643104511423019 ) ) ;
#169299=CARTESIAN_POINT ( 'NONE',  ( 22.01447462590973458, -1.448975298746754792, -193.8814978911055107 ) ) ;
#169317=EDGE_LOOP ( 'NONE', ( #31891, #58021, #152961 ) ) ;
#169359=DIRECTION ( 'NONE',  ( 1.000000000000000000, 2.885090398161910739E-16, 6.283419270304611573E-17 ) ) ;
#169376=DIRECTION ( 'NONE',  ( -0.000000000000000000, 0.08413937888704771384, -0.9964539953858891908 ) ) ;
#169383=ORIENTED_EDGE ( 'NONE', *, *, #174786, .F. ) ;
#169414=DIRECTION ( 'NONE',  ( -1.000000000000000000, -0.000000000000000000, -0.000000000000000000 ) ) ;
#169422=DIRECTION ( 'NONE',  ( 0.000000000000000000, 0.2211802418851555596, -0.9752329468386637945 ) ) ;
#169435=CARTESIAN_POINT ( 'NONE',  ( -22.49756042579671700, -2.402844128467869655, -189.6003603154819359 ) ) ;
#169439=ORIENTED_EDGE ( 'NONE', *, *, #132391, .T. ) ;
#169474=AXIS2_PLACEMENT_3D ( 'NONE', #56561, #254749, #95710 ) ;
#169502=EDGE_LOOP ( 'NONE', ( #45302, #32398, #132314, #81835 ) ) ;
#169579=AXIS2_PLACEMENT_3D ( 'NONE', #190797, #211619, #111227 ) ;
#169599=LINE ( 'NONE', #86122, #237575 ) ;
#169620=AXIS2_PLACEMENT_3D ( 'NONE', #56429, #117701, #201091 ) ;
#169642=DIRECTION ( 'NONE',  ( 0.000000000000000000, 0.2128009952263603677, -0.9770955615653313941 ) ) ;
#169654=CARTESIAN_POINT ( 'NONE',  ( -18.59999999999999787, 8.980461154494397746, -187.0187154576991304 ) ) ;
#169660=AXIS2_PLACEMENT_3D ( 'NONE', #131677, #225613, #207382 ) ;
#169666=DIRECTION ( 'NONE',  ( 1.000000000000000000, 0.000000000000000000, 0.000000000000000000 ) ) ;
#169675=CARTESIAN_POINT ( 'NONE',  ( 22.42196299218230493, -2.476663215497191040, -189.6166965207286523 ) ) ;
#169718=DIRECTION ( 'NONE',  ( 0.000000000000000000, -0.2128009952263603954, 0.9770955615653315052 ) ) ;
#169723=DIRECTION ( 'NONE',  ( 1.000000000000000000, 0.000000000000000000, 0.000000000000000000 ) ) ;
#169727=DIRECTION ( 'NONE',  ( -1.000000000000000000, 0.000000000000000000, 0.000000000000000000 ) ) ;
#169729=EDGE_LOOP ( 'NONE', ( #166296, #120599, #208253, #8629 ) ) ;
#169754=CARTESIAN_POINT ( 'NONE',  ( -20.94999999999999929, 14.86477715130881272, -235.7932433709592601 ) ) ;
#169755=LINE ( 'NONE', #31523, #58611 ) ;
#169772=ORIENTED_EDGE ( 'NONE', *, *, #202327, .T. ) ;
#169773=EDGE_LOOP ( 'NONE', ( #181010, #43012, #139622, #78448 ) ) ;
#169785=ORIENTED_EDGE ( 'NONE', *, *, #150371, .F. ) ;
#169789=CIRCLE ( 'NONE', #144608, 0.1000000000000055844 ) ;
#169808=DIRECTION ( 'NONE',  ( 1.000000000000000000, 0.000000000000000000, 0.000000000000000000 ) ) ;
#169830=EDGE_CURVE ( 'NONE', #176941, #154288, #1631, .T. ) ;
#169834=EDGE_CURVE ( 'NONE', #16905, #90944, #209241, .T. ) ;
#169846=CARTESIAN_POINT ( 'NONE',  ( -23.25000000000000000, 11.48087284840413425, -198.4995883060917663 ) ) ;
#169857=ORIENTED_EDGE ( 'NONE', *, *, #239650, .F. ) ;
#169883=DIRECTION ( 'NONE',  ( -1.000000000000000000, -3.190570557967288949E-16, -6.948722487160392945E-17 ) ) ;
#169933=DIRECTION ( 'NONE',  ( -0.000000000000000000, -0.2128009952263604232, 0.9770955615653316162 ) ) ;
#169938=TOROIDAL_SURFACE ( 'NONE', #57443, 2.100000000000002309, 0.1000000000000000056 ) ;
#169956=DIRECTION ( 'NONE',  ( 0.000000000000000000, -0.2128009952258890225, 0.9770955615654342008 ) ) ;
#169960=DIRECTION ( 'NONE',  ( 0.000000000000000000, 0.9770955615653316162, 0.2128009952263604232 ) ) ;
#169963=VERTEX_POINT ( 'NONE', #34492 ) ;
#169968=CARTESIAN_POINT ( 'NONE',  ( 21.05000000000000071, 1.148907358139439339E-11, -201.0000000000015064 ) ) ;
#169993=ADVANCED_FACE ( 'NONE', ( #213096 ), #175294, .F. ) ;
#169994=DIRECTION ( 'NONE',  ( 0.000000000000000000, 0.2128009952263602844, -0.9770955615653315052 ) ) ;
#170006=CIRCLE ( 'NONE', #228231, 0.1000000000000055844 ) ;
#170026=CARTESIAN_POINT ( 'NONE',  ( -22.50000000000000000, 1.148907358139439339E-11, -201.0000000000015064 ) ) ;
#170035=DIRECTION ( 'NONE',  ( 1.000000000000000000, 0.000000000000000000, 0.000000000000000000 ) ) ;
#170038=ORIENTED_EDGE ( 'NONE', *, *, #211769, .T. ) ;
#170045=FACE_OUTER_BOUND ( 'NONE', #130636, .T. ) ;
#170047=CARTESIAN_POINT ( 'NONE',  ( -20.64999999999999858, 9.593045456726526865, -211.4478935133083439 ) ) ;
#170049=DIRECTION ( 'NONE',  ( -4.391705002472928105E-16, 0.9770955615653315052, 0.2128009952263601179 ) ) ;
#170057=ORIENTED_EDGE ( 'NONE', *, *, #97754, .T. ) ;
#170104=EDGE_LOOP ( 'NONE', ( #28906, #256168, #46284, #5144 ) ) ;
#170123=DIRECTION ( 'NONE',  ( 0.000000000000000000, 0.2128009952263601456, -0.9770955615653316162 ) ) ;
#170143=CARTESIAN_POINT ( 'NONE',  ( -18.42609945526383086, -7.792936248106745900, -209.8606554160495250 ) ) ;
#170146=AXIS2_PLACEMENT_3D ( 'NONE', #13780, #30802, #172901 ) ;
#170173=DIRECTION ( 'NONE',  ( 1.000000000000000000, 0.000000000000000000, 0.000000000000000000 ) ) ;
#170199=EDGE_CURVE ( 'NONE', #149075, #20245, #14338, .T. ) ;
#170209=VERTEX_POINT ( 'NONE', #30327 ) ;
#170211=DIRECTION ( 'NONE',  ( -1.000000000000000000, -2.885090398161910739E-16, -6.283419270304611573E-17 ) ) ;
#170223=DIRECTION ( 'NONE',  ( -1.000000000000000000, -0.000000000000000000, -0.000000000000000000 ) ) ;
#170267=CIRCLE ( 'NONE', #116066, 0.1000000000000018513 ) ;
#170276=DIRECTION ( 'NONE',  ( 0.000000000000000000, -0.2128009952263403282, 0.9770955615653358350 ) ) ;
#170303=CARTESIAN_POINT ( 'NONE',  ( -23.15000000000000213, -11.38316329222462464, -203.4791315943886048 ) ) ;
#170312=AXIS2_PLACEMENT_3D ( 'NONE', #71078, #206716, #68497 ) ;
#170314=EDGE_LOOP ( 'NONE', ( #240048, #65344, #233505, #182345 ) ) ;
#170349=AXIS2_PLACEMENT_3D ( 'NONE', #43875, #84220, #166419 ) ;
#170351=AXIS2_PLACEMENT_3D ( 'NONE', #103554, #26634, #164847 ) ;
#170352=ORIENTED_EDGE ( 'NONE', *, *, #81627, .T. ) ;
#170375=FACE_OUTER_BOUND ( 'NONE', #97024, .T. ) ;
#170381=CARTESIAN_POINT ( 'NONE',  ( -22.59999999999999787, 11.45898712536580177, -198.4011321578509524 ) ) ;
#170441=EDGE_LOOP ( 'NONE', ( #118945, #50380, #125947, #94282 ) ) ;
#170446=EDGE_CURVE ( 'NONE', #163287, #234881, #65278, .T. ) ;
#170464=EDGE_CURVE ( 'NONE', #44597, #206865, #230990, .T. ) ;
#170466=VERTEX_POINT ( 'NONE', #104379 ) ;
#170522=CYLINDRICAL_SURFACE ( 'NONE', #199008, 0.09999999999999724387 ) ;
#170544=DIRECTION ( 'NONE',  ( 1.000000000000000000, 0.000000000000000000, 0.000000000000000000 ) ) ;
#170548=ORIENTED_EDGE ( 'NONE', *, *, #102941, .T. ) ;
#170558=AXIS2_PLACEMENT_3D ( 'NONE', #75379, #154918, #135305 ) ;
#170560=VERTEX_POINT ( 'NONE', #6584 ) ;
#170588=CARTESIAN_POINT ( 'NONE',  ( 20.89192007715127986, 18.40923646582965034, -236.9894833875398206 ) ) ;
#170614=ORIENTED_EDGE ( 'NONE', *, *, #51005, .F. ) ;
#170623=EDGE_LOOP ( 'NONE', ( #55831, #226187, #111000, #118439 ) ) ;
#170635=EDGE_CURVE ( 'NONE', #38009, #168616, #165693, .T. ) ;
#170650=DIRECTION ( 'NONE',  ( 1.000000000000000000, -5.204170427930452838E-14, 0.000000000000000000 ) ) ;
#170654=CARTESIAN_POINT ( 'NONE',  ( 18.59999999999999076, 11.01970663298110154, -220.3481540650095098 ) ) ;
#170685=FACE_OUTER_BOUND ( 'NONE', #249439, .T. ) ;
#170698=CARTESIAN_POINT ( 'NONE',  ( 18.33683296300427656, -0.6949276719145931480, -242.5042195544717742 ) ) ;
#170741=DIRECTION ( 'NONE',  ( 0.000000000000000000, -0.2128009952263605897, 0.9770955615653315052 ) ) ;
#170763=CARTESIAN_POINT ( 'NONE',  ( 18.49999999999999645, 0.6770221356676882074, -212.8807256103264649 ) ) ;
#170768=DIRECTION ( 'NONE',  ( 1.836970198721029934E-16, -0.9770955615653316162, -0.2128009952263604232 ) ) ;
#170806=FACE_OUTER_BOUND ( 'NONE', #71862, .T. ) ;
#170825=ADVANCED_FACE ( 'NONE', ( #42503 ), #206721, .F. ) ;
#170834=ORIENTED_EDGE ( 'NONE', *, *, #237275, .T. ) ;
#170836=FACE_OUTER_BOUND ( 'NONE', #37474, .T. ) ;
#170925=ADVANCED_FACE ( 'NONE', ( #163754 ), #5928, .T. ) ;
#171002=CARTESIAN_POINT ( 'NONE',  ( -21.45000000000000284, 10.16011026985487398, -211.4267369781599939 ) ) ;
#171005=AXIS2_PLACEMENT_3D ( 'NONE', #13234, #51020, #247962 ) ;
#171020=ORIENTED_EDGE ( 'NONE', *, *, #19115, .T. ) ;
#171040=DIRECTION ( 'NONE',  ( 0.000000000000000000, 0.2128009952263605620, -0.9770955615653315052 ) ) ;
#171068=ORIENTED_EDGE ( 'NONE', *, *, #241553, .F. ) ;
#171105=ORIENTED_EDGE ( 'NONE', *, *, #125056, .F. ) ;
#171107=AXIS2_PLACEMENT_3D ( 'NONE', #28972, #68044, #91469 ) ;
#171122=CARTESIAN_POINT ( 'NONE',  ( 18.53317502108576420, 18.39833411442328170, -236.9692678682430085 ) ) ;
#171126=CARTESIAN_POINT ( 'NONE',  ( 23.15000000000000213, -4.259020970815407203, -226.0869574510824123 ) ) ;
#171155=ADVANCED_FACE ( 'NONE', ( #61769 ), #104706, .T. ) ;
#171202=VECTOR ( 'NONE', #87135, 1000.000000000000227 ) ;
#171218=CARTESIAN_POINT ( 'NONE',  ( -23.25000000000000000, -10.72348020702290583, -206.5081278352411402 ) ) ;
#171257=FACE_OUTER_BOUND ( 'NONE', #15610, .T. ) ;
#171264=CARTESIAN_POINT ( 'NONE',  ( 20.95392731769792150, 10.49313854003750635, -207.4367068100602012 ) ) ;
#171288=CARTESIAN_POINT ( 'NONE',  ( -20.54999999999999716, 2.761092913073515120, -213.6778149113116854 ) ) ;
#171337=CARTESIAN_POINT ( 'NONE',  ( 21.14999999999999858, 9.083217576421224848, -211.4565844547649931 ) ) ;
#171341=( BOUNDED_CURVE ( )  B_SPLINE_CURVE ( 3, ( #84396, #184827, #62329, #223949 ),
 .UNSPECIFIED., .F., .F. ) 
 B_SPLINE_CURVE_WITH_KNOTS ( ( 4, 4 ),
 ( 4.712388980384691450, 6.231880751915386263 ),
 .UNSPECIFIED. ) 
 CURVE ( )  GEOMETRIC_REPRESENTATION_ITEM ( )  RATIONAL_B_SPLINE_CURVE ( ( 1.000000000000000000, 0.8166740347213231610, 0.8166740347213231610, 1.000000000000000000 ) ) 
 REPRESENTATION_ITEM ( '' )  );
#171356=DIRECTION ( 'NONE',  ( 1.000000000000000000, -7.136802563874195162E-16, -1.554319503706929005E-16 ) ) ;
#171366=EDGE_CURVE ( 'NONE', #233386, #255134, #131562, .T. ) ;
#171417=DIRECTION ( 'NONE',  ( -0.000000000000000000, -0.2128009952263603677, 0.9770955615653313941 ) ) ;
#171420=VERTEX_POINT ( 'NONE', #29114 ) ;
#171423=CARTESIAN_POINT ( 'NONE',  ( -18.60000000000000142, -7.567701079425733113, -210.0537230116848377 ) ) ;
#171435=AXIS2_PLACEMENT_3D ( 'NONE', #257332, #174052, #95734 ) ;
#171449=DIRECTION ( 'NONE',  ( 0.000000000000000000, -0.07893460099012301889, 0.9968797965484754720 ) ) ;
#171461=CIRCLE ( 'NONE', #58966, 0.09999999999999632794 ) ;
#171477=DIRECTION ( 'NONE',  ( 1.000000000000000000, -0.000000000000000000, -0.000000000000000000 ) ) ;
#171513=ORIENTED_EDGE ( 'NONE', *, *, #240391, .F. ) ;
#171514=AXIS2_PLACEMENT_3D ( 'NONE', #150443, #229957, #153032 ) ;
#171555=ORIENTED_EDGE ( 'NONE', *, *, #54292, .F. ) ;
#171565=CARTESIAN_POINT ( 'NONE',  ( -20.54999999999999716, 5.159242054424403534, -213.4109969955686665 ) ) ;
#171631=DIRECTION ( 'NONE',  ( 1.000000000000000000, 0.000000000000000000, 0.000000000000000000 ) ) ;
#171670=CARTESIAN_POINT ( 'NONE',  ( -23.25000000000000000, 11.38316329224760359, -198.5208684056144079 ) ) ;
#171685=ORIENTED_EDGE ( 'NONE', *, *, #123843, .F. ) ;
#171713=CIRCLE ( 'NONE', #246690, 0.1000000000000025591 ) ;
#171729=TOROIDAL_SURFACE ( 'NONE', #121651, 3.899999999999999467, 0.1000000000000000056 ) ;
#171750=CARTESIAN_POINT ( 'NONE',  ( -20.54999999999999716, 7.128833340094563376, -233.7327013124401276 ) ) ;
#171764=ORIENTED_EDGE ( 'NONE', *, *, #229981, .T. ) ;
#171783=ORIENTED_EDGE ( 'NONE', *, *, #68217, .F. ) ;
#171794=SPHERICAL_SURFACE ( 'NONE', #62149, 0.1000000000000000056 ) ;
#171796=ORIENTED_EDGE ( 'NONE', *, *, #112447, .F. ) ;
#171865=CARTESIAN_POINT ( 'NONE',  ( 20.84999999999999432, 7.675662554762638479, -241.7139905447625381 ) ) ;
#171903=CARTESIAN_POINT ( 'NONE',  ( 23.14999999999998437, 3.957237024351080823, -200.1381559693347754 ) ) ;
#171908=AXIS2_PLACEMENT_3D ( 'NONE', #61021, #97559, #174623 ) ;
#171918=DIRECTION ( 'NONE',  ( -2.602085213965226419E-14, 0.2128009952263604232, -0.9770955615653316162 ) ) ;
#171920=DIRECTION ( 'NONE',  ( 0.000000000000000000, -0.9976611540403004241, -0.06835365183350541884 ) ) ;
#171931=CARTESIAN_POINT ( 'NONE',  ( 21.05000000000000426, -1.358660982773625348, -194.8406220977909982 ) ) ;
#171949=ORIENTED_EDGE ( 'NONE', *, *, #156392, .F. ) ;
#171956=CYLINDRICAL_SURFACE ( 'NONE', #1882, 0.09999999999999939493 ) ;
#171968=TOROIDAL_SURFACE ( 'NONE', #238370, 0.2000000000000000111, 0.1000000000000000056 ) ;
#171970=TOROIDAL_SURFACE ( 'NONE', #59447, 11.90000000000000391, 0.1000000000000000056 ) ;
#171971=CARTESIAN_POINT ( 'NONE',  ( -18.59999999999999787, 0.4879293624014888198, -209.1697915983179428 ) ) ;
#171975=CARTESIAN_POINT ( 'NONE',  ( 18.59999999999999076, 2.923777413779048207, -208.5507632484912222 ) ) ;
#172026=ORIENTED_EDGE ( 'NONE', *, *, #164431, .T. ) ;
#172043=FACE_OUTER_BOUND ( 'NONE', #30301, .T. ) ;
#172058=ORIENTED_EDGE ( 'NONE', *, *, #152170, .F. ) ;
#172092=EDGE_CURVE ( 'NONE', #246033, #173624, #211045, .T. ) ;
#172105=VERTEX_POINT ( 'NONE', #161576 ) ;
#172109=DIRECTION ( 'NONE',  ( 0.000000000000000000, -0.9550021345545507412, 0.2965989261549202838 ) ) ;
#172140=CIRCLE ( 'NONE', #59622, 4.049999999999995381 ) ;
#172141=AXIS2_PLACEMENT_3D ( 'NONE', #59155, #3054, #239122 ) ;
#172183=CIRCLE ( 'NONE', #163753, 0.1000000000000054040 ) ;
#172187=ADVANCED_FACE ( 'NONE', ( #190109 ), #89699, .F. ) ;
#172199=AXIS2_PLACEMENT_3D ( 'NONE', #67973, #113192, #14114 ) ;
#172244=DIRECTION ( 'NONE',  ( 1.000000000000000000, 0.000000000000000000, 0.000000000000000000 ) ) ;
#172251=CARTESIAN_POINT ( 'NONE',  ( -21.07933241753356413, -1.255501372899540780, -194.7964368633462300 ) ) ;
#172265=CIRCLE ( 'NONE', #47108, 12.77500000000000391 ) ;
#172287=EDGE_CURVE ( 'NONE', #127248, #10248, #128856, .T. ) ;
#172292=DIRECTION ( 'NONE',  ( 0.000000000000000000, -0.2128009952263485993, 0.9770955615653341697 ) ) ;
#172307=CIRCLE ( 'NONE', #51412, 0.1000000000000116629 ) ;
#172319=DIRECTION ( 'NONE',  ( 1.000000000000000000, 0.000000000000000000, 0.000000000000000000 ) ) ;
#172346=AXIS2_PLACEMENT_3D ( 'NONE', #93611, #216114, #253949 ) ;
#172347=FACE_OUTER_BOUND ( 'NONE', #215733, .T. ) ;
#172380=ADVANCED_FACE ( 'NONE', ( #74040 ), #115349, .T. ) ;
#172393=ORIENTED_EDGE ( 'NONE', *, *, #25148, .T. ) ;
#172420=ORIENTED_EDGE ( 'NONE', *, *, #185625, .F. ) ;
#172433=CARTESIAN_POINT ( 'NONE',  ( 23.25000000000000000, -6.688413578037176066, -212.5825622730469036 ) ) ;
#172442=TOROIDAL_SURFACE ( 'NONE', #209819, 2.100000000000002309, 0.1000000000000000056 ) ;
#172526=CARTESIAN_POINT ( 'NONE',  ( 21.05000000000000071, 6.164605728109038729, -199.6790125993524043 ) ) ;
#172567=CARTESIAN_POINT ( 'NONE',  ( -18.59999999999999787, -0.7124800764063081715, -242.4837965912295772 ) ) ;
#172609=EDGE_LOOP ( 'NONE', ( #132291, #133123, #31979, #127009 ) ) ;
#172622=VECTOR ( 'NONE', #123488, 1000.000000000000000 ) ;
#172627=EDGE_CURVE ( 'NONE', #254024, #111950, #2535, .T. ) ;
#172655=FACE_OUTER_BOUND ( 'NONE', #122001, .T. ) ;
#172717=CARTESIAN_POINT ( 'NONE',  ( -18.46093223321777899, -7.755933848802606612, -209.9397816339188125 ) ) ;
#172723=CARTESIAN_POINT ( 'NONE',  ( -22.49231231312463208, 11.37015642645466684, -198.4612171126308624 ) ) ;
#172748=DIRECTION ( 'NONE',  ( -1.000000000000000000, 0.000000000000000000, 0.000000000000000000 ) ) ;
#172758=CARTESIAN_POINT ( 'NONE',  ( 20.94999999999999574, 4.252251777740766236, -211.8999245327126744 ) ) ;
#172764=DIRECTION ( 'NONE',  ( 1.000000000000000000, 0.000000000000000000, 0.000000000000000000 ) ) ;
#172827=( BOUNDED_SURFACE ( )  B_SPLINE_SURFACE ( 3, 2, ( 
 ( #141497, #16447, #236737 ),
 ( #235457, #56796, #101036 ),
 ( #257537, #60664, #140195 ),
 ( #136334, #97192, #217168 ) ),
 .UNSPECIFIED., .F., .F., .F. ) 
 B_SPLINE_SURFACE_WITH_KNOTS ( ( 4, 4 ),
 ( 3, 3 ),
 ( -5.204170427930421283E-18, 0.001979672783031571903 ),
 ( 0.000000000000000000, 1.000000000000000000 ),
 .UNSPECIFIED. ) 
 GEOMETRIC_REPRESENTATION_ITEM ( )  RATIONAL_B_SPLINE_SURFACE ( (
 ( 1.000000000000000000, 0.7103081912007942478, 1.000000000000000000),
 ( 1.000000000000000000, 0.7104998333557805967, 1.000000000000000000),
 ( 1.000000000000000000, 0.7107238315756059244, 1.000000000000000000),
 ( 1.000000000000000000, 0.7110073749539113086, 1.000000000000000000) ) ) 
 REPRESENTATION_ITEM ( '' )  SURFACE ( )  );
#172851=AXIS2_PLACEMENT_3D ( 'NONE', #66116, #86932, #169108 ) ;
#172863=DIRECTION ( 'NONE',  ( 0.000000000000000000, -0.2128009952263602567, 0.9770955615653315052 ) ) ;
#172865=CARTESIAN_POINT ( 'NONE',  ( -23.15000000000000213, 14.08768503992705057, -210.4690089352671123 ) ) ;
#172885=AXIS2_PLACEMENT_3D ( 'NONE', #31982, #209301, #57601 ) ;
#172901=DIRECTION ( 'NONE',  ( 0.000000000000000000, 0.2128009952263600624, -0.9770955615653316162 ) ) ;
#172917=ORIENTED_EDGE ( 'NONE', *, *, #169834, .T. ) ;
#172922=ORIENTED_EDGE ( 'NONE', *, *, #2659, .T. ) ;
#172937=DIRECTION ( 'NONE',  ( 1.000000000000000000, 0.000000000000000000, 0.000000000000000000 ) ) ;
#172957=TOROIDAL_SURFACE ( 'NONE', #98045, 11.90000000000000391, 0.1000000000000000056 ) ;
#172982=EDGE_CURVE ( 'NONE', #162643, #125420, #37746, .T. ) ;
#172984=ORIENTED_EDGE ( 'NONE', *, *, #186013, .F. ) ;
#172997=CARTESIAN_POINT ( 'NONE',  ( -21.05000000000000071, -2.576841150532142244, -189.6381168072880428 ) ) ;
#173016=VERTEX_POINT ( 'NONE', #81942 ) ;
#173017=DIRECTION ( 'NONE',  ( 0.000000000000000000, -0.2128009952263604232, 0.9770955615653316162 ) ) ;
#173019=AXIS2_PLACEMENT_3D ( 'NONE', #81524, #22896, #102368 ) ;
#173028=ORIENTED_EDGE ( 'NONE', *, *, #32553, .F. ) ;
#173058=ORIENTED_EDGE ( 'NONE', *, *, #54708, .F. ) ;
#173063=ORIENTED_EDGE ( 'NONE', *, *, #77195, .T. ) ;
#173068=AXIS2_PLACEMENT_3D ( 'NONE', #143240, #124982, #155477 ) ;
#173135=CARTESIAN_POINT ( 'NONE',  ( -23.25000000000000000, -0.8831241301779060304, -196.9450534195053706 ) ) ;
#173143=ORIENTED_EDGE ( 'NONE', *, *, #222511, .F. ) ;
#173153=VERTEX_POINT ( 'NONE', #191382 ) ;
#173157=DIRECTION ( 'NONE',  ( 0.000000000000000000, 0.6728388485993083146, -0.7397890806274158848 ) ) ;
#173161=DIRECTION ( 'NONE',  ( 0.000000000000000000, 0.2128009952263485993, -0.9770955615653341697 ) ) ;
#173192=AXIS2_PLACEMENT_3D ( 'NONE', #30981, #244845, #68798 ) ;
#173206=EDGE_LOOP ( 'NONE', ( #204449, #250752, #191059 ) ) ;
#173210=CARTESIAN_POINT ( 'NONE',  ( -20.94999999999999929, 12.80863705670245878, -205.3010250813005655 ) ) ;
#173241=AXIS2_PLACEMENT_3D ( 'NONE', #93095, #153126, #227464 ) ;
#173267=CARTESIAN_POINT ( 'NONE',  ( 18.50000000000000711, -0.6576273345615416543, -242.5323337003319182 ) ) ;
#173276=DIRECTION ( 'NONE',  ( 0.000000000000000000, 0.2128009952263605065, -0.9770955615653315052 ) ) ;
#173307=AXIS2_PLACEMENT_3D ( 'NONE', #102506, #256757, #156469 ) ;
#173329=EDGE_CURVE ( 'NONE', #18136, #140605, #23620, .T. ) ;
#173341=EDGE_LOOP ( 'NONE', ( #255368, #167468, #79780, #151807, #77829 ) ) ;
#173354=LINE ( 'NONE', #175894, #159492 ) ;
#173358=FACE_OUTER_BOUND ( 'NONE', #64721, .T. ) ;
#173378=ORIENTED_EDGE ( 'NONE', *, *, #219956, .F. ) ;
#173380=CARTESIAN_POINT ( 'NONE',  ( -18.42637059832564717, -0.7441716900925177125, -242.2113608637883146 ) ) ;
#173420=EDGE_CURVE ( 'NONE', #27566, #10248, #84172, .T. ) ;
#173428=ORIENTED_EDGE ( 'NONE', *, *, #195714, .T. ) ;
#173430=CARTESIAN_POINT ( 'NONE',  ( 18.39999999999999858, -0.7490476236415681832, -242.2033265267442061 ) ) ;
#173495=DIRECTION ( 'NONE',  ( 1.000000000000000000, 0.000000000000000000, 0.000000000000000000 ) ) ;
#173517=CARTESIAN_POINT ( 'NONE',  ( 22.59999985501178799, 11.46678616150633268, -198.4355198451642650 ) ) ;
#173518=CARTESIAN_POINT ( 'NONE',  ( 22.50927854361890113, -2.598867553876332614, -189.5410128092696311 ) ) ;
#173519=ORIENTED_EDGE ( 'NONE', *, *, #10222, .T. ) ;
#173532=FACE_OUTER_BOUND ( 'NONE', #124531, .T. ) ;
#173549=EDGE_CURVE ( 'NONE', #150544, #237840, #140258, .T. ) ;
#173550=CARTESIAN_POINT ( 'NONE',  ( 21.05000000000000071, 10.68863688179707694, -222.5873974249509217 ) ) ;
#173555=DIRECTION ( 'NONE',  ( 0.000000000000000000, 0.9770955615653315052, 0.2128009952263603954 ) ) ;
#173564=ORIENTED_EDGE ( 'NONE', *, *, #143356, .F. ) ;
#173565=LINE ( 'NONE', #253037, #76600 ) ;
#173590=CARTESIAN_POINT ( 'NONE',  ( -18.59999999999999787, -0.5913595841389547303, -242.4574432119242999 ) ) ;
#173603=ORIENTED_EDGE ( 'NONE', *, *, #226370, .F. ) ;
#173624=VERTEX_POINT ( 'NONE', #240135 ) ;
#173648=CARTESIAN_POINT ( 'NONE',  ( 20.95265033839679347, 11.88147568740731330, -206.1554567466520780 ) ) ;
#173684=ORIENTED_EDGE ( 'NONE', *, *, #132107, .T. ) ;
#173690=ORIENTED_EDGE ( 'NONE', *, *, #209446, .T. ) ;
#173703=ORIENTED_EDGE ( 'NONE', *, *, #195440, .T. ) ;
#173711=ADVANCED_FACE ( 'NONE', ( #208723 ), #45771, .F. ) ;
#173789=CIRCLE ( 'NONE', #252823, 0.3999999999999952482 ) ;
#173800=( NAMED_UNIT ( * ) SI_UNIT ( $, .STERADIAN. ) SOLID_ANGLE_UNIT ( ) );
#173811=CARTESIAN_POINT ( 'NONE',  ( 21.05000000000000071, 7.554435330547283556, -235.6868924355707691 ) ) ;
#173856=DIRECTION ( 'NONE',  ( 0.000000000000000000, 0.9770955615653388326, 0.2128009952263264781 ) ) ;
#173865=AXIS2_PLACEMENT_3D ( 'NONE', #110632, #11550, #231887 ) ;
#173876=DIRECTION ( 'NONE',  ( 0.000000000000000000, -0.2128009952263485993, 0.9770955615653341697 ) ) ;
#173894=CARTESIAN_POINT ( 'NONE',  ( 21.00000000000000000, 12.15477401631902232, -210.9923204818763622 ) ) ;
#173907=CARTESIAN_POINT ( 'NONE',  ( -20.89878130938411616, 18.40663661316795441, -236.9846611508999388 ) ) ;
#173924=CIRCLE ( 'NONE', #15692, 0.5000000000000005551 ) ;
#173940=EDGE_CURVE ( 'NONE', #80924, #131461, #2472, .T. ) ;
#173947=DIRECTION ( 'NONE',  ( -0.000000000000000000, 0.9770955615653313941, 0.2128009952263603954 ) ) ;
#173974=ORIENTED_EDGE ( 'NONE', *, *, #134636, .F. ) ;
#173977=CARTESIAN_POINT ( 'NONE',  ( -18.59999999999999787, 7.675662554762638479, -241.7139905447625381 ) ) ;
#174012=ADVANCED_FACE ( 'NONE', ( #182429 ), #62477, .F. ) ;
#174022=DIRECTION ( 'NONE',  ( -1.000000000000000000, 0.000000000000000000, 0.000000000000000000 ) ) ;
#174025=CARTESIAN_POINT ( 'NONE',  ( 22.47071067811865319, 7.522163794833003791, -199.2603376134759117 ) ) ;
#174031=AXIS2_PLACEMENT_3D ( 'NONE', #248233, #228685, #47438 ) ;
#174052=DIRECTION ( 'NONE',  ( 1.441126678808781001E-14, 0.9316174814283004757, 0.3634403228828503307 ) ) ;
#174061=CARTESIAN_POINT ( 'NONE',  ( 18.59999999999999076, 8.980461154494401299, -187.0187154576991304 ) ) ;
#174083=CIRCLE ( 'NONE', #98406, 0.2000000000000111688 ) ;
#174092=VECTOR ( 'NONE', #92997, 1000.000000000000114 ) ;
#174111=CARTESIAN_POINT ( 'NONE',  ( -23.15000000000000213, 17.01923898301589944, -224.3994341343041867 ) ) ;
#174121=ORIENTED_EDGE ( 'NONE', *, *, #225104, .F. ) ;
#174145=DIRECTION ( 'NONE',  ( 0.000000000000000000, 0.2128009952263403282, -0.9770955615653358350 ) ) ;
#174168=CARTESIAN_POINT ( 'NONE',  ( 20.94999999999999929, 7.128833340094563376, -233.7327013124401276 ) ) ;
#174180=EDGE_CURVE ( 'NONE', #136982, #208398, #186452, .T. ) ;
#174198=DIRECTION ( 'NONE',  ( -1.000000000000000000, 0.000000000000000000, 0.000000000000000000 ) ) ;
#174211=EDGE_LOOP ( 'NONE', ( #118887, #173058, #183298, #12641 ) ) ;
#174217=LINE ( 'NONE', #256201, #79024 ) ;
#174224=CARTESIAN_POINT ( 'NONE',  ( -20.85000000000000142, 18.41524492703432614, -237.0006385043383546 ) ) ;
#174297=DIRECTION ( 'NONE',  ( -1.000000000000000000, -0.000000000000000000, -0.000000000000000000 ) ) ;
#174303=CARTESIAN_POINT ( 'NONE',  ( 21.46681500593092196, 6.700443717232642982, -199.5407148005082547 ) ) ;
#174318=ORIENTED_EDGE ( 'NONE', *, *, #140843, .T. ) ;
#174351=ORIENTED_EDGE ( 'NONE', *, *, #17839, .T. ) ;
#174355=TOROIDAL_SURFACE ( 'NONE', #57771, 12.97499999999999787, 0.1000000000000000056 ) ;
#174385=CARTESIAN_POINT ( 'NONE',  ( 21.05000000000000071, 19.68370618165487329, -225.3554403480446240 ) ) ;
#174392=EDGE_CURVE ( 'NONE', #60331, #203538, #19865, .T. ) ;
#174441=DIRECTION ( 'NONE',  ( -1.000000000000000000, 0.000000000000000000, 0.000000000000000000 ) ) ;
#174501=CARTESIAN_POINT ( 'NONE',  ( -21.03571358705754335, 12.93326237266432877, -205.1683698891342829 ) ) ;
#174502=EDGE_CURVE ( 'NONE', #258000, #136982, #178280, .T. ) ;
#174509=DIRECTION ( 'NONE',  ( 0.000000000000000000, 0.06835365183351375939, -0.9976611540402997580 ) ) ;
#174518=CARTESIAN_POINT ( 'NONE',  ( 18.50000000000000000, -7.631834139421004970, -210.1304494778856053 ) ) ;
#174545=DIRECTION ( 'NONE',  ( 0.000000000000000000, -0.2128009952261809279, 0.9770955615653705850 ) ) ;
#174552=EDGE_CURVE ( 'NONE', #163287, #117533, #228330, .T. ) ;
#174571=CYLINDRICAL_SURFACE ( 'NONE', #168767, 0.8750000000000007772 ) ;
#174576=CARTESIAN_POINT ( 'NONE',  ( 22.16821283564876666, 7.385839301279039759, -199.3914429501938343 ) ) ;
#174600=CYLINDRICAL_SURFACE ( 'NONE', #128199, 11.80000000000000959 ) ;
#174621=CYLINDRICAL_SURFACE ( 'NONE', #92005, 0.09999999999999691080 ) ;
#174623=DIRECTION ( 'NONE',  ( 0.000000000000000000, 0.2128009952263403282, -0.9770955615653358350 ) ) ;
#174670=DIRECTION ( 'NONE',  ( -1.000000000000000000, -0.000000000000000000, -0.000000000000000000 ) ) ;
#174675=EDGE_LOOP ( 'NONE', ( #4947, #35277, #235515, #160533 ) ) ;
#174681=CARTESIAN_POINT ( 'NONE',  ( 23.14999999999999503, 15.92646454033040371, -219.3818586450342423 ) ) ;
#174683=VERTEX_POINT ( 'NONE', #151988 ) ;
#174690=ORIENTED_EDGE ( 'NONE', *, *, #79484, .F. ) ;
#174697=EDGE_CURVE ( 'NONE', #248011, #149564, #61726, .T. ) ;
#174710=LINE ( 'NONE', #74310, #74793 ) ;
#174720=VECTOR ( 'NONE', #145005, 1000.000000000000000 ) ;
#174772=DIRECTION ( 'NONE',  ( 1.000000000000000000, 7.116814260417643269E-15, 0.000000000000000000 ) ) ;
#174786=EDGE_CURVE ( 'NONE', #103882, #159242, #179245, .T. ) ;
#174807=DIRECTION ( 'NONE',  ( 0.000000000000000000, 0.2128009952263403282, -0.9770955615653358350 ) ) ;
#174819=VERTEX_POINT ( 'NONE', #257411 ) ;
#174829=EDGE_CURVE ( 'NONE', #75051, #118692, #56665, .T. ) ;
#174868=LINE ( 'NONE', #36624, #35090 ) ;
#174887=EDGE_LOOP ( 'NONE', ( #118668, #235166, #26027, #135899 ) ) ;
#174892=DIRECTION ( 'NONE',  ( 0.000000000000000000, -0.9770955615653318382, -0.2128009952263588411 ) ) ;
#174930=CARTESIAN_POINT ( 'NONE',  ( 20.95496329884391784, 11.93721277456621799, -206.1520643135125397 ) ) ;
#174956=DIRECTION ( 'NONE',  ( 0.000000000000000000, 0.9770955615653316162, 0.2128009952263604232 ) ) ;
#174985=ORIENTED_EDGE ( 'NONE', *, *, #175943, .F. ) ;
#174986=CARTESIAN_POINT ( 'NONE',  ( 23.15000000000000213, -4.656943609564678788, -233.1535107627236414 ) ) ;
#174991=ORIENTED_EDGE ( 'NONE', *, *, #64924, .T. ) ;
#175032=EDGE_CURVE ( 'NONE', #237997, #212805, #99472, .T. ) ;
#175081=AXIS2_PLACEMENT_3D ( 'NONE', #57166, #158888, #23229 ) ;
#175100=ADVANCED_FACE ( 'NONE', ( #73426 ), #136920, .T. ) ;
#175102=AXIS2_PLACEMENT_3D ( 'NONE', #165581, #63899, #66466 ) ;
#175149=ORIENTED_EDGE ( 'NONE', *, *, #27641, .F. ) ;
#175155=ORIENTED_EDGE ( 'NONE', *, *, #98087, .F. ) ;
#175173=DIRECTION ( 'NONE',  ( 0.000000000000000000, 0.2128009952263618110, -0.9770955615653311721 ) ) ;
#175174=AXIS2_PLACEMENT_3D ( 'NONE', #220864, #235622, #136512 ) ;
#175179=VERTEX_POINT ( 'NONE', #156818 ) ;
#175192=ORIENTED_EDGE ( 'NONE', *, *, #86411, .T. ) ;
#175197=AXIS2_PLACEMENT_3D ( 'NONE', #229891, #169960, #250725 ) ;
#175208=VERTEX_POINT ( 'NONE', #82345 ) ;
#175234=EDGE_CURVE ( 'NONE', #100848, #22587, #243234, .T. ) ;
#175258=EDGE_LOOP ( 'NONE', ( #92196, #217680, #247188, #91190 ) ) ;
#175278=DIRECTION ( 'NONE',  ( 1.000000000000000000, 0.000000000000000000, 0.000000000000000000 ) ) ;
#175294=PLANE ( 'NONE',  #180724 ) ;
#175305=LINE ( 'NONE', #155741, #42678 ) ;
#175307=EDGE_CURVE ( 'NONE', #126912, #136449, #49439, .T. ) ;
#175317=DIRECTION ( 'NONE',  ( 0.000000000000000000, -0.2128009952263403282, 0.9770955615653358350 ) ) ;
#175321=VERTEX_POINT ( 'NONE', #127935 ) ;
#175393=CARTESIAN_POINT ( 'NONE',  ( -18.31572283045012384, -0.7430829278780020086, -242.4583343033048379 ) ) ;
#175400=DIRECTION ( 'NONE',  ( -0.000000000000000000, -0.2128009952263603677, 0.9770955615653313941 ) ) ;
#175421=DIRECTION ( 'NONE',  ( 1.000000000000000000, -0.000000000000000000, -0.000000000000000000 ) ) ;
#175426=DIRECTION ( 'NONE',  ( 0.000000000000000000, -0.2128009952263479332, 0.9770955615653342807 ) ) ;
#175427=AXIS2_PLACEMENT_3D ( 'NONE', #210569, #33249, #233971 ) ;
#175432=DIRECTION ( 'NONE',  ( 0.000000000000000000, 0.2128009952263601456, -0.9770955615653316162 ) ) ;
#175448=CARTESIAN_POINT ( 'NONE',  ( -22.50000000000000000, 11.48087284840413425, -198.4995883060917947 ) ) ;
#175470=AXIS2_PLACEMENT_3D ( 'NONE', #11527, #55729, #231866 ) ;
#175508=DIRECTION ( 'NONE',  ( 0.000000000000000000, -0.2128009952263603954, 0.9770955615653315052 ) ) ;
#175519=AXIS2_PLACEMENT_3D ( 'NONE', #38890, #80532, #216213 ) ;
#175527=ADVANCED_FACE ( 'NONE', ( #9913 ), #50123, .T. ) ;
#175563=ORIENTED_EDGE ( 'NONE', *, *, #89946, .T. ) ;
#175573=ORIENTED_EDGE ( 'NONE', *, *, #49121, .F. ) ;
#175627=CARTESIAN_POINT ( 'NONE',  ( -18.59999999999999787, 7.675662554762638479, -241.7139905447625381 ) ) ;
#175634=VERTEX_POINT ( 'NONE', #52884 ) ;
#175655=LINE ( 'NONE', #16592, #4493 ) ;
#175664=DIRECTION ( 'NONE',  ( -1.000000000000000000, -3.190570557967288949E-16, -6.948722487160392945E-17 ) ) ;
#175696=CARTESIAN_POINT ( 'NONE',  ( -21.05000000000000071, 6.412126976762837494, -199.7058512474018244 ) ) ;
#175741=EDGE_LOOP ( 'NONE', ( #111075, #167482, #98068, #210889 ) ) ;
#175746=CARTESIAN_POINT ( 'NONE',  ( -18.59999999999999787, 0.5876173420563349792, -209.1618981382189588 ) ) ;
#175749=FACE_OUTER_BOUND ( 'NONE', #71024, .T. ) ;
#175760=CARTESIAN_POINT ( 'NONE',  ( 18.44364597020196683, -7.771168315469450860, -209.9159040159132417 ) ) ;
#175769=ORIENTED_EDGE ( 'NONE', *, *, #10222, .F. ) ;
#175832=EDGE_CURVE ( 'NONE', #243059, #125420, #58147, .T. ) ;
#175863=TOROIDAL_SURFACE ( 'NONE', #17602, 0.6000000000000004219, 0.1000000000000000056 ) ;
#175894=CARTESIAN_POINT ( 'NONE',  ( -21.37071067811865532, 12.40787673083931431, -220.0458254187771558 ) ) ;
#175903=ADVANCED_FACE ( 'NONE', ( #163554 ), #148390, .F. ) ;
#175907=CARTESIAN_POINT ( 'NONE',  ( 23.15000000000000213, -3.770473190032740174, -225.9805569534692324 ) ) ;
#175913=CARTESIAN_POINT ( 'NONE',  ( -21.05000000000000071, 17.11694853917243364, -224.3781540347815451 ) ) ;
#175938=EDGE_CURVE ( 'NONE', #68317, #48752, #224791, .T. ) ;
#175943=EDGE_CURVE ( 'NONE', #26422, #102935, #34500, .T. ) ;
#175952=DIRECTION ( 'NONE',  ( 0.000000000000000000, 0.2002428086779743377, -0.9797463026583749235 ) ) ;
#175961=ORIENTED_EDGE ( 'NONE', *, *, #193351, .F. ) ;
#175967=FACE_OUTER_BOUND ( 'NONE', #235132, .T. ) ;
#176017=DIRECTION ( 'NONE',  ( -1.000000000000000000, 0.000000000000000000, 0.000000000000000000 ) ) ;
#176042=CARTESIAN_POINT ( 'NONE',  ( 18.59999999999999076, 15.24158151457507415, -223.0107194535042083 ) ) ;
#176055=CARTESIAN_POINT ( 'NONE',  ( 22.48660254037843131, 11.47023279864282941, -198.4507335280135294 ) ) ;
#176068=CARTESIAN_POINT ( 'NONE',  ( 23.14999999999998437, 11.48087284840413425, -198.4995883060917663 ) ) ;
#176090=CARTESIAN_POINT ( 'NONE',  ( -23.25000000000000000, 7.958757221477368304, -237.5433740025449083 ) ) ;
#176102=CARTESIAN_POINT ( 'NONE',  ( -23.25000000000000000, 1.148907358139439339E-11, -201.0000000000015064 ) ) ;
#176106=DIRECTION ( 'NONE',  ( 0.000000000000000000, 0.2128009952263485993, -0.9770955615653341697 ) ) ;
#176114=ORIENTED_EDGE ( 'NONE', *, *, #240635, .T. ) ;
#176127=ORIENTED_EDGE ( 'NONE', *, *, #202970, .T. ) ;
#176139=ORIENTED_EDGE ( 'NONE', *, *, #10859, .T. ) ;
#176151=CARTESIAN_POINT ( 'NONE',  ( -23.15000000000000213, -4.756823075239757337, -233.1486023682345490 ) ) ;
#176181=ORIENTED_EDGE ( 'NONE', *, *, #148023, .F. ) ;
#176203=FACE_OUTER_BOUND ( 'NONE', #20246, .T. ) ;
#176225=ADVANCED_FACE ( 'NONE', ( #16067 ), #177711, .F. ) ;
#176253=AXIS2_PLACEMENT_3D ( 'NONE', #140924, #58785, #217857 ) ;
#176332=EDGE_CURVE ( 'NONE', #51404, #78551, #104135, .T. ) ;
#176372=CARTESIAN_POINT ( 'NONE',  ( 20.95224633520496127, 10.50403838541865831, -207.4047027453351006 ) ) ;
#176376=CARTESIAN_POINT ( 'NONE',  ( 20.94999999999999929, 17.05609719657923407, -224.5686720499523119 ) ) ;
#176396=EDGE_LOOP ( 'NONE', ( #192468, #66421, #237055 ) ) ;
#176404=AXIS2_PLACEMENT_3D ( 'NONE', #171002, #208800, #147536 ) ;
#176450=EDGE_CURVE ( 'NONE', #201052, #183877, #123341, .T. ) ;
#176455=AXIS2_PLACEMENT_3D ( 'NONE', #245459, #26415, #207619 ) ;
#176458=CIRCLE ( 'NONE', #159696, 0.09999999999999939493 ) ;
#176471=CARTESIAN_POINT ( 'NONE',  ( 19.99999999999998934, 15.90518444080776383, -219.2841490888777116 ) ) ;
#176492=VECTOR ( 'NONE', #94153, 1000.000000000000227 ) ;
#176533=DIRECTION ( 'NONE',  ( 0.000000000000000000, 0.5000683049008540770, 0.8659859643398306606 ) ) ;
#176545=CARTESIAN_POINT ( 'NONE',  ( -22.50000000000000000, 11.36403278914770176, -198.4341430231427807 ) ) ;
#176555=VERTEX_POINT ( 'NONE', #158039 ) ;
#176579=CARTESIAN_POINT ( 'NONE',  ( -18.50000000000000000, -0.5913595841389538421, -242.4574432119242999 ) ) ;
#176581=( BOUNDED_CURVE ( )  B_SPLINE_CURVE ( 3, ( #160994, #75381, #159709, #99694 ),
 .UNSPECIFIED., .F., .F. ) 
 B_SPLINE_CURVE_WITH_KNOTS ( ( 4, 4 ),
 ( 3.141592653589793116, 4.712388980384689674 ),
 .UNSPECIFIED. ) 
 CURVE ( )  GEOMETRIC_REPRESENTATION_ITEM ( )  RATIONAL_B_SPLINE_CURVE ( ( 1.000000000000000000, 0.8047378541243649375, 0.8047378541243649375, 1.000000000000000000 ) ) 
 REPRESENTATION_ITEM ( '' )  );
#176623=VECTOR ( 'NONE', #124427, 1000.000000000000227 ) ;
#176646=DIRECTION ( 'NONE',  ( 0.000000000000000000, -0.9770955615653381665, -0.2128009952263304749 ) ) ;
#176661=ORIENTED_EDGE ( 'NONE', *, *, #248556, .T. ) ;
#176674=CARTESIAN_POINT ( 'NONE',  ( -20.54999999999999716, 1.148907358139439339E-11, -201.0000000000015064 ) ) ;
#176711=CARTESIAN_POINT ( 'NONE',  ( 20.21494484322213125, 10.86490356972843152, -207.1695121093801504 ) ) ;
#176714=AXIS2_PLACEMENT_3D ( 'NONE', #18669, #173947, #196035 ) ;
#176725=DIRECTION ( 'NONE',  ( -1.000000000000000000, 0.000000000000000000, 0.000000000000000000 ) ) ;
#176731=AXIS2_PLACEMENT_3D ( 'NONE', #165154, #67328, #66040 ) ;
#176765=CARTESIAN_POINT ( 'NONE',  ( -22.59066674512270012, 11.47438154053713966, -198.4697828622833811 ) ) ;
#176772=CARTESIAN_POINT ( 'NONE',  ( 23.25000000000000000, -13.98128454229088291, -192.0195388455185821 ) ) ;
#176781=CARTESIAN_POINT ( 'NONE',  ( -21.14999999999999858, -1.391858308744747807, -194.6091531227727955 ) ) ;
#176798=AXIS2_PLACEMENT_3D ( 'NONE', #79358, #80635, #160228 ) ;
#176859=CARTESIAN_POINT ( 'NONE',  ( -18.59999999999999787, 13.65786464920749843, -219.7735913778983559 ) ) ;
#176917=ORIENTED_EDGE ( 'NONE', *, *, #210933, .F. ) ;
#176927=VERTEX_POINT ( 'NONE', #15642 ) ;
#176941=VERTEX_POINT ( 'NONE', #92560 ) ;
#176946=VECTOR ( 'NONE', #220365, 1000.000000000000227 ) ;
#176986=EDGE_LOOP ( 'NONE', ( #215149, #193642, #24996 ) ) ;
#177008=CARTESIAN_POINT ( 'NONE',  ( -20.94999999999999929, -10.76604040606817847, -206.3127087229280789 ) ) ;
#177010=DIRECTION ( 'NONE',  ( 0.000000000000000000, -0.2128009952263603677, 0.9770955615653313941 ) ) ;
#177031=DIRECTION ( 'NONE',  ( 0.000000000000000000, 0.9525900758537773072, -0.3042567129660331271 ) ) ;
#177042=CARTESIAN_POINT ( 'NONE',  ( 20.85000000000000142, 17.16609282392354174, -224.6038045889790453 ) ) ;
#177067=EDGE_LOOP ( 'NONE', ( #149019, #201320, #184129, #168300 ) ) ;
#177083=DIRECTION ( 'NONE',  ( 0.000000000000000000, 0.2128009952263485993, -0.9770955615653341697 ) ) ;
#177091=ORIENTED_EDGE ( 'NONE', *, *, #51935, .T. ) ;
#177095=ORIENTED_EDGE ( 'NONE', *, *, #245146, .F. ) ;
#177150=AXIS2_PLACEMENT_3D ( 'NONE', #34495, #72327, #91871 ) ;
#177272=CARTESIAN_POINT ( 'NONE',  ( -18.47653818581422058, -7.732071902224467941, -209.9769657719527629 ) ) ;
#177274=TOROIDAL_SURFACE ( 'NONE', #85607, 0.4000000000000003553, 0.1000000000000000056 ) ;
#177315=CARTESIAN_POINT ( 'NONE',  ( -23.25000000000000000, 14.80545736607782814, -235.9842437978701639 ) ) ;
#177342=DIRECTION ( 'NONE',  ( -1.000000000000000000, -0.000000000000000000, -0.000000000000000000 ) ) ;
#177350=AXIS2_PLACEMENT_3D ( 'NONE', #167388, #68264, #244312 ) ;
#177353=LINE ( 'NONE', #117345, #46543 ) ;
#177360=CARTESIAN_POINT ( 'NONE',  ( -18.50000000000000000, 14.80545736607782814, -235.9842437978701639 ) ) ;
#177363=CARTESIAN_POINT ( 'NONE',  ( 21.04999999999999716, -1.391858308744753359, -194.6091531227728524 ) ) ;
#177378=LINE ( 'NONE', #44262, #257648 ) ;
#177383=EDGE_LOOP ( 'NONE', ( #137059, #245474, #64933, #205660 ) ) ;
#177430=CARTESIAN_POINT ( 'NONE',  ( -23.15000000000000213, 1.148907358139439339E-11, -201.0000000000015064 ) ) ;
#177435=ORIENTED_EDGE ( 'NONE', *, *, #257364, .T. ) ;
#177459=ORIENTED_EDGE ( 'NONE', *, *, #6445, .T. ) ;
#177510=CIRCLE ( 'NONE', #194258, 0.1000000000000003525 ) ;
#177522=DIRECTION ( 'NONE',  ( 1.000000000000000000, -0.000000000000000000, -0.000000000000000000 ) ) ;
#177549=EDGE_LOOP ( 'NONE', ( #191086, #183906, #65962, #44333 ) ) ;
#177555=ORIENTED_EDGE ( 'NONE', *, *, #81865, .F. ) ;
#177558=EDGE_CURVE ( 'NONE', #164661, #250321, #161396, .T. ) ;
#177562=EDGE_LOOP ( 'NONE', ( #189153, #105247, #41311, #26184 ) ) ;
#177591=ORIENTED_EDGE ( 'NONE', *, *, #93729, .F. ) ;
#177598=AXIS2_PLACEMENT_3D ( 'NONE', #106942, #108249, #186504 ) ;
#177608=DIRECTION ( 'NONE',  ( -1.000000000000000000, -0.000000000000000000, -0.000000000000000000 ) ) ;
#177614=DIRECTION ( 'NONE',  ( 0.000000000000000000, 0.2128009952263485993, -0.9770955615653341697 ) ) ;
#177616=AXIS2_PLACEMENT_3D ( 'NONE', #191130, #175421, #72457 ) ;
#177638=ORIENTED_EDGE ( 'NONE', *, *, #30353, .F. ) ;
#177658=FACE_OUTER_BOUND ( 'NONE', #23230, .T. ) ;
#177660=ORIENTED_EDGE ( 'NONE', *, *, #40866, .F. ) ;
#177675=EDGE_CURVE ( 'NONE', #145277, #219574, #206793, .T. ) ;
#177711=PLANE ( 'NONE',  #141555 ) ;
#177717=CARTESIAN_POINT ( 'NONE',  ( -23.15000000000000213, 17.01923898301589944, -224.3994341343041867 ) ) ;
#177727=EDGE_CURVE ( 'NONE', #95913, #185684, #98994, .T. ) ;
#177749=VECTOR ( 'NONE', #65168, 1000.000000000000227 ) ;
#177791=CIRCLE ( 'NONE', #161211, 0.09999999999999574507 ) ;
#177838=ORIENTED_EDGE ( 'NONE', *, *, #38561, .F. ) ;
#177845=EDGE_CURVE ( 'NONE', #227071, #24822, #125640, .T. ) ;
#177856=VECTOR ( 'NONE', #84845, 1000.000000000000000 ) ;
#177866=DIRECTION ( 'NONE',  ( -1.000000000000000000, 0.000000000000000000, 0.000000000000000000 ) ) ;
#177905=DIRECTION ( 'NONE',  ( 0.000000000000000000, 0.9770955615653548199, 0.2128009952262535920 ) ) ;
#177914=ORIENTED_EDGE ( 'NONE', *, *, #22089, .T. ) ;
#177928=ADVANCED_FACE ( 'NONE', ( #104757, #184319, #181770 ), #43550, .F. ) ;
#177938=CARTESIAN_POINT ( 'NONE',  ( 19.75857864376268935, 16.76897757977919312, -222.7804130109902871 ) ) ;
#177970=EDGE_CURVE ( 'NONE', #55636, #239248, #174083, .T. ) ;
#177971=EDGE_LOOP ( 'NONE', ( #157650, #38602, #118872, #113395 ) ) ;
#177984=CARTESIAN_POINT ( 'NONE',  ( 22.00411653889225860, -1.446770167443869104, -193.8916177604842517 ) ) ;
#177990=ORIENTED_EDGE ( 'NONE', *, *, #90332, .T. ) ;
#177994=CARTESIAN_POINT ( 'NONE',  ( 20.22516295850462598, 11.35589477125217250, -206.6222955247963000 ) ) ;
#178004=ORIENTED_EDGE ( 'NONE', *, *, #160778, .T. ) ;
#178013=FACE_OUTER_BOUND ( 'NONE', #10691, .T. ) ;
#178040=AXIS2_PLACEMENT_3D ( 'NONE', #92063, #89488, #189891 ) ;
#178050=CARTESIAN_POINT ( 'NONE',  ( -22.49544290803762792, 11.46684760846028084, -198.4357998940973573 ) ) ;
#178056=CARTESIAN_POINT ( 'NONE',  ( 23.14999999999999503, 17.11694853917244075, -224.3781540347815451 ) ) ;
#178058=FACE_OUTER_BOUND ( 'NONE', #183579, .T. ) ;
#178093=DIRECTION ( 'NONE',  ( 0.000000000000000000, 0.2128009952263485993, -0.9770955615653341697 ) ) ;
#178095=AXIS2_PLACEMENT_3D ( 'NONE', #24024, #239195, #63109 ) ;
#178122=CARTESIAN_POINT ( 'NONE',  ( 22.47007471830798409, 7.543872110139020037, -199.3570250894167941 ) ) ;
#178131=ORIENTED_EDGE ( 'NONE', *, *, #113389, .T. ) ;
#178135=AXIS2_PLACEMENT_3D ( 'NONE', #223486, #83938, #125682 ) ;
#178138=ORIENTED_EDGE ( 'NONE', *, *, #158945, .T. ) ;
#178145=CARTESIAN_POINT ( 'NONE',  ( -20.54999999999999716, 6.703231349641842307, -231.7785101893094577 ) ) ;
#178148=CIRCLE ( 'NONE', #36695, 0.1000000000000054040 ) ;
#178151=( BOUNDED_CURVE ( )  B_SPLINE_CURVE ( 3, ( #70584, #129247, #208789, #225748 ),
 .UNSPECIFIED., .F., .T. ) 
 B_SPLINE_CURVE_WITH_KNOTS ( ( 4, 4 ),
 ( 3.141592653589793116, 4.712388980384689674 ),
 .UNSPECIFIED. ) 
 CURVE ( )  GEOMETRIC_REPRESENTATION_ITEM ( )  RATIONAL_B_SPLINE_CURVE ( ( 1.000000000000000000, 0.8047378541243649375, 0.8047378541243649375, 1.000000000000000000 ) ) 
 REPRESENTATION_ITEM ( '' )  );
#178158=CARTESIAN_POINT ( 'NONE',  ( 22.39999999999999503, -1.232296663996729880, -194.8718726406955568 ) ) ;
#178165=CIRCLE ( 'NONE', #211287, 0.09999999999999080458 ) ;
#178200=VERTEX_POINT ( 'NONE', #215446 ) ;
#178241=CARTESIAN_POINT ( 'NONE',  ( -21.14999999999999858, 11.40444339177023814, -198.6185779617709670 ) ) ;
#178262=CIRCLE ( 'NONE', #224000, 0.1000000000000055844 ) ;
#178280=CIRCLE ( 'NONE', #11675, 0.1000000000000054040 ) ;
#178283=LINE ( 'NONE', #257728, #8691 ) ;
#178299=AXIS2_PLACEMENT_3D ( 'NONE', #118534, #181070, #217583 ) ;
#178322=ORIENTED_EDGE ( 'NONE', *, *, #151356, .T. ) ;
#178381=CIRCLE ( 'NONE', #45067, 0.09999999999999939493 ) ;
#178396=CARTESIAN_POINT ( 'NONE',  ( 21.33487959338958362, 6.571513019293449887, -199.5687945318220500 ) ) ;
#178452=CARTESIAN_POINT ( 'NONE',  ( 23.24999999999997513, 17.11694853917244075, -224.3781540347815451 ) ) ;
#178462=EDGE_LOOP ( 'NONE', ( #211362, #242749, #247705, #124389 ) ) ;
#178470=ORIENTED_EDGE ( 'NONE', *, *, #37920, .F. ) ;
#178481=DIRECTION ( 'NONE',  ( 0.000000000000000000, 0.2128009952263603399, -0.9770955615653315052 ) ) ;
#178498=TOROIDAL_SURFACE ( 'NONE', #207711, 11.70000000000000639, 0.1000000000000000056 ) ;
#178551=AXIS2_PLACEMENT_3D ( 'NONE', #130368, #108256, #52107 ) ;
#178569=CARTESIAN_POINT ( 'NONE',  ( -22.39999999999999858, -1.330006220153263641, -194.8931527402181700 ) ) ;
#178573=DIRECTION ( 'NONE',  ( -1.000000000000000000, -3.190570557967288949E-16, -6.948722487160392945E-17 ) ) ;
#178618=CARTESIAN_POINT ( 'NONE',  ( 20.85000000000000142, 7.783179459866048866, -245.3643104511423019 ) ) ;
#178624=CIRCLE ( 'NONE', #136894, 0.1999999999999987343 ) ;
#178632=ADVANCED_FACE ( 'NONE', ( #129829 ), #144245, .F. ) ;
#178694=CARTESIAN_POINT ( 'NONE',  ( -20.94999999999999929, 3.047642603966940200, -208.5984958277594785 ) ) ;
#178701=CARTESIAN_POINT ( 'NONE',  ( -21.05000000000000071, 7.872214528623314500, -209.6555322433423783 ) ) ;
#178723=ORIENTED_EDGE ( 'NONE', *, *, #165052, .T. ) ;
#178740=CARTESIAN_POINT ( 'NONE',  ( -18.50000000000000000, -7.558719773525646168, -210.9360835033311332 ) ) ;
#178754=CARTESIAN_POINT ( 'NONE',  ( 19.99999999738088974, 16.73432760861077995, -222.6213144456777400 ) ) ;
#178765=EDGE_CURVE ( 'NONE', #137793, #151535, #240652, .T. ) ;
#178767=ORIENTED_EDGE ( 'NONE', *, *, #159858, .T. ) ;
#178817=DIRECTION ( 'NONE',  ( 0.000000000000000000, -0.9770955615653316162, -0.2128009952263604232 ) ) ;
#178828=CARTESIAN_POINT ( 'NONE',  ( -18.59999999999999787, 4.252251777740764460, -211.8999245327126744 ) ) ;
#178842=ORIENTED_EDGE ( 'NONE', *, *, #198651, .F. ) ;
#178846=CARTESIAN_POINT ( 'NONE',  ( -22.59999999999999787, -2.401771312552908544, -189.4980873520049727 ) ) ;
#178893=DIRECTION ( 'NONE',  ( -1.000000000000000000, 0.000000000000000000, 0.000000000000000000 ) ) ;
#178896=CARTESIAN_POINT ( 'NONE',  ( 21.05000000000000071, 11.77895973109482952, -206.1023438919106070 ) ) ;
#178910=ORIENTED_EDGE ( 'NONE', *, *, #70904, .T. ) ;
#178921=CARTESIAN_POINT ( 'NONE',  ( 18.59999999999999076, 7.128833340094563376, -233.7327013124401276 ) ) ;
#178943=EDGE_CURVE ( 'NONE', #170466, #39339, #111475, .T. ) ;
#178957=AXIS2_PLACEMENT_3D ( 'NONE', #99414, #21215, #324 ) ;
#178962=ADVANCED_FACE ( 'NONE', ( #48706 ), #25326, .T. ) ;
#178966=CARTESIAN_POINT ( 'NONE',  ( 20.94999999999999929, 14.80545736607782814, -235.9842437978701639 ) ) ;
#178976=CARTESIAN_POINT ( 'NONE',  ( 19.99999999999998934, 16.02417409648692725, -219.3605785455116006 ) ) ;
#178977=CARTESIAN_POINT ( 'NONE',  ( -23.25000000000000000, -3.770473190032741062, -225.9805569534692324 ) ) ;
#179018=DIRECTION ( 'NONE',  ( -2.952720810173289112E-16, 0.9770955615653316162, 0.2128009952263604232 ) ) ;
#179092=EDGE_LOOP ( 'NONE', ( #250817, #102093, #31033 ) ) ;
#179103=CIRCLE ( 'NONE', #41538, 0.09999999999999600875 ) ;
#179121=ORIENTED_EDGE ( 'NONE', *, *, #139144, .T. ) ;
#179130=DIRECTION ( 'NONE',  ( -0.7070776581708964059, -0.6909393522475117955, -0.1504792239192832004 ) ) ;
#179165=VERTEX_POINT ( 'NONE', #51255 ) ;
#179198=ORIENTED_EDGE ( 'NONE', *, *, #39746, .F. ) ;
#179210=VECTOR ( 'NONE', #233038, 1000.000000000000114 ) ;
#179224=DIRECTION ( 'NONE',  ( -0.000000000000000000, -0.9770955615653316162, -0.2128009952263604232 ) ) ;
#179239=CARTESIAN_POINT ( 'NONE',  ( -18.41817142474042157, -0.7469768386996047393, -242.2067401450736668 ) ) ;
#179245=LINE ( 'NONE', #240475, #203385 ) ;
#179263=CARTESIAN_POINT ( 'NONE',  ( 23.14999999999999858, 7.244009986534929446, -211.6437749090809177 ) ) ;
#179265=DIRECTION ( 'NONE',  ( -1.000000000000000000, -0.000000000000000000, -0.000000000000000000 ) ) ;
#179291=CARTESIAN_POINT ( 'NONE',  ( 20.77766267348356166, 11.82544895625581738, -206.1952355620770732 ) ) ;
#179341=DIRECTION ( 'NONE',  ( -1.000000000000000000, 0.000000000000000000, 0.000000000000000000 ) ) ;
#179347=CIRCLE ( 'NONE', #225086, 7.800000000000002487 ) ;
#179348=ORIENTED_EDGE ( 'NONE', *, *, #78800, .T. ) ;
#179353=CARTESIAN_POINT ( 'NONE',  ( 18.49999999999999645, 7.128833340094563376, -233.7327013124401276 ) ) ;
#179362=EDGE_CURVE ( 'NONE', #158102, #17245, #7616, .T. ) ;
#179384=EDGE_LOOP ( 'NONE', ( #199401, #60613, #70854, #114950 ) ) ;
#179401=AXIS2_PLACEMENT_3D ( 'NONE', #21255, #42094, #141174 ) ;
#179432=AXIS2_PLACEMENT_3D ( 'NONE', #102728, #84427, #143148 ) ;
#179463=ORIENTED_EDGE ( 'NONE', *, *, #60824, .F. ) ;
#179471=DIRECTION ( 'NONE',  ( 1.000000000000000000, 0.000000000000000000, 0.000000000000000000 ) ) ;
#179504=CARTESIAN_POINT ( 'NONE',  ( 23.14999999999999858, 1.148907358139439339E-11, -201.0000000000015064 ) ) ;
#179533=EDGE_CURVE ( 'NONE', #232829, #89128, #104503, .T. ) ;
#179543=ORIENTED_EDGE ( 'NONE', *, *, #104198, .F. ) ;
#179598=FACE_OUTER_BOUND ( 'NONE', #205014, .T. ) ;
#179630=AXIS2_PLACEMENT_3D ( 'NONE', #24797, #80864, #165574 ) ;
#179666=ORIENTED_EDGE ( 'NONE', *, *, #48407, .T. ) ;
#179675=EDGE_LOOP ( 'NONE', ( #176114, #254725, #250288, #148499 ) ) ;
#179681=DIRECTION ( 'NONE',  ( 1.000000000000000000, -0.000000000000000000, -0.000000000000000000 ) ) ;
#179716=ORIENTED_EDGE ( 'NONE', *, *, #185625, .T. ) ;
#179726=CARTESIAN_POINT ( 'NONE',  ( -23.15000000000000213, 7.128833340094563376, -233.7327013124401276 ) ) ;
#179736=DIRECTION ( 'NONE',  ( 1.000000000000000000, 0.000000000000000000, 0.000000000000000000 ) ) ;
#179778=AXIS2_PLACEMENT_3D ( 'NONE', #81691, #131125, #90710 ) ;
#179825=CARTESIAN_POINT ( 'NONE',  ( -18.42554971533679264, -7.781550387048931761, -209.8995886608980470 ) ) ;
#179833=EDGE_LOOP ( 'NONE', ( #223627, #213270, #243923 ) ) ;
#179849=DIRECTION ( 'NONE',  ( -1.000000000000000000, 0.000000000000000000, 0.000000000000000000 ) ) ;
#179858=DIRECTION ( 'NONE',  ( 0.000000000000000000, 0.2128009952263568427, -0.9770955615653322823 ) ) ;
#179861=ADVANCED_FACE ( 'NONE', ( #90929 ), #171794, .F. ) ;
#179882=AXIS2_PLACEMENT_3D ( 'NONE', #195988, #96831, #223219 ) ;
#179904=VERTEX_POINT ( 'NONE', #34516 ) ;
#179928=CARTESIAN_POINT ( 'NONE',  ( -21.06715728752538652, 12.97363049771892207, -205.3537238898406656 ) ) ;
#179949=FACE_OUTER_BOUND ( 'NONE', #32184, .T. ) ;
#180009=ADVANCED_FACE ( 'NONE', ( #13646 ), #14944, .T. ) ;
#180019=ORIENTED_EDGE ( 'NONE', *, *, #70596, .T. ) ;
#180043=ORIENTED_EDGE ( 'NONE', *, *, #212912, .F. ) ;
#180067=AXIS2_PLACEMENT_3D ( 'NONE', #116885, #39943, #59435 ) ;
#180076=ORIENTED_EDGE ( 'NONE', *, *, #28311, .T. ) ;
#180084=CARTESIAN_POINT ( 'NONE',  ( 21.05000000000000071, 3.047642603966940200, -208.5984958277594785 ) ) ;
#180130=CARTESIAN_POINT ( 'NONE',  ( 21.05000000000000071, -3.363022478626109368, -226.2703567425896267 ) ) ;
#180178=DIRECTION ( 'NONE',  ( 0.000000000000000000, -0.9770955615653312831, -0.2128009952263615612 ) ) ;
#180181=TOROIDAL_SURFACE ( 'NONE', #80164, 12.97499999999999609, 0.1000000000000000056 ) ;
#180207=DIRECTION ( 'NONE',  ( -0.000000000000000000, -0.2814428106787469352, -0.9595780032479105381 ) ) ;
#180214=CARTESIAN_POINT ( 'NONE',  ( 21.09696443733127325, 13.08195529389994860, -210.6724668423044307 ) ) ;
#180217=LINE ( 'NONE', #176376, #194920 ) ;
#180218=EDGE_CURVE ( 'NONE', #257097, #163312, #20648, .T. ) ;
#180243=DIRECTION ( 'NONE',  ( 0.000000000000000000, 0.9770955615653315052, 0.2128009952263605065 ) ) ;
#180245=VECTOR ( 'NONE', #145627, 1000.000000000000000 ) ;
#180286=DIRECTION ( 'NONE',  ( 2.952720810173289605E-16, -0.9770955615653315052, -0.2128009952263610061 ) ) ;
#180307=DIRECTION ( 'NONE',  ( 0.000000000000000000, -0.2128009952263403282, 0.9770955615653358350 ) ) ;
#180348=ORIENTED_EDGE ( 'NONE', *, *, #192481, .F. ) ;
#180354=CIRCLE ( 'NONE', #209572, 0.09999999999999895084 ) ;
#180376=EDGE_LOOP ( 'NONE', ( #93841, #213464, #256213, #81202 ) ) ;
#180389=EDGE_LOOP ( 'NONE', ( #130111, #210226, #4581, #164341 ) ) ;
#180411=AXIS2_PLACEMENT_3D ( 'NONE', #38165, #139795, #96801 ) ;
#180421=DIRECTION ( 'NONE',  ( -1.000000000000000000, 0.000000000000000000, 0.000000000000000000 ) ) ;
#180443=AXIS2_PLACEMENT_3D ( 'NONE', #85916, #165505, #29859 ) ;
#180455=CARTESIAN_POINT ( 'NONE',  ( -21.05000000000000071, 1.148907358139439339E-11, -201.0000000000015064 ) ) ;
#180466=AXIS2_PLACEMENT_3D ( 'NONE', #220653, #38177, #257149 ) ;
#180475=CARTESIAN_POINT ( 'NONE',  ( 20.94999999999999929, -10.38870553492056104, -206.3818953267866902 ) ) ;
#180478=CARTESIAN_POINT ( 'NONE',  ( -20.85000000000000142, -4.969162394454528453, -233.3995358778103935 ) ) ;
#180489=CIRCLE ( 'NONE', #172346, 0.1000000000000054040 ) ;
#180553=DIRECTION ( 'NONE',  ( 1.000000000000000000, 0.000000000000000000, 0.000000000000000000 ) ) ;
#180593=ORIENTED_EDGE ( 'NONE', *, *, #212530, .T. ) ;
#180597=EDGE_CURVE ( 'NONE', #253651, #254124, #191538, .T. ) ;
#180606=AXIS2_PLACEMENT_3D ( 'NONE', #207050, #66255, #187505 ) ;
#180628=CARTESIAN_POINT ( 'NONE',  ( 21.05000000000000071, 10.40519331719241336, -207.3517860968744628 ) ) ;
#180664=VECTOR ( 'NONE', #58000, 1000.000000000000000 ) ;
#180675=ORIENTED_EDGE ( 'NONE', *, *, #176450, .F. ) ;
#180688=CARTESIAN_POINT ( 'NONE',  ( 18.39999999999999858, -0.8254770802754703984, -242.3223161824233500 ) ) ;
#180692=EDGE_LOOP ( 'NONE', ( #209044, #34115, #161160, #37978, #150248, #245866, #173519, #150855 ) ) ;
#180702=ORIENTED_EDGE ( 'NONE', *, *, #201813, .F. ) ;
#180724=AXIS2_PLACEMENT_3D ( 'NONE', #236506, #233947, #174022 ) ;
#180729=EDGE_CURVE ( 'NONE', #174819, #245138, #33324, .T. ) ;
#180744=FACE_OUTER_BOUND ( 'NONE', #35565, .T. ) ;
#180747=SPHERICAL_SURFACE ( 'NONE', #187587, 0.1000000000000000056 ) ;
#180798=LINE ( 'NONE', #60823, #249895 ) ;
#180818=DIRECTION ( 'NONE',  ( -3.265361837132813586E-16, 0.9770955615653357240, 0.2128009952263412996 ) ) ;
#180829=EDGE_CURVE ( 'NONE', #115361, #170560, #233225, .T. ) ;
#180846=CARTESIAN_POINT ( 'NONE',  ( 22.59999999999999432, 11.45898712536580177, -198.4011321578509524 ) ) ;
#180861=VECTOR ( 'NONE', #158636, 1000.000000000000000 ) ;
#180886=EDGE_CURVE ( 'NONE', #68947, #145361, #12456, .T. ) ;
#180895=ADVANCED_FACE ( 'NONE', ( #184956 ), #221493, .F. ) ;
#180902=ORIENTED_EDGE ( 'NONE', *, *, #128684, .F. ) ;
#180925=CARTESIAN_POINT ( 'NONE',  ( -23.15000000000000213, -7.274670914976377745, -212.7102428701827250 ) ) ;
#180941=CARTESIAN_POINT ( 'NONE',  ( -21.05000000000000071, 7.939498413483247141, -209.7295111514051200 ) ) ;
#180961=ORIENTED_EDGE ( 'NONE', *, *, #239080, .T. ) ;
#181010=ORIENTED_EDGE ( 'NONE', *, *, #223848, .F. ) ;
#181011=DIRECTION ( 'NONE',  ( 0.000000000000000000, 0.2128009952263403282, -0.9770955615653358350 ) ) ;
#181047=CARTESIAN_POINT ( 'NONE',  ( 23.15000000000000213, -6.438379425586758131, -212.1495692908769684 ) ) ;
#181070=DIRECTION ( 'NONE',  ( 0.000000000000000000, 0.2128009952263604232, -0.9770955615653316162 ) ) ;
#181081=CIRCLE ( 'NONE', #176798, 0.1000000000000028227 ) ;
#181122=ORIENTED_EDGE ( 'NONE', *, *, #219245, .T. ) ;
#181145=DIRECTION ( 'NONE',  ( 0.000000000000000000, 0.2128009952263403282, -0.9770955615653358350 ) ) ;
#181173=ADVANCED_FACE ( 'NONE', ( #21418 ), #187608, .T. ) ;
#181177=CARTESIAN_POINT ( 'NONE',  ( -20.85000000000000142, 7.128833340094563376, -233.7327013124401276 ) ) ;
#181194=CARTESIAN_POINT ( 'NONE',  ( 23.14999999999999858, 7.128833340094563376, -233.7327013124401276 ) ) ;
#181226=VECTOR ( 'NONE', #21881, 1000.000000000000000 ) ;
#181247=DIRECTION ( 'NONE',  ( 0.000000000000000000, 0.2128009952263403282, -0.9770955615653358350 ) ) ;
#181294=EDGE_LOOP ( 'NONE', ( #31865, #190295, #95549 ) ) ;
#181295=ORIENTED_EDGE ( 'NONE', *, *, #116493, .F. ) ;
#181313=VERTEX_POINT ( 'NONE', #166070 ) ;
#181322=EDGE_CURVE ( 'NONE', #41827, #134704, #123068, .T. ) ;
#181338=ORIENTED_EDGE ( 'NONE', *, *, #204532, .T. ) ;
#181380=CARTESIAN_POINT ( 'NONE',  ( 21.05000000000000071, -4.914013037343259782, -233.1828366659746905 ) ) ;
#181386=LINE ( 'NONE', #36749, #207006 ) ;
#181389=ORIENTED_EDGE ( 'NONE', *, *, #207387, .F. ) ;
#181430=AXIS2_PLACEMENT_3D ( 'NONE', #93740, #53331, #49483 ) ;
#181512=TOROIDAL_SURFACE ( 'NONE', #69082, 0.9750000000000019762, 0.1000000000000000056 ) ;
#181532=PLANE ( 'NONE',  #138657 ) ;
#181556=ORIENTED_EDGE ( 'NONE', *, *, #149800, .F. ) ;
#181571=ORIENTED_EDGE ( 'NONE', *, *, #48838, .F. ) ;
#181604=DIRECTION ( 'NONE',  ( -0.000000000000000000, 0.9770955615653313941, 0.2128009952263603954 ) ) ;
#181607=ADVANCED_FACE ( 'NONE', ( #24965 ), #4087, .T. ) ;
#181609=DIRECTION ( 'NONE',  ( 0.000000000000000000, -0.3042567129660269654, -0.9525900758537791946 ) ) ;
#181619=EDGE_CURVE ( 'NONE', #155405, #29211, #71269, .T. ) ;
#181649=CYLINDRICAL_SURFACE ( 'NONE', #120354, 0.09999999999999939493 ) ;
#181677=EDGE_LOOP ( 'NONE', ( #55048, #227588, #4747 ) ) ;
#181757=CARTESIAN_POINT ( 'NONE',  ( 23.14999999999999858, 7.187745831299792165, -211.5611048126997389 ) ) ;
#181770=FACE_BOUND ( 'NONE', #180692, .T. ) ;
#181792=CIRCLE ( 'NONE', #69381, 11.89999999999998792 ) ;
#181851=DIRECTION ( 'NONE',  ( -5.603264701231742896E-32, 0.2128009952263605620, -0.9770955615653313941 ) ) ;
#181864=ORIENTED_EDGE ( 'NONE', *, *, #201488, .F. ) ;
#181922=CARTESIAN_POINT ( 'NONE',  ( 23.24999999999999645, 10.93950603019935564, -232.9027774310573022 ) ) ;
#181936=DIRECTION ( 'NONE',  ( 0.000000000000000000, -0.9770955615653321713, -0.2128009952263581472 ) ) ;
#181957=CARTESIAN_POINT ( 'NONE',  ( -21.05000000000000071, 0.6656436123793491033, -212.6810495496487476 ) ) ;
#181972=EDGE_CURVE ( 'NONE', #34155, #135145, #224109, .T. ) ;
#181988=( BOUNDED_CURVE ( )  B_SPLINE_CURVE ( 3, ( #66370, #27281, #205870, #164196 ),
 .UNSPECIFIED., .F., .T. ) 
 B_SPLINE_CURVE_WITH_KNOTS ( ( 4, 4 ),
 ( 0.06456096931748397938, 3.077031684272309331 ),
 .UNSPECIFIED. ) 
 CURVE ( )  GEOMETRIC_REPRESENTATION_ITEM ( )  RATIONAL_B_SPLINE_CURVE ( ( 1.000000000000000000, 0.3763440860215099271, 0.3763440860215099271, 1.000000000000000000 ) ) 
 REPRESENTATION_ITEM ( '' )  );
#182000=FACE_OUTER_BOUND ( 'NONE', #116705, .T. ) ;
#182016=CARTESIAN_POINT ( 'NONE',  ( -22.39999999999999858, 1.148907358139439339E-11, -201.0000000000015064 ) ) ;
#182034=DIRECTION ( 'NONE',  ( 0.000000000000000000, 0.9983803033886529121, 0.05689261644169053833 ) ) ;
#182059=EDGE_CURVE ( 'NONE', #173016, #57651, #17280, .T. ) ;
#182070=DIRECTION ( 'NONE',  ( 0.000000000000000000, -0.9770955615653316162, -0.2128009952263604232 ) ) ;
#182073=CARTESIAN_POINT ( 'NONE',  ( 20.94999999999999574, -10.53375947859273865, -206.2621204135720632 ) ) ;
#182079=ORIENTED_EDGE ( 'NONE', *, *, #244160, .F. ) ;
#182086=DIRECTION ( 'NONE',  ( 1.000000000000000000, 0.000000000000000000, 0.000000000000000000 ) ) ;
#182090=CARTESIAN_POINT ( 'NONE',  ( -23.25000000000000000, -6.688413578037177842, -212.5825622730469036 ) ) ;
#182102=FACE_OUTER_BOUND ( 'NONE', #141599, .T. ) ;
#182109=CYLINDRICAL_SURFACE ( 'NONE', #170349, 7.900000000000007461 ) ;
#182140=LINE ( 'NONE', #67313, #101521 ) ;
#182187=DIRECTION ( 'NONE',  ( 2.557131231893036985E-16, -0.9525900758537791946, 0.3042567129660269099 ) ) ;
#182229=EDGE_LOOP ( 'NONE', ( #235415, #151572, #220687, #7612 ) ) ;
#182231=VERTEX_POINT ( 'NONE', #153625 ) ;
#182250=DIRECTION ( 'NONE',  ( 0.000000000000000000, 0.5000683049008606273, 0.8659859643398268858 ) ) ;
#182283=ORIENTED_EDGE ( 'NONE', *, *, #40866, .T. ) ;
#182322=ORIENTED_EDGE ( 'NONE', *, *, #211342, .F. ) ;
#182345=ORIENTED_EDGE ( 'NONE', *, *, #159185, .F. ) ;
#182365=CARTESIAN_POINT ( 'NONE',  ( -20.94999999999999929, 17.12338108143915250, -224.6426509580150537 ) ) ;
#182369=ORIENTED_EDGE ( 'NONE', *, *, #36878, .T. ) ;
#182379=CIRCLE ( 'NONE', #174031, 0.1000000000000050293 ) ;
#182390=DIRECTION ( 'NONE',  ( 0.000000000000000000, -0.9770955615653321713, -0.2128009952263575366 ) ) ;
#182409=VERTEX_POINT ( 'NONE', #160014 ) ;
#182410=ORIENTED_EDGE ( 'NONE', *, *, #128756, .F. ) ;
#182429=FACE_OUTER_BOUND ( 'NONE', #126792, .T. ) ;
#182444=CARTESIAN_POINT ( 'NONE',  ( 22.47071067811865319, 1.148907358139439339E-11, -201.0000000000015064 ) ) ;
#182464=FACE_OUTER_BOUND ( 'NONE', #59825, .T. ) ;
#182471=EDGE_CURVE ( 'NONE', #30937, #248593, #88138, .T. ) ;
#182558=DIRECTION ( 'NONE',  ( -2.252264143451593919E-15, 0.08413937888703756918, -0.9964539953858901900 ) ) ;
#182576=ORIENTED_EDGE ( 'NONE', *, *, #190660, .F. ) ;
#182623=AXIS2_PLACEMENT_3D ( 'NONE', #1274, #185060, #204613 ) ;
#182633=AXIS2_PLACEMENT_3D ( 'NONE', #209498, #251175, #72580 ) ;
#182642=ORIENTED_EDGE ( 'NONE', *, *, #207983, .T. ) ;
#182646=DIRECTION ( 'NONE',  ( -6.938893903907222856E-15, 0.9770955615653316162, 0.2128009952263604232 ) ) ;
#182714=ORIENTED_EDGE ( 'NONE', *, *, #15413, .F. ) ;
#182729=CARTESIAN_POINT ( 'NONE',  ( 20.94999999999999929, 11.84624361595474795, -206.1763227999733203 ) ) ;
#182813=CARTESIAN_POINT ( 'NONE',  ( 21.14999999999999858, 8.980461154494404852, -187.0187154576991304 ) ) ;
#182868=VECTOR ( 'NONE', #81304, 1000.000000000000227 ) ;
#182874=FACE_OUTER_BOUND ( 'NONE', #109705, .T. ) ;
#182918=VERTEX_POINT ( 'NONE', #166143 ) ;
#182968=ORIENTED_EDGE ( 'NONE', *, *, #251364, .T. ) ;
#182973=ADVANCED_FACE ( 'NONE', ( #107406 ), #87823, .T. ) ;
#183011=DIRECTION ( 'NONE',  ( 0.000000000000000000, -0.9770955615653316162, -0.2128009952263604232 ) ) ;
#183059=ORIENTED_EDGE ( 'NONE', *, *, #70897, .T. ) ;
#183094=CIRCLE ( 'NONE', #145648, 12.87499999999999467 ) ;
#183128=CARTESIAN_POINT ( 'NONE',  ( 21.13461538461538680, 12.99955419111918786, -210.8083363671015604 ) ) ;
#183130=CYLINDRICAL_SURFACE ( 'NONE', #170351, 0.1000000000000055844 ) ;
#183133=DIRECTION ( 'NONE',  ( 0.000000000000000000, 0.2128009952263605620, -0.9770955615653313941 ) ) ;
#183146=DIRECTION ( 'NONE',  ( -2.952720810173288126E-16, 0.9770955615653313941, 0.2128009952263603677 ) ) ;
#183162=CARTESIAN_POINT ( 'NONE',  ( -20.94999999999999929, 18.51199663233067483, -231.2535697180530292 ) ) ;
#183181=ORIENTED_EDGE ( 'NONE', *, *, #143541, .T. ) ;
#183200=CARTESIAN_POINT ( 'NONE',  ( 21.04999999999999716, 10.48937277454169781, -207.4747812581268249 ) ) ;
#183206=VECTOR ( 'NONE', #58587, 1000.000000000000227 ) ;
#183277=DIRECTION ( 'NONE',  ( 0.000000000000000000, 0.2128009952263485993, -0.9770955615653341697 ) ) ;
#183279=DIRECTION ( 'NONE',  ( 0.000000000000000000, -0.2128009952263603677, 0.9770955615653313941 ) ) ;
#183293=DIRECTION ( 'NONE',  ( 1.000000000000000000, 0.000000000000000000, 0.000000000000000000 ) ) ;
#183298=ORIENTED_EDGE ( 'NONE', *, *, #202908, .F. ) ;
#183323=EDGE_CURVE ( 'NONE', #36199, #222722, #213050, .T. ) ;
#183324=EDGE_CURVE ( 'NONE', #204466, #39339, #146398, .T. ) ;
#183327=LINE ( 'NONE', #248433, #59959 ) ;
#183339=DIRECTION ( 'NONE',  ( -0.000000000000000000, 0.9770955615653313941, 0.2128009952263603677 ) ) ;
#183341=EDGE_CURVE ( 'NONE', #26422, #151535, #196518, .T. ) ;
#183349=VERTEX_POINT ( 'NONE', #65916 ) ;
#183350=AXIS2_PLACEMENT_3D ( 'NONE', #47172, #58068, #201132 ) ;
#183360=FACE_OUTER_BOUND ( 'NONE', #118670, .T. ) ;
#183374=AXIS2_PLACEMENT_3D ( 'NONE', #159542, #9128, #6545 ) ;
#183380=VERTEX_POINT ( 'NONE', #42490 ) ;
#183392=DIRECTION ( 'NONE',  ( 1.000000000000000000, 0.000000000000000000, 0.000000000000000000 ) ) ;
#183397=PLANE ( 'NONE',  #96160 ) ;
#183445=ADVANCED_FACE ( 'NONE', ( #247103 ), #196482, .F. ) ;
#183485=ORIENTED_EDGE ( 'NONE', *, *, #169830, .F. ) ;
#183500=ORIENTED_EDGE ( 'NONE', *, *, #28609, .T. ) ;
#183537=AXIS2_PLACEMENT_3D ( 'NONE', #186249, #242355, #46713 ) ;
#183554=VERTEX_POINT ( 'NONE', #249333 ) ;
#183562=DIRECTION ( 'NONE',  ( 0.000000000000000000, 0.9770955615653312831, 0.2128009952263621163 ) ) ;
#183574=AXIS2_PLACEMENT_3D ( 'NONE', #72724, #136491, #53124 ) ;
#183579=EDGE_LOOP ( 'NONE', ( #89745, #252844 ) ) ;
#183586=LINE ( 'NONE', #6212, #66993 ) ;
#183588=AXIS2_PLACEMENT_3D ( 'NONE', #130104, #28491, #225339 ) ;
#183592=CARTESIAN_POINT ( 'NONE',  ( -18.39999999999999858, -0.8254770802754705095, -242.3223161824233500 ) ) ;
#183614=EDGE_CURVE ( 'NONE', #212703, #160183, #108996, .T. ) ;
#183646=EDGE_CURVE ( 'NONE', #38095, #22582, #200895, .T. ) ;
#183650=CARTESIAN_POINT ( 'NONE',  ( 22.50000000000000000, -1.560176095955058129, -193.3663837337745122 ) ) ;
#183689=VERTEX_POINT ( 'NONE', #160516 ) ;
#183694=DIRECTION ( 'NONE',  ( -1.000000000000000000, -3.190570557967288949E-16, -6.948722487160392945E-17 ) ) ;
#183713=TOROIDAL_SURFACE ( 'NONE', #71291, 3.899999999999999467, 0.1000000000000000056 ) ;
#183724=AXIS2_PLACEMENT_3D ( 'NONE', #39219, #198257, #75762 ) ;
#183742=VERTEX_POINT ( 'NONE', #203474 ) ;
#183749=FACE_OUTER_BOUND ( 'NONE', #21678, .T. ) ;
#183753=CARTESIAN_POINT ( 'NONE',  ( 21.05000000000000071, -1.448466219907752039, -194.7514528548905730 ) ) ;
#183781=CARTESIAN_POINT ( 'NONE',  ( -20.94999999999999929, 2.859758780633683273, -208.6670499591424459 ) ) ;
#183850=DIRECTION ( 'NONE',  ( 0.000000000000000000, 0.2128009952263600346, -0.9770955615653315052 ) ) ;
#183856=CARTESIAN_POINT ( 'NONE',  ( 22.39999999999999503, -2.598867842139048090, -189.5410128746472083 ) ) ;
#183876=ORIENTED_EDGE ( 'NONE', *, *, #6684, .F. ) ;
#183877=VERTEX_POINT ( 'NONE', #50783 ) ;
#183887=ORIENTED_EDGE ( 'NONE', *, *, #25218, .F. ) ;
#183904=CARTESIAN_POINT ( 'NONE',  ( -21.05000000000000071, 7.939498413483247141, -209.7295111514051200 ) ) ;
#183906=ORIENTED_EDGE ( 'NONE', *, *, #235590, .F. ) ;
#183937=AXIS2_PLACEMENT_3D ( 'NONE', #180475, #86471, #26547 ) ;
#183944=FACE_OUTER_BOUND ( 'NONE', #133891, .T. ) ;
#183965=DIRECTION ( 'NONE',  ( -4.701977403289178058E-30, 0.2128009952263773819, -0.9770955615653279525 ) ) ;
#183980=ORIENTED_EDGE ( 'NONE', *, *, #186908, .F. ) ;
#184013=ORIENTED_EDGE ( 'NONE', *, *, #163929, .F. ) ;
#184073=EDGE_CURVE ( 'NONE', #68947, #83472, #100766, .T. ) ;
#184077=CIRCLE ( 'NONE', #250703, 0.1000000000000128147 ) ;
#184110=EDGE_LOOP ( 'NONE', ( #218570, #57204, #104684, #32207 ) ) ;
#184129=ORIENTED_EDGE ( 'NONE', *, *, #116277, .F. ) ;
#184130=CARTESIAN_POINT ( 'NONE',  ( 23.14999999999999858, 7.128833340094563376, -233.7327013124401276 ) ) ;
#184177=ORIENTED_EDGE ( 'NONE', *, *, #221528, .F. ) ;
#184179=VERTEX_POINT ( 'NONE', #26789 ) ;
#184204=EDGE_CURVE ( 'NONE', #17857, #126912, #246731, .T. ) ;
#184213=ORIENTED_EDGE ( 'NONE', *, *, #150697, .F. ) ;
#184284=CARTESIAN_POINT ( 'NONE',  ( -20.64999999999999858, 9.712035112405693837, -211.5243229699422614 ) ) ;
#184290=FACE_OUTER_BOUND ( 'NONE', #97127, .T. ) ;
#184299=DIRECTION ( 'NONE',  ( -1.000000000000000000, -0.000000000000000000, -0.000000000000000000 ) ) ;
#184318=DIRECTION ( 'NONE',  ( -1.000000000000000000, -1.794895427898103559E-16, -3.909090864890002444E-17 ) ) ;
#184319=FACE_BOUND ( 'NONE', #43474, .T. ) ;
#184331=DIRECTION ( 'NONE',  ( 1.000000000000000000, 0.000000000000000000, 0.000000000000000000 ) ) ;
#184347=LINE ( 'NONE', #30441, #88652 ) ;
#184389=AXIS2_PLACEMENT_3D ( 'NONE', #240052, #140960, #3994 ) ;
#184406=AXIS2_PLACEMENT_3D ( 'NONE', #64380, #104747, #239162 ) ;
#184437=ORIENTED_EDGE ( 'NONE', *, *, #98087, .T. ) ;
#184453=ORIENTED_EDGE ( 'NONE', *, *, #138338, .F. ) ;
#184467=FACE_OUTER_BOUND ( 'NONE', #156047, .T. ) ;
#184473=EDGE_LOOP ( 'NONE', ( #78186, #186936, #15864, #103021 ) ) ;
#184481=AXIS2_PLACEMENT_3D ( 'NONE', #170303, #204236, #6027 ) ;
#184486=ORIENTED_EDGE ( 'NONE', *, *, #231641, .F. ) ;
#184568=VERTEX_POINT ( 'NONE', #167284 ) ;
#184569=DIRECTION ( 'NONE',  ( 0.000000000000000000, 0.2128009952263607285, -0.9770955615653316162 ) ) ;
#184610=CARTESIAN_POINT ( 'NONE',  ( -23.25000000000000000, 7.128833340094563376, -233.7327013124401276 ) ) ;
#184628=DIRECTION ( 'NONE',  ( -0.000000000000000000, -0.7397890806274287634, -0.6728388485992942147 ) ) ;
#184642=ORIENTED_EDGE ( 'NONE', *, *, #170635, .F. ) ;
#184650=ORIENTED_EDGE ( 'NONE', *, *, #72688, .T. ) ;
#184684=CARTESIAN_POINT ( 'NONE',  ( 20.99749315643146730, 17.11694853957538598, -224.3781540366317131 ) ) ;
#184721=DIRECTION ( 'NONE',  ( -0.000000000000000000, 0.2128009952263603677, -0.9770955615653313941 ) ) ;
#184746=EDGE_CURVE ( 'NONE', #96338, #74028, #213597, .T. ) ;
#184764=AXIS2_PLACEMENT_3D ( 'NONE', #124864, #84392, #145690 ) ;
#184777=LINE ( 'NONE', #180941, #5259 ) ;
#184795=DIRECTION ( 'NONE',  ( 1.000000000000000000, 0.000000000000000000, 0.000000000000000000 ) ) ;
#184823=CARTESIAN_POINT ( 'NONE',  ( -20.54999999999999716, -4.161311414658873886, -226.0656773515597706 ) ) ;
#184827=CARTESIAN_POINT ( 'NONE',  ( 20.12499999999999645, 11.68002377302066463, -206.5006728669541189 ) ) ;
#184847=VERTEX_POINT ( 'NONE', #178846 ) ;
#184872=DIRECTION ( 'NONE',  ( -0.000000000000000000, -0.9770955615653313941, -0.2128009952263603677 ) ) ;
#184889=DIRECTION ( 'NONE',  ( 1.000000000000000000, 0.000000000000000000, 0.000000000000000000 ) ) ;
#184900=AXIS2_PLACEMENT_3D ( 'NONE', #43063, #242535, #62630 ) ;
#184904=ORIENTED_EDGE ( 'NONE', *, *, #172092, .F. ) ;
#184956=FACE_OUTER_BOUND ( 'NONE', #2968, .T. ) ;
#184958=CIRCLE ( 'NONE', #184764, 0.3999999999999948597 ) ;
#184968=CARTESIAN_POINT ( 'NONE',  ( 21.40925344232283223, -1.320255649883980809, -194.4729340772759372 ) ) ;
#184988=EDGE_LOOP ( 'NONE', ( #246223, #240015, #53647, #237398 ) ) ;
#185024=CYLINDRICAL_SURFACE ( 'NONE', #65237, 4.049999999999995381 ) ;
#185025=DIRECTION ( 'NONE',  ( 0.000000000000000000, 0.2128009952263620885, -0.9770955615653311721 ) ) ;
#185027=ADVANCED_FACE ( 'NONE', ( #183944 ), #228218, .F. ) ;
#185030=CARTESIAN_POINT ( 'NONE',  ( 23.24999999999999289, 11.50215294792677767, -198.5972978622482970 ) ) ;
#185055=CARTESIAN_POINT ( 'NONE',  ( -18.50016250449483479, 18.35558276679128298, -236.8903279188150748 ) ) ;
#185060=DIRECTION ( 'NONE',  ( 1.000000000000000000, 0.000000000000000000, 0.000000000000000000 ) ) ;
#185063=AXIS2_PLACEMENT_3D ( 'NONE', #29256, #108746, #89174 ) ;
#185071=CARTESIAN_POINT ( 'NONE',  ( 18.49362639424899157, -0.6580137145852484881, -242.3516021320601794 ) ) ;
#185102=SPHERICAL_SURFACE ( 'NONE', #154976, 0.1000000000000000056 ) ;
#185110=EDGE_CURVE ( 'NONE', #248008, #146487, #91276, .T. ) ;
#185124=VERTEX_POINT ( 'NONE', #135507 ) ;
#185126=CARTESIAN_POINT ( 'NONE',  ( 21.05000000000000071, 10.39655183198268418, -207.4949966697317620 ) ) ;
#185151=ORIENTED_EDGE ( 'NONE', *, *, #72898, .F. ) ;
#185185=AXIS2_PLACEMENT_3D ( 'NONE', #225722, #207490, #125374 ) ;
#185201=AXIS2_PLACEMENT_3D ( 'NONE', #215566, #78615, #1642 ) ;
#185239=LINE ( 'NONE', #220524, #57742 ) ;
#185265=TOROIDAL_SURFACE ( 'NONE', #51372, 0.2000000000000000111, 0.1000000000000000056 ) ;
#185295=AXIS2_PLACEMENT_3D ( 'NONE', #42686, #244720, #954 ) ;
#185299=CARTESIAN_POINT ( 'NONE',  ( 23.24999999999999645, 7.128833340094563376, -233.7327013124401276 ) ) ;
#185302=LINE ( 'NONE', #151336, #76433 ) ;
#185327=CARTESIAN_POINT ( 'NONE',  ( -18.59999999999999787, -0.6576273345615599730, -242.5323337003318898 ) ) ;
#185363=DIRECTION ( 'NONE',  ( 0.000000000000000000, -0.2128009952263604787, 0.9770955615653313941 ) ) ;
#185398=SPHERICAL_SURFACE ( 'NONE', #156237, 0.1000000000000000056 ) ;
#185405=VERTEX_POINT ( 'NONE', #183650 ) ;
#185419=CARTESIAN_POINT ( 'NONE',  ( -21.07094088545304089, 6.154362662572049558, -199.5584335273501324 ) ) ;
#185428=CARTESIAN_POINT ( 'NONE',  ( -22.39999999999999858, 11.50215294792677057, -198.5972978622482970 ) ) ;
#185440=FACE_OUTER_BOUND ( 'NONE', #60997, .T. ) ;
#185452=CARTESIAN_POINT ( 'NONE',  ( 20.94999999999999929, 1.148907358139439339E-11, -201.0000000000015064 ) ) ;
#185466=ORIENTED_EDGE ( 'NONE', *, *, #127761, .F. ) ;
#185469=ORIENTED_EDGE ( 'NONE', *, *, #25218, .T. ) ;
#185470=CARTESIAN_POINT ( 'NONE',  ( -18.59999999999999787, 0.5876173420563349792, -209.1618981382189588 ) ) ;
#185479=AXIS2_PLACEMENT_3D ( 'NONE', #224889, #106221, #181936 ) ;
#185482=VERTEX_POINT ( 'NONE', #93516 ) ;
#185483=CARTESIAN_POINT ( 'NONE',  ( -20.64999999999999858, 6.724511449164477739, -231.8762197454659884 ) ) ;
#185489=CIRCLE ( 'NONE', #206342, 0.09999999999999895084 ) ;
#185490=ORIENTED_EDGE ( 'NONE', *, *, #208587, .T. ) ;
#185499=DIRECTION ( 'NONE',  ( 1.000000000000000000, 0.000000000000000000, 0.000000000000000000 ) ) ;
#185504=CIRCLE ( 'NONE', #227187, 0.1000000000000054040 ) ;
#185522=EDGE_CURVE ( 'NONE', #57917, #234078, #139111, .T. ) ;
#185554=DIRECTION ( 'NONE',  ( -0.000000000000000000, 0.9770955615653313941, 0.2128009952263603954 ) ) ;
#185574=DIRECTION ( 'NONE',  ( 0.000000000000000000, -0.9770955615653315052, -0.2128009952263607008 ) ) ;
#185625=EDGE_CURVE ( 'NONE', #34477, #102301, #6041, .T. ) ;
#185634=ADVANCED_FACE ( 'NONE', ( #90952 ), #131362, .T. ) ;
#185643=DIRECTION ( 'NONE',  ( 2.952720810173289605E-16, -0.9770955615653313941, -0.2128009952263610893 ) ) ;
#185665=CARTESIAN_POINT ( 'NONE',  ( 18.59999999999999787, -7.567701079425742883, -210.0537230116848377 ) ) ;
#185673=DIRECTION ( 'NONE',  ( 0.000000000000000000, -0.9770955615653357240, -0.2128009952263410220 ) ) ;
#185676=ORIENTED_EDGE ( 'NONE', *, *, #92597, .T. ) ;
#185684=VERTEX_POINT ( 'NONE', #200328 ) ;
#185688=CARTESIAN_POINT ( 'NONE',  ( 20.95512840106821528, 12.97721512785410702, -210.6622227115684325 ) ) ;
#185714=CARTESIAN_POINT ( 'NONE',  ( 20.04142135623730070, 15.92646454033040015, -219.3818586450342423 ) ) ;
#185749=ORIENTED_EDGE ( 'NONE', *, *, #81222, .T. ) ;
#185760=AXIS2_PLACEMENT_3D ( 'NONE', #11239, #229009, #12541 ) ;
#185772=VERTEX_POINT ( 'NONE', #28135 ) ;
#185808=ORIENTED_EDGE ( 'NONE', *, *, #154330, .T. ) ;
#185820=EDGE_CURVE ( 'NONE', #16905, #212172, #193324, .T. ) ;
#185822=DIRECTION ( 'NONE',  ( 0.000000000000000000, 0.2128009952263485993, -0.9770955615653341697 ) ) ;
#185880=CIRCLE ( 'NONE', #219197, 0.09999999999999724387 ) ;
#185893=CARTESIAN_POINT ( 'NONE',  ( -18.39999999999999858, -7.817436562502981801, -209.8389866834999111 ) ) ;
#185907=FACE_OUTER_BOUND ( 'NONE', #122645, .T. ) ;
#185984=EDGE_CURVE ( 'NONE', #188047, #37415, #132334, .T. ) ;
#186001=EDGE_CURVE ( 'NONE', #235587, #86393, #10360, .T. ) ;
#186013=EDGE_CURVE ( 'NONE', #14295, #103755, #43655, .T. ) ;
#186022=CARTESIAN_POINT ( 'NONE',  ( -23.25000000000000000, 10.74948822439028895, -222.3968794097801549 ) ) ;
#186050=DIRECTION ( 'NONE',  ( 1.000000000000000000, 0.000000000000000000, 0.000000000000000000 ) ) ;
#186111=DIRECTION ( 'NONE',  ( 0.000000000000000000, -0.2128009952263604232, 0.9770955615653316162 ) ) ;
#186124=EDGE_CURVE ( 'NONE', #71912, #246315, #56100, .T. ) ;
#186125=CARTESIAN_POINT ( 'NONE',  ( -21.05000000000000071, 2.838478681111047841, -208.5693404029859437 ) ) ;
#186138=ORIENTED_EDGE ( 'NONE', *, *, #253664, .T. ) ;
#186143=ORIENTED_EDGE ( 'NONE', *, *, #251716, .T. ) ;
#186163=LINE ( 'NONE', #208309, #57830 ) ;
#186249=CARTESIAN_POINT ( 'NONE',  ( -23.24999999999999645, -0.8467571797981052750, -242.2246066262668194 ) ) ;
#186256=ORIENTED_EDGE ( 'NONE', *, *, #126410, .F. ) ;
#186283=EDGE_CURVE ( 'NONE', #183380, #225002, #72917, .T. ) ;
#186305=ORIENTED_EDGE ( 'NONE', *, *, #217838, .F. ) ;
#186339=PRODUCT_DEFINITION_FORMATION_WITH_SPECIFIED_SOURCE ( 'ANY', '', #188868, .NOT_KNOWN. ) ;
#186360=FACE_OUTER_BOUND ( 'NONE', #208601, .T. ) ;
#186371=CARTESIAN_POINT ( 'NONE',  ( 18.47135592147653327, -0.7030496522306831642, -242.2786693462419123 ) ) ;
#186418=ORIENTED_EDGE ( 'NONE', *, *, #192038, .T. ) ;
#186424=AXIS2_PLACEMENT_3D ( 'NONE', #89620, #50480, #32254 ) ;
#186452=CIRCLE ( 'NONE', #7366, 0.2000000000000111688 ) ;
#186460=EDGE_CURVE ( 'NONE', #158102, #193505, #185489, .T. ) ;
#186486=ORIENTED_EDGE ( 'NONE', *, *, #166810, .T. ) ;
#186487=ADVANCED_FACE ( 'NONE', ( #254213 ), #234671, .T. ) ;
#186504=DIRECTION ( 'NONE',  ( -1.000000000000000000, 0.000000000000000000, 0.000000000000000000 ) ) ;
#186514=AXIS2_PLACEMENT_3D ( 'NONE', #56601, #215694, #39676 ) ;
#186526=ORIENTED_EDGE ( 'NONE', *, *, #58441, .T. ) ;
#186553=ORIENTED_EDGE ( 'NONE', *, *, #90244, .F. ) ;
#186563=ADVANCED_FACE ( 'NONE', ( #159016 ), #238517, .T. ) ;
#186577=ORIENTED_EDGE ( 'NONE', *, *, #219615, .F. ) ;
#186579=CARTESIAN_POINT ( 'NONE',  ( 21.05000000000000071, 12.04125963260215393, -206.0806513715932624 ) ) ;
#186580=EDGE_CURVE ( 'NONE', #235714, #59070, #76868, .T. ) ;
#186593=ADVANCED_FACE ( 'NONE', ( #7613 ), #81224, .F. ) ;
#186607=ORIENTED_EDGE ( 'NONE', *, *, #174502, .T. ) ;
#186624=AXIS2_PLACEMENT_3D ( 'NONE', #89816, #169414, #173276 ) ;
#186637=AXIS2_PLACEMENT_3D ( 'NONE', #142827, #222358, #244514 ) ;
#186642=DIRECTION ( 'NONE',  ( 0.000000000000000000, 0.9770955615653313941, 0.2128009952263603677 ) ) ;
#186657=CARTESIAN_POINT ( 'NONE',  ( -20.54999999999999716, 7.128833340094563376, -233.7327013124401276 ) ) ;
#186683=ORIENTED_EDGE ( 'NONE', *, *, #201935, .T. ) ;
#186696=FACE_OUTER_BOUND ( 'NONE', #130306, .T. ) ;
#186698=EDGE_CURVE ( 'NONE', #142313, #117463, #204516, .T. ) ;
#186732=CARTESIAN_POINT ( 'NONE',  ( 20.94999999999999929, 13.09728821260366161, -219.8956789487585013 ) ) ;
#186749=CARTESIAN_POINT ( 'NONE',  ( -18.59999999999999787, -0.8760381862371811046, -190.6771195118613207 ) ) ;
#186778=EDGE_CURVE ( 'NONE', #230675, #232353, #177791, .T. ) ;
#186780=ORIENTED_EDGE ( 'NONE', *, *, #149677, .T. ) ;
#186789=ORIENTED_EDGE ( 'NONE', *, *, #160936, .T. ) ;
#186802=CARTESIAN_POINT ( 'NONE',  ( 23.24999999999999289, -4.054946580484636520, -201.8831241301909074 ) ) ;
#186803=ORIENTED_EDGE ( 'NONE', *, *, #32553, .T. ) ;
#186844=ORIENTED_EDGE ( 'NONE', *, *, #207593, .T. ) ;
#186858=EDGE_LOOP ( 'NONE', ( #206372, #234257, #73234, #100107 ) ) ;
#186878=CARTESIAN_POINT ( 'NONE',  ( 20.94999999999999929, -4.161311414658873886, -226.0656773515597706 ) ) ;
#186908=EDGE_CURVE ( 'NONE', #194263, #242169, #102919, .T. ) ;
#186936=ORIENTED_EDGE ( 'NONE', *, *, #72089, .F. ) ;
#186959=EDGE_LOOP ( 'NONE', ( #84094, #226406, #25161, #189921 ) ) ;
#186981=CARTESIAN_POINT ( 'NONE',  ( 20.85000000000000142, 18.51199663233068193, -231.2535697180530292 ) ) ;
#186993=DIRECTION ( 'NONE',  ( 1.000000000000000000, 0.000000000000000000, 0.000000000000000000 ) ) ;
#187030=CARTESIAN_POINT ( 'NONE',  ( -18.50000000000000000, 6.266619843005246437, -211.3861694115776402 ) ) ;
#187033=EDGE_CURVE ( 'NONE', #97608, #256235, #156944, .T. ) ;
#187053=DIRECTION ( 'NONE',  ( 0.000000000000000000, 0.2128009952263604232, -0.9770955615653316162 ) ) ;
#187092=AXIS2_PLACEMENT_3D ( 'NONE', #209967, #91296, #230822 ) ;
#187099=AXIS2_PLACEMENT_3D ( 'NONE', #163, #126209, #205749 ) ;
#187154=CARTESIAN_POINT ( 'NONE',  ( 20.94999999999999574, -10.76604040606816959, -206.3127087229280789 ) ) ;
#187193=DIRECTION ( 'NONE',  ( 0.000000000000000000, 0.2128009952263603677, -0.9770955615653313941 ) ) ;
#187200=AXIS2_PLACEMENT_3D ( 'NONE', #193023, #75655, #57328 ) ;
#187227=CARTESIAN_POINT ( 'NONE',  ( -23.25000000000000000, 6.298909458711757559, -229.9220286223353185 ) ) ;
#187272=CYLINDRICAL_SURFACE ( 'NONE', #6700, 0.09999999999999691080 ) ;
#187288=CARTESIAN_POINT ( 'NONE',  ( 22.39999999999999858, -1.560176095955058129, -193.3663837337745122 ) ) ;
#187289=CARTESIAN_POINT ( 'NONE',  ( -20.94999999999999929, 6.277629359189121239, -229.8243190661787878 ) ) ;
#187347=EDGE_LOOP ( 'NONE', ( #4643, #100040, #130044, #213040 ) ) ;
#187350=CARTESIAN_POINT ( 'NONE',  ( -23.25000000000000000, 0.8831241302008846494, -205.0549465804976421 ) ) ;
#187370=DIRECTION ( 'NONE',  ( -1.000000000000000000, -0.000000000000000000, -0.000000000000000000 ) ) ;
#187385=ADVANCED_FACE ( 'NONE', ( #64264 ), #87659, .F. ) ;
#187397=CARTESIAN_POINT ( 'NONE',  ( 18.59999999999999076, 7.804459559388684298, -245.4620200072988325 ) ) ;
#187404=VERTEX_POINT ( 'NONE', #190822 ) ;
#187418=VERTEX_POINT ( 'NONE', #51242 ) ;
#187449=DIRECTION ( 'NONE',  ( 0.000000000000000000, 0.2128009952263630322, -0.9770955615653309501 ) ) ;
#187458=CIRCLE ( 'NONE', #16779, 12.87499999999999289 ) ;
#187474=EDGE_LOOP ( 'NONE', ( #23599, #74888, #157018 ) ) ;
#187480=DIRECTION ( 'NONE',  ( 7.304098846218132695E-16, 0.9770955615653315052, 0.2128009952263603954 ) ) ;
#187494=CIRCLE ( 'NONE', #41754, 0.1000000000000055844 ) ;
#187505=DIRECTION ( 'NONE',  ( 0.000000000000000000, -0.2965989261549410450, -0.9550021345545443019 ) ) ;
#187508=ORIENTED_EDGE ( 'NONE', *, *, #240275, .F. ) ;
#187578=EDGE_CURVE ( 'NONE', #255134, #256176, #231431, .T. ) ;
#187587=AXIS2_PLACEMENT_3D ( 'NONE', #163750, #62079, #64636 ) ;
#187608=TOROIDAL_SURFACE ( 'NONE', #175174, 12.77499999999999858, 0.1000000000000000056 ) ;
#187616=EDGE_CURVE ( 'NONE', #227071, #236905, #98065, .T. ) ;
#187620=CARTESIAN_POINT ( 'NONE',  ( 21.05000000000000071, -1.489567864901280680, -194.6304332222954372 ) ) ;
#187642=LINE ( 'NONE', #8983, #168150 ) ;
#187644=CIRCLE ( 'NONE', #29439, 0.1000000000000008937 ) ;
#187653=FACE_BOUND ( 'NONE', #97558, .T. ) ;
#187668=DIRECTION ( 'NONE',  ( 0.000000000000000000, 0.2128009952263403282, -0.9770955615653358350 ) ) ;
#187681=FACE_OUTER_BOUND ( 'NONE', #208013, .T. ) ;
#187683=AXIS2_PLACEMENT_3D ( 'NONE', #167887, #70067, #166603 ) ;
#187690=DIRECTION ( 'NONE',  ( 0.000000000000000000, 0.6728388485993177515, -0.7397890806274072251 ) ) ;
#187735=EDGE_CURVE ( 'NONE', #145681, #198700, #87505, .T. ) ;
#187789=AXIS2_PLACEMENT_3D ( 'NONE', #243978, #87463, #83589 ) ;
#187810=ADVANCED_FACE ( 'NONE', ( #175749 ), #108763, .T. ) ;
#187826=DIRECTION ( 'NONE',  ( -1.000000000000000000, 0.000000000000000000, 0.000000000000000000 ) ) ;
#187867=CYLINDRICAL_SURFACE ( 'NONE', #38120, 0.09999999999999939493 ) ;
#187885=CYLINDRICAL_SURFACE ( 'NONE', #1613, 0.1000000000000055844 ) ;
#187892=ORIENTED_EDGE ( 'NONE', *, *, #249335, .T. ) ;
#187895=ORIENTED_EDGE ( 'NONE', *, *, #22600, .F. ) ;
#187910=CARTESIAN_POINT ( 'NONE',  ( 18.59999999999999432, 0.4879293624014888198, -209.1697915983179428 ) ) ;
#187919=CARTESIAN_POINT ( 'NONE',  ( 22.39999999999999503, -2.479040261793999722, -189.6172560698084624 ) ) ;
#187923=CARTESIAN_POINT ( 'NONE',  ( -21.52071067811865746, 12.10185011759185691, -220.0101306172581417 ) ) ;
#187924=VERTEX_POINT ( 'NONE', #16667 ) ;
#187942=VERTEX_POINT ( 'NONE', #42628 ) ;
#187958=CARTESIAN_POINT ( 'NONE',  ( 21.05095171578076574, 11.16407634812396488, -211.0196409686826371 ) ) ;
#188002=LINE ( 'NONE', #9345, #241962 ) ;
#188017=CARTESIAN_POINT ( 'NONE',  ( 18.49999999999999289, 15.27230207784559113, -223.0085293587735009 ) ) ;
#188037=CARTESIAN_POINT ( 'NONE',  ( 21.11927991906888025, 6.298860988841674668, -199.6188786237795796 ) ) ;
#188043=DIRECTION ( 'NONE',  ( 1.000000000000000000, 0.000000000000000000, 0.000000000000000000 ) ) ;
#188047=VERTEX_POINT ( 'NONE', #64754 ) ;
#188057=CARTESIAN_POINT ( 'NONE',  ( -23.24999999999999645, -0.8254770802754692882, -242.3223161824233500 ) ) ;
#188089=EDGE_CURVE ( 'NONE', #253449, #57651, #210947, .T. ) ;
#188091=VECTOR ( 'NONE', #63442, 1000.000000000000000 ) ;
#188092=ORIENTED_EDGE ( 'NONE', *, *, #64924, .F. ) ;
#188134=DIRECTION ( 'NONE',  ( 0.000000000000000000, 0.2128009952263485993, -0.9770955615653341697 ) ) ;
#188204=DIRECTION ( 'NONE',  ( 1.000000000000000000, 0.000000000000000000, 0.000000000000000000 ) ) ;
#188230=LINE ( 'NONE', #47415, #26233 ) ;
#188271=EDGE_LOOP ( 'NONE', ( #242525, #195554, #256877, #19335 ) ) ;
#188272=CIRCLE ( 'NONE', #113446, 0.1000000000000054040 ) ;
#188310=ADVANCED_FACE ( 'NONE', ( #254887 ), #252363, .F. ) ;
#188321=FACE_OUTER_BOUND ( 'NONE', #214978, .T. ) ;
#188333=CARTESIAN_POINT ( 'NONE',  ( -23.25000000000000000, -3.642792592896924919, -226.5668142904084164 ) ) ;
#188374=CARTESIAN_POINT ( 'NONE',  ( -18.46946985241261174, -7.804742910430244152, -209.8502291530988373 ) ) ;
#188384=FACE_OUTER_BOUND ( 'NONE', #93124, .T. ) ;
#188402=DIRECTION ( 'NONE',  ( 0.000000000000000000, -0.9968797965484670343, -0.07893460099023182075 ) ) ;
#188439=AXIS2_PLACEMENT_3D ( 'NONE', #197919, #218760, #40175 ) ;
#188472=DIRECTION ( 'NONE',  ( 1.000000000000000000, 0.000000000000000000, 0.000000000000000000 ) ) ;
#188518=CIRCLE ( 'NONE', #55205, 11.74999999999999822 ) ;
#188519=CARTESIAN_POINT ( 'NONE',  ( -23.25000000000000000, 8.980461154494397746, -187.0187154576991304 ) ) ;
#188536=FACE_OUTER_BOUND ( 'NONE', #48570, .T. ) ;
#188555=AXIS2_PLACEMENT_3D ( 'NONE', #229617, #228336, #249187 ) ;
#188592=CARTESIAN_POINT ( 'NONE',  ( -18.59999999999999787, 11.76393579169289083, -211.0774408799668720 ) ) ;
#188624=CIRCLE ( 'NONE', #213763, 4.150000000000001243 ) ;
#188665=ADVANCED_FACE ( 'NONE', ( #22486 ), #199837, .T. ) ;
#188678=CARTESIAN_POINT ( 'NONE',  ( 18.49999999999999645, 2.899901325892989767, -187.5321506284477096 ) ) ;
#188686=FACE_OUTER_BOUND ( 'NONE', #90526, .T. ) ;
#188718=ORIENTED_EDGE ( 'NONE', *, *, #156369, .T. ) ;
#188737=CARTESIAN_POINT ( 'NONE',  ( -20.00857864376270001, 11.74265569217025629, -210.9797313238103698 ) ) ;
#188738=TOROIDAL_SURFACE ( 'NONE', #18053, 12.77500000000000036, 0.1000000000000000056 ) ;
#188745=ORIENTED_EDGE ( 'NONE', *, *, #189403, .T. ) ;
#188778=VECTOR ( 'NONE', #78914, 1000.000000000000000 ) ;
#188796=ORIENTED_EDGE ( 'NONE', *, *, #186283, .T. ) ;
#188833=ORIENTED_EDGE ( 'NONE', *, *, #93786, .F. ) ;
#188861=EDGE_CURVE ( 'NONE', #143844, #44981, #143906, .T. ) ;
#188868=PRODUCT ( 'Injection Molded Chain Links 7', 'Injection Molded Chain Links 7', '', ( #193033 ) ) ;
#188899=ADVANCED_FACE ( 'NONE', ( #148842 ), #177274, .F. ) ;
#188923=DIRECTION ( 'NONE',  ( -1.000000000000000000, -0.000000000000000000, -0.000000000000000000 ) ) ;
#188957=ADVANCED_FACE ( 'NONE', ( #247917 ), #30186, .F. ) ;
#188972=CARTESIAN_POINT ( 'NONE',  ( -20.94999999999999929, 4.273531877263399892, -211.9976340888692050 ) ) ;
#188989=DIRECTION ( 'NONE',  ( -1.000000000000000000, 0.000000000000000000, 0.000000000000000000 ) ) ;
#189025=AXIS2_PLACEMENT_3D ( 'NONE', #194442, #193145, #232286 ) ;
#189030=EDGE_CURVE ( 'NONE', #148114, #194623, #110777, .T. ) ;
#189043=ORIENTED_EDGE ( 'NONE', *, *, #239502, .F. ) ;
#189046=AXIS2_PLACEMENT_3D ( 'NONE', #43922, #160048, #120925 ) ;
#189075=AXIS2_PLACEMENT_3D ( 'NONE', #181380, #236502, #243887 ) ;
#189090=CARTESIAN_POINT ( 'NONE',  ( 23.14999999999999858, 2.739812813550880577, -213.5801053551551547 ) ) ;
#189104=ORIENTED_EDGE ( 'NONE', *, *, #193679, .T. ) ;
#189110=DIRECTION ( 'NONE',  ( -1.000000000000000000, 0.000000000000000000, 0.000000000000000000 ) ) ;
#189116=DIRECTION ( 'NONE',  ( 1.000000000000000000, 3.190570557967288949E-16, 6.948722487160392945E-17 ) ) ;
#189132=EDGE_CURVE ( 'NONE', #237457, #256235, #248329, .T. ) ;
#189135=CARTESIAN_POINT ( 'NONE',  ( 18.59999999999999076, 10.99842653345846699, -220.2504445088529792 ) ) ;
#189153=ORIENTED_EDGE ( 'NONE', *, *, #124860, .F. ) ;
#189207=CARTESIAN_POINT ( 'NONE',  ( -21.08621493067320429, -1.296228415900023023, -194.7841744112582205 ) ) ;
#189226=ORIENTED_EDGE ( 'NONE', *, *, #222191, .F. ) ;
#189252=FACE_OUTER_BOUND ( 'NONE', #143502, .T. ) ;
#189258=TOROIDAL_SURFACE ( 'NONE', #18373, 0.2000000000000000111, 0.1000000000000000056 ) ;
#189290=ORIENTED_EDGE ( 'NONE', *, *, #71831, .T. ) ;
#189298=VERTEX_POINT ( 'NONE', #204626 ) ;
#189377=AXIS2_PLACEMENT_3D ( 'NONE', #167231, #169808, #10698 ) ;
#189393=AXIS2_PLACEMENT_3D ( 'NONE', #194085, #214905, #196619 ) ;
#189403=EDGE_CURVE ( 'NONE', #231604, #232502, #12887, .T. ) ;
#189412=EDGE_CURVE ( 'NONE', #22873, #21979, #27795, .T. ) ;
#189432=EDGE_CURVE ( 'NONE', #55636, #63493, #127736, .T. ) ;
#189443=DIRECTION ( 'NONE',  ( 0.000000000000000000, -0.2128009952263650861, 0.9770955615653305060 ) ) ;
#189449=LINE ( 'NONE', #249427, #30977 ) ;
#189469=TOROIDAL_SURFACE ( 'NONE', #110159, 2.100000000000002309, 0.1000000000000000056 ) ;
#189513=EDGE_CURVE ( 'NONE', #179904, #145361, #102743, .T. ) ;
#189553=CARTESIAN_POINT ( 'NONE',  ( -21.05000000000000071, 1.148907358139439339E-11, -201.0000000000015064 ) ) ;
#189586=CARTESIAN_POINT ( 'NONE',  ( -22.39999999999999858, -2.598867842139048534, -189.5410128746472083 ) ) ;
#189626=ORIENTED_EDGE ( 'NONE', *, *, #186460, .T. ) ;
#189636=DIRECTION ( 'NONE',  ( 1.000000000000000000, 7.136802563874199107E-16, 1.554319503706929991E-16 ) ) ;
#189663=CARTESIAN_POINT ( 'NONE',  ( -18.51991288638565081, -7.657214099531299389, -209.9783737948318389 ) ) ;
#189749=DIRECTION ( 'NONE',  ( -1.000000000000000000, 0.000000000000000000, 0.000000000000000000 ) ) ;
#189781=DIRECTION ( 'NONE',  ( 1.000000000000000000, 2.885090398161910739E-16, 6.283419270304611573E-17 ) ) ;
#189791=EDGE_CURVE ( 'NONE', #63493, #237457, #155630, .T. ) ;
#189793=ORIENTED_EDGE ( 'NONE', *, *, #41578, .T. ) ;
#189864=VECTOR ( 'NONE', #252651, 1000.000000000000000 ) ;
#189884=ORIENTED_EDGE ( 'NONE', *, *, #183646, .T. ) ;
#189889=ORIENTED_EDGE ( 'NONE', *, *, #171366, .T. ) ;
#189891=DIRECTION ( 'NONE',  ( -1.000000000000000000, 0.000000000000000000, 0.000000000000000000 ) ) ;
#189904=CARTESIAN_POINT ( 'NONE',  ( -23.15000000000000213, 8.751106741858205140, -220.7398867978735950 ) ) ;
#189921=ORIENTED_EDGE ( 'NONE', *, *, #4317, .T. ) ;
#189955=CARTESIAN_POINT ( 'NONE',  ( -18.59999999999999787, 18.60970618848720903, -231.2322896185303875 ) ) ;
#189980=DIRECTION ( 'NONE',  ( 1.000000000000000000, 0.000000000000000000, 0.000000000000000000 ) ) ;
#189990=ORIENTED_EDGE ( 'NONE', *, *, #65568, .T. ) ;
#190001=DIRECTION ( 'NONE',  ( 0.000000000000000000, -0.9525900758537790836, 0.3042567129660269099 ) ) ;
#190010=ORIENTED_EDGE ( 'NONE', *, *, #115142, .T. ) ;
#190012=CARTESIAN_POINT ( 'NONE',  ( -23.25000000000000000, 14.73746888278882494, -235.8584165281851028 ) ) ;
#190038=CARTESIAN_POINT ( 'NONE',  ( 21.05000000000000426, 11.90764318652833431, -206.0382540159556015 ) ) ;
#190047=AXIS2_PLACEMENT_3D ( 'NONE', #127940, #9268, #168398 ) ;
#190062=DIRECTION ( 'NONE',  ( 0.000000000000000000, -0.9770955615653316162, -0.2128009952263604232 ) ) ;
#190072=VERTEX_POINT ( 'NONE', #169754 ) ;
#190089=AXIS2_PLACEMENT_3D ( 'NONE', #22853, #197600, #18962 ) ;
#190100=CIRCLE ( 'NONE', #77443, 0.1000000000000055844 ) ;
#190102=ADVANCED_FACE ( 'NONE', ( #215261 ), #250525, .T. ) ;
#190109=FACE_OUTER_BOUND ( 'NONE', #238114, .T. ) ;
#190132=CARTESIAN_POINT ( 'NONE',  ( -21.05000000000000071, 0.6656436123793473270, -212.6810495496487476 ) ) ;
#190144=AXIS2_PLACEMENT_3D ( 'NONE', #147628, #167227, #9392 ) ;
#190179=EDGE_CURVE ( 'NONE', #30493, #137285, #173924, .T. ) ;
#190209=ORIENTED_EDGE ( 'NONE', *, *, #124860, .T. ) ;
#190218=CARTESIAN_POINT ( 'NONE',  ( 18.40916198585734875, -0.7490475724413914183, -242.2033267618345747 ) ) ;
#190225=ORIENTED_EDGE ( 'NONE', *, *, #27115, .F. ) ;
#190245=CARTESIAN_POINT ( 'NONE',  ( 18.59999999999999432, 7.783179459866048866, -245.3643104511423303 ) ) ;
#190269=EDGE_LOOP ( 'NONE', ( #171020, #120219 ) ) ;
#190283=LINE ( 'NONE', #91164, #123815 ) ;
#190295=ORIENTED_EDGE ( 'NONE', *, *, #70438, .T. ) ;
#190342=ORIENTED_EDGE ( 'NONE', *, *, #65579, .T. ) ;
#190352=AXIS2_PLACEMENT_3D ( 'NONE', #49386, #191492, #134037 ) ;
#190390=CARTESIAN_POINT ( 'NONE',  ( -21.05000000000000071, -5.011722593499800205, -233.2041167654973322 ) ) ;
#190400=VECTOR ( 'NONE', #41341, 1000.000000000000227 ) ;
#190423=VECTOR ( 'NONE', #58857, 1000.000000000000000 ) ;
#190450=ADVANCED_FACE ( 'NONE', ( #27376 ), #243807, .F. ) ;
#190453=AXIS2_PLACEMENT_3D ( 'NONE', #147027, #66232, #84454 ) ;
#190486=EDGE_LOOP ( 'NONE', ( #173564, #7846, #249354, #98699 ) ) ;
#190519=VERTEX_POINT ( 'NONE', #132865 ) ;
#190562=TOROIDAL_SURFACE ( 'NONE', #48877, 11.90000000000000213, 0.1000000000000000056 ) ;
#190570=CARTESIAN_POINT ( 'NONE',  ( -20.85000000000000142, 7.476371755685457643, -241.7308184205399471 ) ) ;
#190572=EDGE_CURVE ( 'NONE', #110145, #30493, #91153, .T. ) ;
#190594=EDGE_CURVE ( 'NONE', #29211, #68130, #149139, .T. ) ;
#190602=CARTESIAN_POINT ( 'NONE',  ( -22.50000000000000000, 7.591056067193246548, -199.2444047917219052 ) ) ;
#190633=ORIENTED_EDGE ( 'NONE', *, *, #105356, .F. ) ;
#190635=ORIENTED_EDGE ( 'NONE', *, *, #89406, .T. ) ;
#190660=EDGE_CURVE ( 'NONE', #225002, #49064, #70028, .T. ) ;
#190666=FACE_OUTER_BOUND ( 'NONE', #29423, .T. ) ;
#190671=ORIENTED_EDGE ( 'NONE', *, *, #84968, .T. ) ;
#190673=ORIENTED_EDGE ( 'NONE', *, *, #83032, .F. ) ;
#190721=CARTESIAN_POINT ( 'NONE',  ( -18.50000000000000000, 14.61354176542825201, -235.9279552357344016 ) ) ;
#190797=CARTESIAN_POINT ( 'NONE',  ( -21.05000000000000071, 4.252251777740764460, -211.8999245327126744 ) ) ;
#190822=CARTESIAN_POINT ( 'NONE',  ( -18.50000000000000000, 13.67914474873013475, -219.8713009340548865 ) ) ;
#190838=CARTESIAN_POINT ( 'NONE',  ( -20.94999999999999929, -10.51247937907010233, -206.3598299697285654 ) ) ;
#190889=CARTESIAN_POINT ( 'NONE',  ( -22.50047199487510596, -2.456544280668254476, -189.5095247662567033 ) ) ;
#190895=VECTOR ( 'NONE', #155191, 1000.000000000000227 ) ;
#190906=ORIENTED_EDGE ( 'NONE', *, *, #22600, .T. ) ;
#190923=VERTEX_POINT ( 'NONE', #92116 ) ;
#190932=EDGE_CURVE ( 'NONE', #145377, #192844, #16059, .T. ) ;
#190948=ORIENTED_EDGE ( 'NONE', *, *, #180729, .F. ) ;
#190982=CARTESIAN_POINT ( 'NONE',  ( -18.50000000000000000, 4.252251777740764460, -211.8999245327126744 ) ) ;
#191059=ORIENTED_EDGE ( 'NONE', *, *, #62025, .F. ) ;
#191069=EDGE_CURVE ( 'NONE', #64897, #144682, #124361, .T. ) ;
#191086=ORIENTED_EDGE ( 'NONE', *, *, #58551, .T. ) ;
#191097=ORIENTED_EDGE ( 'NONE', *, *, #219956, .T. ) ;
#191130=CARTESIAN_POINT ( 'NONE',  ( -21.05000000000000071, 7.128833340094563376, -233.7327013124401276 ) ) ;
#191146=DIRECTION ( 'NONE',  ( 0.000000000000000000, 0.2128009952263603677, -0.9770955615653313941 ) ) ;
#191173=ORIENTED_EDGE ( 'NONE', *, *, #109595, .F. ) ;
#191212=VERTEX_POINT ( 'NONE', #82226 ) ;
#191226=FACE_OUTER_BOUND ( 'NONE', #39950, .T. ) ;
#191249=ORIENTED_EDGE ( 'NONE', *, *, #132643, .T. ) ;
#191276=ADVANCED_FACE ( 'NONE', ( #125248 ), #7842, .F. ) ;
#191280=EDGE_CURVE ( 'NONE', #248650, #217539, #228603, .T. ) ;
#191283=LINE ( 'NONE', #92147, #239119 ) ;
#191349=CARTESIAN_POINT ( 'NONE',  ( 21.05000000000000071, 12.10919762232931163, -206.2073353557311748 ) ) ;
#191352=DIRECTION ( 'NONE',  ( 0.000000000000000000, 0.2128009952263604232, -0.9770955615653316162 ) ) ;
#191382=CARTESIAN_POINT ( 'NONE',  ( 21.05000000000000071, -3.664072692419559907, -226.4691047342518857 ) ) ;
#191384=VERTEX_POINT ( 'NONE', #191672 ) ;
#191387=ADVANCED_FACE ( 'NONE', ( #127821, #28765 ), #71710, .F. ) ;
#191405=CARTESIAN_POINT ( 'NONE',  ( -23.15000000000000213, 1.148907358139439339E-11, -201.0000000000015064 ) ) ;
#191412=CARTESIAN_POINT ( 'NONE',  ( 20.91682497891423154, 18.39833411442327105, -236.9692678682430085 ) ) ;
#191422=FACE_OUTER_BOUND ( 'NONE', #107054, .T. ) ;
#191452=LINE ( 'NONE', #33677, #189864 ) ;
#191456=CARTESIAN_POINT ( 'NONE',  ( 18.59999999999999076, 14.51805813080544638, -219.6885945441820809 ) ) ;
#191482=CARTESIAN_POINT ( 'NONE',  ( -21.14999999999999858, 6.390846877240202950, -199.6081416912452653 ) ) ;
#191492=DIRECTION ( 'NONE',  ( 1.000000000000000000, 0.000000000000000000, 0.000000000000000000 ) ) ;
#191500=( BOUNDED_SURFACE ( )  B_SPLINE_SURFACE ( 3, 2, ( 
 ( #180846, #74400, #221226 ),
 ( #173517, #215152, #54781 ),
 ( #36554, #76917, #93917 ),
 ( #240817, #176055, #13114 ) ),
 .UNSPECIFIED., .F., .F., .F. ) 
 B_SPLINE_SURFACE_WITH_KNOTS ( ( 4, 4 ),
 ( 3, 3 ),
 ( 0.0006461284895273737604, 0.0007503702773985880276 ),
 ( 0.000000000000000000, 1.000000000000000000 ),
 .UNSPECIFIED. ) 
 GEOMETRIC_REPRESENTATION_ITEM ( )  RATIONAL_B_SPLINE_SURFACE ( (
 ( 1.000000000000000000, 0.7071067811865318076, 1.000000000000000000),
 ( 1.000000000000000000, 0.7076476444648033270, 1.000000000000000000),
 ( 1.000000000000000000, 0.7075727925192996093, 1.000000000000000000),
 ( 1.000000000000000000, 0.7071067811865210384, 1.000000000000000000) ) ) 
 REPRESENTATION_ITEM ( '' )  SURFACE ( )  );
#191505=CYLINDRICAL_SURFACE ( 'NONE', #180443, 0.1000000000000054040 ) ;
#191538=CIRCLE ( 'NONE', #50035, 0.1000000000000055844 ) ;
#191623=DIRECTION ( 'NONE',  ( -0.000000000000000000, 0.9770955615653313941, 0.2128009952263603954 ) ) ;
#191646=EDGE_CURVE ( 'NONE', #212023, #70808, #45394, .T. ) ;
#191648=CARTESIAN_POINT ( 'NONE',  ( -18.47690164073607022, -0.6931637155149755758, -242.2947192224642379 ) ) ;
#191650=AXIS2_PLACEMENT_3D ( 'NONE', #156069, #251271, #17789 ) ;
#191672=CARTESIAN_POINT ( 'NONE',  ( -21.44999999999999929, 9.712035112405693837, -211.5243229699422614 ) ) ;
#191679=CARTESIAN_POINT ( 'NONE',  ( -18.59999999999999787, 7.576017155224048061, -241.7224044826512284 ) ) ;
#191694=CARTESIAN_POINT ( 'NONE',  ( -21.05000000000000071, -1.489567864901281791, -194.6304332222954372 ) ) ;
#191729=ORIENTED_EDGE ( 'NONE', *, *, #211769, .F. ) ;
#191735=DIRECTION ( 'NONE',  ( 0.000000000000000000, 0.9770955615653551529, 0.2128009952262517601 ) ) ;
#191746=CARTESIAN_POINT ( 'NONE',  ( -18.50000000000000000, 11.76393579169289083, -211.0774408799668720 ) ) ;
#191761=CIRCLE ( 'NONE', #41715, 0.1000000000000054040 ) ;
#191789=DIRECTION ( 'NONE',  ( 0.000000000000000000, 0.2128009952263485993, -0.9770955615653341697 ) ) ;
#191794=CIRCLE ( 'NONE', #33592, 11.80000000000000959 ) ;
#191815=CARTESIAN_POINT ( 'NONE',  ( -20.94999999999999929, 0.6656436123793491033, -212.6810495496487476 ) ) ;
#191838=DIRECTION ( 'NONE',  ( 1.000000000000000000, 2.885090398161910739E-16, 6.283419270304611573E-17 ) ) ;
#191841=CARTESIAN_POINT ( 'NONE',  ( 18.59999999999999432, 4.064367954407507533, -211.9684786640956418 ) ) ;
#191857=DIRECTION ( 'NONE',  ( -3.265361837132813586E-16, 0.9770955615653313941, 0.2128009952263610893 ) ) ;
#191898=CARTESIAN_POINT ( 'NONE',  ( 20.95132126680579887, 11.86065605514014898, -206.1646587338731251 ) ) ;
#191931=FACE_OUTER_BOUND ( 'NONE', #234442, .T. ) ;
#192009=ORIENTED_EDGE ( 'NONE', *, *, #33811, .T. ) ;
#192030=AXIS2_PLACEMENT_3D ( 'NONE', #34280, #74699, #77209 ) ;
#192038=EDGE_CURVE ( 'NONE', #254024, #44597, #179103, .T. ) ;
#192050=DIRECTION ( 'NONE',  ( 0.000000000000000000, 0.2128009952263403282, -0.9770955615653358350 ) ) ;
#192059=AXIS2_PLACEMENT_3D ( 'NONE', #186981, #167412, #5714 ) ;
#192078=DIRECTION ( 'NONE',  ( -1.000000000000000000, 0.000000000000000000, 0.000000000000000000 ) ) ;
#192098=CARTESIAN_POINT ( 'NONE',  ( -23.15000000000000213, -3.770473190032741062, -225.9805569534692324 ) ) ;
#192129=CARTESIAN_POINT ( 'NONE',  ( 21.76363531954645936, 6.831241477096051895, -199.4109058311904619 ) ) ;
#192133=ORIENTED_EDGE ( 'NONE', *, *, #27936, .T. ) ;
#192139=FACE_OUTER_BOUND ( 'NONE', #98515, .T. ) ;
#192145=EDGE_CURVE ( 'NONE', #44901, #2619, #14960, .T. ) ;
#192180=DIRECTION ( 'NONE',  ( -1.000000000000000000, 7.136802563874200093E-16, 1.554319503706930238E-16 ) ) ;
#192203=FACE_OUTER_BOUND ( 'NONE', #13598, .T. ) ;
#192204=EDGE_CURVE ( 'NONE', #15753, #168569, #191761, .T. ) ;
#192224=ORIENTED_EDGE ( 'NONE', *, *, #186124, .F. ) ;
#192280=DIRECTION ( 'NONE',  ( 1.000000000000000000, 0.000000000000000000, 0.000000000000000000 ) ) ;
#192304=DIRECTION ( 'NONE',  ( -0.000000000000000000, -0.2128009952263603677, 0.9770955615653313941 ) ) ;
#192351=VERTEX_POINT ( 'NONE', #248108 ) ;
#192353=AXIS2_PLACEMENT_3D ( 'NONE', #144592, #7683, #128909 ) ;
#192370=DIRECTION ( 'NONE',  ( 1.000000000000000000, 0.000000000000000000, 0.000000000000000000 ) ) ;
#192373=EDGE_CURVE ( 'NONE', #219574, #68492, #100112, .T. ) ;
#192375=VERTEX_POINT ( 'NONE', #186878 ) ;
#192394=CARTESIAN_POINT ( 'NONE',  ( -21.05000000000000071, -5.616267472387885817, -233.5404684641580673 ) ) ;
#192403=CARTESIAN_POINT ( 'NONE',  ( 18.45139536634708577, -0.7268675243558969656, -242.2397633716003327 ) ) ;
#192405=LINE ( 'NONE', #194993, #75933 ) ;
#192410=AXIS2_PLACEMENT_3D ( 'NONE', #11964, #17097, #156627 ) ;
#192433=CIRCLE ( 'NONE', #113317, 0.1000000000000054040 ) ;
#192442=EDGE_CURVE ( 'NONE', #164661, #147767, #48622, .T. ) ;
#192459=FACE_OUTER_BOUND ( 'NONE', #34094, .T. ) ;
#192468=ORIENTED_EDGE ( 'NONE', *, *, #32862, .F. ) ;
#192481=EDGE_CURVE ( 'NONE', #143844, #162306, #19473, .T. ) ;
#192483=CARTESIAN_POINT ( 'NONE',  ( -20.00857864376270001, 13.44116543737180081, -219.7184420207870801 ) ) ;
#192490=ORIENTED_EDGE ( 'NONE', *, *, #220121, .F. ) ;
#192518=VERTEX_POINT ( 'NONE', #235933 ) ;
#192520=EDGE_CURVE ( 'NONE', #74531, #235411, #75221, .T. ) ;
#192524=CARTESIAN_POINT ( 'NONE',  ( -18.59999999999999787, 7.788796164756791818, -245.4641525896719543 ) ) ;
#192537=VERTEX_POINT ( 'NONE', #121169 ) ;
#192589=CIRCLE ( 'NONE', #238372, 0.09999999999999939493 ) ;
#192623=CARTESIAN_POINT ( 'NONE',  ( -23.15000000000000213, 7.128833340094563376, -233.7327013124401276 ) ) ;
#192628=AXIS2_PLACEMENT_3D ( 'NONE', #34614, #59239, #154574 ) ;
#192634=ORIENTED_EDGE ( 'NONE', *, *, #71695, .F. ) ;
#192636=DIRECTION ( 'NONE',  ( 1.000000000000000000, 0.000000000000000000, 0.000000000000000000 ) ) ;
#192646=CIRCLE ( 'NONE', #5170, 0.1000000000000055844 ) ;
#192662=ADVANCED_FACE ( 'NONE', ( #243641 ), #145814, .T. ) ;
#192684=CARTESIAN_POINT ( 'NONE',  ( -23.15000000000000213, 7.128833340094563376, -233.7327013124401276 ) ) ;
#192688=FACE_OUTER_BOUND ( 'NONE', #38166, .T. ) ;
#192713=AXIS2_PLACEMENT_3D ( 'NONE', #98020, #21111, #135872 ) ;
#192715=DIRECTION ( 'NONE',  ( -1.836970198721029934E-16, 0.9770955615653316162, 0.2128009952263604232 ) ) ;
#192734=AXIS2_PLACEMENT_3D ( 'NONE', #135690, #193126, #151439 ) ;
#192805=TOROIDAL_SURFACE ( 'NONE', #230205, 0.2000000000000000111, 0.1000000000000000056 ) ;
#192811=CYLINDRICAL_SURFACE ( 'NONE', #205180, 0.09999999999999691080 ) ;
#192814=AXIS2_PLACEMENT_3D ( 'NONE', #78349, #254400, #152801 ) ;
#192823=DIRECTION ( 'NONE',  ( 1.000000000000000000, 3.190570557967288949E-16, 6.948722487160392945E-17 ) ) ;
#192831=DIRECTION ( 'NONE',  ( 1.000000000000000000, 3.190570557967288949E-16, 6.948722487160392945E-17 ) ) ;
#192843=CARTESIAN_POINT ( 'NONE',  ( -20.94999999999999929, 7.128833340094563376, -233.7327013124401276 ) ) ;
#192844=VERTEX_POINT ( 'NONE', #154841 ) ;
#192888=DIRECTION ( 'NONE',  ( 1.000000000000000000, 0.000000000000000000, 0.000000000000000000 ) ) ;
#192899=ORIENTED_EDGE ( 'NONE', *, *, #53200, .T. ) ;
#192908=ORIENTED_EDGE ( 'NONE', *, *, #172982, .T. ) ;
#192919=PLANE ( 'NONE',  #248701 ) ;
#192956=ORIENTED_EDGE ( 'NONE', *, *, #8430, .F. ) ;
#193005=AXIS2_PLACEMENT_3D ( 'NONE', #204049, #161092, #222299 ) ;
#193007=DIRECTION ( 'NONE',  ( 1.000000000000000000, -0.000000000000000000, -0.000000000000000000 ) ) ;
#193023=CARTESIAN_POINT ( 'NONE',  ( -18.59999999999999787, 15.92646454033039305, -219.3818586450342707 ) ) ;
#193033=PRODUCT_CONTEXT ( 'NONE', #100702, 'mechanical' ) ;
#193040=EDGE_CURVE ( 'NONE', #223782, #27458, #89378, .T. ) ;
#193048=DIRECTION ( 'NONE',  ( 1.000000000000000000, -0.000000000000000000, -0.000000000000000000 ) ) ;
#193053=CARTESIAN_POINT ( 'NONE',  ( 22.49436431346199683, -2.413750014042771230, -189.6026474988864550 ) ) ;
#193059=DIRECTION ( 'NONE',  ( 0.000000000000000000, 0.2128009952263403282, -0.9770955615653358350 ) ) ;
#193062=AXIS2_PLACEMENT_3D ( 'NONE', #237333, #155259, #58662 ) ;
#193065=CARTESIAN_POINT ( 'NONE',  ( -21.09813707148783735, -1.328114159632769020, -194.7545125258655219 ) ) ;
#193088=DIRECTION ( 'NONE',  ( 0.000000000000000000, 0.2128009952263568427, -0.9770955615653322823 ) ) ;
#193106=DIRECTION ( 'NONE',  ( 0.000000000000000000, -0.6626775042260708570, -0.7489048840758791847 ) ) ;
#193126=DIRECTION ( 'NONE',  ( 1.224646799147353454E-16, 0.9770955615653316162, 0.2128009952263604232 ) ) ;
#193127=EDGE_CURVE ( 'NONE', #75618, #163761, #37420, .T. ) ;
#193135=DIRECTION ( 'NONE',  ( 0.000000000000000000, -0.2128009952263678062, 0.9770955615653298398 ) ) ;
#193145=DIRECTION ( 'NONE',  ( 1.000000000000000000, 0.000000000000000000, 0.000000000000000000 ) ) ;
#193177=ORIENTED_EDGE ( 'NONE', *, *, #175234, .T. ) ;
#193185=EDGE_CURVE ( 'NONE', #178200, #32893, #208683, .T. ) ;
#193197=DIRECTION ( 'NONE',  ( 0.000000000000000000, -0.2128009952263403282, 0.9770955615653358350 ) ) ;
#193204=AXIS2_PLACEMENT_3D ( 'NONE', #189904, #204313, #85624 ) ;
#193210=CARTESIAN_POINT ( 'NONE',  ( 21.05000000000000071, 7.128833340094563376, -233.7327013124401276 ) ) ;
#193217=CARTESIAN_POINT ( 'NONE',  ( 18.50000972452444969, 18.34807417603286339, -236.8765254748878704 ) ) ;
#193237=AXIS2_PLACEMENT_3D ( 'NONE', #213590, #136612, #17956 ) ;
#193291=TOROIDAL_SURFACE ( 'NONE', #139079, 4.149999999999999467, 0.1000000000000000056 ) ;
#193292=DIRECTION ( 'NONE',  ( -2.827886303505248273E-16, 0.7397890806274222131, 0.6728388485993010981 ) ) ;
#193316=VERTEX_POINT ( 'NONE', #236589 ) ;
#193319=CARTESIAN_POINT ( 'NONE',  ( 18.43565242384935488, -7.817436562502985353, -209.8389866835000532 ) ) ;
#193324=CIRCLE ( 'NONE', #139305, 0.1000000000000055844 ) ;
#193332=( BOUNDED_CURVE ( )  B_SPLINE_CURVE ( 3, ( #175913, #198001, #37682, #239716 ),
 .UNSPECIFIED., .F., .F. ) 
 B_SPLINE_CURVE_WITH_KNOTS ( ( 4, 4 ),
 ( 3.141592653589791784, 4.712388980384688786 ),
 .UNSPECIFIED. ) 
 CURVE ( )  GEOMETRIC_REPRESENTATION_ITEM ( )  RATIONAL_B_SPLINE_CURVE ( ( 1.000000000000000000, 0.8047378541243649375, 0.8047378541243649375, 1.000000000000000000 ) ) 
 REPRESENTATION_ITEM ( '' )  );
#193344=CIRCLE ( 'NONE', #80883, 0.1000000000000055844 ) ;
#193351=EDGE_CURVE ( 'NONE', #200569, #86393, #133259, .T. ) ;
#193365=DIRECTION ( 'NONE',  ( 0.000000000000000000, -0.2128009952263485993, 0.9770955615653341697 ) ) ;
#193381=CARTESIAN_POINT ( 'NONE',  ( -18.39999999999999858, -0.9152171842607024210, -242.2974985173726452 ) ) ;
#193428=ORIENTED_EDGE ( 'NONE', *, *, #190932, .F. ) ;
#193459=LINE ( 'NONE', #72229, #24111 ) ;
#193465=SPHERICAL_SURFACE ( 'NONE', #130640, 0.1000000000000000056 ) ;
#193476=AXIS2_PLACEMENT_3D ( 'NONE', #72884, #169422, #248934 ) ;
#193488=DIRECTION ( 'NONE',  ( 0.000000000000000000, 0.2128009952263603677, -0.9770955615653315052 ) ) ;
#193505=VERTEX_POINT ( 'NONE', #107356 ) ;
#193522=CIRCLE ( 'NONE', #47739, 0.2000000000000003997 ) ;
#193523=DIRECTION ( 'NONE',  ( 0.000000000000000000, 0.8659859643398428730, -0.5000683049008328718 ) ) ;
#193533=CARTESIAN_POINT ( 'NONE',  ( -22.48970261584617703, 11.37138061004976208, -198.4667671244310441 ) ) ;
#193562=ORIENTED_EDGE ( 'NONE', *, *, #132726, .T. ) ;
#193577=LINE ( 'NONE', #215680, #117235 ) ;
#193612=ORIENTED_EDGE ( 'NONE', *, *, #190572, .T. ) ;
#193613=VECTOR ( 'NONE', #256926, 1000.000000000000000 ) ;
#193626=DIRECTION ( 'NONE',  ( -0.000000000000000000, 0.2128009952263603677, -0.9770955615653313941 ) ) ;
#193631=ORIENTED_EDGE ( 'NONE', *, *, #7523, .F. ) ;
#193642=ORIENTED_EDGE ( 'NONE', *, *, #194981, .T. ) ;
#193646=DIRECTION ( 'NONE',  ( 1.000000000000000000, -0.000000000000000000, -0.000000000000000000 ) ) ;
#193656=CYLINDRICAL_SURFACE ( 'NONE', #78695, 0.5000000000000007772 ) ;
#193666=DIRECTION ( 'NONE',  ( 0.000000000000000000, 0.2128009952263585358, -0.9770955615653319493 ) ) ;
#193672=CARTESIAN_POINT ( 'NONE',  ( -18.59999999999999787, 14.70949956575304185, -235.9560995168023112 ) ) ;
#193679=EDGE_CURVE ( 'NONE', #145681, #227928, #46133, .T. ) ;
#193684=DIRECTION ( 'NONE',  ( 0.000000000000000000, 0.9770955615653316162, 0.2128009952263604232 ) ) ;
#193720=DIRECTION ( 'NONE',  ( 0.000000000000000000, -0.2128009952263609783, 0.9770955615653315052 ) ) ;
#193780=AXIS2_PLACEMENT_3D ( 'NONE', #209982, #133015, #52164 ) ;
#193787=DIRECTION ( 'NONE',  ( 1.000000000000000000, 0.000000000000000000, 0.000000000000000000 ) ) ;
#193794=EDGE_CURVE ( 'NONE', #212805, #103755, #103186, .T. ) ;
#193861=TOROIDAL_SURFACE ( 'NONE', #119039, 7.791421356237316687, 0.1000000000000000056 ) ;
#193877=ADVANCED_FACE ( 'NONE', ( #224429 ), #212574, .F. ) ;
#193886=ORIENTED_EDGE ( 'NONE', *, *, #220810, .T. ) ;
#193915=CIRCLE ( 'NONE', #214740, 0.1000000000000054040 ) ;
#193917=ORIENTED_EDGE ( 'NONE', *, *, #103698, .F. ) ;
#193934=EDGE_LOOP ( 'NONE', ( #5608, #223990, #131061, #128851 ) ) ;
#193937=DIRECTION ( 'NONE',  ( 1.000000000000000000, 0.000000000000000000, 0.000000000000000000 ) ) ;
#193974=CARTESIAN_POINT ( 'NONE',  ( -20.94999999999999929, 4.252251777740766236, -211.8999245327126744 ) ) ;
#194021=CARTESIAN_POINT ( 'NONE',  ( 22.39999999999999503, -1.560176095955058129, -193.3663837337745122 ) ) ;
#194028=VECTOR ( 'NONE', #118965, 1000.000000000000227 ) ;
#194061=TOROIDAL_SURFACE ( 'NONE', #32127, 1.900000000000002576, 0.1000000000000000056 ) ;
#194072=CARTESIAN_POINT ( 'NONE',  ( -23.25000000000000000, 1.148907358139439339E-11, -201.0000000000015064 ) ) ;
#194085=CARTESIAN_POINT ( 'NONE',  ( -23.15000000000000213, -4.914013037343267776, -233.1828366659746905 ) ) ;
#194102=CARTESIAN_POINT ( 'NONE',  ( 22.39999999999999503, 7.612336166715857111, -199.3421143478784359 ) ) ;
#194163=DIRECTION ( 'NONE',  ( 1.000000000000000000, 0.000000000000000000, 0.000000000000000000 ) ) ;
#194168=ORIENTED_EDGE ( 'NONE', *, *, #138928, .F. ) ;
#194173=ORIENTED_EDGE ( 'NONE', *, *, #239502, .T. ) ;
#194199=ORIENTED_EDGE ( 'NONE', *, *, #110373, .F. ) ;
#194200=CARTESIAN_POINT ( 'NONE',  ( -20.64999999999999858, 7.128833340094563376, -233.7327013124401276 ) ) ;
#194207=FACE_OUTER_BOUND ( 'NONE', #165996, .T. ) ;
#194212=ORIENTED_EDGE ( 'NONE', *, *, #70438, .F. ) ;
#194223=AXIS2_PLACEMENT_3D ( 'NONE', #127433, #165274, #84398 ) ;
#194253=CARTESIAN_POINT ( 'NONE',  ( -21.05000000000000071, -1.391858308744749362, -194.6091531227727955 ) ) ;
#194256=CIRCLE ( 'NONE', #131684, 0.2000000000000003997 ) ;
#194258=AXIS2_PLACEMENT_3D ( 'NONE', #25861, #90949, #229194 ) ;
#194263=VERTEX_POINT ( 'NONE', #8622 ) ;
#194279=CARTESIAN_POINT ( 'NONE',  ( 23.25000000000000000, -8.895340756380869962, -215.3721227669300049 ) ) ;
#194352=CARTESIAN_POINT ( 'NONE',  ( 21.13435531349809438, -1.381870305043258584, -194.6550139707225355 ) ) ;
#194362=CIRCLE ( 'NONE', #210894, 0.1000000000000055844 ) ;
#194375=CARTESIAN_POINT ( 'NONE',  ( -23.25000000000000000, 17.01923898301589944, -224.3994341343041867 ) ) ;
#194380=AXIS2_PLACEMENT_3D ( 'NONE', #19991, #43388, #1676 ) ;
#194438=DIRECTION ( 'NONE',  ( 0.000000000000000000, 0.2128009952263485993, -0.9770955615653341697 ) ) ;
#194441=ORIENTED_EDGE ( 'NONE', *, *, #74303, .F. ) ;
#194442=CARTESIAN_POINT ( 'NONE',  ( -23.25000000000000000, 7.783179459866048866, -245.3643104511423019 ) ) ;
#194453=DIRECTION ( 'NONE',  ( 0.000000000000000000, -0.9770955615653315052, -0.2128009952263603954 ) ) ;
#194540=EDGE_CURVE ( 'NONE', #173153, #214061, #12042, .T. ) ;
#194546=VECTOR ( 'NONE', #104121, 1000.000000000000000 ) ;
#194548=ORIENTED_EDGE ( 'NONE', *, *, #172627, .F. ) ;
#194554=CARTESIAN_POINT ( 'NONE',  ( -23.15000000000000213, 11.38316329224760359, -198.5208684056144079 ) ) ;
#194583=EDGE_LOOP ( 'NONE', ( #41913, #241882, #99658, #26250 ) ) ;
#194590=DIRECTION ( 'NONE',  ( -2.081668171172008469E-13, -0.6413305999522614931, -0.7672646620071019719 ) ) ;
#194623=VERTEX_POINT ( 'NONE', #210976 ) ;
#194664=CIRCLE ( 'NONE', #227958, 0.1000000000000001305 ) ;
#194680=ORIENTED_EDGE ( 'NONE', *, *, #5285, .T. ) ;
#194681=FACE_OUTER_BOUND ( 'NONE', #180389, .T. ) ;
#194682=DIRECTION ( 'NONE',  ( 8.673617379884087537E-15, -0.2128009952263604232, 0.9770955615653316162 ) ) ;
#194685=FACE_OUTER_BOUND ( 'NONE', #198386, .T. ) ;
#194689=CARTESIAN_POINT ( 'NONE',  ( 18.45036689428330234, -7.780508153564097640, -209.8715945982282278 ) ) ;
#194701=CARTESIAN_POINT ( 'NONE',  ( -22.42357213249529480, -1.535990215375571788, -193.4817260165448545 ) ) ;
#194715=CYLINDRICAL_SURFACE ( 'NONE', #224929, 0.5000000000000009992 ) ;
#194734=AXIS2_PLACEMENT_3D ( 'NONE', #174111, #154537, #12444 ) ;
#194744=TOROIDAL_SURFACE ( 'NONE', #236224, 0.2000000000000000111, 0.1000000000000000056 ) ;
#194773=DIRECTION ( 'NONE',  ( -0.7071067811865388020, 0.6909108974501111389, 0.1504730267679034728 ) ) ;
#194809=DIRECTION ( 'NONE',  ( 1.000000000000000000, 0.000000000000000000, 0.000000000000000000 ) ) ;
#194831=CARTESIAN_POINT ( 'NONE',  ( -22.49806830649814415, 11.36657099087203093, -198.4452018475131183 ) ) ;
#194859=AXIS2_PLACEMENT_3D ( 'NONE', #170026, #31788, #8348 ) ;
#194861=ORIENTED_EDGE ( 'NONE', *, *, #95128, .F. ) ;
#194880=ORIENTED_EDGE ( 'NONE', *, *, #101358, .F. ) ;
#194920=VECTOR ( 'NONE', #255837, 1000.000000000000227 ) ;
#194944=DIRECTION ( 'NONE',  ( 1.000000000000000000, 0.000000000000000000, 0.000000000000000000 ) ) ;
#194947=ORIENTED_EDGE ( 'NONE', *, *, #18965, .T. ) ;
#194950=CIRCLE ( 'NONE', #94967, 0.2000000000000111688 ) ;
#194981=EDGE_CURVE ( 'NONE', #68824, #248715, #121721, .T. ) ;
#194991=CARTESIAN_POINT ( 'NONE',  ( 18.50000000000000000, -0.5913595841389442942, -242.4574432119242999 ) ) ;
#194993=CARTESIAN_POINT ( 'NONE',  ( 20.94999999999999929, 18.44490481964982465, -236.9051382908829169 ) ) ;
#195029=EDGE_CURVE ( 'NONE', #218226, #20649, #234117, .T. ) ;
#195048=DIRECTION ( 'NONE',  ( 0.000000000000000000, 0.2128009952263605342, -0.9770955615653315052 ) ) ;
#195060=ORIENTED_EDGE ( 'NONE', *, *, #25886, .T. ) ;
#195098=ORIENTED_EDGE ( 'NONE', *, *, #237762, .T. ) ;
#195102=ORIENTED_EDGE ( 'NONE', *, *, #212301, .T. ) ;
#195124=CARTESIAN_POINT ( 'NONE',  ( 21.53699400381533380, 6.632243066309477797, -199.5555681750802819 ) ) ;
#195206=DIRECTION ( 'NONE',  ( 0.000000000000000000, 0.2128009952263601456, -0.9770955615653316162 ) ) ;
#195208=CIRCLE ( 'NONE', #3623, 2.100000000000008527 ) ;
#195214=ADVANCED_FACE ( 'NONE', ( #217055 ), #1045, .T. ) ;
#195228=CIRCLE ( 'NONE', #149433, 0.5000000000000007772 ) ;
#195230=AXIS2_PLACEMENT_3D ( 'NONE', #224191, #128963, #109370 ) ;
#195237=VERTEX_POINT ( 'NONE', #193672 ) ;
#195257=CARTESIAN_POINT ( 'NONE',  ( 20.92356734117541706, 18.39335631088232503, -236.9600537807593241 ) ) ;
#195264=VECTOR ( 'NONE', #204902, 1000.000000000000000 ) ;
#195301=ORIENTED_EDGE ( 'NONE', *, *, #220698, .T. ) ;
#195324=DIRECTION ( 'NONE',  ( 1.000000000000000000, 0.000000000000000000, 0.000000000000000000 ) ) ;
#195333=DIRECTION ( 'NONE',  ( 1.000000000000000000, 0.000000000000000000, 0.000000000000000000 ) ) ;
#195345=VERTEX_POINT ( 'NONE', #75037 ) ;
#195356=EDGE_CURVE ( 'NONE', #84780, #183877, #159329, .T. ) ;
#195358=DIRECTION ( 'NONE',  ( -1.000000000000000000, 0.000000000000000000, 0.000000000000000000 ) ) ;
#195381=EDGE_CURVE ( 'NONE', #248593, #38453, #47042, .T. ) ;
#195385=DIRECTION ( 'NONE',  ( 0.000000000000000000, -0.2128009952263604232, 0.9770955615653316162 ) ) ;
#195413=ORIENTED_EDGE ( 'NONE', *, *, #14021, .F. ) ;
#195422=CARTESIAN_POINT ( 'NONE',  ( 18.59999999999999076, 14.51805813080544638, -219.6885945441820809 ) ) ;
#195433=DIRECTION ( 'NONE',  ( 0.000000000000000000, 0.6728388485993177515, -0.7397890806274072251 ) ) ;
#195436=DIRECTION ( 'NONE',  ( 0.000000000000000000, 0.2128009952263485993, -0.9770955615653341697 ) ) ;
#195440=EDGE_CURVE ( 'NONE', #184847, #59486, #188518, .T. ) ;
#195531=ORIENTED_EDGE ( 'NONE', *, *, #43853, .F. ) ;
#195541=EDGE_CURVE ( 'NONE', #132220, #115886, #188230, .T. ) ;
#195554=ORIENTED_EDGE ( 'NONE', *, *, #169834, .F. ) ;
#195563=ORIENTED_EDGE ( 'NONE', *, *, #186778, .F. ) ;
#195578=DIRECTION ( 'NONE',  ( -0.7071067811865302533, 0.6909108974501196876, 0.1504730267679053324 ) ) ;
#195605=DIRECTION ( 'NONE',  ( 0.000000000000000000, -0.2128009952263604232, 0.9770955615653316162 ) ) ;
#195661=CARTESIAN_POINT ( 'NONE',  ( -18.59999999999999787, 7.882824859404637508, -245.3558965132535832 ) ) ;
#195674=ADVANCED_FACE ( 'NONE', ( #194685 ), #99373, .T. ) ;
#195677=DIRECTION ( 'NONE',  ( 0.000000000000000000, 0.2128009952263606175, -0.9770955615653316162 ) ) ;
#195678=FACE_OUTER_BOUND ( 'NONE', #32218, .T. ) ;
#195699=DIRECTION ( 'NONE',  ( -3.787827842127534447E-15, 0.5795995782408164265, 0.8149014228132551718 ) ) ;
#195703=VERTEX_POINT ( 'NONE', #36898 ) ;
#195709=DIRECTION ( 'NONE',  ( 0.000000000000000000, -0.9770955615653316162, -0.2128009952263604232 ) ) ;
#195710=( BOUNDED_SURFACE ( )  B_SPLINE_SURFACE ( 3, 2, ( 
 ( #129903, #90772, #170381 ),
 ( #219713, #99750, #161047 ),
 ( #77615, #178050, #176765 ),
 ( #200170, #42373, #121922 ) ),
 .UNSPECIFIED., .F., .F., .F. ) 
 B_SPLINE_SURFACE_WITH_KNOTS ( ( 4, 4 ),
 ( 3, 3 ),
 ( 0.0006461284895273722425, 0.0007503702773986175179 ),
 ( 0.000000000000000000, 1.000000000000000000 ),
 .UNSPECIFIED. ) 
 GEOMETRIC_REPRESENTATION_ITEM ( )  RATIONAL_B_SPLINE_SURFACE ( (
 ( 1.000000000000000000, 0.7071067811865318076, 1.000000000000000000),
 ( 1.000000000000000000, 0.7076476444648260866, 1.000000000000000000),
 ( 1.000000000000000000, 0.7075727925192434320, 1.000000000000000000),
 ( 1.000000000000000000, 0.7071067811865299202, 1.000000000000000000) ) ) 
 REPRESENTATION_ITEM ( '' )  SURFACE ( )  );
#195714=EDGE_CURVE ( 'NONE', #253449, #137759, #151121, .T. ) ;
#195716=AXIS2_PLACEMENT_3D ( 'NONE', #95843, #152019, #136243 ) ;
#195723=CARTESIAN_POINT ( 'NONE',  ( 21.05000000000000071, 17.11694853917244075, -224.3781540347815451 ) ) ;
#195801=AXIS2_PLACEMENT_3D ( 'NONE', #52934, #172937, #251119 ) ;
#195825=ORIENTED_EDGE ( 'NONE', *, *, #77062, .F. ) ;
#195847=VECTOR ( 'NONE', #119873, 1000.000000000000227 ) ;
#195870=CARTESIAN_POINT ( 'NONE',  ( 18.49999999999998934, 19.88098775990103562, -199.0038892813511779 ) ) ;
#195905=CARTESIAN_POINT ( 'NONE',  ( 21.11833042828174456, 6.296499826410054013, -199.6214225183865665 ) ) ;
#195929=CARTESIAN_POINT ( 'NONE',  ( 20.95443524775735611, 10.49118055759163504, -207.4488969755982737 ) ) ;
#195964=EDGE_CURVE ( 'NONE', #142228, #113101, #30513, .T. ) ;
#195971=CARTESIAN_POINT ( 'NONE',  ( -21.30740335185486600, -1.298594845133715259, -194.5724652801384309 ) ) ;
#195975=EDGE_CURVE ( 'NONE', #195703, #100848, #251222, .T. ) ;
#195981=CARTESIAN_POINT ( 'NONE',  ( -23.15000000000000213, 15.92646454033039660, -219.3818586450342707 ) ) ;
#195988=CARTESIAN_POINT ( 'NONE',  ( 23.24999999999999645, 1.148907358139439339E-11, -201.0000000000015064 ) ) ;
#196032=AXIS2_PLACEMENT_3D ( 'NONE', #190982, #231377, #29354 ) ;
#196033=ORIENTED_EDGE ( 'NONE', *, *, #118359, .F. ) ;
#196035=DIRECTION ( 'NONE',  ( 1.000000000000000000, 0.000000000000000000, 0.000000000000000000 ) ) ;
#196038=LINE ( 'NONE', #96886, #253917 ) ;
#196046=DIRECTION ( 'NONE',  ( -0.000000000000000000, -0.9770955615653316162, -0.2128009952263597848 ) ) ;
#196203=DIRECTION ( 'NONE',  ( 0.000000000000000000, -0.2128009952263651694, 0.9770955615653305060 ) ) ;
#196220=DIRECTION ( 'NONE',  ( -0.000000000000000000, 0.9770955615653313941, 0.2128009952263606730 ) ) ;
#196243=DIRECTION ( 'NONE',  ( -1.000000000000000000, -0.000000000000000000, -0.000000000000000000 ) ) ;
#196247=DIRECTION ( 'NONE',  ( 0.000000000000000000, 0.9550021345545507412, -0.2965989261549202838 ) ) ;
#196248=CARTESIAN_POINT ( 'NONE',  ( 20.44999100639885725, 11.85173402866923986, -206.3597776261780155 ) ) ;
#196267=VERTEX_POINT ( 'NONE', #169043 ) ;
#196297=DIRECTION ( 'NONE',  ( 0.000000000000000000, -0.2128009952263678062, 0.9770955615653298398 ) ) ;
#196315=CARTESIAN_POINT ( 'NONE',  ( -21.05000000000000426, 12.80863705670246411, -205.3010250813005655 ) ) ;
#196319=CARTESIAN_POINT ( 'NONE',  ( 18.49999999999999645, 4.158309866074138661, -211.9342015984041439 ) ) ;
#196346=CARTESIAN_POINT ( 'NONE',  ( -23.15000000000000213, 2.718532714028243369, -213.4823957989985956 ) ) ;
#196348=EDGE_LOOP ( 'NONE', ( #133498, #27620, #46957, #154717 ) ) ;
#196367=DIRECTION ( 'NONE',  ( 1.000000000000000000, 0.000000000000000000, 0.000000000000000000 ) ) ;
#196399=EDGE_CURVE ( 'NONE', #232502, #205893, #254896, .T. ) ;
#196418=CYLINDRICAL_SURFACE ( 'NONE', #66882, 0.09999999999999939493 ) ;
#196459=ORIENTED_EDGE ( 'NONE', *, *, #72576, .F. ) ;
#196482=TOROIDAL_SURFACE ( 'NONE', #133942, 7.791421356237335338, 0.1000000000000000056 ) ;
#196497=ORIENTED_EDGE ( 'NONE', *, *, #238869, .F. ) ;
#196501=ORIENTED_EDGE ( 'NONE', *, *, #51478, .F. ) ;
#196518=B_SPLINE_CURVE_WITH_KNOTS ( 'NONE', 3,
 ( #127176, #243250, #206709, #25517, #103722, #43786, #22966, #145438 ),
 .UNSPECIFIED., .F., .F.,
 ( 4, 2, 2, 4 ),
 ( 0.000000000000000000, 6.534141206312327069E-05, 0.0001306828241262465414, 0.0002613656482524937333 ),
 .UNSPECIFIED. ) ;
#196522=AXIS2_PLACEMENT_3D ( 'NONE', #196346, #17697, #178093 ) ;
#196575=CARTESIAN_POINT ( 'NONE',  ( 18.45068634130097962, -7.764979893827074875, -209.9256099644128994 ) ) ;
#196579=ADVANCED_FACE ( 'NONE', ( #5751 ), #42340, .F. ) ;
#196582=DIRECTION ( 'NONE',  ( 1.000000000000000000, 0.000000000000000000, 0.000000000000000000 ) ) ;
#196606=CARTESIAN_POINT ( 'NONE',  ( -18.59999999999999787, 12.87592094156238609, -205.3750039893633073 ) ) ;
#196612=CIRCLE ( 'NONE', #121812, 0.09999999999999939493 ) ;
#196619=DIRECTION ( 'NONE',  ( 0.000000000000000000, 0.2128009952263485993, -0.9770955615653341697 ) ) ;
#196633=CIRCLE ( 'NONE', #5074, 0.6000000000000064171 ) ;
#196655=ADVANCED_FACE ( 'NONE', ( #250802 ), #188738, .T. ) ;
#196675=VECTOR ( 'NONE', #154113, 1000.000000000000000 ) ;
#196682=CIRCLE ( 'NONE', #67503, 0.09999999999999939493 ) ;
#196723=CARTESIAN_POINT ( 'NONE',  ( -18.50000000000000000, 14.80545736607782814, -235.9842437978701639 ) ) ;
#196725=VERTEX_POINT ( 'NONE', #89157 ) ;
#196741=ORIENTED_EDGE ( 'NONE', *, *, #142926, .T. ) ;
#196753=DIRECTION ( 'NONE',  ( 0.000000000000000000, -0.2128009952263604232, 0.9770955615653316162 ) ) ;
#196765=ORIENTED_EDGE ( 'NONE', *, *, #88771, .F. ) ;
#196766=LINE ( 'NONE', #182365, #121717 ) ;
#196779=EDGE_CURVE ( 'NONE', #56802, #170560, #242906, .T. ) ;
#196793=ADVANCED_FACE ( 'NONE', ( #233824 ), #99419, .T. ) ;
#196795=CARTESIAN_POINT ( 'NONE',  ( -23.25000000000000000, 7.783179459866048866, -245.3643104511423019 ) ) ;
#196810=ADVANCED_FACE ( 'NONE', ( #219375 ), #35654, .T. ) ;
#196866=DIRECTION ( 'NONE',  ( 1.000000000000000000, 0.000000000000000000, 0.000000000000000000 ) ) ;
#196896=AXIS2_PLACEMENT_3D ( 'NONE', #94255, #257135, #56402 ) ;
#196957=CIRCLE ( 'NONE', #184481, 0.09999999999999939493 ) ;
#196962=CARTESIAN_POINT ( 'NONE',  ( 20.85000000000000142, 17.16609282392354174, -224.6038045889790453 ) ) ;
#196976=CARTESIAN_POINT ( 'NONE',  ( 19.75857864376269291, 16.76897757977919667, -222.7804130109903156 ) ) ;
#196981=ORIENTED_EDGE ( 'NONE', *, *, #123843, .T. ) ;
#197007=ORIENTED_EDGE ( 'NONE', *, *, #198946, .F. ) ;
#197018=ADVANCED_FACE ( 'NONE', ( #186696 ), #126390, .T. ) ;
#197064=CIRCLE ( 'NONE', #193005, 0.1000000000000054040 ) ;
#197093=ORIENTED_EDGE ( 'NONE', *, *, #205577, .T. ) ;
#197107=FACE_OUTER_BOUND ( 'NONE', #25809, .T. ) ;
#197114=LINE ( 'NONE', #35524, #33122 ) ;
#197142=EDGE_CURVE ( 'NONE', #138601, #7989, #201393, .T. ) ;
#197178=CIRCLE ( 'NONE', #34923, 0.1000000000000054040 ) ;
#197194=ORIENTED_EDGE ( 'NONE', *, *, #254605, .F. ) ;
#197203=DIRECTION ( 'NONE',  ( 0.000000000000000000, 0.2128009952263403282, -0.9770955615653358350 ) ) ;
#197229=FACE_OUTER_BOUND ( 'NONE', #168725, .T. ) ;
#197249=ORIENTED_EDGE ( 'NONE', *, *, #136681, .T. ) ;
#197327=AXIS2_PLACEMENT_3D ( 'NONE', #76581, #257732, #19182 ) ;
#197347=CARTESIAN_POINT ( 'NONE',  ( -20.64999999999999858, 4.768403829798271154, -213.4961173936592331 ) ) ;
#197404=EDGE_CURVE ( 'NONE', #59486, #154024, #914, .T. ) ;
#197415=EDGE_CURVE ( 'NONE', #81210, #52494, #205664, .T. ) ;
#197423=PLANE ( 'NONE',  #227661 ) ;
#197434=ORIENTED_EDGE ( 'NONE', *, *, #143237, .T. ) ;
#197435=EDGE_CURVE ( 'NONE', #7468, #201052, #89819, .T. ) ;
#197436=DIRECTION ( 'NONE',  ( 0.000000000000000000, 0.2128009952263603122, -0.9770955615653315052 ) ) ;
#197441=DIRECTION ( 'NONE',  ( 1.000000000000000000, -0.000000000000000000, -0.000000000000000000 ) ) ;
#197524=DIRECTION ( 'NONE',  ( 4.336808689942128177E-15, 0.9525900758537759749, -0.3042567129660372904 ) ) ;
#197529=CARTESIAN_POINT ( 'NONE',  ( 20.13684514580420526, 11.01120340441282153, -206.9357926396625089 ) ) ;
#197554=ORIENTED_EDGE ( 'NONE', *, *, #252999, .T. ) ;
#197600=DIRECTION ( 'NONE',  ( 0.000000000000000000, -0.9770955615653315052, -0.2128009952263603954 ) ) ;
#197607=EDGE_CURVE ( 'NONE', #63849, #20437, #60100, .T. ) ;
#197644=EDGE_CURVE ( 'NONE', #118817, #30421, #164894, .T. ) ;
#197651=FACE_OUTER_BOUND ( 'NONE', #10678, .T. ) ;
#197719=EDGE_LOOP ( 'NONE', ( #21725, #255312, #124660, #73353 ) ) ;
#197732=CIRCLE ( 'NONE', #22983, 0.09999999999999574507 ) ;
#197764=ORIENTED_EDGE ( 'NONE', *, *, #33315, .F. ) ;
#197822=DIRECTION ( 'NONE',  ( 1.000000000000000000, 0.000000000000000000, 0.000000000000000000 ) ) ;
#197852=CARTESIAN_POINT ( 'NONE',  ( -23.25000000000000000, 8.980461154494397746, -187.0187154576991304 ) ) ;
#197856=EDGE_CURVE ( 'NONE', #241591, #134704, #56187, .T. ) ;
#197858=CARTESIAN_POINT ( 'NONE',  ( 18.41356215285962605, -7.785976468740678946, -209.8926132507865532 ) ) ;
#197883=ORIENTED_EDGE ( 'NONE', *, *, #28737, .T. ) ;
#197919=CARTESIAN_POINT ( 'NONE',  ( 23.14999999999999858, 9.374458193048763377, -220.5475659691911119 ) ) ;
#197951=EDGE_CURVE ( 'NONE', #103565, #201031, #21258, .T. ) ;
#197964=DIRECTION ( 'NONE',  ( 0.000000000000000000, -0.7397890806274222131, -0.6728388485993012091 ) ) ;
#197971=CARTESIAN_POINT ( 'NONE',  ( -21.05000000000000071, 1.148907358139439339E-11, -201.0000000000015064 ) ) ;
#197976=DIRECTION ( 'NONE',  ( 0.000000000000000000, -0.9797463026583741463, -0.2002428086779788896 ) ) ;
#197981=FACE_OUTER_BOUND ( 'NONE', #96194, .T. ) ;
#197983=CIRCLE ( 'NONE', #10573, 7.900000000000002132 ) ;
#198001=CARTESIAN_POINT ( 'NONE',  ( -20.93284271247462058, 17.11694853917243719, -224.3781540347815451 ) ) ;
#198018=CARTESIAN_POINT ( 'NONE',  ( 23.14999999999998437, 1.148907358139439339E-11, -201.0000000000015064 ) ) ;
#198051=AXIS2_PLACEMENT_3D ( 'NONE', #151661, #228615, #231190 ) ;
#198092=TOROIDAL_SURFACE ( 'NONE', #210558, 0.6000000000000013101, 0.1000000000000000056 ) ;
#198099=CARTESIAN_POINT ( 'NONE',  ( -22.39999999999999858, 7.591056067193246548, -199.2444047917219052 ) ) ;
#198121=CARTESIAN_POINT ( 'NONE',  ( -18.59999999999999787, 14.73746888278882494, -235.8584165281851028 ) ) ;
#198124=ORIENTED_EDGE ( 'NONE', *, *, #77062, .T. ) ;
#198153=VECTOR ( 'NONE', #66972, 1000.000000000000227 ) ;
#198155=FACE_OUTER_BOUND ( 'NONE', #119715, .T. ) ;
#198195=AXIS2_PLACEMENT_3D ( 'NONE', #62772, #107016, #143589 ) ;
#198228=DIRECTION ( 'NONE',  ( 2.840903330521632762E-16, -0.9550021345545507412, 0.2965989261549202838 ) ) ;
#198257=DIRECTION ( 'NONE',  ( 1.000000000000000000, 0.000000000000000000, 0.000000000000000000 ) ) ;
#198273=DIRECTION ( 'NONE',  ( 0.000000000000000000, 0.2128009952263242854, -0.9770955615653393878 ) ) ;
#198282=LINE ( 'NONE', #63916, #193613 ) ;
#198350=ORIENTED_EDGE ( 'NONE', *, *, #117352, .T. ) ;
#198353=CARTESIAN_POINT ( 'NONE',  ( -18.50000000000000000, 7.128833340094563376, -233.7327013124401276 ) ) ;
#198359=AXIS2_PLACEMENT_3D ( 'NONE', #154030, #195699, #34069 ) ;
#198369=DIRECTION ( 'NONE',  ( -1.000000000000000000, 0.000000000000000000, 0.000000000000000000 ) ) ;
#198370=EDGE_LOOP ( 'NONE', ( #88752, #221202, #175155, #57885 ) ) ;
#198375=CARTESIAN_POINT ( 'NONE',  ( 18.49999999999999645, 0.5876173420563333138, -209.1618981382189588 ) ) ;
#198386=EDGE_LOOP ( 'NONE', ( #42734, #45875, #165061 ) ) ;
#198387=ORIENTED_EDGE ( 'NONE', *, *, #119560, .T. ) ;
#198426=AXIS2_PLACEMENT_3D ( 'NONE', #198797, #128267, #224773 ) ;
#198429=ADVANCED_FACE ( 'NONE', ( #121205 ), #172957, .T. ) ;
#198456=VERTEX_POINT ( 'NONE', #63757 ) ;
#198496=CARTESIAN_POINT ( 'NONE',  ( 18.49999999999999645, 7.128833340094563376, -233.7327013124401276 ) ) ;
#198522=DIRECTION ( 'NONE',  ( 2.952720810173289605E-16, -0.9770955615653318382, -0.2128009952263588411 ) ) ;
#198525=ORIENTED_EDGE ( 'NONE', *, *, #97703, .F. ) ;
#198568=DIRECTION ( 'NONE',  ( 1.000000000000000000, 3.190570557967288949E-16, 6.948722487160392945E-17 ) ) ;
#198577=ORIENTED_EDGE ( 'NONE', *, *, #244692, .T. ) ;
#198582=ORIENTED_EDGE ( 'NONE', *, *, #128585, .F. ) ;
#198589=DIRECTION ( 'NONE',  ( 0.000000000000000000, -0.2128009952263601734, 0.9770955615653315052 ) ) ;
#198619=CIRCLE ( 'NONE', #219456, 0.1999999999999987899 ) ;
#198643=ORIENTED_EDGE ( 'NONE', *, *, #97982, .T. ) ;
#198651=EDGE_CURVE ( 'NONE', #126149, #243059, #154883, .T. ) ;
#198700=VERTEX_POINT ( 'NONE', #98686 ) ;
#198729=EDGE_LOOP ( 'NONE', ( #89407, #39538, #98127, #8808 ) ) ;
#198733=ORIENTED_EDGE ( 'NONE', *, *, #207197, .F. ) ;
#198784=DIRECTION ( 'NONE',  ( 1.000000000000000000, 0.000000000000000000, 0.000000000000000000 ) ) ;
#198797=CARTESIAN_POINT ( 'NONE',  ( 20.94999999999999929, 9.083217576421224848, -211.4565844547649931 ) ) ;
#198809=DIRECTION ( 'NONE',  ( 0.000000000000000000, 0.9770955615653313941, 0.2128009952263603677 ) ) ;
#198878=FACE_OUTER_BOUND ( 'NONE', #1078, .T. ) ;
#198882=DIRECTION ( 'NONE',  ( -1.000000000000000000, -2.885090398161910246E-16, -6.283419270304610340E-17 ) ) ;
#198886=ORIENTED_EDGE ( 'NONE', *, *, #108866, .T. ) ;
#198895=CARTESIAN_POINT ( 'NONE',  ( 21.14999999999999858, 11.50215294792677767, -198.5972978622482970 ) ) ;
#198907=DIRECTION ( 'NONE',  ( 1.000000000000000000, 2.885090398161910739E-16, 6.283419270304611573E-17 ) ) ;
#198909=ORIENTED_EDGE ( 'NONE', *, *, #89846, .T. ) ;
#198938=CARTESIAN_POINT ( 'NONE',  ( 21.07016717456945898, 6.176163237836302500, -199.6548974988868679 ) ) ;
#198946=EDGE_CURVE ( 'NONE', #22410, #193505, #152977, .T. ) ;
#198968=VECTOR ( 'NONE', #82556, 1000.000000000000227 ) ;
#198972=AXIS2_PLACEMENT_3D ( 'NONE', #245597, #3103, #66949 ) ;
#198998=ORIENTED_EDGE ( 'NONE', *, *, #129772, .T. ) ;
#199008=AXIS2_PLACEMENT_3D ( 'NONE', #250002, #71386, #231735 ) ;
#199059=ORIENTED_EDGE ( 'NONE', *, *, #5642, .T. ) ;
#199062=DIRECTION ( 'NONE',  ( 1.000000000000000000, 0.000000000000000000, 0.000000000000000000 ) ) ;
#199063=CARTESIAN_POINT ( 'NONE',  ( -21.05000000000000071, 14.90151243843701856, -203.3975529985363551 ) ) ;
#199074=EDGE_LOOP ( 'NONE', ( #60711, #229676, #81459, #93762 ) ) ;
#199076=AXIS2_PLACEMENT_3D ( 'NONE', #245041, #165519, #87230 ) ;
#199109=EDGE_CURVE ( 'NONE', #102935, #245138, #164348, .T. ) ;
#199120=ORIENTED_EDGE ( 'NONE', *, *, #219245, .F. ) ;
#199131=ADVANCED_FACE ( 'NONE', ( #245322 ), #50937, .T. ) ;
#199157=AXIS2_PLACEMENT_3D ( 'NONE', #149041, #68205, #69507 ) ;
#199160=CARTESIAN_POINT ( 'NONE',  ( 20.94999999999999929, 9.863005973831429074, -220.4411654715779321 ) ) ;
#199179=EDGE_CURVE ( 'NONE', #146352, #89391, #71832, .T. ) ;
#199192=CARTESIAN_POINT ( 'NONE',  ( 20.94999999999999929, 0.6656436123793473270, -212.6810495496487476 ) ) ;
#199257=EDGE_LOOP ( 'NONE', ( #27087, #250795, #254480, #4400 ) ) ;
#199296=CARTESIAN_POINT ( 'NONE',  ( -18.50000000000000000, 11.76393579169289083, -211.0774408799668720 ) ) ;
#199317=ORIENTED_EDGE ( 'NONE', *, *, #202750, .F. ) ;
#199324=ORIENTED_EDGE ( 'NONE', *, *, #13041, .T. ) ;
#199328=ADVANCED_FACE ( 'NONE', ( #131781 ), #189469, .T. ) ;
#199351=CARTESIAN_POINT ( 'NONE',  ( 20.94999999999999929, 10.29970289650803572, -222.9162226222096308 ) ) ;
#199401=ORIENTED_EDGE ( 'NONE', *, *, #108806, .T. ) ;
#199406=CARTESIAN_POINT ( 'NONE',  ( 21.14999999999999858, 2.585532092011767702, -212.8717110730202933 ) ) ;
#199426=VECTOR ( 'NONE', #142431, 1000.000000000000227 ) ;
#199434=CARTESIAN_POINT ( 'NONE',  ( 22.39999999999999503, -1.649207712992805996, -193.4275093978701818 ) ) ;
#199456=EDGE_CURVE ( 'NONE', #234078, #97897, #110528, .T. ) ;
#199468=CARTESIAN_POINT ( 'NONE',  ( 21.05000000000000071, 9.480858690661944976, -221.0361137499737936 ) ) ;
#199487=AXIS2_PLACEMENT_3D ( 'NONE', #112531, #192078, #113803 ) ;
#199490=VERTEX_POINT ( 'NONE', #58642 ) ;
#199522=DIRECTION ( 'NONE',  ( 1.000000000000000000, 0.000000000000000000, 0.000000000000000000 ) ) ;
#199536=EDGE_CURVE ( 'NONE', #252276, #196725, #8964, .T. ) ;
#199554=ADVANCED_FACE ( 'NONE', ( #225420 ), #52071, .T. ) ;
#199578=CARTESIAN_POINT ( 'NONE',  ( -21.14999999999999858, 11.48087284840413425, -198.4995883060917947 ) ) ;
#199633=EDGE_CURVE ( 'NONE', #111449, #102386, #235410, .T. ) ;
#199676=ORIENTED_EDGE ( 'NONE', *, *, #93729, .T. ) ;
#199742=EDGE_LOOP ( 'NONE', ( #108477, #72886, #153433, #33206 ) ) ;
#199770=CARTESIAN_POINT ( 'NONE',  ( -21.07928932188134041, -1.250084634896336366, -194.7953894783290423 ) ) ;
#199800=CYLINDRICAL_SURFACE ( 'NONE', #241880, 0.5000000000000007772 ) ;
#199804=DIRECTION ( 'NONE',  ( 0.000000000000000000, 0.2128009952263582305, -0.9770955615653319493 ) ) ;
#199837=SPHERICAL_SURFACE ( 'NONE', #19001, 0.1000000000000000056 ) ;
#199850=ORIENTED_EDGE ( 'NONE', *, *, #254307, .T. ) ;
#199868=ADVANCED_FACE ( 'NONE', ( #25654 ), #85577, .F. ) ;
#199959=EDGE_LOOP ( 'NONE', ( #244348, #178470, #211101 ) ) ;
#199967=AXIS2_PLACEMENT_3D ( 'NONE', #39068, #155180, #179858 ) ;
#199986=CIRCLE ( 'NONE', #112503, 0.3999999999999952482 ) ;
#199988=EDGE_LOOP ( 'NONE', ( #229070, #184213, #133159, #38147 ) ) ;
#199999=CARTESIAN_POINT ( 'NONE',  ( -21.05000000000000071, 0.5876173420563349792, -209.1618981382189588 ) ) ;
#200013=CARTESIAN_POINT ( 'NONE',  ( -21.05000000000000071, 1.148907358139439339E-11, -201.0000000000015064 ) ) ;
#200100=CIRCLE ( 'NONE', #87650, 0.1000000000000060424 ) ;
#200108=CARTESIAN_POINT ( 'NONE',  ( -23.15000000000000213, 7.128833340094563376, -233.7327013124401276 ) ) ;
#200133=AXIS2_PLACEMENT_3D ( 'NONE', #75788, #34127, #113621 ) ;
#200161=VERTEX_POINT ( 'NONE', #119317 ) ;
#200170=CARTESIAN_POINT ( 'NONE',  ( -22.48660254037842776, 11.37252324248628987, -198.4720136275361710 ) ) ;
#200195=CARTESIAN_POINT ( 'NONE',  ( -20.07928932188135107, 13.51025652711681069, -219.7033947181103031 ) ) ;
#200202=FACE_OUTER_BOUND ( 'NONE', #227494, .T. ) ;
#200205=FACE_OUTER_BOUND ( 'NONE', #60798, .T. ) ;
#200274=CARTESIAN_POINT ( 'NONE',  ( -20.64999999999999858, 6.294532028225942710, -220.7845521659012888 ) ) ;
#200289=VERTEX_POINT ( 'NONE', #78873 ) ;
#200292=ORIENTED_EDGE ( 'NONE', *, *, #1060, .T. ) ;
#200315=LINE ( 'NONE', #174385, #133109 ) ;
#200328=CARTESIAN_POINT ( 'NONE',  ( -20.94999999999999929, 6.256349259666489360, -229.7266095100222572 ) ) ;
#200330=CARTESIAN_POINT ( 'NONE',  ( -18.46902351632713746, -7.804936695476651032, -209.8500578355755692 ) ) ;
#200331=DIRECTION ( 'NONE',  ( 0.000000000000000000, -0.9770955615653318382, -0.2128009952263588411 ) ) ;
#200389=ADVANCED_FACE ( 'NONE', ( #64484 ), #143996, .T. ) ;
#200393=DIRECTION ( 'NONE',  ( -1.836970198721029934E-16, 0.9770955615653316162, 0.2128009952263604232 ) ) ;
#200394=CARTESIAN_POINT ( 'NONE',  ( 23.24999999999999645, 9.960715529987961503, -220.4198853720552904 ) ) ;
#200408=DIRECTION ( 'NONE',  ( -0.000000000000000000, 0.9770955615653313941, 0.2128009952263603954 ) ) ;
#200409=CARTESIAN_POINT ( 'NONE',  ( -18.59999999999999787, 4.324939842317335525, -212.0862480289983409 ) ) ;
#200457=DIRECTION ( 'NONE',  ( 0.000000000000000000, -0.3042567129659849434, -0.9525900758537926283 ) ) ;
#200487=CARTESIAN_POINT ( 'NONE',  ( -20.64999999999999858, 4.768403829798271154, -213.4961173936592331 ) ) ;
#200489=DIRECTION ( 'NONE',  ( 0.000000000000000000, 0.2128009952263601456, -0.9770955615653316162 ) ) ;
#200518=VERTEX_POINT ( 'NONE', #210426 ) ;
#200532=ORIENTED_EDGE ( 'NONE', *, *, #103489, .F. ) ;
#200559=ORIENTED_EDGE ( 'NONE', *, *, #202464, .F. ) ;
#200569=VERTEX_POINT ( 'NONE', #170047 ) ;
#200590=DIRECTION ( 'NONE',  ( 0.000000000000000000, 0.2128009952263603677, -0.9770955615653313941 ) ) ;
#200621=ORIENTED_EDGE ( 'NONE', *, *, #134485, .T. ) ;
#200637=EDGE_CURVE ( 'NONE', #211554, #200161, #81823, .T. ) ;
#200638=DIRECTION ( 'NONE',  ( -1.000000000000000000, -0.000000000000000000, -0.000000000000000000 ) ) ;
#200650=DIRECTION ( 'NONE',  ( 0.000000000000000000, 0.2128009952263603677, -0.9770955615653313941 ) ) ;
#200665=FACE_OUTER_BOUND ( 'NONE', #103663, .T. ) ;
#200681=DIRECTION ( 'NONE',  ( 0.000000000000000000, -0.2128009952263403282, 0.9770955615653358350 ) ) ;
#200684=ADVANCED_FACE ( 'NONE', ( #209777 ), #229086, .T. ) ;
#200686=ORIENTED_EDGE ( 'NONE', *, *, #234546, .T. ) ;
#200691=CARTESIAN_POINT ( 'NONE',  ( -20.85000000000000142, 7.882824859404637508, -245.3558965132535832 ) ) ;
#200696=DIRECTION ( 'NONE',  ( -0.000000000000000000, -0.9550021345545507412, 0.2965989261549202838 ) ) ;
#200699=ORIENTED_EDGE ( 'NONE', *, *, #251716, .F. ) ;
#200705=LINE ( 'NONE', #75641, #190895 ) ;
#200710=CARTESIAN_POINT ( 'NONE',  ( -23.25000000000000000, 7.804459559388685186, -245.4620200072988325 ) ) ;
#200749=DIRECTION ( 'NONE',  ( 0.000000000000000000, -0.2128009952263604232, 0.9770955615653316162 ) ) ;
#200760=FACE_OUTER_BOUND ( 'NONE', #164629, .T. ) ;
#200800=DIRECTION ( 'NONE',  ( 0.000000000000000000, 0.2128009952263403282, -0.9770955615653358350 ) ) ;
#200816=DIRECTION ( 'NONE',  ( 1.000000000000000000, 0.000000000000000000, 0.000000000000000000 ) ) ;
#200834=EDGE_LOOP ( 'NONE', ( #147172, #220865, #229061, #42161 ) ) ;
#200848=CARTESIAN_POINT ( 'NONE',  ( 20.01093837587850288, 16.74863325871518427, -222.6870001686604610 ) ) ;
#200891=( BOUNDED_SURFACE ( )  B_SPLINE_SURFACE ( 3, 2, ( 
 ( #102378, #24182, #133538 ),
 ( #110119, #170143, #93119 ),
 ( #150543, #211802, #188374 ),
 ( #172717, #210512, #12333 ),
 ( #13601, #53998, #11024 ),
 ( #29344, #189663, #112697 ),
 ( #230070, #151845, #91845 ),
 ( #69730, #149272, #171423 ) ),
 .UNSPECIFIED., .F., .F., .F. ) 
 B_SPLINE_SURFACE_WITH_KNOTS ( ( 4, 2, 2, 4 ),
 ( 3, 3 ),
 ( 0.0001723339234021455915, 0.0002782939632049884118, 0.0003842540030078312862, 0.0005961740826135169266 ),
 ( 0.000000000000000000, 1.000000000000000000 ),
 .UNSPECIFIED. ) 
 GEOMETRIC_REPRESENTATION_ITEM ( )  RATIONAL_B_SPLINE_SURFACE ( (
 ( 1.000000000000000000, 0.9504532311154330060, 1.000000000000000000),
 ( 1.000000000000000000, 0.9506023220711246058, 1.000000000000000000),
 ( 1.000000000000000000, 0.9395774818179986054, 1.000000000000000000),
 ( 1.000000000000000000, 0.9079328464648975805, 1.000000000000000000),
 ( 1.000000000000000000, 0.8875702416209027001, 1.000000000000000000),
 ( 1.000000000000000000, 0.8205919608032546941, 1.000000000000000000),
 ( 1.000000000000000000, 0.7666842783603454725, 1.000000000000000000),
 ( 1.000000000000000000, 0.7071067811865618946, 1.000000000000000000) ) ) 
 REPRESENTATION_ITEM ( '' )  SURFACE ( )  );
#200893=EDGE_CURVE ( 'NONE', #159889, #38095, #19701, .T. ) ;
#200895=LINE ( 'NONE', #97909, #117387 ) ;
#200910=VERTEX_POINT ( 'NONE', #244716 ) ;
#200913=ORIENTED_EDGE ( 'NONE', *, *, #11855, .F. ) ;
#200920=DIRECTION ( 'NONE',  ( -0.000000000000000000, 0.9770955615653313941, 0.2128009952263603954 ) ) ;
#200923=VECTOR ( 'NONE', #247199, 1000.000000000000227 ) ;
#200930=CARTESIAN_POINT ( 'NONE',  ( -20.64999999999999858, -3.363022478626109368, -226.2703567425896267 ) ) ;
#200965=ORIENTED_EDGE ( 'NONE', *, *, #72575, .T. ) ;
#200993=DIRECTION ( 'NONE',  ( 0.000000000000000000, 0.2128009952263596183, -0.9770955615653316162 ) ) ;
#201031=VERTEX_POINT ( 'NONE', #12567 ) ;
#201043=ADVANCED_FACE ( 'NONE', ( #133766 ), #123752, .T. ) ;
#201052=VERTEX_POINT ( 'NONE', #111641 ) ;
#201091=DIRECTION ( 'NONE',  ( 0.000000000000000000, 0.2128009952264214300, -0.9770955615653181825 ) ) ;
#201117=VERTEX_POINT ( 'NONE', #178056 ) ;
#201127=AXIS2_PLACEMENT_3D ( 'NONE', #207715, #29108, #108596 ) ;
#201132=DIRECTION ( 'NONE',  ( 0.000000000000000000, 0.2128009952263618110, -0.9770955615653311721 ) ) ;
#201140=ORIENTED_EDGE ( 'NONE', *, *, #121476, .T. ) ;
#201170=ORIENTED_EDGE ( 'NONE', *, *, #3562, .T. ) ;
#201183=DIRECTION ( 'NONE',  ( 0.000000000000000000, 0.2128009952263578142, -0.9770955615653320603 ) ) ;
#201195=ORIENTED_EDGE ( 'NONE', *, *, #165116, .F. ) ;
#201224=EDGE_LOOP ( 'NONE', ( #51758, #33950, #153424, #106923 ) ) ;
#201229=CARTESIAN_POINT ( 'NONE',  ( 21.08489834409762764, 13.00711782211248035, -210.8066890889169258 ) ) ;
#201258=CARTESIAN_POINT ( 'NONE',  ( 18.59999999999999787, 0.6713328740235187109, -212.7808875799876205 ) ) ;
#201261=ORIENTED_EDGE ( 'NONE', *, *, #254307, .F. ) ;
#201268=CARTESIAN_POINT ( 'NONE',  ( 18.59999999999999076, 15.51794587355511545, -222.9505302427971003 ) ) ;
#201285=DIRECTION ( 'NONE',  ( 0.000000000000000000, 0.2128009952263603677, -0.9770955615653313941 ) ) ;
#201289=CARTESIAN_POINT ( 'NONE',  ( -20.00857864376270001, 13.46244553689443535, -219.8161515769436107 ) ) ;
#201301=ORIENTED_EDGE ( 'NONE', *, *, #27971, .F. ) ;
#201314=LINE ( 'NONE', #240448, #128144 ) ;
#201320=ORIENTED_EDGE ( 'NONE', *, *, #122142, .F. ) ;
#201346=AXIS2_PLACEMENT_3D ( 'NONE', #26755, #250898, #245781 ) ;
#201352=AXIS2_PLACEMENT_3D ( 'NONE', #62044, #2037, #157309 ) ;
#201355=EDGE_LOOP ( 'NONE', ( #174351, #48855, #201195, #218538 ) ) ;
#201385=CARTESIAN_POINT ( 'NONE',  ( 20.75572585718252938, 10.48709729568783722, -207.4124676271370333 ) ) ;
#201393=CIRCLE ( 'NONE', #234726, 4.049999999999995381 ) ;
#201458=ORIENTED_EDGE ( 'NONE', *, *, #160872, .F. ) ;
#201461=ORIENTED_EDGE ( 'NONE', *, *, #199179, .F. ) ;
#201488=EDGE_CURVE ( 'NONE', #32779, #3546, #69774, .T. ) ;
#201492=DIRECTION ( 'NONE',  ( -1.000000000000000000, -3.190570557967288949E-16, -6.948722487160392945E-17 ) ) ;
#201511=DIRECTION ( 'NONE',  ( -0.000000000000000000, -0.07893460099012301889, 0.9968797965484754720 ) ) ;
#201580=ORIENTED_EDGE ( 'NONE', *, *, #183646, .F. ) ;
#201619=DIRECTION ( 'NONE',  ( 0.000000000000000000, -0.2128009952263485993, 0.9770955615653341697 ) ) ;
#201624=CYLINDRICAL_SURFACE ( 'NONE', #95662, 0.09999999999999939493 ) ;
#201658=CARTESIAN_POINT ( 'NONE',  ( -18.59999999999999787, 4.158309866074138661, -211.9342015984041439 ) ) ;
#201694=DIRECTION ( 'NONE',  ( 2.952720810173289605E-16, -0.9770955615653313941, -0.2128009952263610616 ) ) ;
#201699=CIRCLE ( 'NONE', #214184, 0.1000000000000055844 ) ;
#201708=DIRECTION ( 'NONE',  ( 0.000000000000000000, -0.2128009952263604232, 0.9770955615653316162 ) ) ;
#201795=CARTESIAN_POINT ( 'NONE',  ( -21.05000000000000071, 11.40444339177023814, -198.6185779617709670 ) ) ;
#201811=EDGE_CURVE ( 'NONE', #194623, #184568, #257318, .T. ) ;
#201813=EDGE_CURVE ( 'NONE', #232370, #190072, #208646, .T. ) ;
#201847=EDGE_CURVE ( 'NONE', #78551, #22582, #15813, .T. ) ;
#201902=ORIENTED_EDGE ( 'NONE', *, *, #146564, .T. ) ;
#201907=EDGE_CURVE ( 'NONE', #145277, #128109, #140670, .T. ) ;
#201935=EDGE_CURVE ( 'NONE', #7608, #121941, #132476, .T. ) ;
#201942=DIRECTION ( 'NONE',  ( 0.000000000000000000, -0.2128009952263604232, 0.9770955615653316162 ) ) ;
#201961=DIRECTION ( 'NONE',  ( 0.000000000000000000, -0.2128009952263604232, 0.9770955615653316162 ) ) ;
#201978=CARTESIAN_POINT ( 'NONE',  ( -21.04999999999896687, 6.296993352176364134, -199.6465916771296349 ) ) ;
#202004=ORIENTED_EDGE ( 'NONE', *, *, #40094, .T. ) ;
#202012=TOROIDAL_SURFACE ( 'NONE', #43779, 0.2000000000000000111, 0.1000000000000000056 ) ;
#202021=VERTEX_POINT ( 'NONE', #145755 ) ;
#202028=CARTESIAN_POINT ( 'NONE',  ( -23.25000000000000000, 1.148907358139439339E-11, -201.0000000000015064 ) ) ;
#202039=ORIENTED_EDGE ( 'NONE', *, *, #190179, .F. ) ;
#202130=CARTESIAN_POINT ( 'NONE',  ( 19.87657994472051115, 16.75105720888964100, -222.6981299613315741 ) ) ;
#202140=DIRECTION ( 'NONE',  ( -1.000000000000000000, -0.000000000000000000, -0.000000000000000000 ) ) ;
#202173=DIRECTION ( 'NONE',  ( -1.000000000000000000, -0.000000000000000000, -0.000000000000000000 ) ) ;
#202174=AXIS2_PLACEMENT_3D ( 'NONE', #114595, #214971, #54608 ) ;
#202196=EDGE_CURVE ( 'NONE', #230675, #112967, #256922, .T. ) ;
#202224=ORIENTED_EDGE ( 'NONE', *, *, #69077, .T. ) ;
#202233=CARTESIAN_POINT ( 'NONE',  ( 18.59999999999998721, 14.61354176542825201, -235.9279552357344016 ) ) ;
#202241=CIRCLE ( 'NONE', #48106, 0.1000000000000055844 ) ;
#202278=CARTESIAN_POINT ( 'NONE',  ( 20.95262331984781667, 11.87253000080046306, -206.1524153088024320 ) ) ;
#202327=EDGE_CURVE ( 'NONE', #83582, #26573, #166016, .T. ) ;
#202337=CARTESIAN_POINT ( 'NONE',  ( -23.15000000000000213, -13.98128454229089357, -192.0195388455185821 ) ) ;
#202358=CARTESIAN_POINT ( 'NONE',  ( -20.64999999999999858, -3.770473190032741062, -225.9805569534692324 ) ) ;
#202387=VERTEX_POINT ( 'NONE', #223691 ) ;
#202393=DIRECTION ( 'NONE',  ( 0.000000000000000000, -0.9770955615653320603, -0.2128009952263577587 ) ) ;
#202401=FACE_OUTER_BOUND ( 'NONE', #184988, .T. ) ;
#202433=AXIS2_PLACEMENT_3D ( 'NONE', #18457, #238796, #135817 ) ;
#202435=ADVANCED_FACE ( 'NONE', ( #180744 ), #249386, .T. ) ;
#202436=DIRECTION ( 'NONE',  ( 1.000000000000000000, -7.136802563874198121E-16, -1.554319503706929745E-16 ) ) ;
#202464=EDGE_CURVE ( 'NONE', #14295, #237997, #153199, .T. ) ;
#202509=DIRECTION ( 'NONE',  ( -1.000000000000000000, 0.000000000000000000, 0.000000000000000000 ) ) ;
#202524=CARTESIAN_POINT ( 'NONE',  ( 23.14999999999999503, 10.99842653345846699, -220.2504445088529792 ) ) ;
#202532=CARTESIAN_POINT ( 'NONE',  ( -21.05000000000000071, -4.892732937820630568, -233.2805462221312496 ) ) ;
#202533=DIRECTION ( 'NONE',  ( 0.000000000000000000, -0.2128009952263601456, 0.9770955615653316162 ) ) ;
#202578=AXIS2_PLACEMENT_3D ( 'NONE', #36076, #748, #217241 ) ;
#202588=CARTESIAN_POINT ( 'NONE',  ( -18.50000000000000000, 13.53887499352833146, -219.6971619212644669 ) ) ;
#202615=DIRECTION ( 'NONE',  ( -0.000000000000000000, 0.9770955615653316162, 0.2128009952263604232 ) ) ;
#202628=DIRECTION ( 'NONE',  ( 0.000000000000000000, -0.2128009952263604232, 0.9770955615653316162 ) ) ;
#202643=DIRECTION ( 'NONE',  ( 1.000000000000000000, 0.000000000000000000, 0.000000000000000000 ) ) ;
#202656=DIRECTION ( 'NONE',  ( 1.000000000000000000, 0.000000000000000000, 0.000000000000000000 ) ) ;
#202670=CARTESIAN_POINT ( 'NONE',  ( 21.05000000000000071, 13.06362847850371445, -210.5896934006125889 ) ) ;
#202735=ORIENTED_EDGE ( 'NONE', *, *, #148817, .F. ) ;
#202748=ORIENTED_EDGE ( 'NONE', *, *, #34340, .T. ) ;
#202750=EDGE_CURVE ( 'NONE', #185772, #224326, #255684, .T. ) ;
#202775=ORIENTED_EDGE ( 'NONE', *, *, #216611, .T. ) ;
#202816=VECTOR ( 'NONE', #98018, 1000.000000000000000 ) ;
#202845=CARTESIAN_POINT ( 'NONE',  ( 21.05000000000000071, 1.148907358139439339E-11, -201.0000000000015064 ) ) ;
#202883=EDGE_CURVE ( 'NONE', #54334, #163312, #72057, .T. ) ;
#202908=EDGE_CURVE ( 'NONE', #154129, #148702, #112209, .T. ) ;
#202909=CARTESIAN_POINT ( 'NONE',  ( 20.94999999999999574, 8.366615838327078336, -209.3410474610450365 ) ) ;
#202969=CARTESIAN_POINT ( 'NONE',  ( 20.96077737575322431, 17.02684875966464872, -224.5570219545472810 ) ) ;
#202970=EDGE_CURVE ( 'NONE', #109854, #107334, #197114, .T. ) ;
#202987=CARTESIAN_POINT ( 'NONE',  ( -21.05000000000000071, 1.148907358139439339E-11, -201.0000000000015064 ) ) ;
#202996=EDGE_CURVE ( 'NONE', #245998, #122770, #113734, .T. ) ;
#203031=VERTEX_POINT ( 'NONE', #34233 ) ;
#203032=ORIENTED_EDGE ( 'NONE', *, *, #118359, .T. ) ;
#203057=DIRECTION ( 'NONE',  ( -0.000000000000000000, 0.9770955615653313941, 0.2128009952263603954 ) ) ;
#203078=ORIENTED_EDGE ( 'NONE', *, *, #51186, .F. ) ;
#203098=CARTESIAN_POINT ( 'NONE',  ( -20.54999999999999716, -3.444512620907437039, -226.2123967847655592 ) ) ;
#203113=FACE_OUTER_BOUND ( 'NONE', #133412, .T. ) ;
#203118=ORIENTED_EDGE ( 'NONE', *, *, #78815, .T. ) ;
#203180=DIRECTION ( 'NONE',  ( -3.265361837132812600E-16, 0.9770955615653313941, 0.2128009952263603677 ) ) ;
#203202=ADVANCED_FACE ( 'NONE', ( #100558 ), #79721, .F. ) ;
#203210=VERTEX_POINT ( 'NONE', #164433 ) ;
#203211=AXIS2_PLACEMENT_3D ( 'NONE', #54678, #250318, #53403 ) ;
#203212=ORIENTED_EDGE ( 'NONE', *, *, #100074, .T. ) ;
#203216=DIRECTION ( 'NONE',  ( 0.000000000000000000, 0.2128009952263611726, -0.9770955615653312831 ) ) ;
#203276=DIRECTION ( 'NONE',  ( -1.000000000000000000, 8.034189347746081825E-16, -2.566115377699053685E-16 ) ) ;
#203311=FACE_OUTER_BOUND ( 'NONE', #42660, .T. ) ;
#203346=CARTESIAN_POINT ( 'NONE',  ( -18.52643265882458579, 18.39335631088233214, -236.9600537807593525 ) ) ;
#203354=DIRECTION ( 'NONE',  ( 1.000000000000000000, 0.000000000000000000, 0.000000000000000000 ) ) ;
#203379=AXIS2_PLACEMENT_3D ( 'NONE', #238911, #124108, #163231 ) ;
#203385=VECTOR ( 'NONE', #175400, 1000.000000000000227 ) ;
#203423=FACE_OUTER_BOUND ( 'NONE', #252825, .T. ) ;
#203474=CARTESIAN_POINT ( 'NONE',  ( 18.49999999999999645, 0.8650195716890431985, -212.6652626294507229 ) ) ;
#203490=CARTESIAN_POINT ( 'NONE',  ( -23.25000000000000000, 7.783179459866048866, -245.3643104511423019 ) ) ;
#203510=FACE_OUTER_BOUND ( 'NONE', #199257, .T. ) ;
#203517=DIRECTION ( 'NONE',  ( 0.000000000000000000, 0.2128009952263403282, -0.9770955615653358350 ) ) ;
#203538=VERTEX_POINT ( 'NONE', #102495 ) ;
#203651=AXIS2_PLACEMENT_3D ( 'NONE', #245201, #66562, #146078 ) ;
#203661=CARTESIAN_POINT ( 'NONE',  ( 21.06600267594171783, 11.17125508431878878, -211.0573669240345112 ) ) ;
#203667=ORIENTED_EDGE ( 'NONE', *, *, #100150, .F. ) ;
#203679=CARTESIAN_POINT ( 'NONE',  ( -21.05000000000000071, 2.817198581588411077, -208.4716308468294130 ) ) ;
#203699=CARTESIAN_POINT ( 'NONE',  ( 23.14999999999999858, 7.128833340094563376, -233.7327013124401276 ) ) ;
#203767=FACE_OUTER_BOUND ( 'NONE', #23616, .T. ) ;
#203779=VERTEX_POINT ( 'NONE', #85185 ) ;
#203855=CARTESIAN_POINT ( 'NONE',  ( 19.99999999999998934, 16.76897757977919312, -222.7804130109902871 ) ) ;
#203873=ORIENTED_EDGE ( 'NONE', *, *, #79163, .F. ) ;
#203938=ORIENTED_EDGE ( 'NONE', *, *, #104406, .T. ) ;
#203955=CARTESIAN_POINT ( 'NONE',  ( 20.95512820512820440, 12.96604748760833203, -210.6109454999921411 ) ) ;
#204002=ORIENTED_EDGE ( 'NONE', *, *, #199536, .F. ) ;
#204013=DIRECTION ( 'NONE',  ( 0.000000000000000000, 0.9394191166662618775, 0.3427706569150580362 ) ) ;
#204049=CARTESIAN_POINT ( 'NONE',  ( 18.59999999999999076, 16.67126802362266247, -222.8016931105129004 ) ) ;
#204080=ORIENTED_EDGE ( 'NONE', *, *, #34592, .F. ) ;
#204110=CARTESIAN_POINT ( 'NONE',  ( 18.49999999999999645, 4.324939842317335525, -212.0862480289983409 ) ) ;
#204134=CARTESIAN_POINT ( 'NONE',  ( 18.49999999999999289, 18.51199663233067838, -231.2535697180530292 ) ) ;
#204137=CARTESIAN_POINT ( 'NONE',  ( 23.14999999999999858, -13.98128454229088291, -192.0195388455185821 ) ) ;
#204167=VERTEX_POINT ( 'NONE', #173811 ) ;
#204181=CYLINDRICAL_SURFACE ( 'NONE', #213538, 0.1000000000000057648 ) ;
#204226=CARTESIAN_POINT ( 'NONE',  ( -18.59999999999999787, 14.80545736607782814, -235.9842437978701639 ) ) ;
#204236=DIRECTION ( 'NONE',  ( -0.000000000000000000, 0.2128009952263604232, -0.9770955615653316162 ) ) ;
#204237=CARTESIAN_POINT ( 'NONE',  ( -20.94999999999999929, 7.872214528623318053, -209.6555322433423498 ) ) ;
#204248=CARTESIAN_POINT ( 'NONE',  ( 20.87155475150661132, 17.14044013043753267, -224.4860178609578156 ) ) ;
#204260=FACE_OUTER_BOUND ( 'NONE', #48145, .T. ) ;
#204270=CARTESIAN_POINT ( 'NONE',  ( 18.49999999999998934, 15.28205413790855971, -223.0019049476732675 ) ) ;
#204277=ORIENTED_EDGE ( 'NONE', *, *, #118530, .T. ) ;
#204303=DIRECTION ( 'NONE',  ( 9.044546369203337730E-15, -0.5795995782408065455, -0.8149014228132623883 ) ) ;
#204313=DIRECTION ( 'NONE',  ( 1.000000000000000000, 0.000000000000000000, 0.000000000000000000 ) ) ;
#204346=VECTOR ( 'NONE', #89490, 1000.000000000000227 ) ;
#204368=EDGE_CURVE ( 'NONE', #75640, #22692, #183094, .T. ) ;
#204373=AXIS2_PLACEMENT_3D ( 'NONE', #205715, #104033, #164041 ) ;
#204381=LINE ( 'NONE', #188678, #206272 ) ;
#204395=EDGE_CURVE ( 'NONE', #109854, #98224, #120563, .T. ) ;
#204399=CARTESIAN_POINT ( 'NONE',  ( 20.04142135623730070, 16.62870782457739338, -222.6062739981998391 ) ) ;
#204414=CIRCLE ( 'NONE', #91999, 0.09999999999999899247 ) ;
#204448=CARTESIAN_POINT ( 'NONE',  ( 18.59999999999999076, 16.76897757977919312, -222.7804130109902871 ) ) ;
#204449=ORIENTED_EDGE ( 'NONE', *, *, #200637, .F. ) ;
#204466=VERTEX_POINT ( 'NONE', #153938 ) ;
#204473=CARTESIAN_POINT ( 'NONE',  ( 20.04142135623730070, 16.72641738073392403, -222.5849938986771974 ) ) ;
#204475=CIRCLE ( 'NONE', #129483, 0.09999999999999939493 ) ;
#204482=VERTEX_POINT ( 'NONE', #37817 ) ;
#204489=CARTESIAN_POINT ( 'NONE',  ( 23.14999999999998437, 1.148907358139439339E-11, -201.0000000000015064 ) ) ;
#204508=ADVANCED_FACE ( 'NONE', ( #156491 ), #215143, .T. ) ;
#204516=LINE ( 'NONE', #25904, #194546 ) ;
#204521=DIRECTION ( 'NONE',  ( -0.000000000000000000, -0.2128009952263603677, 0.9770955615653313941 ) ) ;
#204527=CYLINDRICAL_SURFACE ( 'NONE', #87651, 0.09999999999999810429 ) ;
#204528=EDGE_CURVE ( 'NONE', #227433, #102301, #91505, .T. ) ;
#204532=EDGE_CURVE ( 'NONE', #9164, #159242, #149796, .T. ) ;
#204579=CARTESIAN_POINT ( 'NONE',  ( -23.15000000000000213, 16.02417409648692725, -219.3605785455116006 ) ) ;
#204581=DIRECTION ( 'NONE',  ( 0.000000000000000000, 0.2128009952263603677, -0.9770955615653313941 ) ) ;
#204605=AXIS2_PLACEMENT_3D ( 'NONE', #98021, #257078, #237573 ) ;
#204613=DIRECTION ( 'NONE',  ( 0.000000000000000000, 0.2128009952263601456, -0.9770955615653316162 ) ) ;
#204616=CARTESIAN_POINT ( 'NONE',  ( -18.59999999999999787, 7.783179459866048866, -245.3643104511423019 ) ) ;
#204623=DIRECTION ( 'NONE',  ( -1.000000000000000000, 0.000000000000000000, 0.000000000000000000 ) ) ;
#204626=CARTESIAN_POINT ( 'NONE',  ( 21.14999999999999858, 11.19216743630477673, -211.0996217964688810 ) ) ;
#204627=ORIENTED_EDGE ( 'NONE', *, *, #123972, .T. ) ;
#204681=CIRCLE ( 'NONE', #113119, 12.77500000000000391 ) ;
#204745=ORIENTED_EDGE ( 'NONE', *, *, #234125, .T. ) ;
#204757=DIRECTION ( 'NONE',  ( -0.000000000000000000, -0.2814428106787469352, -0.9595780032479105381 ) ) ;
#204764=DIRECTION ( 'NONE',  ( 1.000000000000000000, 0.000000000000000000, 0.000000000000000000 ) ) ;
#204779=DIRECTION ( 'NONE',  ( 0.000000000000000000, -0.9595780032479205301, 0.2814428106787130734 ) ) ;
#204795=CARTESIAN_POINT ( 'NONE',  ( 23.15000000000000213, -4.914013037343258894, -233.1828366659746905 ) ) ;
#204825=CIRCLE ( 'NONE', #246353, 0.09999999999999609201 ) ;
#204831=DIRECTION ( 'NONE',  ( 0.000000000000000000, 0.2128009952263601734, -0.9770955615653316162 ) ) ;
#204833=CARTESIAN_POINT ( 'NONE',  ( -21.05000000000000071, 14.90151243843701856, -203.3975529985363551 ) ) ;
#204874=EDGE_LOOP ( 'NONE', ( #227895, #102569, #160990, #138327 ) ) ;
#204880=CARTESIAN_POINT ( 'NONE',  ( 21.05193202509564543, 13.06863776538323307, -210.6116652761761827 ) ) ;
#204885=DIRECTION ( 'NONE',  ( 1.000000000000000000, 0.000000000000000000, 0.000000000000000000 ) ) ;
#204902=DIRECTION ( 'NONE',  ( -1.000000000000000000, -0.000000000000000000, -0.000000000000000000 ) ) ;
#204918=CARTESIAN_POINT ( 'NONE',  ( 21.05000000000000071, 0.7653315920341953182, -212.6731560895497353 ) ) ;
#204950=ORIENTED_EDGE ( 'NONE', *, *, #7523, .T. ) ;
#204956=CARTESIAN_POINT ( 'NONE',  ( 19.97071067811867451, 16.71026450801412366, -222.6484636283461498 ) ) ;
#204983=CARTESIAN_POINT ( 'NONE',  ( -20.64999999999999858, -3.770473190032741062, -225.9805569534692324 ) ) ;
#204984=ORIENTED_EDGE ( 'NONE', *, *, #138589, .T. ) ;
#204997=CARTESIAN_POINT ( 'NONE',  ( 21.09813707148777340, 6.232144213543900690, -199.6106190182799480 ) ) ;
#205001=FACE_OUTER_BOUND ( 'NONE', #254782, .T. ) ;
#205014=EDGE_LOOP ( 'NONE', ( #172922, #147302, #83762, #66753 ) ) ;
#205038=CIRCLE ( 'NONE', #9248, 0.1000000000000017542 ) ;
#205093=CARTESIAN_POINT ( 'NONE',  ( -20.64999999999999858, 8.751106741858205140, -220.7398867978736234 ) ) ;
#205111=CARTESIAN_POINT ( 'NONE',  ( -20.85000000000000142, 7.783179459866048866, -245.3643104511423019 ) ) ;
#205119=CARTESIAN_POINT ( 'NONE',  ( -21.05000000000000071, 0.6656436123793491033, -212.6810495496487476 ) ) ;
#205129=ADVANCED_FACE ( 'NONE', ( #43900 ), #233367, .F. ) ;
#205150=EDGE_CURVE ( 'NONE', #103023, #182231, #146023, .T. ) ;
#205180=AXIS2_PLACEMENT_3D ( 'NONE', #14192, #108134, #187690 ) ;
#205207=CARTESIAN_POINT ( 'NONE',  ( 20.94999999999999929, -3.685352791942192674, -226.3713951780953550 ) ) ;
#205225=CARTESIAN_POINT ( 'NONE',  ( 21.14999999999999858, 13.07482039728800061, -210.6896000549707537 ) ) ;
#205238=ORIENTED_EDGE ( 'NONE', *, *, #244692, .F. ) ;
#205280=DIRECTION ( 'NONE',  ( 4.239556034732056743E-17, 0.08413937888704772772, -0.9964539953858894128 ) ) ;
#205281=ADVANCED_FACE ( 'NONE', ( #230217 ), #225114, .F. ) ;
#205325=AXIS2_PLACEMENT_3D ( 'NONE', #186732, #26362, #657 ) ;
#205379=CARTESIAN_POINT ( 'NONE',  ( -20.94999999999999929, -0.2576658302507160991, -201.0204024091695487 ) ) ;
#205385=ADVANCED_FACE ( 'NONE', ( #81375 ), #99662, .T. ) ;
#205392=DIRECTION ( 'NONE',  ( 0.000000000000000000, 0.2128009952263604232, -0.9770955615653316162 ) ) ;
#205437=EDGE_LOOP ( 'NONE', ( #95070, #41160, #49096, #255413, #107628, #165011 ) ) ;
#205462=CARTESIAN_POINT ( 'NONE',  ( 20.94999999999999574, 2.838478681111047841, -208.5693404029859437 ) ) ;
#205468=CARTESIAN_POINT ( 'NONE',  ( -20.94999999999999929, 4.639061695946149477, -222.3006832421257286 ) ) ;
#205516=CARTESIAN_POINT ( 'NONE',  ( 21.00000000000000000, 12.15477401631902232, -210.9923204818763622 ) ) ;
#205528=DIRECTION ( 'NONE',  ( 1.000000000000000000, 0.000000000000000000, 0.000000000000000000 ) ) ;
#205562=CARTESIAN_POINT ( 'NONE',  ( 21.09546886439506608, 11.27926058993681302, -211.0674451492174057 ) ) ;
#205565=AXIS2_PLACEMENT_3D ( 'NONE', #251105, #72507, #231575 ) ;
#205577=EDGE_CURVE ( 'NONE', #141902, #39339, #85229, .T. ) ;
#205623=CARTESIAN_POINT ( 'NONE',  ( 18.59999999999999432, 0.5876173420563349792, -209.1618981382189588 ) ) ;
#205660=ORIENTED_EDGE ( 'NONE', *, *, #175032, .T. ) ;
#205663=DIRECTION ( 'NONE',  ( 0.000000000000000000, 0.3565161741896938907, -0.9342891509276685102 ) ) ;
#205664=CIRCLE ( 'NONE', #51709, 0.1000000000000054040 ) ;
#205715=CARTESIAN_POINT ( 'NONE',  ( 20.85000000000000142, 7.225717546301074989, -233.4207493275448257 ) ) ;
#205746=ADVANCED_FACE ( 'NONE', ( #212924 ), #19874, .F. ) ;
#205747=EDGE_LOOP ( 'NONE', ( #239373, #118372, #244085, #198909 ) ) ;
#205749=DIRECTION ( 'NONE',  ( 0.000000000000000000, -0.2128009952263625604, 0.9770955615653310611 ) ) ;
#205753=VERTEX_POINT ( 'NONE', #75980 ) ;
#205768=CIRCLE ( 'NONE', #14259, 4.000000000000006217 ) ;
#205772=ADVANCED_FACE ( 'NONE', ( #134641 ), #199800, .F. ) ;
#205794=DIRECTION ( 'NONE',  ( -1.000000000000000000, -0.000000000000000000, -0.000000000000000000 ) ) ;
#205868=CARTESIAN_POINT ( 'NONE',  ( 21.05000000000000071, 7.128833340094563376, -233.7327013124401276 ) ) ;
#205870=CARTESIAN_POINT ( 'NONE',  ( 19.58285714285715073, 10.60044124276980959, -207.3093812031132472 ) ) ;
#205883=VECTOR ( 'NONE', #55633, 1000.000000000000000 ) ;
#205888=EDGE_LOOP ( 'NONE', ( #38485, #108702, #171783, #165008, #229762 ) ) ;
#205893=VERTEX_POINT ( 'NONE', #241476 ) ;
#205907=CIRCLE ( 'NONE', #185063, 0.1000000000000055844 ) ;
#205913=CARTESIAN_POINT ( 'NONE',  ( -18.50000000000000355, 7.576017155224048061, -241.7224044826512284 ) ) ;
#205941=CYLINDRICAL_SURFACE ( 'NONE', #110374, 0.1000000000000001305 ) ;
#206021=ORIENTED_EDGE ( 'NONE', *, *, #111069, .T. ) ;
#206033=VECTOR ( 'NONE', #142352, 1000.000000000000000 ) ;
#206064=DIRECTION ( 'NONE',  ( 0.000000000000000000, -0.6728388485993130885, 0.7397890806274115549 ) ) ;
#206107=AXIS2_PLACEMENT_3D ( 'NONE', #69351, #90159, #109727 ) ;
#206121=CARTESIAN_POINT ( 'NONE',  ( 18.49999999999999289, 15.24523260243583600, -223.0274837629937963 ) ) ;
#206142=EDGE_CURVE ( 'NONE', #107106, #19404, #242546, .T. ) ;
#206160=CARTESIAN_POINT ( 'NONE',  ( 21.07946286933444924, -1.271897997408519165, -194.7996073284550675 ) ) ;
#206170=DIRECTION ( 'NONE',  ( 0.000000000000000000, 0.2128009952263603954, -0.9770955615653315052 ) ) ;
#206183=CARTESIAN_POINT ( 'NONE',  ( 21.08750232978087524, 13.08152960257287489, -210.6665014416416284 ) ) ;
#206186=PRESENTATION_STYLE_ASSIGNMENT (( #43265 ) ) ;
#206200=ORIENTED_EDGE ( 'NONE', *, *, #143991, .F. ) ;
#206217=CARTESIAN_POINT ( 'NONE',  ( -18.50000000000000000, 7.783179459866045313, -245.3643104511423303 ) ) ;
#206238=CIRCLE ( 'NONE', #222971, 0.09999999999999810429 ) ;
#206246=ORIENTED_EDGE ( 'NONE', *, *, #108673, .F. ) ;
#206258=FACE_OUTER_BOUND ( 'NONE', #235041, .T. ) ;
#206272=VECTOR ( 'NONE', #6180, 1000.000000000000114 ) ;
#206288=DIRECTION ( 'NONE',  ( -3.265361837132813093E-16, 0.9770955615653316162, 0.2128009952263604232 ) ) ;
#206342=AXIS2_PLACEMENT_3D ( 'NONE', #229547, #35223, #252935 ) ;
#206349=ORIENTED_EDGE ( 'NONE', *, *, #17941, .T. ) ;
#206372=ORIENTED_EDGE ( 'NONE', *, *, #1928, .T. ) ;
#206398=CARTESIAN_POINT ( 'NONE',  ( 20.95512820512820440, 11.25838014693916378, -210.9828572391344039 ) ) ;
#206404=VERTEX_POINT ( 'NONE', #95862 ) ;
#206424=SPHERICAL_SURFACE ( 'NONE', #199157, 0.1000000000000000056 ) ;
#206454=CARTESIAN_POINT ( 'NONE',  ( 18.59999999999999787, 0.6869237119019839799, -212.7787591058053067 ) ) ;
#206467=CIRCLE ( 'NONE', #94028, 0.1000000000000066946 ) ;
#206501=CARTESIAN_POINT ( 'NONE',  ( -23.15000000000000213, 8.674677285224309031, -220.8588764535527957 ) ) ;
#206504=FACE_OUTER_BOUND ( 'NONE', #210601, .T. ) ;
#206561=ORIENTED_EDGE ( 'NONE', *, *, #33260, .T. ) ;
#206577=ORIENTED_EDGE ( 'NONE', *, *, #2659, .F. ) ;
#206616=CARTESIAN_POINT ( 'NONE',  ( 23.14999999999999503, 8.930358663153430854, -211.6945637661233377 ) ) ;
#206655=DIRECTION ( 'NONE',  ( 1.000000000000000000, -6.239415780002328221E-16, -5.674754385112862884E-16 ) ) ;
#206671=ADVANCED_FACE ( 'NONE', ( #192139 ), #211701, .T. ) ;
#206703=AXIS2_PLACEMENT_3D ( 'NONE', #218335, #80090, #202643 ) ;
#206709=CARTESIAN_POINT ( 'NONE',  ( -21.08479644141221598, 6.187248666789188611, -199.5925561729470701 ) ) ;
#206716=DIRECTION ( 'NONE',  ( -1.000000000000000000, 0.000000000000000000, 0.000000000000000000 ) ) ;
#206721=CYLINDRICAL_SURFACE ( 'NONE', #18933, 2.000000000000003109 ) ;
#206726=CARTESIAN_POINT ( 'NONE',  ( -21.45000000000000284, 12.03275902784684703, -220.0251779199349187 ) ) ;
#206730=CARTESIAN_POINT ( 'NONE',  ( -18.59999999999999787, 0.6656436123793491033, -212.6810495496487476 ) ) ;
#206732=VECTOR ( 'NONE', #183339, 1000.000000000000227 ) ;
#206745=DIRECTION ( 'NONE',  ( 0.000000000000000000, 0.2128009952263603954, -0.9770955615653315052 ) ) ;
#206747=ADVANCED_FACE ( 'NONE', ( #90432 ), #134055, .T. ) ;
#206793=CIRCLE ( 'NONE', #165688, 11.74999999999999467 ) ;
#206807=ORIENTED_EDGE ( 'NONE', *, *, #249604, .F. ) ;
#206823=ORIENTED_EDGE ( 'NONE', *, *, #189432, .T. ) ;
#206830=CIRCLE ( 'NONE', #77614, 11.65000000000000036 ) ;
#206845=LINE ( 'NONE', #103864, #99469 ) ;
#206865=VERTEX_POINT ( 'NONE', #325 ) ;
#206911=DIRECTION ( 'NONE',  ( 0.000000000000000000, 0.9770955615653316162, 0.2128009952263604232 ) ) ;
#206914=EDGE_CURVE ( 'NONE', #171420, #21650, #79871, .T. ) ;
#206932=CARTESIAN_POINT ( 'NONE',  ( -20.54999999999999716, 4.389020526555173163, -221.1525959572864792 ) ) ;
#206983=ORIENTED_EDGE ( 'NONE', *, *, #47606, .T. ) ;
#206988=ORIENTED_EDGE ( 'NONE', *, *, #125434, .F. ) ;
#206994=CARTESIAN_POINT ( 'NONE',  ( 20.94999999999999574, -10.56629024491939894, -206.4738935375009703 ) ) ;
#207003=AXIS2_PLACEMENT_3D ( 'NONE', #67447, #251208, #226502 ) ;
#207006=VECTOR ( 'NONE', #118838, 1000.000000000000000 ) ;
#207021=CIRCLE ( 'NONE', #127926, 0.1000000000000054040 ) ;
#207036=DIRECTION ( 'NONE',  ( 0.000000000000000000, 0.9394191166662618775, 0.3427706569150580362 ) ) ;
#207044=EDGE_CURVE ( 'NONE', #118980, #187404, #230105, .T. ) ;
#207050=CARTESIAN_POINT ( 'NONE',  ( 18.59999999999999076, 14.86477715130881272, -235.7932433709592601 ) ) ;
#207110=LINE ( 'NONE', #165415, #171202 ) ;
#207141=ADVANCED_FACE ( 'NONE', ( #189252 ), #38575, .T. ) ;
#207152=ORIENTED_EDGE ( 'NONE', *, *, #70388, .T. ) ;
#207159=AXIS2_PLACEMENT_3D ( 'NONE', #205093, #185554, #222076 ) ;
#207173=DIRECTION ( 'NONE',  ( 0.000000000000000000, -0.2128009952263603677, 0.9770955615653313941 ) ) ;
#207197=EDGE_CURVE ( 'NONE', #195237, #106096, #163474, .T. ) ;
#207222=FACE_OUTER_BOUND ( 'NONE', #208958, .T. ) ;
#207233=DIRECTION ( 'NONE',  ( 0.000000000000000000, -0.9770955615653316162, -0.2128009952263604232 ) ) ;
#207244=VERTEX_POINT ( 'NONE', #96533 ) ;
#207276=EDGE_LOOP ( 'NONE', ( #72369, #31896, #10033, #59746 ) ) ;
#207316=ADVANCED_FACE ( 'NONE', ( #6438 ), #44303, .T. ) ;
#207327=DIRECTION ( 'NONE',  ( 1.000000000000000000, 0.000000000000000000, 0.000000000000000000 ) ) ;
#207331=ORIENTED_EDGE ( 'NONE', *, *, #205577, .F. ) ;
#207371=ORIENTED_EDGE ( 'NONE', *, *, #87040, .F. ) ;
#207382=DIRECTION ( 'NONE',  ( 0.000000000000000000, 0.2128009952263485993, -0.9770955615653341697 ) ) ;
#207387=EDGE_CURVE ( 'NONE', #24784, #148073, #80040, .T. ) ;
#207426=CARTESIAN_POINT ( 'NONE',  ( -20.94999999999999929, 2.838478681111047841, -208.5693404029859437 ) ) ;
#207437=CYLINDRICAL_SURFACE ( 'NONE', #198195, 0.09999999999999939493 ) ;
#207450=FACE_OUTER_BOUND ( 'NONE', #77622, .T. ) ;
#207454=CARTESIAN_POINT ( 'NONE',  ( -23.15000000000000213, 1.148907358139439339E-11, -201.0000000000015064 ) ) ;
#207486=FILL_AREA_STYLE ('',( #64110 ) ) ;
#207487=VECTOR ( 'NONE', #165811, 1000.000000000000227 ) ;
#207490=DIRECTION ( 'NONE',  ( 0.000000000000000000, -0.2128009952263604232, 0.9770955615653316162 ) ) ;
#207564=CARTESIAN_POINT ( 'NONE',  ( -21.00023020733438273, 6.244489974106951280, -199.6400166642470140 ) ) ;
#207577=AXIS2_PLACEMENT_3D ( 'NONE', #238126, #179471, #80313 ) ;
#207593=EDGE_CURVE ( 'NONE', #98647, #49064, #213533, .T. ) ;
#207619=DIRECTION ( 'NONE',  ( 0.000000000000000000, 0.2128009952263485993, -0.9770955615653341697 ) ) ;
#207632=DIRECTION ( 'NONE',  ( -0.000000000000000000, 0.9770955615653316162, 0.2128009952263603122 ) ) ;
#207633=EDGE_CURVE ( 'NONE', #32735, #218469, #62258, .T. ) ;
#207697=ORIENTED_EDGE ( 'NONE', *, *, #256490, .T. ) ;
#207711=AXIS2_PLACEMENT_3D ( 'NONE', #145574, #225095, #46467 ) ;
#207715=CARTESIAN_POINT ( 'NONE',  ( -18.59999999999999787, 7.128833340094563376, -233.7327013124401276 ) ) ;
#207724=CARTESIAN_POINT ( 'NONE',  ( -23.15000000000000213, 8.980461154494397746, -187.0187154576991304 ) ) ;
#207733=DIRECTION ( 'NONE',  ( 0.000000000000000000, -0.2128009952263604232, 0.9770955615653316162 ) ) ;
#207742=ORIENTED_EDGE ( 'NONE', *, *, #180829, .T. ) ;
#207752=AXIS2_PLACEMENT_3D ( 'NONE', #196606, #114512, #152385 ) ;
#207753=ORIENTED_EDGE ( 'NONE', *, *, #76395, .F. ) ;
#207755=ORIENTED_EDGE ( 'NONE', *, *, #98706, .T. ) ;
#207767=DIRECTION ( 'NONE',  ( 1.000000000000000000, 0.000000000000000000, 0.000000000000000000 ) ) ;
#207784=EDGE_LOOP ( 'NONE', ( #224058, #67697, #101536, #214628 ) ) ;
#207823=DIRECTION ( 'NONE',  ( 1.000000000000000000, 0.000000000000000000, 0.000000000000000000 ) ) ;
#207831=ORIENTED_EDGE ( 'NONE', *, *, #11855, .T. ) ;
#207875=ORIENTED_EDGE ( 'NONE', *, *, #164339, .T. ) ;
#207904=ORIENTED_EDGE ( 'NONE', *, *, #81735, .T. ) ;
#207910=DIRECTION ( 'NONE',  ( -1.000000000000000000, -0.000000000000000000, -0.000000000000000000 ) ) ;
#207940=CIRCLE ( 'NONE', #70585, 0.09999999999998882005 ) ;
#207977=AXIS2_PLACEMENT_3D ( 'NONE', #218076, #174198, #193720 ) ;
#207983=EDGE_CURVE ( 'NONE', #200289, #168569, #15129, .T. ) ;
#207985=CARTESIAN_POINT ( 'NONE',  ( 22.60000000000000142, 1.148907358139439339E-11, -201.0000000000015064 ) ) ;
#208013=EDGE_LOOP ( 'NONE', ( #127744, #106599, #56832, #52960 ) ) ;
#208020=CARTESIAN_POINT ( 'NONE',  ( -20.00857864376270001, 13.56015509305096778, -219.7948714774209691 ) ) ;
#208037=AXIS2_PLACEMENT_3D ( 'NONE', #226058, #186993, #241801 ) ;
#208071=CARTESIAN_POINT ( 'NONE',  ( 20.94999999999999574, -10.51247937907010410, -206.3598299697285654 ) ) ;
#208080=ADVANCED_FACE ( 'NONE', ( #120666 ), #227110, .F. ) ;
#208128=AXIS2_PLACEMENT_3D ( 'NONE', #136589, #36251, #96180 ) ;
#208135=CARTESIAN_POINT ( 'NONE',  ( 20.94999999999999929, -3.770473190032740174, -225.9805569534692324 ) ) ;
#208154=AXIS2_PLACEMENT_3D ( 'NONE', #254669, #73546, #232615 ) ;
#208171=DIRECTION ( 'NONE',  ( 1.000000000000000000, 0.000000000000000000, 0.000000000000000000 ) ) ;
#208178=AXIS2_PLACEMENT_3D ( 'NONE', #213123, #38352, #175317 ) ;
#208253=ORIENTED_EDGE ( 'NONE', *, *, #25852, .T. ) ;
#208265=AXIS2_PLACEMENT_3D ( 'NONE', #100255, #105379, #1162 ) ;
#208269=ADVANCED_FACE ( 'NONE', ( #250533 ), #114882, .F. ) ;
#208295=DIRECTION ( 'NONE',  ( 1.000000000000000000, 0.000000000000000000, 0.000000000000000000 ) ) ;
#208305=VECTOR ( 'NONE', #208985, 1000.000000000000227 ) ;
#208309=CARTESIAN_POINT ( 'NONE',  ( -21.05000000000000071, -0.2576658302507160991, -201.0204024091695487 ) ) ;
#208380=DIRECTION ( 'NONE',  ( -1.000000000000000000, 0.000000000000000000, 0.000000000000000000 ) ) ;
#208398=VERTEX_POINT ( 'NONE', #132729 ) ;
#208402=VERTEX_POINT ( 'NONE', #190132 ) ;
#208403=DIRECTION ( 'NONE',  ( 2.557131231893036492E-16, -0.9525900758537790836, 0.3042567129660269099 ) ) ;
#208406=CARTESIAN_POINT ( 'NONE',  ( 21.59780538579342135, -1.360356060411589185, -194.2886754741613231 ) ) ;
#208457=ORIENTED_EDGE ( 'NONE', *, *, #182059, .F. ) ;
#208461=ADVANCED_FACE ( 'NONE', ( #99968 ), #97398, .F. ) ;
#208500=CARTESIAN_POINT ( 'NONE',  ( -18.59999999999999787, 18.41524492703432614, -237.0006385043383546 ) ) ;
#208587=EDGE_CURVE ( 'NONE', #1731, #117008, #247205, .T. ) ;
#208589=AXIS2_PLACEMENT_3D ( 'NONE', #211262, #32668, #232123 ) ;
#208594=EDGE_LOOP ( 'NONE', ( #222851, #48671, #153133 ) ) ;
#208601=EDGE_LOOP ( 'NONE', ( #129518, #246064, #192224, #198582, #4758, #89719, #202004, #129801, #21269, #206021, #155052, #113323, #154672, #95020, #87473, #111104 ) ) ;
#208646=LINE ( 'NONE', #50808, #99144 ) ;
#208657=ORIENTED_EDGE ( 'NONE', *, *, #20944, .F. ) ;
#208666=ORIENTED_EDGE ( 'NONE', *, *, #12510, .F. ) ;
#208680=VECTOR ( 'NONE', #12478, 1000.000000000000000 ) ;
#208683=CIRCLE ( 'NONE', #129562, 2.000000000000002220 ) ;
#208696=VERTEX_POINT ( 'NONE', #245941 ) ;
#208723=FACE_OUTER_BOUND ( 'NONE', #177971, .T. ) ;
#208739=DIRECTION ( 'NONE',  ( -1.000000000000000000, 0.000000000000000000, 0.000000000000000000 ) ) ;
#208744=CARTESIAN_POINT ( 'NONE',  ( 21.07928932188134397, -1.250084634896337255, -194.7953894783290423 ) ) ;
#208760=EDGE_CURVE ( 'NONE', #44981, #200910, #247395, .T. ) ;
#208767=CARTESIAN_POINT ( 'NONE',  ( 22.41477678272288188, -2.478238346927450930, -189.6170666049704323 ) ) ;
#208789=CARTESIAN_POINT ( 'NONE',  ( -21.05000000000000071, 12.81615072508355802, -205.2382006284440763 ) ) ;
#208800=DIRECTION ( 'NONE',  ( -0.000000000000000000, -0.2128009952263607285, 0.9770955615653316162 ) ) ;
#208816=DIRECTION ( 'NONE',  ( 0.000000000000000000, 0.2128009952263688886, -0.9770955615653297288 ) ) ;
#208821=FACE_OUTER_BOUND ( 'NONE', #57676, .T. ) ;
#208831=ADVANCED_FACE ( 'NONE', ( #211197 ), #13026, .T. ) ;
#208858=FACE_OUTER_BOUND ( 'NONE', #221549, .T. ) ;
#208871=CARTESIAN_POINT ( 'NONE',  ( -23.15000000000000213, 2.739812813550878801, -213.5801053551551547 ) ) ;
#208907=EDGE_CURVE ( 'NONE', #47690, #63666, #139338, .T. ) ;
#208911=CARTESIAN_POINT ( 'NONE',  ( 18.55807992284871588, 18.40923646582965745, -236.9894833875398206 ) ) ;
#208932=CIRCLE ( 'NONE', #250614, 0.1999999999999987899 ) ;
#208938=ADVANCED_FACE ( 'NONE', ( #25843 ), #66248, .F. ) ;
#208958=EDGE_LOOP ( 'NONE', ( #137972, #129481, #186138, #150413, #25880, #100320, #152858, #223726, #110461, #157347, #157035, #94068, #84455, #255153, #144057, #196497, #54000, #252786, #239818, #242200, #129340, #257541, #237317, #62646, #37253 ) ) ;
#208985=DIRECTION ( 'NONE',  ( -0.000000000000000000, -0.2128009952263603677, 0.9770955615653313941 ) ) ;
#209019=TOROIDAL_SURFACE ( 'NONE', #154887, 0.9750000000000019762, 0.1000000000000000056 ) ;
#209032=CARTESIAN_POINT ( 'NONE',  ( -23.15000000000000213, 10.71906255309368383, -222.4921384173655383 ) ) ;
#209039=CYLINDRICAL_SURFACE ( 'NONE', #175197, 0.1000000000000054040 ) ;
#209044=ORIENTED_EDGE ( 'NONE', *, *, #57839, .T. ) ;
#209080=ORIENTED_EDGE ( 'NONE', *, *, #230940, .T. ) ;
#209113=DIRECTION ( 'NONE',  ( 0.000000000000000000, 0.2128009952263602844, -0.9770955615653315052 ) ) ;
#209123=CARTESIAN_POINT ( 'NONE',  ( -20.94999675878240808, 18.34775554461856828, -236.8759397601555179 ) ) ;
#209174=FACE_OUTER_BOUND ( 'NONE', #127653, .T. ) ;
#209192=FACE_OUTER_BOUND ( 'NONE', #20250, .T. ) ;
#209199=CARTESIAN_POINT ( 'NONE',  ( -23.15000000000000213, 8.555687629545136730, -220.7824469969188783 ) ) ;
#209206=ORIENTED_EDGE ( 'NONE', *, *, #186460, .F. ) ;
#209217=EDGE_CURVE ( 'NONE', #86372, #52350, #251863, .T. ) ;
#209228=CARTESIAN_POINT ( 'NONE',  ( 22.50000000000000000, 7.591056067193225232, -199.2444047917219052 ) ) ;
#209234=EDGE_CURVE ( 'NONE', #53701, #200289, #97331, .T. ) ;
#209241=LINE ( 'NONE', #249668, #30907 ) ;
#209287=LINE ( 'NONE', #74947, #161037 ) ;
#209301=DIRECTION ( 'NONE',  ( 0.000000000000000000, -0.2128009952263603954, 0.9770955615653315052 ) ) ;
#209302=ORIENTED_EDGE ( 'NONE', *, *, #193040, .T. ) ;
#209370=LINE ( 'NONE', #49011, #208680 ) ;
#209386=AXIS2_PLACEMENT_3D ( 'NONE', #31272, #191623, #229437 ) ;
#209425=CARTESIAN_POINT ( 'NONE',  ( 21.05000005001206276, 11.25956737883785941, -211.0112013901115517 ) ) ;
#209431=CARTESIAN_POINT ( 'NONE',  ( -20.54999999999999716, -3.685352791942193562, -226.3713951780953550 ) ) ;
#209446=EDGE_CURVE ( 'NONE', #235545, #122770, #224977, .T. ) ;
#209474=CIRCLE ( 'NONE', #221928, 0.09999999999999895084 ) ;
#209476=CARTESIAN_POINT ( 'NONE',  ( -23.15000000000000213, 13.96869538424788360, -210.3925794786331949 ) ) ;
#209498=CARTESIAN_POINT ( 'NONE',  ( 23.14999999999998437, 1.148907358139439339E-11, -201.0000000000015064 ) ) ;
#209556=ADVANCED_FACE ( 'NONE', ( #15946 ), #147255, .F. ) ;
#209558=ORIENTED_EDGE ( 'NONE', *, *, #139144, .F. ) ;
#209570=CIRCLE ( 'NONE', #168110, 11.80000000000000604 ) ;
#209572=AXIS2_PLACEMENT_3D ( 'NONE', #95958, #12614, #215897 ) ;
#209578=DIRECTION ( 'NONE',  ( 1.000000000000000000, 0.000000000000000000, 0.000000000000000000 ) ) ;
#209582=ORIENTED_EDGE ( 'NONE', *, *, #201935, .F. ) ;
#209593=ORIENTED_EDGE ( 'NONE', *, *, #68755, .F. ) ;
#209628=VECTOR ( 'NONE', #132116, 1000.000000000000227 ) ;
#209633=ORIENTED_EDGE ( 'NONE', *, *, #34592, .T. ) ;
#209650=VERTEX_POINT ( 'NONE', #61462 ) ;
#209661=AXIS2_PLACEMENT_3D ( 'NONE', #144178, #3385, #163773 ) ;
#209670=CARTESIAN_POINT ( 'NONE',  ( -21.05000000000000071, 4.252251777740764460, -211.8999245327126744 ) ) ;
#209682=ORIENTED_EDGE ( 'NONE', *, *, #128684, .T. ) ;
#209689=DIRECTION ( 'NONE',  ( -1.000000000000000000, 0.000000000000000000, 0.000000000000000000 ) ) ;
#209705=AXIS2_PLACEMENT_3D ( 'NONE', #88861, #91463, #193135 ) ;
#209712=FACE_OUTER_BOUND ( 'NONE', #427, .T. ) ;
#209743=FACE_OUTER_BOUND ( 'NONE', #19984, .T. ) ;
#209775=DIRECTION ( 'NONE',  ( 1.000000000000000000, 0.000000000000000000, 0.000000000000000000 ) ) ;
#209777=FACE_OUTER_BOUND ( 'NONE', #233922, .T. ) ;
#209783=CARTESIAN_POINT ( 'NONE',  ( 21.05000000000000071, 1.148907358139439339E-11, -201.0000000000015064 ) ) ;
#209786=CARTESIAN_POINT ( 'NONE',  ( 20.04142135623730070, 15.92646454033040015, -219.3818586450342423 ) ) ;
#209797=DIRECTION ( 'NONE',  ( 2.978066053179067751E-16, -0.9770955615653316162, -0.2128009952263596738 ) ) ;
#209810=CARTESIAN_POINT ( 'NONE',  ( -22.49072729836729678, -2.423945104021340224, -189.6048092360547059 ) ) ;
#209815=DIRECTION ( 'NONE',  ( 0.000000000000000000, 0.3042567129660163627, 0.9525900758537824142 ) ) ;
#209819=AXIS2_PLACEMENT_3D ( 'NONE', #203699, #220695, #180286 ) ;
#209862=EDGE_CURVE ( 'NONE', #20649, #208696, #239017, .T. ) ;
#209880=ORIENTED_EDGE ( 'NONE', *, *, #113389, .F. ) ;
#209905=CARTESIAN_POINT ( 'NONE',  ( -18.44448725179914916, -0.7332340351039789983, -242.2293278273956787 ) ) ;
#209907=AXIS2_PLACEMENT_3D ( 'NONE', #150908, #75248, #136448 ) ;
#209914=ORIENTED_EDGE ( 'NONE', *, *, #165233, .F. ) ;
#209915=ORIENTED_EDGE ( 'NONE', *, *, #90270, .T. ) ;
#209925=FACE_BOUND ( 'NONE', #34159, .T. ) ;
#209967=CARTESIAN_POINT ( 'NONE',  ( 21.30000000000002558, 1.148907358139439339E-11, -201.0000000000015064 ) ) ;
#209973=CARTESIAN_POINT ( 'NONE',  ( 18.59999999999997655, 7.675662554762638479, -241.7139905447625381 ) ) ;
#209982=CARTESIAN_POINT ( 'NONE',  ( 20.94999999999999929, 4.252251777740766236, -211.8999245327126744 ) ) ;
#209983=CARTESIAN_POINT ( 'NONE',  ( 18.49999999999999289, 15.37733547974377402, -223.0834978222773657 ) ) ;
#209988=CARTESIAN_POINT ( 'NONE',  ( 23.14999999999999503, 3.801854678198143933, -188.1465607323988252 ) ) ;
#209990=DIRECTION ( 'NONE',  ( -1.836970198721029934E-16, 0.9770955615653316162, 0.2128009952263604232 ) ) ;
#210013=DIRECTION ( 'NONE',  ( -1.000000000000000000, 0.000000000000000000, 0.000000000000000000 ) ) ;
#210054=CARTESIAN_POINT ( 'NONE',  ( 22.49806830649814060, -2.403418073154200307, -189.6004600419238102 ) ) ;
#210057=CARTESIAN_POINT ( 'NONE',  ( -21.64999999999999858, 9.788464569039593499, -211.4053333142630891 ) ) ;
#210062=CARTESIAN_POINT ( 'NONE',  ( -21.11101077989000174, -1.352031336145134821, -194.7201934363683904 ) ) ;
#210068=DIRECTION ( 'NONE',  ( 0.000000000000000000, 0.2128009952263568427, -0.9770955615653323934 ) ) ;
#210109=EDGE_CURVE ( 'NONE', #92384, #103375, #23347, .T. ) ;
#210126=CARTESIAN_POINT ( 'NONE',  ( -20.64999999999999858, 9.712035112405693837, -211.5243229699422614 ) ) ;
#210135=CARTESIAN_POINT ( 'NONE',  ( -21.04999999999999716, -7.883686024897174072, -209.9138933503092233 ) ) ;
#210160=ORIENTED_EDGE ( 'NONE', *, *, #58741, .T. ) ;
#210163=ADVANCED_FACE ( 'NONE', ( #218934 ), #239807, .T. ) ;
#210226=ORIENTED_EDGE ( 'NONE', *, *, #131211, .T. ) ;
#210234=TOROIDAL_SURFACE ( 'NONE', #189377, 4.099999999999999645, 0.1000000000000000056 ) ;
#210243=EDGE_LOOP ( 'NONE', ( #209302, #17696, #35476, #227064, #57134, #37282, #216235, #132945, #130881, #138890 ) ) ;
#210279=CARTESIAN_POINT ( 'NONE',  ( 23.25000000000000000, -7.274670914976375968, -212.7102428701827250 ) ) ;
#210312=( NAMED_UNIT ( * ) SI_UNIT ( $, .STERADIAN. ) SOLID_ANGLE_UNIT ( ) );
#210319=DIRECTION ( 'NONE',  ( 0.000000000000000000, 0.2128009952263606452, -0.9770955615653313941 ) ) ;
#210343=CARTESIAN_POINT ( 'NONE',  ( 18.49999999999999289, 16.76897757977918957, -222.7804130109902871 ) ) ;
#210375=EDGE_LOOP ( 'NONE', ( #154894, #56333, #103242, #236777 ) ) ;
#210387=PLANE ( 'NONE',  #79141 ) ;
#210395=AXIS2_PLACEMENT_3D ( 'NONE', #99526, #179130, #1725 ) ;
#210399=CARTESIAN_POINT ( 'NONE',  ( -22.47071067811865319, 7.522163794833024220, -199.2603376134758832 ) ) ;
#210405=ADVANCED_FACE ( 'NONE', ( #141661 ), #77827, .T. ) ;
#210426=CARTESIAN_POINT ( 'NONE',  ( 21.05000000000000071, 6.703231349641842307, -231.7785101893094577 ) ) ;
#210485=VERTEX_POINT ( 'NONE', #145507 ) ;
#210501=DIRECTION ( 'NONE',  ( -0.000000000000000000, 0.2128009952263603677, -0.9770955615653313941 ) ) ;
#210512=CARTESIAN_POINT ( 'NONE',  ( -18.48550754432010379, -7.746656446482333536, -209.9011620725964633 ) ) ;
#210523=ADVANCED_FACE ( 'NONE', ( #64691 ), #24310, .T. ) ;
#210535=DIRECTION ( 'NONE',  ( 0.000000000000000000, -0.2128009952263604232, 0.9770955615653316162 ) ) ;
#210544=CARTESIAN_POINT ( 'NONE',  ( 20.85000000000000142, 7.783179459866048866, -245.3643104511423303 ) ) ;
#210558=AXIS2_PLACEMENT_3D ( 'NONE', #68032, #5462, #246660 ) ;
#210569=CARTESIAN_POINT ( 'NONE',  ( 20.94999999999999929, -4.756823075239758225, -233.1486023682345490 ) ) ;
#210584=DIRECTION ( 'NONE',  ( 0.000000000000000000, -0.2128009952263603677, 0.9770955615653313941 ) ) ;
#210600=AXIS2_PLACEMENT_3D ( 'NONE', #250579, #151516, #109781 ) ;
#210601=EDGE_LOOP ( 'NONE', ( #93158, #25975, #142874, #247408 ) ) ;
#210612=DIRECTION ( 'NONE',  ( 1.000000000000000000, 0.000000000000000000, 0.000000000000000000 ) ) ;
#210626=EDGE_LOOP ( 'NONE', ( #107173, #245234, #253020, #217881 ) ) ;
#210648=AXIS2_PLACEMENT_3D ( 'NONE', #185714, #72200, #8367 ) ;
#210664=DIRECTION ( 'NONE',  ( 0.000000000000000000, -0.9770955615653313941, -0.2128009952263603677 ) ) ;
#210681=LINE ( 'NONE', #187289, #121912 ) ;
#210687=EDGE_CURVE ( 'NONE', #107334, #245093, #122879, .T. ) ;
#210702=CYLINDRICAL_SURFACE ( 'NONE', #54886, 0.1000000000000124262 ) ;
#210718=FACE_OUTER_BOUND ( 'NONE', #53692, .T. ) ;
#210734=DIRECTION ( 'NONE',  ( -1.000000000000000000, 0.000000000000000000, 0.000000000000000000 ) ) ;
#210738=LINE ( 'NONE', #112924, #33726 ) ;
#210826=ORIENTED_EDGE ( 'NONE', *, *, #145300, .T. ) ;
#210832=CIRCLE ( 'NONE', #244132, 3.900000000000000799 ) ;
#210859=CARTESIAN_POINT ( 'NONE',  ( -20.64999999999999858, -6.688413578037177842, -212.5825622730469036 ) ) ;
#210888=AXIS2_PLACEMENT_3D ( 'NONE', #246586, #28884, #204885 ) ;
#210889=ORIENTED_EDGE ( 'NONE', *, *, #197856, .T. ) ;
#210894=AXIS2_PLACEMENT_3D ( 'NONE', #210544, #30643, #107576 ) ;
#210918=AXIS2_PLACEMENT_3D ( 'NONE', #13564, #213029, #193488 ) ;
#210920=DIRECTION ( 'NONE',  ( 1.000000000000000000, 0.000000000000000000, 0.000000000000000000 ) ) ;
#210926=CARTESIAN_POINT ( 'NONE',  ( -18.59999999999999787, 7.128833340094563376, -233.7327013124401276 ) ) ;
#210933=EDGE_CURVE ( 'NONE', #142313, #201052, #252035, .T. ) ;
#210947=CIRCLE ( 'NONE', #65194, 0.09999999999999767408 ) ;
#210976=CARTESIAN_POINT ( 'NONE',  ( 23.24999999999999645, 3.318160649989770672, -234.5626251938229245 ) ) ;
#210984=DIRECTION ( 'NONE',  ( 1.000000000000000000, -7.136802563874200093E-16, -1.554319503706932210E-16 ) ) ;
#210986=LINE ( 'NONE', #10228, #136532 ) ;
#211045=CIRCLE ( 'NONE', #119464, 11.80000000000000782 ) ;
#211080=DIRECTION ( 'NONE',  ( -0.7071067811865474617, -0.6909108974501236844, -0.1504730267678055788 ) ) ;
#211089=DIRECTION ( 'NONE',  ( 1.000000000000000000, -0.000000000000000000, -0.000000000000000000 ) ) ;
#211092=DIRECTION ( 'NONE',  ( 1.000000000000000000, 0.000000000000000000, 0.000000000000000000 ) ) ;
#211097=DIRECTION ( 'NONE',  ( 1.000000000000000000, 3.816239940179503281E-14, -1.218904804407150903E-14 ) ) ;
#211101=ORIENTED_EDGE ( 'NONE', *, *, #133824, .T. ) ;
#211129=DIRECTION ( 'NONE',  ( 1.000000000000000000, 2.885090398161910739E-16, 6.283419270304611573E-17 ) ) ;
#211197=FACE_OUTER_BOUND ( 'NONE', #17497, .T. ) ;
#211201=CIRCLE ( 'NONE', #98728, 0.5000000000000002220 ) ;
#211262=CARTESIAN_POINT ( 'NONE',  ( -20.15000000000000568, 11.70669885886984751, -211.0899064736586013 ) ) ;
#211275=ORIENTED_EDGE ( 'NONE', *, *, #221043, .T. ) ;
#211287=AXIS2_PLACEMENT_3D ( 'NONE', #153661, #171920, #174509 ) ;
#211342=EDGE_CURVE ( 'NONE', #225002, #190519, #191452, .T. ) ;
#211362=ORIENTED_EDGE ( 'NONE', *, *, #194540, .F. ) ;
#211372=DIRECTION ( 'NONE',  ( 0.000000000000000000, 0.2128009952263603677, -0.9770955615653313941 ) ) ;
#211390=DIRECTION ( 'NONE',  ( 1.000000000000000000, 3.190570557967288949E-16, 6.948722487160392945E-17 ) ) ;
#211402=AXIS2_PLACEMENT_3D ( 'NONE', #176674, #22741, #159668 ) ;
#211408=ORIENTED_EDGE ( 'NONE', *, *, #248042, .T. ) ;
#211410=ORIENTED_EDGE ( 'NONE', *, *, #202196, .F. ) ;
#211413=VERTEX_POINT ( 'NONE', #219957 ) ;
#211459=DIRECTION ( 'NONE',  ( 0.9880948137434723000, 0.1503223940869687913, 0.03273861465020814349 ) ) ;
#211485=DIRECTION ( 'NONE',  ( 1.000000000000000000, 0.000000000000000000, 0.000000000000000000 ) ) ;
#211501=FACE_OUTER_BOUND ( 'NONE', #207276, .T. ) ;
#211532=TOROIDAL_SURFACE ( 'NONE', #70079, 0.2000000000000000111, 0.1000000000000000056 ) ;
#211542=ADVANCED_FACE ( 'NONE', ( #124717 ), #187272, .F. ) ;
#211548=CIRCLE ( 'NONE', #128350, 0.6000000000000064171 ) ;
#211554=VERTEX_POINT ( 'NONE', #86842 ) ;
#211578=AXIS2_PLACEMENT_3D ( 'NONE', #8590, #133664, #170276 ) ;
#211586=FACE_OUTER_BOUND ( 'NONE', #2459, .T. ) ;
#211594=VECTOR ( 'NONE', #77284, 1000.000000000000227 ) ;
#211606=CARTESIAN_POINT ( 'NONE',  ( 21.05000000000000071, 6.093673009692417430, -199.5727803633481301 ) ) ;
#211619=DIRECTION ( 'NONE',  ( 1.000000000000000000, 0.000000000000000000, 0.000000000000000000 ) ) ;
#211633=CARTESIAN_POINT ( 'NONE',  ( 20.94999999999999929, 7.128833340094563376, -233.7327013124401276 ) ) ;
#211640=TOROIDAL_SURFACE ( 'NONE', #16022, 12.97499999999999609, 0.1000000000000000056 ) ;
#211657=CARTESIAN_POINT ( 'NONE',  ( -18.59999999999999787, -0.6576273345615599730, -242.5323337003318898 ) ) ;
#211660=DIRECTION ( 'NONE',  ( -1.000000000000000000, -0.000000000000000000, -0.000000000000000000 ) ) ;
#211670=VECTOR ( 'NONE', #36921, 1000.000000000000227 ) ;
#211701=CYLINDRICAL_SURFACE ( 'NONE', #167419, 0.1000000000000055844 ) ;
#211743=AXIS2_PLACEMENT_3D ( 'NONE', #96222, #256527, #240886 ) ;
#211744=CARTESIAN_POINT ( 'NONE',  ( -18.59999999999999787, 15.92646454033039305, -219.3818586450342707 ) ) ;
#211747=DIRECTION ( 'NONE',  ( -1.000000000000000000, 0.000000000000000000, 0.000000000000000000 ) ) ;
#211752=EDGE_CURVE ( 'NONE', #365, #245608, #31855, .T. ) ;
#211765=DIRECTION ( 'NONE',  ( 0.000000000000000000, 0.2128009952263403282, -0.9770955615653358350 ) ) ;
#211766=CARTESIAN_POINT ( 'NONE',  ( -20.85000000000000142, 14.80545736607782814, -235.9842437978701639 ) ) ;
#211769=EDGE_CURVE ( 'NONE', #46074, #217380, #115408, .T. ) ;
#211781=CYLINDRICAL_SURFACE ( 'NONE', #102234, 0.1000000000000055844 ) ;
#211802=CARTESIAN_POINT ( 'NONE',  ( -18.45037301276683195, -7.780528700220050276, -209.8715768735301594 ) ) ;
#211815=VERTEX_POINT ( 'NONE', #41041 ) ;
#211893=EDGE_CURVE ( 'NONE', #54334, #208398, #52657, .T. ) ;
#211971=CYLINDRICAL_SURFACE ( 'NONE', #246354, 0.1000000000000055844 ) ;
#211980=DIRECTION ( 'NONE',  ( 1.000000000000000000, 0.000000000000000000, 0.000000000000000000 ) ) ;
#212022=EDGE_CURVE ( 'NONE', #77477, #106096, #69446, .T. ) ;
#212023=VERTEX_POINT ( 'NONE', #200930 ) ;
#212053=CARTESIAN_POINT ( 'NONE',  ( 21.05000000000000071, -10.60885044396467158, -206.2784744251879374 ) ) ;
#212054=AXIS2_PLACEMENT_3D ( 'NONE', #83315, #140758, #220308 ) ;
#212066=CARTESIAN_POINT ( 'NONE',  ( -20.15000000000000568, 13.57934761686182057, -219.6883474154335261 ) ) ;
#212110=CARTESIAN_POINT ( 'NONE',  ( 21.00000000000000000, 12.13349391679638778, -210.8946109257198032 ) ) ;
#212135=EDGE_LOOP ( 'NONE', ( #60557, #153012, #151554, #178842 ) ) ;
#212141=LINE ( 'NONE', #113028, #6810 ) ;
#212148=VECTOR ( 'NONE', #9490, 1000.000000000000227 ) ;
#212151=ADVANCED_FACE ( 'NONE', ( #86080 ), #108254, .T. ) ;
#212172=VERTEX_POINT ( 'NONE', #226904 ) ;
#212244=ORIENTED_EDGE ( 'NONE', *, *, #32282, .T. ) ;
#212245=EDGE_LOOP ( 'NONE', ( #83393, #168106, #105933, #221724 ) ) ;
#212247=ORIENTED_EDGE ( 'NONE', *, *, #195541, .T. ) ;
#212288=DIRECTION ( 'NONE',  ( 1.000000000000000000, 3.190570557967288949E-16, 6.948722487160392945E-17 ) ) ;
#212294=DIRECTION ( 'NONE',  ( 0.000000000000000000, 0.3042567129660006531, 0.9525900758537875213 ) ) ;
#212301=EDGE_CURVE ( 'NONE', #203779, #190519, #98602, .T. ) ;
#212306=DIRECTION ( 'NONE',  ( -1.000000000000000000, -2.885090398161910739E-16, -6.283419270304611573E-17 ) ) ;
#212309=CARTESIAN_POINT ( 'NONE',  ( 20.94999999999999929, -4.557064143889601127, -233.1584191572127622 ) ) ;
#212375=DIRECTION ( 'NONE',  ( 0.000000000000000000, 0.7397890806274345366, 0.6728388485992877754 ) ) ;
#212381=FACE_OUTER_BOUND ( 'NONE', #234767, .T. ) ;
#212419=EDGE_LOOP ( 'NONE', ( #86371, #27411, #254309, #138481 ) ) ;
#212424=DIRECTION ( 'NONE',  ( -1.000000000000000000, 0.000000000000000000, 0.000000000000000000 ) ) ;
#212426=DIRECTION ( 'NONE',  ( 7.589415207398576792E-15, -0.9770955615653316162, -0.2128009952263604232 ) ) ;
#212428=CARTESIAN_POINT ( 'NONE',  ( -23.15000000000000213, -0.8618440306552707098, -197.0427629756619297 ) ) ;
#212449=ORIENTED_EDGE ( 'NONE', *, *, #220128, .F. ) ;
#212450=ORIENTED_EDGE ( 'NONE', *, *, #30707, .F. ) ;
#212452=AXIS2_PLACEMENT_3D ( 'NONE', #190012, #93461, #89608 ) ;
#212459=LINE ( 'NONE', #114624, #76414 ) ;
#212471=CARTESIAN_POINT ( 'NONE',  ( -18.45140287520618472, -0.7268611856809952254, -242.2397737697636444 ) ) ;
#212481=ORIENTED_EDGE ( 'NONE', *, *, #184204, .T. ) ;
#212490=EDGE_CURVE ( 'NONE', #179904, #16905, #161198, .T. ) ;
#212520=DIRECTION ( 'NONE',  ( -2.557131231893036492E-16, 0.9525900758537791946, -0.3042567129660267988 ) ) ;
#212530=EDGE_CURVE ( 'NONE', #132241, #100848, #149526, .T. ) ;
#212535=ORIENTED_EDGE ( 'NONE', *, *, #101421, .F. ) ;
#212565=CARTESIAN_POINT ( 'NONE',  ( 20.85000000000000142, 7.788796164756791818, -245.4641525896719543 ) ) ;
#212574=TOROIDAL_SURFACE ( 'NONE', #233428, 0.2000000000000000111, 0.1000000000000000056 ) ;
#212607=ORIENTED_EDGE ( 'NONE', *, *, #90289, .F. ) ;
#212647=CARTESIAN_POINT ( 'NONE',  ( 20.85000000000000142, -4.871452838297987142, -233.3782557782877518 ) ) ;
#212703=VERTEX_POINT ( 'NONE', #133783 ) ;
#212704=CARTESIAN_POINT ( 'NONE',  ( 23.14999999999999858, 9.374458193048763377, -220.5475659691911119 ) ) ;
#212720=CARTESIAN_POINT ( 'NONE',  ( 18.49999999999999289, 15.22030141505243428, -222.9130098973476777 ) ) ;
#212759=ADVANCED_FACE ( 'NONE', ( #35991 ), #115575, .F. ) ;
#212763=AXIS2_PLACEMENT_3D ( 'NONE', #193974, #216074, #15345 ) ;
#212777=AXIS2_PLACEMENT_3D ( 'NONE', #93780, #254133, #155084 ) ;
#212787=DIRECTION ( 'NONE',  ( 0.000000000000000000, 0.2280421351061330537, -0.9736512643735621975 ) ) ;
#212805=VERTEX_POINT ( 'NONE', #102326 ) ;
#212806=ORIENTED_EDGE ( 'NONE', *, *, #139801, .T. ) ;
#212886=VERTEX_POINT ( 'NONE', #20275 ) ;
#212887=CARTESIAN_POINT ( 'NONE',  ( 21.05000000000000071, 6.108733535351102972, -199.6370801574273628 ) ) ;
#212912=EDGE_CURVE ( 'NONE', #203031, #156064, #223890, .T. ) ;
#212924=FACE_OUTER_BOUND ( 'NONE', #253724, .T. ) ;
#212944=CIRCLE ( 'NONE', #217006, 0.1999999999999987899 ) ;
#212955=CARTESIAN_POINT ( 'NONE',  ( -22.01447462590972748, 7.076351764553705515, -199.3574874748654224 ) ) ;
#212981=EDGE_CURVE ( 'NONE', #139309, #46709, #148914, .T. ) ;
#212986=EDGE_CURVE ( 'NONE', #79677, #34477, #103089, .T. ) ;
#213000=CARTESIAN_POINT ( 'NONE',  ( 21.05000000000000071, -11.38316329222461754, -203.4791315943886048 ) ) ;
#213011=CIRCLE ( 'NONE', #100549, 0.09999999999999939493 ) ;
#213026=DIRECTION ( 'NONE',  ( 0.000000000000000000, 0.2128009952263606730, -0.9770955615653313941 ) ) ;
#213029=DIRECTION ( 'NONE',  ( 1.000000000000000000, 0.000000000000000000, 0.000000000000000000 ) ) ;
#213040=ORIENTED_EDGE ( 'NONE', *, *, #29094, .F. ) ;
#213050=CIRCLE ( 'NONE', #142320, 0.09999999999999852063 ) ;
#213062=CIRCLE ( 'NONE', #71628, 0.1000000000000054040 ) ;
#213066=ORIENTED_EDGE ( 'NONE', *, *, #220128, .T. ) ;
#213082=AXIS2_PLACEMENT_3D ( 'NONE', #136176, #116649, #176646 ) ;
#213096=FACE_OUTER_BOUND ( 'NONE', #128965, .T. ) ;
#213119=DIRECTION ( 'NONE',  ( 0.000000000000000000, -0.9770955615653315052, -0.2128009952263603954 ) ) ;
#213123=CARTESIAN_POINT ( 'NONE',  ( 18.59999999999999076, 14.51805813080544638, -219.6885945441820809 ) ) ;
#213180=CARTESIAN_POINT ( 'NONE',  ( 23.14999999999999858, 9.125777775466493935, -211.6520035670780544 ) ) ;
#213196=AXIS2_PLACEMENT_3D ( 'NONE', #241770, #164817, #163526 ) ;
#213197=FACE_OUTER_BOUND ( 'NONE', #144369, .T. ) ;
#213220=DIRECTION ( 'NONE',  ( 0.000000000000000000, -0.2128009952263485993, 0.9770955615653341697 ) ) ;
#213237=AXIS2_PLACEMENT_3D ( 'NONE', #80196, #239312, #251829 ) ;
#213242=CARTESIAN_POINT ( 'NONE',  ( -20.94999999999999929, 7.791794839520818527, -245.4663415047620845 ) ) ;
#213264=CYLINDRICAL_SURFACE ( 'NONE', #178957, 0.5000000000000007772 ) ;
#213270=ORIENTED_EDGE ( 'NONE', *, *, #16199, .T. ) ;
#213298=DIRECTION ( 'NONE',  ( 0.000000000000000000, 0.2128009952263601734, -0.9770955615653315052 ) ) ;
#213305=LINE ( 'NONE', #12577, #72514 ) ;
#213329=CARTESIAN_POINT ( 'NONE',  ( -20.64999999999999858, 4.768403829798271154, -213.4961173936592331 ) ) ;
#213335=AXIS2_PLACEMENT_3D ( 'NONE', #5038, #160323, #84556 ) ;
#213347=ORIENTED_EDGE ( 'NONE', *, *, #39483, .T. ) ;
#213352=CARTESIAN_POINT ( 'NONE',  ( -18.39999999999999858, -0.7490476236415750666, -242.2033265267442061 ) ) ;
#213410=ORIENTED_EDGE ( 'NONE', *, *, #232062, .T. ) ;
#213422=ADVANCED_FACE ( 'NONE', ( #60053 ), #77053, .F. ) ;
#213442=DIRECTION ( 'NONE',  ( -0.000000000000000000, 0.9770955615653313941, 0.2128009952263603954 ) ) ;
#213445=ORIENTED_EDGE ( 'NONE', *, *, #128615, .T. ) ;
#213464=ORIENTED_EDGE ( 'NONE', *, *, #209862, .T. ) ;
#213480=FACE_OUTER_BOUND ( 'NONE', #101722, .T. ) ;
#213489=ORIENTED_EDGE ( 'NONE', *, *, #229534, .T. ) ;
#213533=CIRCLE ( 'NONE', #92727, 0.3999999999999965250 ) ;
#213538=AXIS2_PLACEMENT_3D ( 'NONE', #182073, #3409, #5975 ) ;
#213578=EDGE_LOOP ( 'NONE', ( #40645, #198350, #120549, #247172 ) ) ;
#213590=CARTESIAN_POINT ( 'NONE',  ( 21.05000000000000071, 7.128833340094563376, -233.7327013124401276 ) ) ;
#213596=DIRECTION ( 'NONE',  ( -1.000000000000000000, 0.000000000000000000, 0.000000000000000000 ) ) ;
#213597=CIRCLE ( 'NONE', #22099, 0.5999999999999987566 ) ;
#213602=DIRECTION ( 'NONE',  ( 1.000000000000000000, -0.000000000000000000, -0.000000000000000000 ) ) ;
#213661=DIRECTION ( 'NONE',  ( 0.000000000000000000, -0.2128009952263601456, 0.9770955615653316162 ) ) ;
#213670=DIRECTION ( 'NONE',  ( 1.000000000000000000, 0.000000000000000000, 0.000000000000000000 ) ) ;
#213682=EDGE_LOOP ( 'NONE', ( #38388, #46360, #66325, #102 ) ) ;
#213711=SPHERICAL_SURFACE ( 'NONE', #209386, 0.1000000000000000056 ) ;
#213735=CARTESIAN_POINT ( 'NONE',  ( -18.39999999999999858, -0.7490476236415750666, -242.2033265267442061 ) ) ;
#213749=AXIS2_PLACEMENT_3D ( 'NONE', #220204, #200638, #42843 ) ;
#213763=AXIS2_PLACEMENT_3D ( 'NONE', #36269, #33730, #153690 ) ;
#213785=CARTESIAN_POINT ( 'NONE',  ( -21.04999999999979821, -1.396821799461749780, -194.6552352087717850 ) ) ;
#213815=AXIS2_PLACEMENT_3D ( 'NONE', #167293, #169883, #250637 ) ;
#213820=VERTEX_POINT ( 'NONE', #257564 ) ;
#213869=CARTESIAN_POINT ( 'NONE',  ( 22.49999999999999645, -2.381330705637466405, -189.5959759702857923 ) ) ;
#213886=CARTESIAN_POINT ( 'NONE',  ( -20.54999999999999716, 4.768403829798271154, -213.4961173936592331 ) ) ;
#213889=AXIS2_PLACEMENT_3D ( 'NONE', #70976, #53942, #153092 ) ;
#213911=AXIS2_PLACEMENT_3D ( 'NONE', #142297, #1498, #177614 ) ;
#213955=DIRECTION ( 'NONE',  ( -0.000000000000000000, 0.9770955615653313941, 0.2128009952263603677 ) ) ;
#213964=CARTESIAN_POINT ( 'NONE',  ( 23.14999999999999503, 17.01923898301590654, -224.3994341343041867 ) ) ;
#213987=DIRECTION ( 'NONE',  ( 1.000000000000000000, 0.000000000000000000, 0.000000000000000000 ) ) ;
#213996=AXIS2_PLACEMENT_3D ( 'NONE', #200108, #196243, #239229 ) ;
#214053=CARTESIAN_POINT ( 'NONE',  ( 23.15000000000000213, -4.892732937820623462, -233.2805462221312496 ) ) ;
#214061=VERTEX_POINT ( 'NONE', #149256 ) ;
#214062=DIRECTION ( 'NONE',  ( 2.952720810173288126E-16, -0.9770955615653313941, -0.2128009952263603677 ) ) ;
#214065=DIRECTION ( 'NONE',  ( -1.000000000000000000, 0.000000000000000000, 0.000000000000000000 ) ) ;
#214097=LINE ( 'NONE', #216660, #68250 ) ;
#214099=EDGE_LOOP ( 'NONE', ( #101960, #180961, #90977, #179543 ) ) ;
#214151=EDGE_LOOP ( 'NONE', ( #126890, #37902, #143082, #122400, #160535, #252626, #186844, #67431, #67030, #134181, #63606 ) ) ;
#214152=AXIS2_PLACEMENT_3D ( 'NONE', #178694, #10, #135661 ) ;
#214184=AXIS2_PLACEMENT_3D ( 'NONE', #17725, #240645, #140238 ) ;
#214208=CIRCLE ( 'NONE', #47581, 0.1000000000000005607 ) ;
#214209=CARTESIAN_POINT ( 'NONE',  ( -21.05000000000000071, 1.148907358139439339E-11, -201.0000000000015064 ) ) ;
#214213=CARTESIAN_POINT ( 'NONE',  ( 22.49436431346199683, 11.36887822570846041, -198.4555077020579290 ) ) ;
#214227=EDGE_CURVE ( 'NONE', #76729, #130685, #40774, .T. ) ;
#214242=CARTESIAN_POINT ( 'NONE',  ( -21.78635804494510708, 6.853445233358327116, -199.4060668238051051 ) ) ;
#214246=LINE ( 'NONE', #215517, #211594 ) ;
#214267=CIRCLE ( 'NONE', #251676, 4.150000000000000355 ) ;
#214273=CARTESIAN_POINT ( 'NONE',  ( -20.94983749550516450, 18.35558276679135048, -236.8903279188150464 ) ) ;
#214288=EDGE_LOOP ( 'NONE', ( #170614, #212535, #98220, #123672 ) ) ;
#214314=VERTEX_POINT ( 'NONE', #219463 ) ;
#214321=CARTESIAN_POINT ( 'NONE',  ( 23.24999999999999289, 11.04098673250373785, -220.4458636211660689 ) ) ;
#214338=EDGE_CURVE ( 'NONE', #122837, #192375, #257329, .T. ) ;
#214371=DIRECTION ( 'NONE',  ( 0.000000000000000000, -0.2128009952263479332, 0.9770955615653342807 ) ) ;
#214389=DIRECTION ( 'NONE',  ( -0.000000000000000000, -0.2128009952263604232, 0.9770955615653316162 ) ) ;
#214417=DIRECTION ( 'NONE',  ( 0.000000000000000000, 0.9770955615653316162, 0.2128009952263597848 ) ) ;
#214471=EDGE_LOOP ( 'NONE', ( #69760, #88376, #99348, #165760 ) ) ;
#214477=FACE_OUTER_BOUND ( 'NONE', #52044, .T. ) ;
#214488=CARTESIAN_POINT ( 'NONE',  ( -21.05000000000000071, 0.6713328740235187109, -212.7808875799876205 ) ) ;
#214524=CIRCLE ( 'NONE', #160404, 11.74999999999998757 ) ;
#214555=CARTESIAN_POINT ( 'NONE',  ( -23.25000000000000000, 7.128833340094563376, -233.7327013124401276 ) ) ;
#214565=ADVANCED_FACE ( 'NONE', ( #57513 ), #7404, .F. ) ;
#214571=DIRECTION ( 'NONE',  ( 0.000000000000000000, 0.2128009952263605897, -0.9770955615653315052 ) ) ;
#214586=CARTESIAN_POINT ( 'NONE',  ( -23.15000000000000213, -13.88357498613435936, -191.9982587459959689 ) ) ;
#214628=ORIENTED_EDGE ( 'NONE', *, *, #212981, .T. ) ;
#214642=AXIS2_PLACEMENT_3D ( 'NONE', #12037, #251900, #52405 ) ;
#214708=EDGE_CURVE ( 'NONE', #74571, #123919, #159223, .T. ) ;
#214740=AXIS2_PLACEMENT_3D ( 'NONE', #171337, #117725, #36947 ) ;
#214750=ORIENTED_EDGE ( 'NONE', *, *, #11716, .T. ) ;
#214754=DIRECTION ( 'NONE',  ( 0.000000000000000000, 0.2128009952263582305, -0.9770955615653319493 ) ) ;
#214760=EDGE_LOOP ( 'NONE', ( #213489, #108366, #239396, #227777, #177638 ) ) ;
#214761=CARTESIAN_POINT ( 'NONE',  ( -20.94999999999999929, 1.148907358139439339E-11, -201.0000000000015064 ) ) ;
#214771=ORIENTED_EDGE ( 'NONE', *, *, #116277, .T. ) ;
#214772=DIRECTION ( 'NONE',  ( 1.000000000000000000, 0.000000000000000000, 0.000000000000000000 ) ) ;
#214843=CARTESIAN_POINT ( 'NONE',  ( -21.12844524849339223, 12.95013890645382837, -205.2458600636644519 ) ) ;
#214859=CARTESIAN_POINT ( 'NONE',  ( 18.47654891039378811, -7.732063376463896631, -209.9769793578955728 ) ) ;
#214876=AXIS2_PLACEMENT_3D ( 'NONE', #107221, #248016, #87647 ) ;
#214892=PRODUCT_DEFINITION_CONTEXT ( 'detailed design', #237440, 'design' ) ;
#214905=DIRECTION ( 'NONE',  ( -0.000000000000000000, -0.9770955615653313941, -0.2128009952263609228 ) ) ;
#214906=DIRECTION ( 'NONE',  ( -0.000000000000000000, 0.9770955615653316162, 0.2128009952263604232 ) ) ;
#214922=CARTESIAN_POINT ( 'NONE',  ( 21.14999999999999858, 6.390846877240206503, -199.6081416912452653 ) ) ;
#214926=AXIS2_PLACEMENT_3D ( 'NONE', #109388, #50683, #149834 ) ;
#214932=CARTESIAN_POINT ( 'NONE',  ( 21.05000000000000071, -4.259020970815407203, -226.0869574510824123 ) ) ;
#214971=DIRECTION ( 'NONE',  ( 1.000000000000000000, 0.000000000000000000, 0.000000000000000000 ) ) ;
#214978=EDGE_LOOP ( 'NONE', ( #245948, #212244, #179198 ) ) ;
#215014=EDGE_LOOP ( 'NONE', ( #136704, #118682, #116018, #26733 ) ) ;
#215055=DIRECTION ( 'NONE',  ( -1.000000000000000000, 0.000000000000000000, 0.000000000000000000 ) ) ;
#215060=ORIENTED_EDGE ( 'NONE', *, *, #16936, .F. ) ;
#215066=CARTESIAN_POINT ( 'NONE',  ( -21.04999999999896687, -1.290533477727345169, -194.8331962964030595 ) ) ;
#215073=AXIS2_PLACEMENT_3D ( 'NONE', #215330, #178817, #159236 ) ;
#215086=FACE_OUTER_BOUND ( 'NONE', #214099, .T. ) ;
#215107=DIRECTION ( 'NONE',  ( 0.000000000000000000, 0.2128009952263604232, -0.9770955615653316162 ) ) ;
#215114=CARTESIAN_POINT ( 'NONE',  ( -21.14999999999999858, -1.489567864901279792, -194.6304332222954372 ) ) ;
#215116=CARTESIAN_POINT ( 'NONE',  ( -20.64999999999999858, -7.176961358819843539, -212.6889627706600834 ) ) ;
#215143=CYLINDRICAL_SURFACE ( 'NONE', #95598, 0.09999999999999939493 ) ;
#215147=CARTESIAN_POINT ( 'NONE',  ( -20.94999999999999929, -10.74476030654554215, -206.4104182790846096 ) ) ;
#215149=ORIENTED_EDGE ( 'NONE', *, *, #40751, .F. ) ;
#215152=CARTESIAN_POINT ( 'NONE',  ( 22.50014994444028105, 11.46291945964638082, -198.4184706950397299 ) ) ;
#215155=CARTESIAN_POINT ( 'NONE',  ( -18.59999999999999787, 15.92646454033039305, -219.3818586450342707 ) ) ;
#215156=DIRECTION ( 'NONE',  ( 1.000000000000000000, -0.000000000000000000, -0.000000000000000000 ) ) ;
#215157=TOROIDAL_SURFACE ( 'NONE', #156924, 3.899999999999999467, 0.1000000000000000056 ) ;
#215167=CARTESIAN_POINT ( 'NONE',  ( 21.04999999999999716, -1.396784380639764622, -194.6548880948980127 ) ) ;
#215195=DIRECTION ( 'NONE',  ( 1.000000000000000000, 0.000000000000000000, 0.000000000000000000 ) ) ;
#215235=EDGE_CURVE ( 'NONE', #65124, #31563, #67486, .T. ) ;
#215242=DIRECTION ( 'NONE',  ( -4.408576920032447355E-17, 0.3427706569149636118, -0.9394191166662961834 ) ) ;
#215261=FACE_OUTER_BOUND ( 'NONE', #89965, .T. ) ;
#215276=TOROIDAL_SURFACE ( 'NONE', #15568, 4.099999999999999645, 0.1000000000000000056 ) ;
#215289=EDGE_CURVE ( 'NONE', #208402, #14866, #186163, .T. ) ;
#215330=CARTESIAN_POINT ( 'NONE',  ( -20.64999999999999858, 2.761092913073515120, -213.6778149113116854 ) ) ;
#215346=AXIS2_PLACEMENT_3D ( 'NONE', #68315, #108719, #248232 ) ;
#215383=ADVANCED_FACE ( 'NONE', ( #33554 ), #83595, .F. ) ;
#215390=DIRECTION ( 'NONE',  ( 0.000000000000000000, 0.2128009952263601179, -0.9770955615653315052 ) ) ;
#215393=VERTEX_POINT ( 'NONE', #251250 ) ;
#215430=CIRCLE ( 'NONE', #61314, 0.09999999999999691080 ) ;
#215438=FACE_OUTER_BOUND ( 'NONE', #251388, .T. ) ;
#215443=CARTESIAN_POINT ( 'NONE',  ( 21.05000000000000071, 6.350467579472245383, -199.7192799711882287 ) ) ;
#215446=CARTESIAN_POINT ( 'NONE',  ( 23.14999999999999858, 7.554435330547283556, -235.6868924355707691 ) ) ;
#215463=CARTESIAN_POINT ( 'NONE',  ( 20.94999999999999574, 10.52493806863738079, -207.3780514093641330 ) ) ;
#215486=ADVANCED_FACE ( 'NONE', ( #39948 ), #196418, .T. ) ;
#215504=AXIS2_PLACEMENT_3D ( 'NONE', #139874, #240290, #180307 ) ;
#215509=CARTESIAN_POINT ( 'NONE',  ( -22.32929514600008503, -1.515937339026276032, -193.5738536982988478 ) ) ;
#215517=CARTESIAN_POINT ( 'NONE',  ( -20.94999999999999929, -4.892732937820632344, -233.2805462221312496 ) ) ;
#215530=DIRECTION ( 'NONE',  ( -0.000000000000000000, 0.2128009952263604232, -0.9770955615653316162 ) ) ;
#215566=CARTESIAN_POINT ( 'NONE',  ( -18.59999999999999787, 4.252251777740764460, -211.8999245327126744 ) ) ;
#215569=DIRECTION ( 'NONE',  ( -0.000000000000000000, 0.9770955615653313941, 0.2128009952263603954 ) ) ;
#215578=ORIENTED_EDGE ( 'NONE', *, *, #193040, .F. ) ;
#215587=CARTESIAN_POINT ( 'NONE',  ( 21.14999999999999503, 11.48087284840413425, -198.4995883060917947 ) ) ;
#215665=DIRECTION ( 'NONE',  ( 1.000000000000000000, 0.000000000000000000, 0.000000000000000000 ) ) ;
#215677=AXIS2_PLACEMENT_3D ( 'NONE', #25960, #105447, #106756 ) ;
#215680=CARTESIAN_POINT ( 'NONE',  ( 21.30000000000002558, 0.8618440306782489957, -204.9572370243411115 ) ) ;
#215694=DIRECTION ( 'NONE',  ( -1.000000000000000000, -0.000000000000000000, -0.000000000000000000 ) ) ;
#215708=ORIENTED_EDGE ( 'NONE', *, *, #237792, .F. ) ;
#215715=ADVANCED_FACE ( 'NONE', ( #253197 ), #95416, .T. ) ;
#215733=EDGE_LOOP ( 'NONE', ( #143400, #37762, #201902, #185490, #30582, #238050, #35707 ) ) ;
#215753=CARTESIAN_POINT ( 'NONE',  ( -18.48179518609380523, -0.7053438610020049682, -242.4901111488185848 ) ) ;
#215798=CARTESIAN_POINT ( 'NONE',  ( 20.84451136049160880, 11.97160813258156331, -206.0623036569039357 ) ) ;
#215809=CARTESIAN_POINT ( 'NONE',  ( -21.52071067811865746, 12.12313021711449323, -220.1078401734146723 ) ) ;
#215814=DIRECTION ( 'NONE',  ( 0.000000000000000000, 0.9770955615653313941, 0.2128009952263606730 ) ) ;
#215821=AXIS2_PLACEMENT_3D ( 'NONE', #158596, #58157, #157315 ) ;
#215855=DIRECTION ( 'NONE',  ( -0.000000000000000000, 0.2128009952263603677, -0.9770955615653313941 ) ) ;
#215897=DIRECTION ( 'NONE',  ( 0.000000000000000000, -0.9964539953858966292, -0.08413937888696132461 ) ) ;
#215980=ADVANCED_FACE ( 'NONE', ( #233281 ), #174621, .F. ) ;
#216001=DIRECTION ( 'NONE',  ( 0.000000000000000000, -0.2128009952263485993, 0.9770955615653341697 ) ) ;
#216006=CARTESIAN_POINT ( 'NONE',  ( -18.59999999999999787, 7.633102355717365839, -241.5185714324494484 ) ) ;
#216048=DIRECTION ( 'NONE',  ( -0.000000000000000000, 0.2128009952263604232, -0.9770955615653316162 ) ) ;
#216057=VERTEX_POINT ( 'NONE', #162711 ) ;
#216068=EDGE_LOOP ( 'NONE', ( #228083, #249352, #182968, #229043 ) ) ;
#216074=DIRECTION ( 'NONE',  ( -0.000000000000000000, 0.9770955615653313941, 0.2128009952263603954 ) ) ;
#216079=AXIS2_PLACEMENT_3D ( 'NONE', #248948, #246373, #131554 ) ;
#216114=DIRECTION ( 'NONE',  ( -1.000000000000000000, 0.000000000000000000, 0.000000000000000000 ) ) ;
#216122=CARTESIAN_POINT ( 'NONE',  ( -21.00448002041627049, 12.93820659955309615, -205.1910717667425104 ) ) ;
#216124=DIRECTION ( 'NONE',  ( 1.000000000000000000, 0.000000000000000000, 0.000000000000000000 ) ) ;
#216136=CARTESIAN_POINT ( 'NONE',  ( 21.05000000000000071, -11.38316329222461576, -203.4791315943886048 ) ) ;
#216153=AXIS2_PLACEMENT_3D ( 'NONE', #218166, #138621, #60392 ) ;
#216155=CARTESIAN_POINT ( 'NONE',  ( 21.05000000000000071, 6.093673009692411213, -199.5727803633481301 ) ) ;
#216213=DIRECTION ( 'NONE',  ( 0.000000000000000000, 0.2128009952264288962, -0.9770955615653166282 ) ) ;
#216235=ORIENTED_EDGE ( 'NONE', *, *, #146764, .T. ) ;
#216251=DIRECTION ( 'NONE',  ( -1.000000000000000000, -8.034189347746081825E-16, 2.566115377699053685E-16 ) ) ;
#216252=DIRECTION ( 'NONE',  ( 0.000000000000000000, 0.2128009952263630322, -0.9770955615653309501 ) ) ;
#216265=ADVANCED_FACE ( 'NONE', ( #85376 ), #164953, .F. ) ;
#216280=DIRECTION ( 'NONE',  ( 1.000000000000000000, -0.000000000000000000, -0.000000000000000000 ) ) ;
#216285=VECTOR ( 'NONE', #85765, 1000.000000000000000 ) ;
#216317=ORIENTED_EDGE ( 'NONE', *, *, #114006, .T. ) ;
#216318=ADVANCED_FACE ( 'NONE', ( #104939 ), #192805, .T. ) ;
#216354=ORIENTED_EDGE ( 'NONE', *, *, #183323, .F. ) ;
#216429=CARTESIAN_POINT ( 'NONE',  ( 22.49999999999999645, -2.434660534977811430, -189.6066352242696382 ) ) ;
#216479=ADVANCED_FACE ( 'NONE', ( #248345 ), #166274, .F. ) ;
#216486=DIRECTION ( 'NONE',  ( 1.000000000000000000, 0.000000000000000000, 0.000000000000000000 ) ) ;
#216525=CARTESIAN_POINT ( 'NONE',  ( 23.14999999999999858, 9.863005973831429074, -220.4411654715779321 ) ) ;
#216527=CARTESIAN_POINT ( 'NONE',  ( -22.47071067811865319, 1.148907358139439339E-11, -201.0000000000015064 ) ) ;
#216552=CARTESIAN_POINT ( 'NONE',  ( 21.98333005346336577, -1.569210568885920809, -193.7948237253318382 ) ) ;
#216566=ORIENTED_EDGE ( 'NONE', *, *, #215289, .T. ) ;
#216576=AXIS2_PLACEMENT_3D ( 'NONE', #56954, #216048, #37446 ) ;
#216609=CARTESIAN_POINT ( 'NONE',  ( -20.94999999999999929, 14.90151243843701856, -203.3975529985363551 ) ) ;
#216611=EDGE_CURVE ( 'NONE', #164130, #59550, #234683, .T. ) ;
#216660=CARTESIAN_POINT ( 'NONE',  ( 21.05000000000000071, 3.017719325445665568, -208.5164861827997242 ) ) ;
#216677=EDGE_CURVE ( 'NONE', #190519, #75640, #109585, .T. ) ;
#216679=LINE ( 'NONE', #156741, #116585 ) ;
#216689=CARTESIAN_POINT ( 'NONE',  ( 18.49999999999998934, 8.531609279343539853, -209.3937462695851366 ) ) ;
#216718=CARTESIAN_POINT ( 'NONE',  ( 18.39999999999999858, -7.817436562502981801, -209.8389866834999395 ) ) ;
#216730=DIRECTION ( 'NONE',  ( 4.377807931758638789E-15, 0.04908394489122119841, 0.9987946567507836049 ) ) ;
#216765=CARTESIAN_POINT ( 'NONE',  ( -18.43707690579160996, -0.9152171842607026431, -242.2974985173727021 ) ) ;
#216769=CARTESIAN_POINT ( 'NONE',  ( -22.50000000000000000, -1.560176095955062348, -193.3663837337744837 ) ) ;
#216774=ORIENTED_EDGE ( 'NONE', *, *, #186908, .T. ) ;
#216785=CYLINDRICAL_SURFACE ( 'NONE', #180466, 0.09999999999999810429 ) ;
#216810=DIRECTION ( 'NONE',  ( -1.000000000000000000, -2.885090398161910739E-16, -6.283419270304611573E-17 ) ) ;
#216834=ORIENTED_EDGE ( 'NONE', *, *, #109751, .T. ) ;
#216853=CIRCLE ( 'NONE', #212777, 12.87499999999999822 ) ;
#216854=DIRECTION ( 'NONE',  ( -1.000000000000000000, 0.000000000000000000, 0.000000000000000000 ) ) ;
#216865=CARTESIAN_POINT ( 'NONE',  ( 18.49999999999999645, 7.476371755685454090, -241.7308184205399471 ) ) ;
#216881=EDGE_CURVE ( 'NONE', #121414, #181313, #93192, .T. ) ;
#216894=AXIS2_PLACEMENT_3D ( 'NONE', #232384, #156709, #131973 ) ;
#216917=ORIENTED_EDGE ( 'NONE', *, *, #165292, .F. ) ;
#216966=FACE_OUTER_BOUND ( 'NONE', #1675, .T. ) ;
#216981=DIRECTION ( 'NONE',  ( 4.408576920032446123E-17, -0.3427706569149635007, 0.9394191166662961834 ) ) ;
#216992=ORIENTED_EDGE ( 'NONE', *, *, #145300, .F. ) ;
#217006=AXIS2_PLACEMENT_3D ( 'NONE', #37618, #234506, #155007 ) ;
#217033=CARTESIAN_POINT ( 'NONE',  ( -18.47130263965438601, -0.7031555602515183745, -242.2784977795686530 ) ) ;
#217041=DIRECTION ( 'NONE',  ( 0.000000000000000000, -0.9770955615653316162, -0.2128009952263604232 ) ) ;
#217051=LINE ( 'NONE', #18867, #121207 ) ;
#217055=FACE_OUTER_BOUND ( 'NONE', #76685, .T. ) ;
#217074=LINE ( 'NONE', #1876, #253526 ) ;
#217078=CARTESIAN_POINT ( 'NONE',  ( 20.97217846901851956, 10.48122442794478637, -207.4178090057411339 ) ) ;
#217079=AXIS2_PLACEMENT_3D ( 'NONE', #227154, #64237, #5522 ) ;
#217089=ADVANCED_FACE ( 'NONE', ( #106590 ), #24535, .T. ) ;
#217099=AXIS2_PLACEMENT_3D ( 'NONE', #171865, #231814, #173161 ) ;
#217106=DIRECTION ( 'NONE',  ( -1.000000000000000000, -0.000000000000000000, -0.000000000000000000 ) ) ;
#217107=DIRECTION ( 'NONE',  ( 0.000000000000000000, 0.2128009952263605065, -0.9770955615653315052 ) ) ;
#217134=ORIENTED_EDGE ( 'NONE', *, *, #204368, .T. ) ;
#217137=DIRECTION ( 'NONE',  ( 0.000000000000000000, 0.2128009952263604232, -0.9770955615653316162 ) ) ;
#217162=EDGE_CURVE ( 'NONE', #38009, #41827, #101551, .T. ) ;
#217168=CARTESIAN_POINT ( 'NONE',  ( -21.00023020733502221, -1.359983335743154331, -194.7555100259054086 ) ) ;
#217241=DIRECTION ( 'NONE',  ( 0.000000000000000000, 0.2128009952263678062, -0.9770955615653298398 ) ) ;
#217242=CIRCLE ( 'NONE', #134053, 0.9750000000000036415 ) ;
#217250=CARTESIAN_POINT ( 'NONE',  ( -21.44999999999999929, 11.70367352607683564, -220.1991933683510467 ) ) ;
#217263=ORIENTED_EDGE ( 'NONE', *, *, #197644, .T. ) ;
#217280=VECTOR ( 'NONE', #235122, 1000.000000000000000 ) ;
#217301=DIRECTION ( 'NONE',  ( 0.000000000000000000, 0.2128009952263604510, -0.9770955615653315052 ) ) ;
#217319=DIRECTION ( 'NONE',  ( 0.000000000000000000, 0.9770955615653548199, 0.2128009952262535920 ) ) ;
#217348=CIRCLE ( 'NONE', #42393, 1.899999999999997913 ) ;
#217375=VECTOR ( 'NONE', #83994, 1000.000000000000114 ) ;
#217380=VERTEX_POINT ( 'NONE', #15234 ) ;
#217450=ORIENTED_EDGE ( 'NONE', *, *, #229017, .F. ) ;
#217473=ORIENTED_EDGE ( 'NONE', *, *, #166916, .F. ) ;
#217496=CARTESIAN_POINT ( 'NONE',  ( -20.64999999999999858, -6.488386256076841718, -212.2361678873109554 ) ) ;
#217520=TOROIDAL_SURFACE ( 'NONE', #51094, 12.97499999999999787, 0.1000000000000000056 ) ;
#217539=VERTEX_POINT ( 'NONE', #131004 ) ;
#217577=EDGE_LOOP ( 'NONE', ( #115210, #174991, #243680, #179666, #75844, #227108, #173378, #53012, #206349, #183500, #1860, #78980 ) ) ;
#217583=DIRECTION ( 'NONE',  ( -1.000000000000000000, 0.000000000000000000, 0.000000000000000000 ) ) ;
#217588=DIRECTION ( 'NONE',  ( 0.000000000000000000, 0.08413937888704772772, -0.9964539953858893018 ) ) ;
#217605=DIRECTION ( 'NONE',  ( 0.000000000000000000, 0.2128009952263604232, -0.9770955615653316162 ) ) ;
#217652=AXIS2_PLACEMENT_3D ( 'NONE', #251040, #16321, #116676 ) ;
#217680=ORIENTED_EDGE ( 'NONE', *, *, #221798, .F. ) ;
#217683=EDGE_CURVE ( 'NONE', #253923, #76080, #118540, .T. ) ;
#217694=AXIS2_PLACEMENT_3D ( 'NONE', #168184, #9061, #127740 ) ;
#217713=DIRECTION ( 'NONE',  ( -1.000000000000000000, -0.000000000000000000, -0.000000000000000000 ) ) ;
#217776=CYLINDRICAL_SURFACE ( 'NONE', #244134, 0.09999999999999156786 ) ;
#217778=EDGE_LOOP ( 'NONE', ( #142029, #78075, #182576, #71060 ) ) ;
#217829=DIRECTION ( 'NONE',  ( 1.000000000000000000, 0.000000000000000000, 0.000000000000000000 ) ) ;
#217832=EDGE_LOOP ( 'NONE', ( #199324, #41867, #8143, #184904 ) ) ;
#217835=TOROIDAL_SURFACE ( 'NONE', #51228, 0.4000000000000003553, 0.1000000000000000056 ) ;
#217838=EDGE_CURVE ( 'NONE', #102301, #145985, #159650, .T. ) ;
#217850=ORIENTED_EDGE ( 'NONE', *, *, #152647, .T. ) ;
#217857=DIRECTION ( 'NONE',  ( -1.000000000000000000, 0.000000000000000000, 0.000000000000000000 ) ) ;
#217863=DIRECTION ( 'NONE',  ( -6.938893903907222856E-15, 0.9770955615653313941, 0.2128009952263603677 ) ) ;
#217881=ORIENTED_EDGE ( 'NONE', *, *, #144461, .F. ) ;
#217921=AXIS2_PLACEMENT_3D ( 'NONE', #195422, #114582, #153762 ) ;
#217936=CARTESIAN_POINT ( 'NONE',  ( 20.94999999999999929, -4.161311414658873886, -226.0656773515597706 ) ) ;
#217959=DIRECTION ( 'NONE',  ( 0.000000000000000000, -0.2128009952263603677, 0.9770955615653313941 ) ) ;
#217981=DIRECTION ( 'NONE',  ( 1.000000000000000000, 3.190570557967288949E-16, 6.948722487160392945E-17 ) ) ;
#217997=AXIS2_PLACEMENT_3D ( 'NONE', #94398, #154426, #77395 ) ;
#218072=EDGE_LOOP ( 'NONE', ( #51285, #145921, #128937, #149483 ) ) ;
#218076=CARTESIAN_POINT ( 'NONE',  ( -21.05000000000000071, 7.128833340094563376, -233.7327013124401276 ) ) ;
#218085=EDGE_CURVE ( 'NONE', #93777, #118692, #222153, .T. ) ;
#218113=EDGE_CURVE ( 'NONE', #202021, #97694, #214097, .T. ) ;
#218118=CARTESIAN_POINT ( 'NONE',  ( 18.59999999999999076, 4.252251777740764460, -211.8999245327126744 ) ) ;
#218121=DIRECTION ( 'NONE',  ( 0.000000000000000000, 0.9770955615653543758, 0.2128009952262553683 ) ) ;
#218166=CARTESIAN_POINT ( 'NONE',  ( 18.59999999999999787, 7.783179459866048866, -245.3643104511423019 ) ) ;
#218188=AXIS2_PLACEMENT_3D ( 'NONE', #101726, #236132, #57475 ) ;
#218192=LINE ( 'NONE', #34480, #79284 ) ;
#218201=EDGE_CURVE ( 'NONE', #58187, #248715, #114991, .T. ) ;
#218226=VERTEX_POINT ( 'NONE', #251933 ) ;
#218245=EDGE_CURVE ( 'NONE', #231604, #14866, #72352, .T. ) ;
#218267=CIRCLE ( 'NONE', #189075, 0.1000000000000055844 ) ;
#218271=EDGE_LOOP ( 'NONE', ( #30595, #85464, #119712, #52592 ) ) ;
#218292=DIRECTION ( 'NONE',  ( 0.000000000000000000, 0.9770955615653310611, 0.2128009952263620608 ) ) ;
#218306=CARTESIAN_POINT ( 'NONE',  ( 20.04142135623730070, 16.72641738073392403, -222.5849938986771974 ) ) ;
#218312=CARTESIAN_POINT ( 'NONE',  ( -18.43459694179556863, -0.7398119410654188099, -242.2185250903025349 ) ) ;
#218335=CARTESIAN_POINT ( 'NONE',  ( -18.59999999999999787, 7.783179459866048866, -245.3643104511423303 ) ) ;
#218348=AXIS2_PLACEMENT_3D ( 'NONE', #74290, #131660, #175952 ) ;
#218349=CYLINDRICAL_SURFACE ( 'NONE', #84281, 0.1000000000000055705 ) ;
#218364=TOROIDAL_SURFACE ( 'NONE', #105937, 0.2000000000000000111, 0.1000000000000000056 ) ;
#218461=EDGE_CURVE ( 'NONE', #234608, #131461, #30858, .T. ) ;
#218469=VERTEX_POINT ( 'NONE', #132650 ) ;
#218477=CARTESIAN_POINT ( 'NONE',  ( -20.54999999999999716, 6.268811756569107274, -220.3853799378769622 ) ) ;
#218483=CARTESIAN_POINT ( 'NONE',  ( 21.93340585972025636, 7.156391548293796312, -199.4414142243540766 ) ) ;
#218538=ORIENTED_EDGE ( 'NONE', *, *, #60314, .F. ) ;
#218551=EDGE_LOOP ( 'NONE', ( #207831, #60073, #143084, #203873 ) ) ;
#218570=ORIENTED_EDGE ( 'NONE', *, *, #32436, .F. ) ;
#218598=AXIS2_PLACEMENT_3D ( 'NONE', #5316, #127874, #228263 ) ;
#218621=EDGE_CURVE ( 'NONE', #31271, #211413, #193344, .T. ) ;
#218681=CARTESIAN_POINT ( 'NONE',  ( -20.95613430942382749, 12.94008388437452162, -205.1996914945986248 ) ) ;
#218704=CARTESIAN_POINT ( 'NONE',  ( 20.94999999999999929, 17.06838326776701109, -224.6250846885016870 ) ) ;
#218760=DIRECTION ( 'NONE',  ( 1.000000000000000000, 2.885090398161910739E-16, 6.283419270304611573E-17 ) ) ;
#218767=ADVANCED_FACE ( 'NONE', ( #231450 ), #105994, .T. ) ;
#218865=SPHERICAL_SURFACE ( 'NONE', #136215, 0.1000000000000000056 ) ;
#218875=DIRECTION ( 'NONE',  ( 1.000000000000000000, 0.000000000000000000, 0.000000000000000000 ) ) ;
#218895=DIRECTION ( 'NONE',  ( 0.000000000000000000, 0.2128009952263601179, -0.9770955615653315052 ) ) ;
#218899=DIRECTION ( 'NONE',  ( -1.000000000000000000, 0.000000000000000000, 0.000000000000000000 ) ) ;
#218901=LINE ( 'NONE', #100223, #11595 ) ;
#218905=CARTESIAN_POINT ( 'NONE',  ( -20.94999999999999929, 7.128833340094563376, -233.7327013124401276 ) ) ;
#218908=CIRCLE ( 'NONE', #94011, 11.65000000000001457 ) ;
#218934=FACE_OUTER_BOUND ( 'NONE', #58503, .T. ) ;
#218935=CARTESIAN_POINT ( 'NONE',  ( 18.59999999999998366, 7.128833340094563376, -233.7327013124401276 ) ) ;
#218945=ORIENTED_EDGE ( 'NONE', *, *, #109583, .F. ) ;
#218963=ADVANCED_FACE ( 'NONE', ( #184290 ), #21401, .T. ) ;
#218969=EDGE_CURVE ( 'NONE', #2619, #77581, #124333, .T. ) ;
#218995=CYLINDRICAL_SURFACE ( 'NONE', #221284, 2.000000000000003109 ) ;
#219064=CARTESIAN_POINT ( 'NONE',  ( -23.15000000000000213, 7.128833340094563376, -233.7327013124401276 ) ) ;
#219069=AXIS2_PLACEMENT_3D ( 'NONE', #105618, #146048, #67803 ) ;
#219103=CARTESIAN_POINT ( 'NONE',  ( 19.81427058490547211, 16.66812670693539289, -222.7000331208559203 ) ) ;
#219111=CARTESIAN_POINT ( 'NONE',  ( -23.15000000000000213, 1.148907358139439339E-11, -201.0000000000015064 ) ) ;
#219112=ORIENTED_EDGE ( 'NONE', *, *, #212986, .F. ) ;
#219143=ORIENTED_EDGE ( 'NONE', *, *, #224634, .F. ) ;
#219197=AXIS2_PLACEMENT_3D ( 'NONE', #226281, #206745, #177905 ) ;
#219228=DIRECTION ( 'NONE',  ( 0.000000000000000000, 0.2128009952263485993, -0.9770955615653341697 ) ) ;
#219230=LINE ( 'NONE', #217936, #232532 ) ;
#219243=EDGE_CURVE ( 'NONE', #154288, #214314, #238020, .T. ) ;
#219245=EDGE_CURVE ( 'NONE', #229005, #75163, #68796, .T. ) ;
#219268=EDGE_CURVE ( 'NONE', #139739, #32735, #214524, .T. ) ;
#219271=( BOUNDED_CURVE ( )  B_SPLINE_CURVE ( 3, ( #150395, #147821, #30447, #229916 ),
 .UNSPECIFIED., .F., .F. ) 
 B_SPLINE_CURVE_WITH_KNOTS ( ( 4, 4 ),
 ( 4.712388980384689674, 6.283185307179586232 ),
 .UNSPECIFIED. ) 
 CURVE ( )  GEOMETRIC_REPRESENTATION_ITEM ( )  RATIONAL_B_SPLINE_CURVE ( ( 1.000000000000000000, 0.8047378541243649375, 0.8047378541243649375, 1.000000000000000000 ) ) 
 REPRESENTATION_ITEM ( '' )  );
#219275=CYLINDRICAL_SURFACE ( 'NONE', #192713, 0.09999999999999939493 ) ;
#219276=CARTESIAN_POINT ( 'NONE',  ( 18.59999999999999432, 0.5876173420563333138, -209.1618981382189588 ) ) ;
#219296=CARTESIAN_POINT ( 'NONE',  ( -20.07928932188135107, 13.53153662663944523, -219.8011042742668337 ) ) ;
#219348=DIRECTION ( 'NONE',  ( 1.000000000000000000, 0.000000000000000000, 0.000000000000000000 ) ) ;
#219370=FACE_OUTER_BOUND ( 'NONE', #65680, .T. ) ;
#219375=FACE_OUTER_BOUND ( 'NONE', #242682, .T. ) ;
#219411=CARTESIAN_POINT ( 'NONE',  ( -21.05000000000000071, -11.38316329222462464, -203.4791315943886048 ) ) ;
#219456=AXIS2_PLACEMENT_3D ( 'NONE', #127430, #167869, #229102 ) ;
#219462=EDGE_CURVE ( 'NONE', #6661, #91518, #85506, .T. ) ;
#219463=CARTESIAN_POINT ( 'NONE',  ( 22.39999999999999503, -2.598867842139048090, -189.5410128746472083 ) ) ;
#219487=VERTEX_POINT ( 'NONE', #148592 ) ;
#219574=VERTEX_POINT ( 'NONE', #166746 ) ;
#219599=CARTESIAN_POINT ( 'NONE',  ( 20.94999999999999929, 8.531609279343539853, -209.3937462695851366 ) ) ;
#219613=CIRCLE ( 'NONE', #215346, 11.69999999999999574 ) ;
#219615=EDGE_CURVE ( 'NONE', #22587, #216057, #27234, .T. ) ;
#219637=DIRECTION ( 'NONE',  ( -0.000000000000000000, -0.9770955615653316162, -0.2128009952263604232 ) ) ;
#219703=EDGE_CURVE ( 'NONE', #191212, #196725, #185504, .T. ) ;
#219713=CARTESIAN_POINT ( 'NONE',  ( -22.50000000000000000, 11.36547683798380959, -198.4402660583092199 ) ) ;
#219758=DIRECTION ( 'NONE',  ( -0.000000000000000000, -0.2128009952263604232, 0.9770955615653316162 ) ) ;
#219759=EDGE_LOOP ( 'NONE', ( #158870, #216774, #99948, #41870 ) ) ;
#219774=EDGE_CURVE ( 'NONE', #202021, #38916, #89619, .T. ) ;
#219783=ADVANCED_FACE ( 'NONE', ( #55699 ), #156159, .T. ) ;
#219801=DIRECTION ( 'NONE',  ( 0.000000000000000000, -0.2128009952263485993, 0.9770955615653341697 ) ) ;
#219805=AXIS2_PLACEMENT_3D ( 'NONE', #192483, #175508, #16434 ) ;
#219824=FACE_OUTER_BOUND ( 'NONE', #157338, .T. ) ;
#219828=CIRCLE ( 'NONE', #19946, 0.1000000000000055844 ) ;
#219847=AXIS2_PLACEMENT_3D ( 'NONE', #169968, #188204, #228630 ) ;
#219858=DIRECTION ( 'NONE',  ( 0.000000000000000000, 0.9770955615653316162, 0.2128009952263604232 ) ) ;
#219886=CARTESIAN_POINT ( 'NONE',  ( -18.58671080940900566, -7.675445184013033106, -209.9627843819515931 ) ) ;
#219895=AXIS2_PLACEMENT_3D ( 'NONE', #72349, #127174, #131016 ) ;
#219897=EDGE_CURVE ( 'NONE', #162084, #130647, #75343, .T. ) ;
#219949=CARTESIAN_POINT ( 'NONE',  ( 20.85000000000000142, -4.990442493977157667, -233.3018263216538628 ) ) ;
#219956=EDGE_CURVE ( 'NONE', #98586, #182409, #19076, .T. ) ;
#219957=CARTESIAN_POINT ( 'NONE',  ( 21.05000000000000071, 6.412126976762841046, -199.7058512474018244 ) ) ;
#219964=ORIENTED_EDGE ( 'NONE', *, *, #4536, .T. ) ;
#219975=AXIS2_PLACEMENT_3D ( 'NONE', #46702, #83246, #126243 ) ;
#219992=ADVANCED_FACE ( 'NONE', ( #145213 ), #245616, .F. ) ;
#220009=ADVANCED_FACE ( 'NONE', ( #228639 ), #52390, .T. ) ;
#220021=CIRCLE ( 'NONE', #45233, 11.70000000000000284 ) ;
#220028=VECTOR ( 'NONE', #22456, 1000.000000000000227 ) ;
#220031=UNCERTAINTY_MEASURE_WITH_UNIT (LENGTH_MEASURE( 1.000000000000000082E-05 ), #248138, 'distance_accuracy_value', 'NONE');
#220060=ORIENTED_EDGE ( 'NONE', *, *, #111253, .T. ) ;
#220069=DIRECTION ( 'NONE',  ( 0.000000000000000000, -0.3427706569149662763, 0.9394191166662954062 ) ) ;
#220087=ORIENTED_EDGE ( 'NONE', *, *, #920, .T. ) ;
#220090=ORIENTED_EDGE ( 'NONE', *, *, #174829, .F. ) ;
#220093=EDGE_CURVE ( 'NONE', #248011, #235587, #147807, .T. ) ;
#220121=EDGE_CURVE ( 'NONE', #182231, #256176, #64867, .T. ) ;
#220127=CARTESIAN_POINT ( 'NONE',  ( 21.05000000000000071, 8.013878543493270001, -211.9507248933737458 ) ) ;
#220128=EDGE_CURVE ( 'NONE', #179165, #120381, #20328, .T. ) ;
#220140=VERTEX_POINT ( 'NONE', #92949 ) ;
#220171=AXIS2_PLACEMENT_3D ( 'NONE', #202987, #3494, #120920 ) ;
#220176=EDGE_LOOP ( 'NONE', ( #172420, #219112, #63466, #186305 ) ) ;
#220184=CYLINDRICAL_SURFACE ( 'NONE', #106522, 0.09999999999999939493 ) ;
#220197=CIRCLE ( 'NONE', #216079, 0.1000000000000035305 ) ;
#220204=CARTESIAN_POINT ( 'NONE',  ( -21.14999999999999858, 1.148907358139439339E-11, -201.0000000000015064 ) ) ;
#220219=AXIS2_PLACEMENT_3D ( 'NONE', #25685, #62242, #239600 ) ;
#220252=AXIS2_PLACEMENT_3D ( 'NONE', #174168, #211980, #175432 ) ;
#220254=ORIENTED_EDGE ( 'NONE', *, *, #20280, .T. ) ;
#220267=DIRECTION ( 'NONE',  ( 1.000000000000000000, 0.000000000000000000, 0.000000000000000000 ) ) ;
#220272=AXIS2_PLACEMENT_3D ( 'NONE', #103879, #119637, #163889 ) ;
#220276=EDGE_CURVE ( 'NONE', #159242, #187404, #57660, .T. ) ;
#220277=EDGE_LOOP ( 'NONE', ( #156879, #10900, #143813, #255334 ) ) ;
#220282=CARTESIAN_POINT ( 'NONE',  ( 18.59999999999999432, 0.6770221356676882074, -212.8807256103264649 ) ) ;
#220308=DIRECTION ( 'NONE',  ( 0.000000000000000000, 0.2128009952263485993, -0.9770955615653341697 ) ) ;
#220328=ORIENTED_EDGE ( 'NONE', *, *, #148032, .T. ) ;
#220334=CARTESIAN_POINT ( 'NONE',  ( -21.14999999999999503, 12.95327426846188779, -205.2602563699350355 ) ) ;
#220365=DIRECTION ( 'NONE',  ( 3.265361837132812600E-16, -0.9770955615653313941, -0.2128009952263603677 ) ) ;
#220378=AXIS2_PLACEMENT_3D ( 'NONE', #232712, #9790, #172764 ) ;
#220387=CARTESIAN_POINT ( 'NONE',  ( 23.15000000000000213, -4.914013037343258894, -233.1828366659746905 ) ) ;
#220388=AXIS2_PLACEMENT_3D ( 'NONE', #246904, #207823, #168718 ) ;
#220406=VERTEX_POINT ( 'NONE', #187910 ) ;
#220413=TOROIDAL_SURFACE ( 'NONE', #132922, 11.70000000000000107, 0.1000000000000000056 ) ;
#220428=CARTESIAN_POINT ( 'NONE',  ( 22.45305468355010703, -2.598867842140088591, -189.5410128746470946 ) ) ;
#220488=ORIENTED_EDGE ( 'NONE', *, *, #72104, .T. ) ;
#220507=ORIENTED_EDGE ( 'NONE', *, *, #68782, .T. ) ;
#220524=CARTESIAN_POINT ( 'NONE',  ( 18.59999999999999076, 14.90151243843702566, -203.3975529985363551 ) ) ;
#220557=DIRECTION ( 'NONE',  ( 0.000000000000000000, 0.2128009952263602844, -0.9770955615653315052 ) ) ;
#220580=CIRCLE ( 'NONE', #237334, 0.09999999999999939493 ) ;
#220590=ORIENTED_EDGE ( 'NONE', *, *, #6719, .F. ) ;
#220592=DIRECTION ( 'NONE',  ( -0.000000000000000000, 0.9770955615653313941, 0.2128009952263603954 ) ) ;
#220653=CARTESIAN_POINT ( 'NONE',  ( -23.15000000000000213, -11.88052908492542770, -191.5620167057819287 ) ) ;
#220687=ORIENTED_EDGE ( 'NONE', *, *, #250758, .F. ) ;
#220695=DIRECTION ( 'NONE',  ( -1.000000000000000000, -2.885090398161910739E-16, -6.283419270304611573E-17 ) ) ;
#220698=EDGE_CURVE ( 'NONE', #181313, #91518, #11263, .T. ) ;
#220714=FACE_OUTER_BOUND ( 'NONE', #64610, .T. ) ;
#220719=TOROIDAL_SURFACE ( 'NONE', #124858, 0.2000000000000000111, 0.1000000000000000056 ) ;
#220733=DIRECTION ( 'NONE',  ( 0.000000000000000000, 0.2211802418851293583, -0.9752329468386697897 ) ) ;
#220736=ADVANCED_FACE ( 'NONE', ( #203311 ), #185024, .F. ) ;
#220740=ORIENTED_EDGE ( 'NONE', *, *, #239586, .T. ) ;
#220753=VERTEX_POINT ( 'NONE', #63797 ) ;
#220773=EDGE_CURVE ( 'NONE', #103755, #20245, #244995, .T. ) ;
#220774=ORIENTED_EDGE ( 'NONE', *, *, #109751, .F. ) ;
#220808=FACE_OUTER_BOUND ( 'NONE', #227157, .T. ) ;
#220810=EDGE_CURVE ( 'NONE', #127836, #231419, #256735, .T. ) ;
#220833=ORIENTED_EDGE ( 'NONE', *, *, #63763, .T. ) ;
#220840=TOROIDAL_SURFACE ( 'NONE', #95930, 0.2000000000000000111, 0.1000000000000000056 ) ;
#220858=EDGE_LOOP ( 'NONE', ( #64318, #126787, #230811, #206246 ) ) ;
#220859=ADVANCED_FACE ( 'NONE', ( #183749 ), #42954, .T. ) ;
#220864=CARTESIAN_POINT ( 'NONE',  ( -23.15000000000000213, 1.148907358139439339E-11, -201.0000000000015064 ) ) ;
#220865=ORIENTED_EDGE ( 'NONE', *, *, #165751, .F. ) ;
#220911=AXIS2_PLACEMENT_3D ( 'NONE', #65365, #82331, #6670 ) ;
#220920=DIRECTION ( 'NONE',  ( -1.000000000000000000, -2.885090398161910739E-16, -6.283419270304611573E-17 ) ) ;
#220929=CARTESIAN_POINT ( 'NONE',  ( 21.07016717457010913, -1.345102501103334403, -194.8238367621760574 ) ) ;
#220937=CARTESIAN_POINT ( 'NONE',  ( 20.97250901189795158, 12.01224122581901277, -206.2280749500426111 ) ) ;
#220940=B_SPLINE_CURVE_WITH_KNOTS ( 'NONE', 3,
 ( #74034, #154845, #113124, #150972, #34907, #170588, #14040, #153587, #191412, #195257, #51841, #132699, #11472, #96107, #92264, #250070, #71453, #255142, #230512 ),
 .UNSPECIFIED., .F., .F.,
 ( 4, 3, 3, 3, 3, 3, 4 ),
 ( 1.387778780781445676E-17, 2.646747978908895087E-05, 5.271166642129234721E-05, 9.008788829885287059E-05, 0.0001426648776561089771, 0.0001897378458659771045, 0.0001917382627806340850 ),
 .UNSPECIFIED. ) ;
#220950=ORIENTED_EDGE ( 'NONE', *, *, #66202, .T. ) ;
#220985=AXIS2_PLACEMENT_3D ( 'NONE', #210859, #209578, #10089 ) ;
#220991=ORIENTED_EDGE ( 'NONE', *, *, #75850, .T. ) ;
#221034=CARTESIAN_POINT ( 'NONE',  ( -20.94999999999999929, -10.56629024491939894, -206.4738935375009703 ) ) ;
#221043=EDGE_CURVE ( 'NONE', #148888, #169963, #77885, .T. ) ;
#221057=ADVANCED_FACE ( 'NONE', ( #100008, #57033 ), #36247, .F. ) ;
#221067=VERTEX_POINT ( 'NONE', #177042 ) ;
#221097=FACE_OUTER_BOUND ( 'NONE', #110414, .T. ) ;
#221157=EDGE_CURVE ( 'NONE', #236966, #81210, #65424, .T. ) ;
#221163=CIRCLE ( 'NONE', #54583, 11.65000000000001457 ) ;
#221181=ORIENTED_EDGE ( 'NONE', *, *, #89165, .F. ) ;
#221187=DIRECTION ( 'NONE',  ( 0.000000000000000000, 0.2128009952263604510, -0.9770955615653315052 ) ) ;
#221202=ORIENTED_EDGE ( 'NONE', *, *, #187735, .F. ) ;
#221226=CARTESIAN_POINT ( 'NONE',  ( 22.49999999999999645, 11.36146383068193622, -198.4232501820394816 ) ) ;
#221234=CARTESIAN_POINT ( 'NONE',  ( 20.85000000106584750, 17.15319076756267691, -224.5445635972164951 ) ) ;
#221284=AXIS2_PLACEMENT_3D ( 'NONE', #80754, #40407, #122486 ) ;
#221286=DIRECTION ( 'NONE',  ( -4.408576920032447355E-17, -0.07893460099012300502, 0.9968797965484754720 ) ) ;
#221301=FACE_OUTER_BOUND ( 'NONE', #150299, .T. ) ;
#221364=ORIENTED_EDGE ( 'NONE', *, *, #80276, .F. ) ;
#221372=EDGE_CURVE ( 'NONE', #20245, #39697, #16372, .T. ) ;
#221404=ORIENTED_EDGE ( 'NONE', *, *, #21809, .F. ) ;
#221414=ORIENTED_EDGE ( 'NONE', *, *, #36878, .F. ) ;
#221425=CARTESIAN_POINT ( 'NONE',  ( -21.05000000000000071, -4.756823075239758225, -233.1486023682345490 ) ) ;
#221450=CARTESIAN_POINT ( 'NONE',  ( 23.14999999999999503, 8.980461154494404852, -187.0187154576991304 ) ) ;
#221472=ADVANCED_FACE ( 'NONE', ( #178013 ), #119309, .F. ) ;
#221493=CYLINDRICAL_SURFACE ( 'NONE', #83317, 0.09999999999999939493 ) ;
#221506=CARTESIAN_POINT ( 'NONE',  ( -23.15000000000000213, 6.396492353704923417, -220.9716372748161746 ) ) ;
#221525=CARTESIAN_POINT ( 'NONE',  ( -23.25000000000000000, 6.396492353704923417, -220.9716372748161746 ) ) ;
#221528=EDGE_CURVE ( 'NONE', #252116, #19033, #74030, .T. ) ;
#221549=EDGE_LOOP ( 'NONE', ( #51943, #204950, #218945, #138528 ) ) ;
#221556=EDGE_CURVE ( 'NONE', #74308, #142228, #100969, .T. ) ;
#221571=FACE_OUTER_BOUND ( 'NONE', #207784, .T. ) ;
#221581=EDGE_CURVE ( 'NONE', #247713, #103565, #82707, .T. ) ;
#221613=ORIENTED_EDGE ( 'NONE', *, *, #222967, .F. ) ;
#221653=FACE_OUTER_BOUND ( 'NONE', #239677, .T. ) ;
#221661=ORIENTED_EDGE ( 'NONE', *, *, #175938, .T. ) ;
#221664=LINE ( 'NONE', #222954, #177749 ) ;
#221667=FACE_OUTER_BOUND ( 'NONE', #177067, .T. ) ;
#221701=ORIENTED_EDGE ( 'NONE', *, *, #102941, .F. ) ;
#221713=DIRECTION ( 'NONE',  ( 0.000000000000000000, 0.2128009952263604787, -0.9770955615653313941 ) ) ;
#221719=ORIENTED_EDGE ( 'NONE', *, *, #247269, .T. ) ;
#221724=ORIENTED_EDGE ( 'NONE', *, *, #33728, .T. ) ;
#221748=ORIENTED_EDGE ( 'NONE', *, *, #216677, .T. ) ;
#221757=ORIENTED_EDGE ( 'NONE', *, *, #202196, .T. ) ;
#221798=EDGE_CURVE ( 'NONE', #169080, #147215, #58676, .T. ) ;
#221807=CARTESIAN_POINT ( 'NONE',  ( 21.05000000000000071, 11.77895973109482419, -206.1023438919106070 ) ) ;
#221823=DIRECTION ( 'NONE',  ( 0.000000000000000000, -0.2128009952263604510, 0.9770955615653315052 ) ) ;
#221880=EDGE_CURVE ( 'NONE', #199490, #55232, #211548, .T. ) ;
#221887=LINE ( 'NONE', #161966, #140938 ) ;
#221918=ORIENTED_EDGE ( 'NONE', *, *, #195964, .F. ) ;
#221928=AXIS2_PLACEMENT_3D ( 'NONE', #105879, #239321, #165908 ) ;
#221933=CARTESIAN_POINT ( 'NONE',  ( -21.05000000000000071, 7.128833340094563376, -233.7327013124401276 ) ) ;
#221941=EDGE_CURVE ( 'NONE', #227124, #109848, #103368, .T. ) ;
#221954=LINE ( 'NONE', #241550, #158327 ) ;
#221967=TOROIDAL_SURFACE ( 'NONE', #67875, 0.2000000000000000111, 0.1000000000000000056 ) ;
#221979=DIRECTION ( 'NONE',  ( 0.000000000000000000, -0.9770955615653316162, -0.2128009952263604232 ) ) ;
#222015=VECTOR ( 'NONE', #107880, 1000.000000000000227 ) ;
#222027=DIRECTION ( 'NONE',  ( -4.336808689941751101E-15, 0.7397890806274315390, 0.6728388485992909951 ) ) ;
#222046=EDGE_CURVE ( 'NONE', #257455, #135756, #170267, .T. ) ;
#222063=AXIS2_PLACEMENT_3D ( 'NONE', #72157, #36903, #34325 ) ;
#222076=DIRECTION ( 'NONE',  ( 1.000000000000000000, 0.000000000000000000, 0.000000000000000000 ) ) ;
#222106=FACE_OUTER_BOUND ( 'NONE', #228475, .T. ) ;
#222129=DIRECTION ( 'NONE',  ( 0.000000000000000000, 0.2128009952263605065, -0.9770955615653313941 ) ) ;
#222142=DIRECTION ( 'NONE',  ( 1.000000000000000000, 0.000000000000000000, 0.000000000000000000 ) ) ;
#222153=CIRCLE ( 'NONE', #213815, 0.09999999999999775735 ) ;
#222176=AXIS2_PLACEMENT_3D ( 'NONE', #257757, #158745, #135281 ) ;
#222181=ADVANCED_FACE ( 'NONE', ( #33744 ), #28616, .F. ) ;
#222191=EDGE_CURVE ( 'NONE', #131951, #52291, #178624, .T. ) ;
#222195=DIRECTION ( 'NONE',  ( 0.000000000000000000, 0.2128009952263403282, -0.9770955615653358350 ) ) ;
#222220=AXIS2_PLACEMENT_3D ( 'NONE', #76022, #155603, #56446 ) ;
#222268=ORIENTED_EDGE ( 'NONE', *, *, #80158, .F. ) ;
#222272=DIRECTION ( 'NONE',  ( 0.000000000000000000, 0.2128009952263601456, -0.9770955615653316162 ) ) ;
#222291=ORIENTED_EDGE ( 'NONE', *, *, #189432, .F. ) ;
#222292=DIRECTION ( 'NONE',  ( 1.000000000000000000, 0.000000000000000000, 0.000000000000000000 ) ) ;
#222299=DIRECTION ( 'NONE',  ( 0.000000000000000000, -0.2128009952263403282, 0.9770955615653358350 ) ) ;
#222358=DIRECTION ( 'NONE',  ( 0.5000000000001140199, 0.1842910678166251592, -0.8461895782405347566 ) ) ;
#222364=ADVANCED_FACE ( 'NONE', ( #68667 ), #174355, .F. ) ;
#222417=CARTESIAN_POINT ( 'NONE',  ( -18.59999999999999787, 4.193200906077805712, -212.0298262072164164 ) ) ;
#222423=CARTESIAN_POINT ( 'NONE',  ( 18.50000000000000000, -7.695243320584908453, -209.8393003250734523 ) ) ;
#222437=CARTESIAN_POINT ( 'NONE',  ( -21.05000000000000071, 1.148907358139439339E-11, -201.0000000000015064 ) ) ;
#222458=ORIENTED_EDGE ( 'NONE', *, *, #147919, .F. ) ;
#222511=EDGE_CURVE ( 'NONE', #146352, #117463, #41241, .T. ) ;
#222546=AXIS2_PLACEMENT_3D ( 'NONE', #72997, #117227, #152533 ) ;
#222563=AXIS2_PLACEMENT_3D ( 'NONE', #148995, #228525, #72019 ) ;
#222573=DIRECTION ( 'NONE',  ( 1.000000000000000000, 0.000000000000000000, 0.000000000000000000 ) ) ;
#222588=DIRECTION ( 'NONE',  ( 1.000000000000000000, -0.000000000000000000, -0.000000000000000000 ) ) ;
#222618=DIRECTION ( 'NONE',  ( 2.952720810173289605E-16, -0.9770955615653315052, -0.2128009952263610061 ) ) ;
#222669=ORIENTED_EDGE ( 'NONE', *, *, #4331, .T. ) ;
#222677=VERTEX_POINT ( 'NONE', #135022 ) ;
#222722=VERTEX_POINT ( 'NONE', #80174 ) ;
#222734=CARTESIAN_POINT ( 'NONE',  ( -20.54999999999999716, -3.363022478626109368, -226.2703567425896267 ) ) ;
#222765=CARTESIAN_POINT ( 'NONE',  ( -18.44362607810621668, -7.771182065979212794, -209.9158824246631241 ) ) ;
#222767=DIRECTION ( 'NONE',  ( 1.000000000000000000, 0.000000000000000000, 0.000000000000000000 ) ) ;
#222796=ADVANCED_FACE ( 'NONE', ( #125749 ), #123197, .T. ) ;
#222826=LINE ( 'NONE', #44218, #161328 ) ;
#222851=ORIENTED_EDGE ( 'NONE', *, *, #114006, .F. ) ;
#222860=DIRECTION ( 'NONE',  ( 1.000000000000000000, 0.000000000000000000, 0.000000000000000000 ) ) ;
#222867=DIRECTION ( 'NONE',  ( 1.000000000000000000, 0.000000000000000000, 0.000000000000000000 ) ) ;
#222892=CARTESIAN_POINT ( 'NONE',  ( -18.51024323315077424, 18.37846419038447010, -236.9325101954433137 ) ) ;
#222901=AXIS2_PLACEMENT_3D ( 'NONE', #53176, #132733, #33670 ) ;
#222929=CIRCLE ( 'NONE', #27356, 3.999999999999998224 ) ;
#222954=CARTESIAN_POINT ( 'NONE',  ( -23.25000000000000000, 16.02417409648692725, -219.3605785455116006 ) ) ;
#222966=ORIENTED_EDGE ( 'NONE', *, *, #195381, .F. ) ;
#222967=EDGE_CURVE ( 'NONE', #97608, #236182, #193459, .T. ) ;
#222970=CARTESIAN_POINT ( 'NONE',  ( 22.50497660315937765, -2.577283117375421817, -189.5360782167620073 ) ) ;
#222971=AXIS2_PLACEMENT_3D ( 'NONE', #247062, #86691, #68450 ) ;
#223055=CARTESIAN_POINT ( 'NONE',  ( -21.55000000000000071, 9.712035112405693837, -211.5243229699422614 ) ) ;
#223075=DIRECTION ( 'NONE',  ( 0.000000000000000000, 0.9968797965484670343, 0.07893460099023182075 ) ) ;
#223131=ADVANCED_FACE ( 'NONE', ( #78614 ), #211532, .T. ) ;
#223155=ORIENTED_EDGE ( 'NONE', *, *, #57620, .F. ) ;
#223181=DIRECTION ( 'NONE',  ( 0.7071067811865475727, 0.6909108974501237954, 0.1504730267678056066 ) ) ;
#223219=DIRECTION ( 'NONE',  ( 0.000000000000000000, -0.9770955615653312831, -0.2128009952263614224 ) ) ;
#223226=CIRCLE ( 'NONE', #110800, 0.1000000000000055844 ) ;
#223230=CIRCLE ( 'NONE', #244083, 0.1000000000000033223 ) ;
#223235=CARTESIAN_POINT ( 'NONE',  ( 21.05000000000000071, 7.300274141770061398, -211.7264450054621534 ) ) ;
#223241=CARTESIAN_POINT ( 'NONE',  ( -22.00411653962173375, 7.066231425286666479, -199.3596904452039382 ) ) ;
#223274=ADVANCED_FACE ( 'NONE', ( #151327 ), #228289, .F. ) ;
#223318=EDGE_CURVE ( 'NONE', #22582, #106308, #200705, .T. ) ;
#223330=TOROIDAL_SURFACE ( 'NONE', #61019, 0.2000000000000000111, 0.1000000000000000056 ) ;
#223352=EDGE_CURVE ( 'NONE', #29761, #118692, #95186, .T. ) ;
#223370=TOROIDAL_SURFACE ( 'NONE', #94375, 0.2000000000000000111, 0.1000000000000000056 ) ;
#223390=CARTESIAN_POINT ( 'NONE',  ( -21.14999999999999858, -10.76604040606818025, -206.3127087229280789 ) ) ;
#223425=CIRCLE ( 'NONE', #94264, 12.87499999999999467 ) ;
#223486=CARTESIAN_POINT ( 'NONE',  ( -18.59999999999999787, -21.97324378644421117, -224.3523082604776562 ) ) ;
#223556=DIRECTION ( 'NONE',  ( 0.000000000000000000, 0.9964539953858966292, 0.08413937888696096379 ) ) ;
#223573=DIRECTION ( 'NONE',  ( -2.978066053179067751E-16, 0.9770955615653316162, 0.2128009952263596738 ) ) ;
#223627=ORIENTED_EDGE ( 'NONE', *, *, #80233, .T. ) ;
#223666=DIRECTION ( 'NONE',  ( -1.000000000000000000, 0.000000000000000000, 0.000000000000000000 ) ) ;
#223689=DIRECTION ( 'NONE',  ( 0.000000000000000000, 0.2128009952263485993, -0.9770955615653341697 ) ) ;
#223691=CARTESIAN_POINT ( 'NONE',  ( 21.05000000000000071, -1.236118717437887371, -194.8647072476926212 ) ) ;
#223705=EDGE_CURVE ( 'NONE', #192537, #102565, #145242, .T. ) ;
#223726=ORIENTED_EDGE ( 'NONE', *, *, #252999, .F. ) ;
#223765=DIRECTION ( 'NONE',  ( -4.801466763864313332E-15, -0.04908394489122119841, -0.9987946567507836049 ) ) ;
#223782=VERTEX_POINT ( 'NONE', #95668 ) ;
#223807=FACE_OUTER_BOUND ( 'NONE', #63658, .T. ) ;
#223821=CARTESIAN_POINT ( 'NONE',  ( 21.00000000000000000, 14.02742277431099538, -219.5907614236512870 ) ) ;
#223824=DIRECTION ( 'NONE',  ( 0.000000000000000000, -0.2128009952263604232, 0.9770955615653316162 ) ) ;
#223848=EDGE_CURVE ( 'NONE', #34155, #235411, #245228, .T. ) ;
#223860=ADVANCED_FACE ( 'NONE', ( #203767 ), #181649, .F. ) ;
#223875=CARTESIAN_POINT ( 'NONE',  ( 18.59999999999999432, 2.953700692300310848, -208.6327728934509764 ) ) ;
#223882=EDGE_CURVE ( 'NONE', #211413, #200161, #103360, .T. ) ;
#223890=CIRCLE ( 'NONE', #144786, 7.900000000000007461 ) ;
#223926=DIRECTION ( 'NONE',  ( -1.836970198721029934E-16, 0.9770955615653316162, 0.2128009952263604232 ) ) ;
#223949=CARTESIAN_POINT ( 'NONE',  ( 20.95512820512820440, 12.01161663143393632, -206.2285874551107554 ) ) ;
#223990=ORIENTED_EDGE ( 'NONE', *, *, #106759, .T. ) ;
#224000=AXIS2_PLACEMENT_3D ( 'NONE', #236065, #79540, #142095 ) ;
#224053=DIRECTION ( 'NONE',  ( 1.000000000000000000, 0.000000000000000000, 0.000000000000000000 ) ) ;
#224058=ORIENTED_EDGE ( 'NONE', *, *, #13314, .F. ) ;
#224109=LINE ( 'NONE', #200710, #242106 ) ;
#224128=CARTESIAN_POINT ( 'NONE',  ( -20.54999999999999716, 6.300962096140152013, -220.8843452229073705 ) ) ;
#224132=VECTOR ( 'NONE', #249472, 1000.000000000000227 ) ;
#224144=AXIS2_PLACEMENT_3D ( 'NONE', #87307, #144713, #166899 ) ;
#224145=CARTESIAN_POINT ( 'NONE',  ( 21.07954640115312728, -1.282382883101060633, -194.8016345785744647 ) ) ;
#224176=CARTESIAN_POINT ( 'NONE',  ( -18.50000000000000000, 18.34711819382569686, -236.8747682978092541 ) ) ;
#224183=LINE ( 'NONE', #246328, #29264 ) ;
#224185=CARTESIAN_POINT ( 'NONE',  ( 23.14999999999999503, 17.01923898301590654, -224.3994341343041867 ) ) ;
#224191=CARTESIAN_POINT ( 'NONE',  ( 18.59999999999999432, 2.859758780633683273, -208.6670499591424459 ) ) ;
#224203=EDGE_CURVE ( 'NONE', #234881, #182918, #62230, .T. ) ;
#224206=CARTESIAN_POINT ( 'NONE',  ( 23.24999999999999645, 1.148907358139439339E-11, -201.0000000000015064 ) ) ;
#224218=EDGE_CURVE ( 'NONE', #256147, #18136, #23585, .T. ) ;
#224228=DIRECTION ( 'NONE',  ( 1.000000000000000000, 0.000000000000000000, 0.000000000000000000 ) ) ;
#224326=VERTEX_POINT ( 'NONE', #123939 ) ;
#224380=DIRECTION ( 'NONE',  ( 0.000000000000000000, 0.2128009952263604232, -0.9770955615653316162 ) ) ;
#224429=FACE_OUTER_BOUND ( 'NONE', #24549, .T. ) ;
#224436=EDGE_CURVE ( 'NONE', #139087, #201117, #166491, .T. ) ;
#224443=VERTEX_POINT ( 'NONE', #129066 ) ;
#224473=TOROIDAL_SURFACE ( 'NONE', #157894, 0.2000000000000000111, 0.1000000000000000056 ) ;
#224479=DIRECTION ( 'NONE',  ( 0.000000000000000000, 0.2128009952263601456, -0.9770955615653316162 ) ) ;
#224501=CARTESIAN_POINT ( 'NONE',  ( 21.11747605621531321, 11.18329185709994888, -211.0959905261389338 ) ) ;
#224508=DIRECTION ( 'NONE',  ( 1.000000000000000000, 0.000000000000000000, 0.000000000000000000 ) ) ;
#224510=EDGE_LOOP ( 'NONE', ( #246230, #255025, #230957 ) ) ;
#224585=ORIENTED_EDGE ( 'NONE', *, *, #163858, .T. ) ;
#224634=EDGE_CURVE ( 'NONE', #19725, #116714, #162379, .T. ) ;
#224639=EDGE_LOOP ( 'NONE', ( #198886, #63448, #240952, #80540 ) ) ;
#224666=CARTESIAN_POINT ( 'NONE',  ( 18.50000000000000000, -0.5913595841389442942, -242.4574432119242999 ) ) ;
#224704=LINE ( 'NONE', #202588, #231804 ) ;
#224738=DIRECTION ( 'NONE',  ( -0.000000000000000000, -0.9770955615653310611, -0.2128009952263620608 ) ) ;
#224765=DIRECTION ( 'NONE',  ( -0.000000000000000000, -0.9770955615653313941, -0.2128009952263603677 ) ) ;
#224773=DIRECTION ( 'NONE',  ( 1.000000000000000000, 0.000000000000000000, 0.000000000000000000 ) ) ;
#224791=LINE ( 'NONE', #26633, #158187 ) ;
#224793=CIRCLE ( 'NONE', #37574, 0.1000000000000054040 ) ;
#224853=DIRECTION ( 'NONE',  ( -1.000000000000000000, -0.000000000000000000, -0.000000000000000000 ) ) ;
#224854=DIRECTION ( 'NONE',  ( 2.952720810173289112E-16, -0.9770955615653301729, -0.2128009952263660853 ) ) ;
#224858=CARTESIAN_POINT ( 'NONE',  ( -20.94999999999999929, 7.128833340094563376, -233.7327013124401276 ) ) ;
#224864=CARTESIAN_POINT ( 'NONE',  ( -20.54999999999999716, 4.590145742703442444, -213.0289728181953706 ) ) ;
#224889=CARTESIAN_POINT ( 'NONE',  ( 23.14999999999999858, 7.525330762710603416, -212.0571253909869256 ) ) ;
#224927=ADVANCED_FACE ( 'NONE', ( #72652 ), #230419, .F. ) ;
#224929=AXIS2_PLACEMENT_3D ( 'NONE', #16082, #95581, #175173 ) ;
#224975=DIRECTION ( 'NONE',  ( 1.000000000000000000, 0.000000000000000000, 0.000000000000000000 ) ) ;
#224977=LINE ( 'NONE', #46351, #176492 ) ;
#224982=CARTESIAN_POINT ( 'NONE',  ( 21.05000000000000071, -10.38870553492056104, -206.3818953267866902 ) ) ;
#225002=VERTEX_POINT ( 'NONE', #37371 ) ;
#225018=DIRECTION ( 'NONE',  ( 0.000000000000000000, -0.6728388485993177515, 0.7397890806274072251 ) ) ;
#225028=DIRECTION ( 'NONE',  ( 0.000000000000000000, -0.9394191166662618775, -0.3427706569150580362 ) ) ;
#225038=EDGE_CURVE ( 'NONE', #98224, #2617, #38639, .T. ) ;
#225063=CARTESIAN_POINT ( 'NONE',  ( 18.59999999999999432, 7.661991824395936845, -241.5144583139544636 ) ) ;
#225081=FACE_OUTER_BOUND ( 'NONE', #208594, .T. ) ;
#225082=EDGE_CURVE ( 'NONE', #1731, #247713, #254112, .T. ) ;
#225086=AXIS2_PLACEMENT_3D ( 'NONE', #192843, #252785, #254073 ) ;
#225087=CARTESIAN_POINT ( 'NONE',  ( -20.99780126800909841, 16.99738886486947465, -224.5087459288188256 ) ) ;
#225095=DIRECTION ( 'NONE',  ( 1.000000000000000000, 0.000000000000000000, 0.000000000000000000 ) ) ;
#225104=EDGE_CURVE ( 'NONE', #204482, #195703, #228914, .T. ) ;
#225105=DIRECTION ( 'NONE',  ( 0.000000000000000000, 0.9525900758537791946, -0.3042567129660269099 ) ) ;
#225114=TOROIDAL_SURFACE ( 'NONE', #4369, 11.70000000000000107, 0.1000000000000000056 ) ;
#225201=LINE ( 'NONE', #46569, #22342 ) ;
#225230=TOROIDAL_SURFACE ( 'NONE', #146151, 0.2000000000000000111, 0.1000000000000000056 ) ;
#225231=ORIENTED_EDGE ( 'NONE', *, *, #141080, .T. ) ;
#225339=DIRECTION ( 'NONE',  ( 0.000000000000000000, -0.05616704890741856110, 0.9984213852963245150 ) ) ;
#225385=DIRECTION ( 'NONE',  ( 1.000000000000000000, 0.000000000000000000, 0.000000000000000000 ) ) ;
#225401=B_SPLINE_CURVE_WITH_KNOTS ( 'NONE', 3,
 ( #20751, #97672, #179825, #222765, #58553, #161547, #177272, #160273, #3730, #258003 ),
 .UNSPECIFIED., .F., .F.,
 ( 4, 2, 2, 2, 4 ),
 ( 0.000000000000000000, 3.990160268012413235E-05, 7.980320536024826470E-05, 0.0001596064107204978033, 0.0003192128214410639114 ),
 .UNSPECIFIED. ) ;
#225409=ORIENTED_EDGE ( 'NONE', *, *, #136292, .T. ) ;
#225420=FACE_OUTER_BOUND ( 'NONE', #219759, .T. ) ;
#225435=CARTESIAN_POINT ( 'NONE',  ( -21.70464131381649509, 6.932842828061964724, -199.4901007520778080 ) ) ;
#225444=DIRECTION ( 'NONE',  ( 0.000000000000000000, -0.9770955615653313941, -0.2128009952263603677 ) ) ;
#225447=CARTESIAN_POINT ( 'NONE',  ( -18.59117750673696889, 18.41524492703433324, -237.0006385043383546 ) ) ;
#225461=ORIENTED_EDGE ( 'NONE', *, *, #179362, .T. ) ;
#225466=VERTEX_POINT ( 'NONE', #19750 ) ;
#225472=DIRECTION ( 'NONE',  ( -1.000000000000000000, -0.000000000000000000, -0.000000000000000000 ) ) ;
#225481=ADVANCED_FACE ( 'NONE', ( #203510 ), #250220, .F. ) ;
#225487=CARTESIAN_POINT ( 'NONE',  ( -22.49917693094574389, -2.395810317367125020, -189.5988992245846134 ) ) ;
#225505=CARTESIAN_POINT ( 'NONE',  ( 21.05000000000000071, 10.40540721059935159, -207.3515911714149809 ) ) ;
#225528=CARTESIAN_POINT ( 'NONE',  ( 20.94999999999999929, -6.488386256076840830, -212.2361678873109554 ) ) ;
#225533=ORIENTED_EDGE ( 'NONE', *, *, #82509, .F. ) ;
#225560=VECTOR ( 'NONE', #19229, 1000.000000000000227 ) ;
#225569=CARTESIAN_POINT ( 'NONE',  ( 21.05000000000000071, 1.148907358139439339E-11, -201.0000000000015064 ) ) ;
#225596=CARTESIAN_POINT ( 'NONE',  ( 20.94999999999999929, 7.872214528623318053, -209.6555322433423783 ) ) ;
#225602=ORIENTED_EDGE ( 'NONE', *, *, #221528, .T. ) ;
#225613=DIRECTION ( 'NONE',  ( 1.000000000000000000, 0.000000000000000000, 0.000000000000000000 ) ) ;
#225683=LINE ( 'NONE', #74060, #241877 ) ;
#225694=CIRCLE ( 'NONE', #213237, 0.09999999999999810429 ) ;
#225704=EDGE_CURVE ( 'NONE', #245998, #98647, #134330, .T. ) ;
#225716=CARTESIAN_POINT ( 'NONE',  ( 21.07189867249812210, 13.07815244086534712, -210.6504456248233623 ) ) ;
#225722=CARTESIAN_POINT ( 'NONE',  ( 20.04142135623730070, 8.882751598337870647, -187.0399955572217721 ) ) ;
#225738=ADVANCED_FACE ( 'NONE', ( #75579 ), #92531, .F. ) ;
#225739=CARTESIAN_POINT ( 'NONE',  ( 23.15000000000000213, -4.356730526971939632, -226.1082375506050539 ) ) ;
#225742=DIRECTION ( 'NONE',  ( 0.000000000000000000, 0.2128009952263666682, -0.9770955615653300619 ) ) ;
#225748=CARTESIAN_POINT ( 'NONE',  ( -21.05000000000000071, 12.82677665681128332, -205.1493534351658354 ) ) ;
#225756=CARTESIAN_POINT ( 'NONE',  ( 18.59999999999999076, 8.433899723187009201, -209.4150263691077782 ) ) ;
#225767=DIRECTION ( 'NONE',  ( 0.000000000000000000, 0.2128009952263604232, -0.9770955615653316162 ) ) ;
#225820=AXIS2_PLACEMENT_3D ( 'NONE', #42751, #105246, #240957 ) ;
#225846=EDGE_CURVE ( 'NONE', #19404, #163287, #196766, .T. ) ;
#225882=ORIENTED_EDGE ( 'NONE', *, *, #53113, .F. ) ;
#225914=EDGE_CURVE ( 'NONE', #24822, #98560, #17922, .T. ) ;
#225975=DIRECTION ( 'NONE',  ( 0.000000000000000000, 0.2128009952263403282, -0.9770955615653358350 ) ) ;
#226036=CARTESIAN_POINT ( 'NONE',  ( 18.50000000000001066, -7.567701079425766864, -210.0537230116848377 ) ) ;
#226047=FACE_OUTER_BOUND ( 'NONE', #47859, .T. ) ;
#226058=CARTESIAN_POINT ( 'NONE',  ( -18.59999999999999787, 13.96869538424787649, -210.3925794786331949 ) ) ;
#226068=VECTOR ( 'NONE', #88226, 1000.000000000000000 ) ;
#226084=CARTESIAN_POINT ( 'NONE',  ( -21.14999999999999858, 1.148907358139439339E-11, -201.0000000000015064 ) ) ;
#226095=LINE ( 'NONE', #102283, #122701 ) ;
#226120=CYLINDRICAL_SURFACE ( 'NONE', #59886, 0.09999999999999939493 ) ;
#226136=AXIS2_PLACEMENT_3D ( 'NONE', #138200, #173555, #253031 ) ;
#226168=CARTESIAN_POINT ( 'NONE',  ( 21.05000000000000071, 10.41478453976545460, -207.3430624819218622 ) ) ;
#226176=LINE ( 'NONE', #46279, #69097 ) ;
#226187=ORIENTED_EDGE ( 'NONE', *, *, #153991, .F. ) ;
#226232=CARTESIAN_POINT ( 'NONE',  ( 20.94999999999999929, 6.277629359189122127, -229.8243190661787878 ) ) ;
#226238=ORIENTED_EDGE ( 'NONE', *, *, #137648, .F. ) ;
#226250=CARTESIAN_POINT ( 'NONE',  ( 18.59999999999999787, -6.937571600298356067, -224.3614019333310807 ) ) ;
#226256=VERTEX_POINT ( 'NONE', #17819 ) ;
#226260=DIRECTION ( 'NONE',  ( 1.000000000000000000, 0.000000000000000000, 0.000000000000000000 ) ) ;
#226265=EDGE_CURVE ( 'NONE', #220406, #142529, #77789, .T. ) ;
#226281=CARTESIAN_POINT ( 'NONE',  ( 23.14999999999999147, -4.054946580484636520, -201.8831241301909074 ) ) ;
#226283=EDGE_CURVE ( 'NONE', #77477, #212886, #47138, .T. ) ;
#226296=CARTESIAN_POINT ( 'NONE',  ( -20.94999999999999929, 14.83511725869332132, -235.8887435844146978 ) ) ;
#226304=ORIENTED_EDGE ( 'NONE', *, *, #57268, .T. ) ;
#226311=DIRECTION ( 'NONE',  ( -1.000000000000000000, -0.000000000000000000, -0.000000000000000000 ) ) ;
#226330=CARTESIAN_POINT ( 'NONE',  ( 21.14999999999999858, 9.125777775466493935, -211.6520035670780544 ) ) ;
#226339=ORIENTED_EDGE ( 'NONE', *, *, #136931, .F. ) ;
#226353=CARTESIAN_POINT ( 'NONE',  ( -18.59999999999999787, 14.90151243843701856, -203.3975529985363551 ) ) ;
#226369=CARTESIAN_POINT ( 'NONE',  ( -20.99551997958315042, 17.15237243733772132, -224.5408061578804961 ) ) ;
#226370=EDGE_CURVE ( 'NONE', #38453, #241591, #67225, .T. ) ;
#226389=CARTESIAN_POINT ( 'NONE',  ( 18.59999999999999076, 14.83511725869332132, -235.8887435844146978 ) ) ;
#226402=CARTESIAN_POINT ( 'NONE',  ( 21.13461538461538325, 11.28871374199622046, -211.0785950404945766 ) ) ;
#226406=ORIENTED_EDGE ( 'NONE', *, *, #202464, .T. ) ;
#226419=CARTESIAN_POINT ( 'NONE',  ( -20.64999999999999858, 8.751106741858205140, -220.7398867978736234 ) ) ;
#226422=LINE ( 'NONE', #107782, #204346 ) ;
#226426=AXIS2_PLACEMENT_3D ( 'NONE', #139468, #119955, #168080 ) ;
#226427=DIRECTION ( 'NONE',  ( 0.000000000000000000, 0.2128009952263485993, -0.9770955615653341697 ) ) ;
#226484=ADVANCED_FACE ( 'NONE', ( #74962 ), #9820, .T. ) ;
#226500=CARTESIAN_POINT ( 'NONE',  ( 23.14999999999999858, 9.863005973831429074, -220.4411654715779321 ) ) ;
#226502=DIRECTION ( 'NONE',  ( 0.000000000000000000, 0.2128009952263601456, -0.9770955615653315052 ) ) ;
#226506=DIRECTION ( 'NONE',  ( 0.000000000000000000, 0.08413937888704771384, -0.9964539953858891908 ) ) ;
#226530=DIRECTION ( 'NONE',  ( -1.000000000000000000, 0.000000000000000000, 0.000000000000000000 ) ) ;
#226565=CARTESIAN_POINT ( 'NONE',  ( 23.14999999999999503, 14.06640494040442135, -210.3712993791105532 ) ) ;
#226573=CARTESIAN_POINT ( 'NONE',  ( 20.94999999999999929, 3.047642603966940200, -208.5984958277594785 ) ) ;
#226583=ADVANCED_FACE ( 'NONE', ( #95756 ), #155784, .F. ) ;
#226618=CARTESIAN_POINT ( 'NONE',  ( 20.94999999999999929, -6.688413578037176066, -212.5825622730469036 ) ) ;
#226621=DIRECTION ( 'NONE',  ( 0.000000000000000000, -0.05616704890745314455, 0.9984213852963225166 ) ) ;
#226646=ORIENTED_EDGE ( 'NONE', *, *, #132202, .T. ) ;
#226675=FACE_OUTER_BOUND ( 'NONE', #257871, .T. ) ;
#226684=ORIENTED_EDGE ( 'NONE', *, *, #66062, .T. ) ;
#226688=DIRECTION ( 'NONE',  ( 0.000000000000000000, -0.9770955615653313941, -0.2128009952263603677 ) ) ;
#226689=VECTOR ( 'NONE', #210984, 1000.000000000000000 ) ;
#226714=DIRECTION ( 'NONE',  ( 1.000000000000000000, 7.136802563874200093E-16, 1.554319503706925554E-16 ) ) ;
#226732=ADVANCED_FACE ( 'NONE', ( #4368 ), #243153, .F. ) ;
#226760=CARTESIAN_POINT ( 'NONE',  ( 18.31572054635827840, -0.7431314789941730892, -242.4582880902354702 ) ) ;
#226786=DIRECTION ( 'NONE',  ( 1.000000000000000000, 0.000000000000000000, 0.000000000000000000 ) ) ;
#226822=CARTESIAN_POINT ( 'NONE',  ( 21.30000000000002558, -0.8618440306552703767, -197.0427629756619297 ) ) ;
#226904=CARTESIAN_POINT ( 'NONE',  ( 20.94999999999999574, 0.6869237119019839799, -212.7787591058053067 ) ) ;
#226909=ADVANCED_FACE ( 'NONE', ( #121365 ), #160479, .T. ) ;
#226930=LINE ( 'NONE', #10461, #149358 ) ;
#226974=CARTESIAN_POINT ( 'NONE',  ( 21.05000000000000071, 11.83124523798471905, -206.0547899340221818 ) ) ;
#226982=DIRECTION ( 'NONE',  ( 0.000000000000000000, 0.6728388485993012091, -0.7397890806274222131 ) ) ;
#227001=DIRECTION ( 'NONE',  ( 1.000000000000000000, 0.000000000000000000, 0.000000000000000000 ) ) ;
#227012=FACE_OUTER_BOUND ( 'NONE', #108190, .T. ) ;
#227032=ORIENTED_EDGE ( 'NONE', *, *, #92768, .T. ) ;
#227036=DIRECTION ( 'NONE',  ( 1.000000000000000000, 3.190570557967288949E-16, 6.948722487160392945E-17 ) ) ;
#227044=EDGE_CURVE ( 'NONE', #32735, #233386, #152133, .T. ) ;
#227045=ORIENTED_EDGE ( 'NONE', *, *, #107595, .T. ) ;
#227053=SPHERICAL_SURFACE ( 'NONE', #102543, 0.1000000000000000056 ) ;
#227054=AXIS2_PLACEMENT_3D ( 'NONE', #67651, #164198, #125071 ) ;
#227064=ORIENTED_EDGE ( 'NONE', *, *, #250429, .T. ) ;
#227071=VERTEX_POINT ( 'NONE', #158549 ) ;
#227100=DIRECTION ( 'NONE',  ( 1.000000000000000000, 0.000000000000000000, 0.000000000000000000 ) ) ;
#227108=ORIENTED_EDGE ( 'NONE', *, *, #159185, .T. ) ;
#227110=CYLINDRICAL_SURFACE ( 'NONE', #205325, 0.09999999999999939493 ) ;
#227124=VERTEX_POINT ( 'NONE', #192524 ) ;
#227129=FACE_OUTER_BOUND ( 'NONE', #74322, .T. ) ;
#227154=CARTESIAN_POINT ( 'NONE',  ( -23.15000000000000213, 14.06640494040442135, -210.3712993791105532 ) ) ;
#227157=EDGE_LOOP ( 'NONE', ( #204080, #23170, #73193, #40559 ) ) ;
#227180=VECTOR ( 'NONE', #163413, 1000.000000000000227 ) ;
#227187=AXIS2_PLACEMENT_3D ( 'NONE', #111884, #209689, #109283 ) ;
#227197=FACE_OUTER_BOUND ( 'NONE', #175741, .T. ) ;
#227237=ORIENTED_EDGE ( 'NONE', *, *, #108866, .F. ) ;
#227256=ORIENTED_EDGE ( 'NONE', *, *, #89724, .T. ) ;
#227261=ORIENTED_EDGE ( 'NONE', *, *, #184746, .F. ) ;
#227325=ORIENTED_EDGE ( 'NONE', *, *, #107891, .T. ) ;
#227373=CARTESIAN_POINT ( 'NONE',  ( 21.05000012384925512, 12.97676112483788735, -210.6372453404386533 ) ) ;
#227407=CARTESIAN_POINT ( 'NONE',  ( -22.59999970745345976, -2.509662979759784029, -189.5206167450800478 ) ) ;
#227423=CARTESIAN_POINT ( 'NONE',  ( -20.94999999999999929, -10.56629024491939894, -206.4738935375009703 ) ) ;
#227428=EDGE_CURVE ( 'NONE', #22692, #59070, #122748, .T. ) ;
#227433=VERTEX_POINT ( 'NONE', #203098 ) ;
#227443=CARTESIAN_POINT ( 'NONE',  ( -21.07928932188134041, 1.148907358139439339E-11, -201.0000000000015064 ) ) ;
#227464=DIRECTION ( 'NONE',  ( 0.000000000000000000, -0.2128009952263602289, 0.9770955615653315052 ) ) ;
#227465=AXIS2_PLACEMENT_3D ( 'NONE', #248349, #51397, #130973 ) ;
#227471=DIRECTION ( 'NONE',  ( -0.000000000000000000, -0.2128009952263604232, 0.9770955615653316162 ) ) ;
#227494=EDGE_LOOP ( 'NONE', ( #173063, #252362, #148019, #14652 ) ) ;
#227508=CIRCLE ( 'NONE', #252636, 0.1000000000000055844 ) ;
#227527=AXIS2_PLACEMENT_3D ( 'NONE', #248753, #167956, #250028 ) ;
#227551=VERTEX_POINT ( 'NONE', #213352 ) ;
#227586=CARTESIAN_POINT ( 'NONE',  ( -20.54999999999999716, -4.259020970815408091, -226.0869574510824123 ) ) ;
#227588=ORIENTED_EDGE ( 'NONE', *, *, #224436, .T. ) ;
#227589=AXIS2_PLACEMENT_3D ( 'NONE', #90670, #71142, #227616 ) ;
#227616=DIRECTION ( 'NONE',  ( 0.000000000000000000, 0.9770955615653551529, 0.2128009952262517601 ) ) ;
#227617=DIRECTION ( 'NONE',  ( 0.000000000000000000, -0.9394191166662628767, -0.3427706569150552052 ) ) ;
#227630=DIRECTION ( 'NONE',  ( 0.000000000000000000, -0.2128009952263604232, 0.9770955615653316162 ) ) ;
#227654=VECTOR ( 'NONE', #115088, 1000.000000000000227 ) ;
#227659=DIRECTION ( 'NONE',  ( 0.000000000000000000, 0.2128009952263602844, -0.9770955615653315052 ) ) ;
#227661=AXIS2_PLACEMENT_3D ( 'NONE', #134861, #18785, #214417 ) ;
#227664=EDGE_CURVE ( 'NONE', #192351, #254124, #6181, .T. ) ;
#227689=DIRECTION ( 'NONE',  ( 0.7071067811865474617, 0.6909108974501236844, 0.1504730267678055788 ) ) ;
#227751=CARTESIAN_POINT ( 'NONE',  ( 23.14999999999999503, 15.90518444080776739, -219.2841490888777116 ) ) ;
#227757=DIRECTION ( 'NONE',  ( 0.000000000000000000, 0.2128009952263623661, -0.9770955615653309501 ) ) ;
#227762=DIRECTION ( 'NONE',  ( 1.734723475976817507E-14, -0.9770955615653316162, -0.2128009952263604232 ) ) ;
#227763=ADVANCED_FACE ( 'NONE', ( #24170 ), #144078, .F. ) ;
#227777=ORIENTED_EDGE ( 'NONE', *, *, #195029, .F. ) ;
#227782=ORIENTED_EDGE ( 'NONE', *, *, #165739, .T. ) ;
#227793=DIRECTION ( 'NONE',  ( 1.000000000000000000, 0.000000000000000000, 0.000000000000000000 ) ) ;
#227802=LINE ( 'NONE', #226500, #164568 ) ;
#227832=DIRECTION ( 'NONE',  ( 1.000000000000000000, 0.000000000000000000, 0.000000000000000000 ) ) ;
#227863=VERTEX_POINT ( 'NONE', #236475 ) ;
#227891=DIRECTION ( 'NONE',  ( -1.000000000000000000, 0.000000000000000000, 0.000000000000000000 ) ) ;
#227895=ORIENTED_EDGE ( 'NONE', *, *, #190572, .F. ) ;
#227905=CARTESIAN_POINT ( 'NONE',  ( 21.14999999999999503, -13.98128454229088469, -192.0195388455185821 ) ) ;
#227914=AXIS2_PLACEMENT_3D ( 'NONE', #2375, #3669, #147023 ) ;
#227927=DIRECTION ( 'NONE',  ( 0.000000000000000000, -0.2128009952263603677, 0.9770955615653313941 ) ) ;
#227928=VERTEX_POINT ( 'NONE', #55238 ) ;
#227958=AXIS2_PLACEMENT_3D ( 'NONE', #191456, #91033, #33679 ) ;
#227959=DIRECTION ( 'NONE',  ( 0.000000000000000000, 0.2128009952263485993, -0.9770955615653341697 ) ) ;
#227979=( BOUNDED_SURFACE ( )  B_SPLINE_SURFACE ( 3, 2, ( 
 ( #161302, #40085, #239542 ),
 ( #141709, #140421, #184684 ),
 ( #23082, #103851, #120903 ),
 ( #202969, #6042, #204248 ),
 ( #85552, #2187, #221234 ),
 ( #42617, #82990, #122164 ) ),
 .UNSPECIFIED., .F., .F., .T. ) 
 B_SPLINE_SURFACE_WITH_KNOTS ( ( 4, 2, 4 ),
 ( 3, 3 ),
 ( -1.776356839400250465E-15, 0.7853981633974468357, 1.570796326794895448 ),
 ( 0.000000000000000000, 1.000000000000000000 ),
 .UNSPECIFIED. ) 
 GEOMETRIC_REPRESENTATION_ITEM ( )  RATIONAL_B_SPLINE_SURFACE ( (
 ( 1.000000000000000000, 0.5000000000000655032, 1.000000000000000000),
 ( 1.000000000000000000, 0.4993418825348334145, 1.000000000000000000),
 ( 1.000000000000000000, 0.5278258667039918972, 1.000000000000000000),
 ( 1.000000000000000000, 0.6092287576712909214, 1.000000000000000000),
 ( 1.000000000000000000, 0.6611148371766234488, 1.000000000000000000),
 ( 1.000000000000000000, 0.7071067811865806574, 1.000000000000000000) ) ) 
 REPRESENTATION_ITEM ( '' )  SURFACE ( )  );
#227992=ADVANCED_FACE ( 'NONE', ( #158272 ), #160528, .T. ) ;
#227994=FACE_OUTER_BOUND ( 'NONE', #246045, .T. ) ;
#228035=TOROIDAL_SURFACE ( 'NONE', #65522, 0.4000000000000009104, 0.1000000000000000056 ) ;
#228052=CARTESIAN_POINT ( 'NONE',  ( -18.39999999999999858, -0.8467571797981087167, -242.2246066262668194 ) ) ;
#228057=CARTESIAN_POINT ( 'NONE',  ( 21.14999999999999858, 11.40444339177024169, -198.6185779617709670 ) ) ;
#228074=CARTESIAN_POINT ( 'NONE',  ( -22.59080734064477625, 11.47432927991817309, -198.4695429027907494 ) ) ;
#228083=ORIENTED_EDGE ( 'NONE', *, *, #173420, .F. ) ;
#228101=VECTOR ( 'NONE', #253789, 1000.000000000000000 ) ;
#228106=AXIS2_PLACEMENT_3D ( 'NONE', #7088, #205280, #223556 ) ;
#228136=DIRECTION ( 'NONE',  ( 1.000000000000000000, 0.000000000000000000, 0.000000000000000000 ) ) ;
#228160=CIRCLE ( 'NONE', #161537, 0.1000000000000061395 ) ;
#228161=ORIENTED_EDGE ( 'NONE', *, *, #160111, .T. ) ;
#228162=FACE_OUTER_BOUND ( 'NONE', #103063, .T. ) ;
#228191=ORIENTED_EDGE ( 'NONE', *, *, #70904, .F. ) ;
#228208=ADVANCED_FACE ( 'NONE', ( #29035 ), #31547, .T. ) ;
#228218=CYLINDRICAL_SURFACE ( 'NONE', #88876, 0.1000000000000036415 ) ;
#228231=AXIS2_PLACEMENT_3D ( 'NONE', #118999, #159410, #173876 ) ;
#228263=DIRECTION ( 'NONE',  ( 0.000000000000000000, 0.2128009952263604510, -0.9770955615653315052 ) ) ;
#228267=FACE_OUTER_BOUND ( 'NONE', #170314, .T. ) ;
#228289=TOROIDAL_SURFACE ( 'NONE', #115849, 0.9750000000000019762, 0.1000000000000000056 ) ;
#228300=DIRECTION ( 'NONE',  ( 0.000000000000000000, -0.3042567129660163627, -0.9525900758537824142 ) ) ;
#228326=AXIS2_PLACEMENT_3D ( 'NONE', #161932, #1537, #160660 ) ;
#228330=CIRCLE ( 'NONE', #103390, 0.09999999999999939493 ) ;
#228335=CARTESIAN_POINT ( 'NONE',  ( -21.13498764882296399, -1.380655549589986375, -194.6528078599425839 ) ) ;
#228336=DIRECTION ( 'NONE',  ( -1.000000000000000000, 0.000000000000000000, 0.000000000000000000 ) ) ;
#228343=DIRECTION ( 'NONE',  ( -1.000000000000000000, -0.000000000000000000, -0.000000000000000000 ) ) ;
#228443=CARTESIAN_POINT ( 'NONE',  ( -21.05000000000000071, 0.6869237119019852011, -212.7787591058053067 ) ) ;
#228475=EDGE_LOOP ( 'NONE', ( #80989, #43530, #202748, #204627, #233342, #168632, #42603, #174318, #216566, #97717, #14815, #76355, #97988, #255689, #221661, #164453, #30022, #227237 ) ) ;
#228480=LINE ( 'NONE', #70702, #102410 ) ;
#228496=LINE ( 'NONE', #49836, #151599 ) ;
#228505=ORIENTED_EDGE ( 'NONE', *, *, #174502, .F. ) ;
#228506=CYLINDRICAL_SURFACE ( 'NONE', #214642, 11.74999999999999289 ) ;
#228525=DIRECTION ( 'NONE',  ( -0.7071067811865474617, -0.6909108974501236844, -0.1504730267678055788 ) ) ;
#228574=CARTESIAN_POINT ( 'NONE',  ( -18.59999999999999787, 0.6869237119019839799, -212.7787591058053067 ) ) ;
#228586=DIRECTION ( 'NONE',  ( 0.000000000000000000, -0.9770955615653551529, -0.2128009952262517601 ) ) ;
#228603=CIRCLE ( 'NONE', #249451, 0.09999999999999632794 ) ;
#228606=DIRECTION ( 'NONE',  ( 0.000000000000000000, -0.2128009952263604232, 0.9770955615653316162 ) ) ;
#228614=CARTESIAN_POINT ( 'NONE',  ( -18.59999999999999787, 0.6656436123793491033, -212.6810495496487476 ) ) ;
#228615=DIRECTION ( 'NONE',  ( -1.000000000000000000, -0.000000000000000000, -0.000000000000000000 ) ) ;
#228620=PRODUCT_DEFINITION ( 'UNKNOWN', '', #186339, #214892 ) ;
#228630=DIRECTION ( 'NONE',  ( 0.000000000000000000, 0.2128009952263608395, -0.9770955615653315052 ) ) ;
#228639=FACE_OUTER_BOUND ( 'NONE', #131226, .T. ) ;
#228672=AXIS2_PLACEMENT_3D ( 'NONE', #165018, #243256, #223689 ) ;
#228675=DIRECTION ( 'NONE',  ( -7.304098846218135653E-16, -0.9770955615653315052, -0.2128009952263603954 ) ) ;
#228685=DIRECTION ( 'NONE',  ( -1.000000000000000000, -0.000000000000000000, -0.000000000000000000 ) ) ;
#228707=CIRCLE ( 'NONE', #62091, 12.97499999999999964 ) ;
#228716=CARTESIAN_POINT ( 'NONE',  ( -20.88420186297724612, 18.41141989892752662, -236.9935361838138022 ) ) ;
#228742=CARTESIAN_POINT ( 'NONE',  ( -23.15000000000000213, 0.04003676617161597284, -188.9658445640203297 ) ) ;
#228763=ORIENTED_EDGE ( 'NONE', *, *, #197404, .T. ) ;
#228792=ORIENTED_EDGE ( 'NONE', *, *, #218621, .T. ) ;
#228847=CARTESIAN_POINT ( 'NONE',  ( -23.15000000000000213, 4.389020526555173163, -221.1525959572864792 ) ) ;
#228874=ORIENTED_EDGE ( 'NONE', *, *, #162707, .F. ) ;
#228879=DIRECTION ( 'NONE',  ( 0.000000000000000000, 0.2128009952263604232, -0.9770955615653316162 ) ) ;
#228883=EDGE_CURVE ( 'NONE', #89546, #232502, #190100, .T. ) ;
#228892=ORIENTED_EDGE ( 'NONE', *, *, #100074, .F. ) ;
#228899=DIRECTION ( 'NONE',  ( -0.000000000000000000, -0.2128009952263604232, 0.9770955615653316162 ) ) ;
#228914=B_SPLINE_CURVE_WITH_KNOTS ( 'NONE', 3,
 ( #103395, #201229, #22625, #82539, #241649, #63003 ),
 .UNSPECIFIED., .F., .F.,
 ( 4, 2, 4 ),
 ( 0.000000000000000000, 0.0001497467027049116195, 0.0002994934054098232390 ),
 .UNSPECIFIED. ) ;
#228923=CARTESIAN_POINT ( 'NONE',  ( -20.94999999999999929, -10.76604040606817847, -206.3127087229280789 ) ) ;
#228931=CARTESIAN_POINT ( 'NONE',  ( -20.54999999999999716, -3.770473190032741062, -225.9805569534692324 ) ) ;
#228956=DIRECTION ( 'NONE',  ( 0.000000000000000000, 0.2128009952263485993, -0.9770955615653341697 ) ) ;
#228998=CIRCLE ( 'NONE', #54192, 0.09999999999999939493 ) ;
#229005=VERTEX_POINT ( 'NONE', #37068 ) ;
#229009=DIRECTION ( 'NONE',  ( -0.000000000000000000, 0.9770955615653316162, 0.2128009952263603122 ) ) ;
#229017=EDGE_CURVE ( 'NONE', #91518, #215393, #152716, .T. ) ;
#229043=ORIENTED_EDGE ( 'NONE', *, *, #172287, .T. ) ;
#229061=ORIENTED_EDGE ( 'NONE', *, *, #219774, .F. ) ;
#229070=ORIENTED_EDGE ( 'NONE', *, *, #53023, .T. ) ;
#229086=( BOUNDED_SURFACE ( )  B_SPLINE_SURFACE ( 3, 2, ( 
 ( #67693, #110671, #71571 ),
 ( #190218, #11589, #106805 ),
 ( #168127, #170698, #247614 ),
 ( #69002, #26012, #245048 ),
 ( #87237, #226760, #148522 ),
 ( #250187, #27328, #131515 ),
 ( #186371, #48123, #127676 ),
 ( #185071, #6429, #85938 ),
 ( #165525, #58364, #251458 ),
 ( #154960, #173267, #234456 ) ),
 .UNSPECIFIED., .F., .F., .F. ) 
 B_SPLINE_SURFACE_WITH_KNOTS ( ( 4, 2, 2, 2, 4 ),
 ( 3, 3 ),
 ( 0.0001701955120502364872, 0.0002247052511886114259, 0.0002792149903269863375, 0.0003882344686037362148, 0.0006062734251572359694 ),
 ( 0.000000000000000000, 1.000000000000000000 ),
 .UNSPECIFIED. ) 
 GEOMETRIC_REPRESENTATION_ITEM ( )  RATIONAL_B_SPLINE_SURFACE ( (
 ( 1.000000000000000000, 0.2966190024559251515, 1.000000000000000000),
 ( 1.000000000000000000, 0.2964522492711451074, 1.000000000000000000),
 ( 1.000000000000000000, 0.3059923531882451364, 1.000000000000000000),
 ( 1.000000000000000000, 0.3355751146951128083, 1.000000000000000000),
 ( 1.000000000000000000, 0.3550672384973958540, 1.000000000000000000),
 ( 1.000000000000000000, 0.4157034672164037770, 1.000000000000000000),
 ( 1.000000000000000000, 0.4588031877646243650, 1.000000000000000000),
 ( 1.000000000000000000, 0.5771441759675220995, 1.000000000000000000),
 ( 1.000000000000000000, 0.6469377121762164284, 1.000000000000000000),
 ( 1.000000000000000000, 0.7071067811865596742, 1.000000000000000000) ) ) 
 REPRESENTATION_ITEM ( '' )  SURFACE ( )  );
#229102=DIRECTION ( 'NONE',  ( -1.000000000000000000, 0.000000000000000000, 0.000000000000000000 ) ) ;
#229126=DIRECTION ( 'NONE',  ( 1.000000000000000000, 0.000000000000000000, 0.000000000000000000 ) ) ;
#229161=EDGE_LOOP ( 'NONE', ( #194441, #171796, #35427, #61370 ) ) ;
#229190=ORIENTED_EDGE ( 'NONE', *, *, #76395, .T. ) ;
#229194=DIRECTION ( 'NONE',  ( 0.000000000000000000, -0.9987946567507778317, 0.04908394489133698774 ) ) ;
#229198=CARTESIAN_POINT ( 'NONE',  ( -22.39999999999999858, 7.591056067193246548, -199.2444047917219052 ) ) ;
#229252=VECTOR ( 'NONE', #193292, 1000.000000000000114 ) ;
#229257=AXIS2_PLACEMENT_3D ( 'NONE', #160019, #73444, #169994 ) ;
#229302=DIRECTION ( 'NONE',  ( 0.000000000000000000, 0.2128009952263603399, -0.9770955615653315052 ) ) ;
#229325=ORIENTED_EDGE ( 'NONE', *, *, #257807, .T. ) ;
#229357=ORIENTED_EDGE ( 'NONE', *, *, #84789, .F. ) ;
#229382=FACE_OUTER_BOUND ( 'NONE', #161456, .T. ) ;
#229383=CARTESIAN_POINT ( 'NONE',  ( 20.94999999999999574, 0.6713328740235187109, -212.7808875799876205 ) ) ;
#229387=CARTESIAN_POINT ( 'NONE',  ( 23.14999999999999858, 6.277629359189123903, -229.8243190661787878 ) ) ;
#229418=ORIENTED_EDGE ( 'NONE', *, *, #115220, .T. ) ;
#229429=ORIENTED_EDGE ( 'NONE', *, *, #197404, .F. ) ;
#229433=ORIENTED_EDGE ( 'NONE', *, *, #125056, .T. ) ;
#229437=DIRECTION ( 'NONE',  ( 1.000000000000000000, 0.000000000000000000, 0.000000000000000000 ) ) ;
#229443=CARTESIAN_POINT ( 'NONE',  ( -21.05000000000000071, -1.299020131538773271, -194.8773804188782606 ) ) ;
#229468=ORIENTED_EDGE ( 'NONE', *, *, #174552, .T. ) ;
#229534=EDGE_CURVE ( 'NONE', #131951, #116019, #111167, .T. ) ;
#229539=DIRECTION ( 'NONE',  ( 0.000000000000000000, 0.2128009952263604232, -0.9770955615653316162 ) ) ;
#229547=CARTESIAN_POINT ( 'NONE',  ( 18.59999999999999432, 7.783179459866045313, -245.3643104511423303 ) ) ;
#229610=CARTESIAN_POINT ( 'NONE',  ( -22.39999999999999858, 7.591056067193246548, -199.2444047917219052 ) ) ;
#229616=CARTESIAN_POINT ( 'NONE',  ( -21.07928932188134041, -1.250084634896336366, -194.7953894783290423 ) ) ;
#229617=CARTESIAN_POINT ( 'NONE',  ( -20.94999999999999929, 7.128833340094563376, -233.7327013124401276 ) ) ;
#229619=EDGE_CURVE ( 'NONE', #162643, #53701, #207021, .T. ) ;
#229672=ADVANCED_FACE ( 'NONE', ( #11759 ), #168288, .T. ) ;
#229676=ORIENTED_EDGE ( 'NONE', *, *, #220773, .F. ) ;
#229705=VERTEX_POINT ( 'NONE', #189090 ) ;
#229741=ORIENTED_EDGE ( 'NONE', *, *, #248140, .F. ) ;
#229758=CARTESIAN_POINT ( 'NONE',  ( 18.49999999999998934, 18.34743685832673421, -236.8753540304231251 ) ) ;
#229762=ORIENTED_EDGE ( 'NONE', *, *, #168013, .F. ) ;
#229789=DIRECTION ( 'NONE',  ( -1.000000000000000000, -2.885090398161910739E-16, -6.283419270304611573E-17 ) ) ;
#229792=VECTOR ( 'NONE', #191146, 1000.000000000000227 ) ;
#229830=CARTESIAN_POINT ( 'NONE',  ( -23.15000000000000213, 15.90518444080776028, -219.2841490888777116 ) ) ;
#229865=( NAMED_UNIT ( * ) PLANE_ANGLE_UNIT ( ) SI_UNIT ( $, .RADIAN. ) );
#229891=CARTESIAN_POINT ( 'NONE',  ( -20.64999999999999858, 11.58468387039766512, -220.1227639117171861 ) ) ;
#229892=FACE_OUTER_BOUND ( 'NONE', #193934, .T. ) ;
#229898=VERTEX_POINT ( 'NONE', #14331 ) ;
#229902=EDGE_CURVE ( 'NONE', #21979, #20437, #152563, .T. ) ;
#229916=CARTESIAN_POINT ( 'NONE',  ( 21.05000000000000071, 16.98881331171930498, -224.4946931418895417 ) ) ;
#229930=CARTESIAN_POINT ( 'NONE',  ( 18.46947024752519795, -7.804717577830918351, -209.8502511493057909 ) ) ;
#229957=DIRECTION ( 'NONE',  ( 1.000000000000000000, 3.190570557967288949E-16, 6.948722487160392945E-17 ) ) ;
#229981=EDGE_CURVE ( 'NONE', #63849, #156342, #218901, .T. ) ;
#230024=CYLINDRICAL_SURFACE ( 'NONE', #255977, 12.87499999999999467 ) ;
#230048=DIRECTION ( 'NONE',  ( -1.000000000000000000, -0.000000000000000000, -0.000000000000000000 ) ) ;
#230070=CARTESIAN_POINT ( 'NONE',  ( -18.50000000000000711, -7.664336336125146865, -210.0813447150619027 ) ) ;
#230091=FACE_OUTER_BOUND ( 'NONE', #212419, .T. ) ;
#230105=CIRCLE ( 'NONE', #13466, 0.2000000000000108080 ) ;
#230111=DIRECTION ( 'NONE',  ( -2.578261006436899437E-14, 0.3427706569149662208, -0.9394191166662952952 ) ) ;
#230121=ORIENTED_EDGE ( 'NONE', *, *, #145097, .F. ) ;
#230148=CARTESIAN_POINT ( 'NONE',  ( 20.85000000000000142, -4.254329952141541860, -236.2118329068272260 ) ) ;
#230162=EDGE_CURVE ( 'NONE', #83472, #229005, #209287, .T. ) ;
#230172=CARTESIAN_POINT ( 'NONE',  ( -18.59999999999999787, 13.44116543737180081, -219.7184420207870801 ) ) ;
#230205=AXIS2_PLACEMENT_3D ( 'NONE', #22902, #161115, #141529 ) ;
#230217=FACE_OUTER_BOUND ( 'NONE', #32783, .T. ) ;
#230240=CARTESIAN_POINT ( 'NONE',  ( 18.44444291854882678, -0.7332650416222138423, -242.2292769306815501 ) ) ;
#230255=ORIENTED_EDGE ( 'NONE', *, *, #77275, .F. ) ;
#230328=DIRECTION ( 'NONE',  ( 1.000000000000000000, 1.734723475976817507E-14, 0.000000000000000000 ) ) ;
#230332=ORIENTED_EDGE ( 'NONE', *, *, #142987, .T. ) ;
#230359=ADVANCED_FACE ( 'NONE', ( #240417 ), #197423, .F. ) ;
#230386=VECTOR ( 'NONE', #135046, 1000.000000000000000 ) ;
#230404=DIRECTION ( 'NONE',  ( 0.000000000000000000, 0.2128009952263403282, -0.9770955615653358350 ) ) ;
#230419=PLANE ( 'NONE',  #212452 ) ;
#230432=ORIENTED_EDGE ( 'NONE', *, *, #6625, .F. ) ;
#230465=ORIENTED_EDGE ( 'NONE', *, *, #119522, .T. ) ;
#230485=CIRCLE ( 'NONE', #213911, 0.2000000000000111688 ) ;
#230499=LINE ( 'NONE', #90975, #145642 ) ;
#230512=CARTESIAN_POINT ( 'NONE',  ( 20.94999999999999929, 18.34711819382569686, -236.8747682978092541 ) ) ;
#230530=AXIS2_PLACEMENT_3D ( 'NONE', #246003, #105149, #208171 ) ;
#230563=DIRECTION ( 'NONE',  ( 1.000000000000000000, 0.000000000000000000, 0.000000000000000000 ) ) ;
#230566=AXIS2_PLACEMENT_3D ( 'NONE', #247554, #31112, #49351 ) ;
#230580=DIRECTION ( 'NONE',  ( 0.000000000000000000, -0.9770955615653357240, -0.2128009952263406890 ) ) ;
#230590=AXIS2_PLACEMENT_3D ( 'NONE', #88617, #192888, #249022 ) ;
#230618=CARTESIAN_POINT ( 'NONE',  ( 23.15000000000000213, -13.88357498613435048, -191.9982587459959689 ) ) ;
#230644=DIRECTION ( 'NONE',  ( 0.000000000000000000, 0.2128009952263982818, -0.9770955615653232895 ) ) ;
#230664=DIRECTION ( 'NONE',  ( 1.000000000000000000, -5.337610695313232452E-15, 0.000000000000000000 ) ) ;
#230670=DIRECTION ( 'NONE',  ( -1.000000000000000000, 0.000000000000000000, 0.000000000000000000 ) ) ;
#230675=VERTEX_POINT ( 'NONE', #178896 ) ;
#230728=EDGE_LOOP ( 'NONE', ( #161103, #102630, #29026, #95739, #221414 ) ) ;
#230740=ORIENTED_EDGE ( 'NONE', *, *, #24405, .F. ) ;
#230783=DIRECTION ( 'NONE',  ( -0.000000000000000000, 0.9770955615653313941, 0.2128009952263603954 ) ) ;
#230786=B_SPLINE_CURVE_WITH_KNOTS ( 'NONE', 3,
 ( #194991, #95845, #254874, #93292, #150709, #192403, #230240, #13764, #76289, #34635 ),
 .UNSPECIFIED., .F., .F.,
 ( 4, 2, 2, 2, 4 ),
 ( 0.000000000000000000, 0.0001660831991682816685, 0.0002491247987523890822, 0.0002906455985444105611, 0.0003321663983364320401 ),
 .UNSPECIFIED. ) ;
#230796=EDGE_LOOP ( 'NONE', ( #160802, #57831, #209582, #47277 ) ) ;
#230804=CARTESIAN_POINT ( 'NONE',  ( -21.05000000000000071, -1.448735025027834800, -194.7511878402588934 ) ) ;
#230811=ORIENTED_EDGE ( 'NONE', *, *, #201847, .F. ) ;
#230822=DIRECTION ( 'NONE',  ( 0.000000000000000000, -0.2128009952263605897, 0.9770955615653315052 ) ) ;
#230857=VECTOR ( 'NONE', #113619, 1000.000000000000114 ) ;
#230897=ORIENTED_EDGE ( 'NONE', *, *, #182059, .T. ) ;
#230898=CIRCLE ( 'NONE', #51976, 7.800000000000002487 ) ;
#230908=DIRECTION ( 'NONE',  ( -1.000000000000000000, 0.000000000000000000, 0.000000000000000000 ) ) ;
#230916=CARTESIAN_POINT ( 'NONE',  ( -21.14250536705909056, -1.387073526285510061, -194.6311228964526663 ) ) ;
#230924=CYLINDRICAL_SURFACE ( 'NONE', #14956, 0.1000000000000122874 ) ;
#230940=EDGE_CURVE ( 'NONE', #191212, #211554, #181386, .T. ) ;
#230954=VERTEX_POINT ( 'NONE', #2704 ) ;
#230957=ORIENTED_EDGE ( 'NONE', *, *, #241553, .T. ) ;
#230974=ORIENTED_EDGE ( 'NONE', *, *, #99395, .T. ) ;
#230990=CIRCLE ( 'NONE', #52062, 11.90000000000001457 ) ;
#230991=CARTESIAN_POINT ( 'NONE',  ( -21.05000000000000071, 0.3882413827466408840, -209.1776850584169551 ) ) ;
#231008=PLANE ( 'NONE',  #92831 ) ;
#231009=CARTESIAN_POINT ( 'NONE',  ( 18.52928932304151033, 15.29497926255971230, -222.9236147070920424 ) ) ;
#231015=ADVANCED_FACE ( 'NONE', ( #80952 ), #41872, .T. ) ;
#231029=AXIS2_PLACEMENT_3D ( 'NONE', #197971, #14236, #64877 ) ;
#231033=CIRCLE ( 'NONE', #131048, 0.09999999999999939493 ) ;
#231075=AXIS2_PLACEMENT_3D ( 'NONE', #218477, #174297, #236768 ) ;
#231122=ORIENTED_EDGE ( 'NONE', *, *, #223318, .T. ) ;
#231127=ORIENTED_EDGE ( 'NONE', *, *, #149382, .F. ) ;
#231135=ADVANCED_FACE ( 'NONE', ( #209925, #233350 ), #192919, .T. ) ;
#231152=ADVANCED_FACE ( 'NONE', ( #170836 ), #194744, .T. ) ;
#231179=LINE ( 'NONE', #10827, #68073 ) ;
#231190=DIRECTION ( 'NONE',  ( 0.000000000000000000, 0.2128009952263485993, -0.9770955615653341697 ) ) ;
#231195=CYLINDRICAL_SURFACE ( 'NONE', #169579, 0.1000000000000055844 ) ;
#231201=LINE ( 'NONE', #210343, #224132 ) ;
#231223=CARTESIAN_POINT ( 'NONE',  ( -18.47140463609786920, -0.9011515821983938634, -242.3107253779298844 ) ) ;
#231255=CARTESIAN_POINT ( 'NONE',  ( 22.47071067811865319, 7.522163794833003791, -199.2603376134759117 ) ) ;
#231282=CARTESIAN_POINT ( 'NONE',  ( -20.85000000000000142, 18.41524492703432614, -237.0006385043383546 ) ) ;
#231330=VECTOR ( 'NONE', #39012, 1000.000000000000114 ) ;
#231349=CARTESIAN_POINT ( 'NONE',  ( 19.75857864376268935, 16.64998792410002793, -222.7039835543563981 ) ) ;
#231377=DIRECTION ( 'NONE',  ( 1.000000000000000000, -0.000000000000000000, -0.000000000000000000 ) ) ;
#231406=AXIS2_PLACEMENT_3D ( 'NONE', #212110, #173017, #251203 ) ;
#231419=VERTEX_POINT ( 'NONE', #46651 ) ;
#231431=CIRCLE ( 'NONE', #94045, 0.2000000000000111688 ) ;
#231450=FACE_OUTER_BOUND ( 'NONE', #89031, .T. ) ;
#231467=DIRECTION ( 'NONE',  ( 1.000000000000000000, -0.000000000000000000, -0.000000000000000000 ) ) ;
#231483=CARTESIAN_POINT ( 'NONE',  ( -20.85000000000000142, 7.128833340094563376, -233.7327013124401276 ) ) ;
#231514=ORIENTED_EDGE ( 'NONE', *, *, #152094, .T. ) ;
#231575=DIRECTION ( 'NONE',  ( 0.000000000000000000, -0.2128009952263605342, 0.9770955615653315052 ) ) ;
#231576=CARTESIAN_POINT ( 'NONE',  ( 21.04999999999999361, 11.16637775885291894, -211.0297240376519596 ) ) ;
#231604=VERTEX_POINT ( 'NONE', #33573 ) ;
#231625=ORIENTED_EDGE ( 'NONE', *, *, #65568, .F. ) ;
#231626=ORIENTED_EDGE ( 'NONE', *, *, #117469, .T. ) ;
#231641=EDGE_CURVE ( 'NONE', #227863, #24784, #57700, .T. ) ;
#231643=FACE_OUTER_BOUND ( 'NONE', #236256, .T. ) ;
#231661=ADVANCED_FACE ( 'NONE', ( #77761 ), #136812, .T. ) ;
#231668=VECTOR ( 'NONE', #224765, 1000.000000000000227 ) ;
#231728=AXIS2_PLACEMENT_3D ( 'NONE', #12038, #148978, #131956 ) ;
#231735=DIRECTION ( 'NONE',  ( 0.000000000000000000, 0.9770955615653548199, 0.2128009952262535920 ) ) ;
#231737=DIRECTION ( 'NONE',  ( 0.000000000000000000, 0.2128009952263606730, -0.9770955615653313941 ) ) ;
#231783=DIRECTION ( 'NONE',  ( 0.000000000000000000, 0.2128009952263603399, -0.9770955615653315052 ) ) ;
#231798=DIRECTION ( 'NONE',  ( 0.000000000000000000, 0.2128009952263605620, -0.9770955615653315052 ) ) ;
#231804=VECTOR ( 'NONE', #184299, 1000.000000000000000 ) ;
#231808=DIRECTION ( 'NONE',  ( 0.000000000000000000, 0.2128009952263603677, -0.9770955615653313941 ) ) ;
#231814=DIRECTION ( 'NONE',  ( 1.000000000000000000, 0.000000000000000000, 0.000000000000000000 ) ) ;
#231815=CARTESIAN_POINT ( 'NONE',  ( -21.05000000000000071, 6.166536471686127285, -199.6742082547079065 ) ) ;
#231866=DIRECTION ( 'NONE',  ( 0.000000000000000000, 0.2128009952263403282, -0.9770955615653358350 ) ) ;
#231887=DIRECTION ( 'NONE',  ( 0.000000000000000000, -0.2128009952264231230, 0.9770955615653178494 ) ) ;
#231924=DIRECTION ( 'NONE',  ( 1.000000000000000000, 0.000000000000000000, 0.000000000000000000 ) ) ;
#231980=FACE_OUTER_BOUND ( 'NONE', #179833, .T. ) ;
#231995=CARTESIAN_POINT ( 'NONE',  ( 20.12500000000000000, 14.02742277431099893, -219.5907614236512870 ) ) ;
#232007=AXIS2_PLACEMENT_3D ( 'NONE', #149616, #87021, #46614 ) ;
#232015=VECTOR ( 'NONE', #48852, 999.9999999999998863 ) ;
#232029=DIRECTION ( 'NONE',  ( 0.000000000000000000, -0.2128009952263606452, 0.9770955615653315052 ) ) ;
#232053=CARTESIAN_POINT ( 'NONE',  ( 20.94999999999999929, 10.68863688179708049, -222.5873974249508933 ) ) ;
#232058=CARTESIAN_POINT ( 'NONE',  ( 20.97239005616513552, 11.27841523495330200, -211.0809943295646747 ) ) ;
#232062=EDGE_CURVE ( 'NONE', #136369, #192375, #219230, .T. ) ;
#232080=ORIENTED_EDGE ( 'NONE', *, *, #152951, .F. ) ;
#232086=CARTESIAN_POINT ( 'NONE',  ( -21.05000000000000426, -1.335570543289804402, -194.7977936451528080 ) ) ;
#232104=DIRECTION ( 'NONE',  ( 0.000000000000000000, -0.2128009952263605342, 0.9770955615653315052 ) ) ;
#232107=VERTEX_POINT ( 'NONE', #180130 ) ;
#232113=DIRECTION ( 'NONE',  ( -1.000000000000000000, 0.000000000000000000, 0.000000000000000000 ) ) ;
#232123=DIRECTION ( 'NONE',  ( 0.7071067811865302533, -0.6909108974501196876, -0.1504730267679053324 ) ) ;
#232132=CARTESIAN_POINT ( 'NONE',  ( 18.59999999999999787, 7.939498413483247141, -209.7295111514051200 ) ) ;
#232177=DIRECTION ( 'NONE',  ( 1.000000000000000000, 0.000000000000000000, 0.000000000000000000 ) ) ;
#232266=DIRECTION ( 'NONE',  ( 0.000000000000000000, 0.2128009952263403282, -0.9770955615653358350 ) ) ;
#232286=DIRECTION ( 'NONE',  ( 0.000000000000000000, 0.2128009952263485993, -0.9770955615653341697 ) ) ;
#232301=CARTESIAN_POINT ( 'NONE',  ( 20.94999999999999574, 11.84624361595475506, -206.1763227999733203 ) ) ;
#232316=CIRCLE ( 'NONE', #86506, 0.09999999999999939493 ) ;
#232330=CARTESIAN_POINT ( 'NONE',  ( 18.59999999999999076, 16.67126802362266247, -222.8016931105129004 ) ) ;
#232353=VERTEX_POINT ( 'NONE', #250363 ) ;
#232370=VERTEX_POINT ( 'NONE', #251645 ) ;
#232372=ADVANCED_FACE ( 'NONE', ( #249099 ), #162150, .F. ) ;
#232381=ORIENTED_EDGE ( 'NONE', *, *, #124889, .T. ) ;
#232384=CARTESIAN_POINT ( 'NONE',  ( -20.85000000000000142, 18.51199663233067483, -231.2535697180530292 ) ) ;
#232396=CIRCLE ( 'NONE', #15742, 4.049999999999995381 ) ;
#232408=FACE_OUTER_BOUND ( 'NONE', #154141, .T. ) ;
#232425=DIRECTION ( 'NONE',  ( 2.952720810173288126E-16, -0.9770955615653313941, -0.2128009952263603677 ) ) ;
#232461=CARTESIAN_POINT ( 'NONE',  ( 18.58685178364169488, -7.675193378770480912, -209.9630017811346079 ) ) ;
#232468=CARTESIAN_POINT ( 'NONE',  ( 21.05000000000326210, 6.351002464453129548, -199.6318190572282845 ) ) ;
#232474=VERTEX_POINT ( 'NONE', #24619 ) ;
#232476=FACE_OUTER_BOUND ( 'NONE', #108818, .T. ) ;
#232487=DIRECTION ( 'NONE',  ( 1.000000000000000000, 0.000000000000000000, 0.000000000000000000 ) ) ;
#232499=CYLINDRICAL_SURFACE ( 'NONE', #11885, 11.80000000000000959 ) ;
#232502=VERTEX_POINT ( 'NONE', #47990 ) ;
#232511=EDGE_CURVE ( 'NONE', #227124, #237840, #207940, .T. ) ;
#232522=CARTESIAN_POINT ( 'NONE',  ( 18.39999999999999858, -7.785976468740638090, -209.8926132507865816 ) ) ;
#232527=CIRCLE ( 'NONE', #182623, 4.000000000000006217 ) ;
#232532=VECTOR ( 'NONE', #241388, 1000.000000000000227 ) ;
#232540=VECTOR ( 'NONE', #67180, 1000.000000000000227 ) ;
#232545=CARTESIAN_POINT ( 'NONE',  ( 21.07928932188134397, 6.162520550847347955, -199.5566553493351307 ) ) ;
#232582=CARTESIAN_POINT ( 'NONE',  ( -22.50000000000094147, -2.381330705637573431, -189.5959759702857923 ) ) ;
#232609=EDGE_CURVE ( 'NONE', #34173, #80924, #149681, .T. ) ;
#232615=DIRECTION ( 'NONE',  ( 0.000000000000000000, 0.2128009952263678062, -0.9770955615653298398 ) ) ;
#232663=CONICAL_SURFACE ( 'NONE', #170146, 6.250000000000010658, 0.7853981633974431720 ) ;
#232673=EDGE_CURVE ( 'NONE', #249430, #59785, #137180, .T. ) ;
#232684=CARTESIAN_POINT ( 'NONE',  ( -21.05000000000000071, 3.047642603966940200, -208.5984958277594785 ) ) ;
#232701=SPHERICAL_SURFACE ( 'NONE', #248876, 0.1000000000000000056 ) ;
#232705=DIRECTION ( 'NONE',  ( -6.938893903906983515E-14, -0.9394191166662618775, -0.3427706569150580362 ) ) ;
#232712=CARTESIAN_POINT ( 'NONE',  ( -18.59999999999999787, 12.87592094156238609, -205.3750039893633073 ) ) ;
#232786=CARTESIAN_POINT ( 'NONE',  ( -20.64999999999999858, 6.878457983866232972, -212.1414458560986986 ) ) ;
#232829=VERTEX_POINT ( 'NONE', #202909 ) ;
#232830=ORIENTED_EDGE ( 'NONE', *, *, #249299, .T. ) ;
#232861=ADVANCED_FACE ( 'NONE', ( #85490 ), #201624, .F. ) ;
#232867=FACE_OUTER_BOUND ( 'NONE', #12270, .T. ) ;
#232881=EDGE_CURVE ( 'NONE', #89128, #124170, #241432, .T. ) ;
#232910=ADVANCED_FACE ( 'NONE', ( #131072 ), #162325, .T. ) ;
#232926=EDGE_CURVE ( 'NONE', #118980, #54351, #220580, .T. ) ;
#232932=DIRECTION ( 'NONE',  ( -1.000000000000000000, -0.000000000000000000, -0.000000000000000000 ) ) ;
#232935=LINE ( 'NONE', #11298, #133774 ) ;
#232938=DIRECTION ( 'NONE',  ( 0.000000000000000000, -0.2128009952263485993, 0.9770955615653341697 ) ) ;
#233023=VERTEX_POINT ( 'NONE', #249743 ) ;
#233038=DIRECTION ( 'NONE',  ( -0.000000000000000000, -0.9770955615653316162, -0.2128009952263597848 ) ) ;
#233066=ORIENTED_EDGE ( 'NONE', *, *, #255162, .T. ) ;
#233074=AXIS2_PLACEMENT_3D ( 'NONE', #200487, #115815, #256545 ) ;
#233082=DIRECTION ( 'NONE',  ( 0.000000000000000000, -0.2128009952263982818, 0.9770955615653232895 ) ) ;
#233086=FACE_OUTER_BOUND ( 'NONE', #18677, .T. ) ;
#233143=DIRECTION ( 'NONE',  ( -4.239556034732055511E-17, -0.08413937888704771384, 0.9964539953858891908 ) ) ;
#233158=CARTESIAN_POINT ( 'NONE',  ( 21.12769345151713196, 13.08004441897819170, -210.6858836008591140 ) ) ;
#233167=FACE_OUTER_BOUND ( 'NONE', #188271, .T. ) ;
#233185=ORIENTED_EDGE ( 'NONE', *, *, #166432, .F. ) ;
#233203=CYLINDRICAL_SURFACE ( 'NONE', #103648, 11.74999999999999289 ) ;
#233216=CARTESIAN_POINT ( 'NONE',  ( -18.59999999999999787, 11.72137559264762174, -210.8820217676538391 ) ) ;
#233225=CIRCLE ( 'NONE', #120787, 0.09999999999999724387 ) ;
#233235=CONICAL_SURFACE ( 'NONE', #154143, 4.299999999999966960, 0.7853981633974466137 ) ;
#233255=CARTESIAN_POINT ( 'NONE',  ( 23.14999999999999858, 17.01923898301590654, -224.3994341343041867 ) ) ;
#233261=EDGE_LOOP ( 'NONE', ( #69692, #38391, #32997, #161756 ) ) ;
#233281=FACE_OUTER_BOUND ( 'NONE', #75830, .T. ) ;
#233332=ORIENTED_EDGE ( 'NONE', *, *, #108317, .F. ) ;
#233342=ORIENTED_EDGE ( 'NONE', *, *, #89213, .T. ) ;
#233350=FACE_OUTER_BOUND ( 'NONE', #117865, .T. ) ;
#233355=EDGE_LOOP ( 'NONE', ( #140331, #144372, #79620, #26825, #189226, #235666, #143564, #21326, #225461, #190342, #245831, #30631, #197249, #103327, #103337, #120769, #118132, #100509, #197883, #158006, #248884, #104729, #193631 ) ) ;
#233367=TOROIDAL_SURFACE ( 'NONE', #229257, 12.97499999999999787, 0.1000000000000000056 ) ;
#233386=VERTEX_POINT ( 'NONE', #47363 ) ;
#233428=AXIS2_PLACEMENT_3D ( 'NONE', #9237, #130468, #227001 ) ;
#233448=DIRECTION ( 'NONE',  ( 1.000000000000000000, 0.000000000000000000, 0.000000000000000000 ) ) ;
#233461=FACE_OUTER_BOUND ( 'NONE', #182229, .T. ) ;
#233469=CIRCLE ( 'NONE', #200133, 0.1000000000000008937 ) ;
#233475=CARTESIAN_POINT ( 'NONE',  ( 20.85000000000000142, 7.882824859404637508, -245.3558965132535832 ) ) ;
#233480=ORIENTED_EDGE ( 'NONE', *, *, #133824, .F. ) ;
#233483=ORIENTED_EDGE ( 'NONE', *, *, #54054, .F. ) ;
#233496=ORIENTED_EDGE ( 'NONE', *, *, #37920, .T. ) ;
#233505=ORIENTED_EDGE ( 'NONE', *, *, #148255, .F. ) ;
#233515=ORIENTED_EDGE ( 'NONE', *, *, #91740, .F. ) ;
#233608=VECTOR ( 'NONE', #196220, 1000.000000000000114 ) ;
#233621=ORIENTED_EDGE ( 'NONE', *, *, #129390, .F. ) ;
#233624=AXIS2_PLACEMENT_3D ( 'NONE', #194200, #174670, #14280 ) ;
#233625=CARTESIAN_POINT ( 'NONE',  ( 18.50211644919734866, 18.36312997293287097, -236.9042258689303821 ) ) ;
#233631=ORIENTED_EDGE ( 'NONE', *, *, #78815, .F. ) ;
#233659=DIRECTION ( 'NONE',  ( 0.000000000000000000, -0.9770955615653357240, -0.2128009952263406890 ) ) ;
#233708=DIRECTION ( 'NONE',  ( -0.000000000000000000, 0.9770955615653313941, 0.2128009952263603954 ) ) ;
#233721=EDGE_CURVE ( 'NONE', #232502, #208402, #187644, .T. ) ;
#233748=ORIENTED_EDGE ( 'NONE', *, *, #121236, .F. ) ;
#233772=CARTESIAN_POINT ( 'NONE',  ( -20.94999999999999929, 7.675662554762638479, -241.7139905447625381 ) ) ;
#233776=DIRECTION ( 'NONE',  ( 1.000000000000000000, 0.000000000000000000, 0.000000000000000000 ) ) ;
#233824=FACE_OUTER_BOUND ( 'NONE', #170104, .T. ) ;
#233836=CARTESIAN_POINT ( 'NONE',  ( -20.93302460841142931, 18.38637412622486877, -236.9471295141160283 ) ) ;
#233870=ORIENTED_EDGE ( 'NONE', *, *, #7318, .F. ) ;
#233878=EDGE_LOOP ( 'NONE', ( #250714, #49669, #79104, #146452 ) ) ;
#233881=EDGE_CURVE ( 'NONE', #8823, #164555, #46152, .T. ) ;
#233921=ORIENTED_EDGE ( 'NONE', *, *, #69256, .F. ) ;
#233922=EDGE_LOOP ( 'NONE', ( #52553, #246751, #245408, #106893, #220833 ) ) ;
#233947=DIRECTION ( 'NONE',  ( 0.000000000000000000, 0.2128009952263603954, -0.9770955615653315052 ) ) ;
#233961=FACE_OUTER_BOUND ( 'NONE', #199959, .T. ) ;
#233963=FACE_OUTER_BOUND ( 'NONE', #70107, .T. ) ;
#233971=DIRECTION ( 'NONE',  ( 0.000000000000000000, 0.2128009952263485993, -0.9770955615653341697 ) ) ;
#234003=DIRECTION ( 'NONE',  ( 0.000000000000000000, -0.9525900758537790836, 0.3042567129660269099 ) ) ;
#234009=EDGE_LOOP ( 'NONE', ( #186486, #181295, #168783, #51256 ) ) ;
#234059=CARTESIAN_POINT ( 'NONE',  ( -21.05000000000000071, 7.128833340094563376, -233.7327013124401276 ) ) ;
#234078=VERTEX_POINT ( 'NONE', #171565 ) ;
#234082=CYLINDRICAL_SURFACE ( 'NONE', #220252, 4.000000000000006217 ) ;
#234087=AXIS2_PLACEMENT_3D ( 'NONE', #139566, #234842, #198273 ) ;
#234117=CIRCLE ( 'NONE', #242504, 0.09999999999999080458 ) ;
#234125=EDGE_CURVE ( 'NONE', #8823, #102962, #209370, .T. ) ;
#234131=AXIS2_PLACEMENT_3D ( 'NONE', #120617, #21511, #124459 ) ;
#234188=AXIS2_PLACEMENT_3D ( 'NONE', #140827, #41746, #200800 ) ;
#234191=AXIS2_PLACEMENT_3D ( 'NONE', #81951, #145801, #2436 ) ;
#234202=EDGE_CURVE ( 'NONE', #159889, #126149, #112842, .T. ) ;
#234211=EDGE_CURVE ( 'NONE', #102386, #229705, #217051, .T. ) ;
#234257=ORIENTED_EDGE ( 'NONE', *, *, #126555, .F. ) ;
#234267=ORIENTED_EDGE ( 'NONE', *, *, #145678, .F. ) ;
#234273=ORIENTED_EDGE ( 'NONE', *, *, #93083, .T. ) ;
#234356=ADVANCED_FACE ( 'NONE', ( #44864 ), #244332, .T. ) ;
#234437=ORIENTED_EDGE ( 'NONE', *, *, #121067, .F. ) ;
#234442=EDGE_LOOP ( 'NONE', ( #233921, #244112, #23457, #234785 ) ) ;
#234456=CARTESIAN_POINT ( 'NONE',  ( 18.60000000000000142, -0.6576273345615386567, -242.5323337003318898 ) ) ;
#234462=EDGE_LOOP ( 'NONE', ( #18916, #56884, #1055, #147049, #81394 ) ) ;
#234491=CARTESIAN_POINT ( 'NONE',  ( -21.05000000000000071, 0.6656436123793491033, -212.6810495496487476 ) ) ;
#234500=VERTEX_POINT ( 'NONE', #157841 ) ;
#234506=DIRECTION ( 'NONE',  ( 0.000000000000000000, -0.2128009952263603954, 0.9770955615653315052 ) ) ;
#234513=CARTESIAN_POINT ( 'NONE',  ( -22.59999999999999787, -2.401771312552908544, -189.4980873520049727 ) ) ;
#234546=EDGE_CURVE ( 'NONE', #86168, #88245, #104736, .T. ) ;
#234555=ORIENTED_EDGE ( 'NONE', *, *, #109583, .T. ) ;
#234608=VERTEX_POINT ( 'NONE', #104218 ) ;
#234630=CARTESIAN_POINT ( 'NONE',  ( -20.54999999999999716, 11.74265569217025629, -210.9797313238103698 ) ) ;
#234643=CIRCLE ( 'NONE', #113838, 11.80000000000000604 ) ;
#234656=DIRECTION ( 'NONE',  ( -2.952720810173288126E-16, 0.9770955615653313941, 0.2128009952263603677 ) ) ;
#234668=ORIENTED_EDGE ( 'NONE', *, *, #139158, .T. ) ;
#234671=CYLINDRICAL_SURFACE ( 'NONE', #48109, 0.09999999999999939493 ) ;
#234676=EDGE_CURVE ( 'NONE', #187924, #54334, #85924, .T. ) ;
#234683=CIRCLE ( 'NONE', #176253, 0.1999999999999987899 ) ;
#234707=CARTESIAN_POINT ( 'NONE',  ( -21.05000000000000071, 16.98881331171929787, -224.4946931418895417 ) ) ;
#234709=ORIENTED_EDGE ( 'NONE', *, *, #195975, .T. ) ;
#234726=AXIS2_PLACEMENT_3D ( 'NONE', #134386, #256869, #99105 ) ;
#234767=EDGE_LOOP ( 'NONE', ( #189626, #67362, #90368, #217473 ) ) ;
#234769=DIRECTION ( 'NONE',  ( -1.000000000000000000, 0.000000000000000000, 0.000000000000000000 ) ) ;
#234785=ORIENTED_EDGE ( 'NONE', *, *, #20280, .F. ) ;
#234787=CARTESIAN_POINT ( 'NONE',  ( -18.59999999999999787, 14.61354176542825201, -235.9279552357344016 ) ) ;
#234827=ORIENTED_EDGE ( 'NONE', *, *, #165292, .T. ) ;
#234828=ORIENTED_EDGE ( 'NONE', *, *, #51005, .T. ) ;
#234829=CYLINDRICAL_SURFACE ( 'NONE', #189025, 0.1000000000000055844 ) ;
#234842=DIRECTION ( 'NONE',  ( -1.000000000000000000, -0.000000000000000000, -0.000000000000000000 ) ) ;
#234875=ORIENTED_EDGE ( 'NONE', *, *, #69030, .F. ) ;
#234881=VERTEX_POINT ( 'NONE', #183162 ) ;
#234886=DIRECTION ( 'NONE',  ( 0.000000000000000000, 0.2128009952263596460, -0.9770955615653317272 ) ) ;
#234889=EDGE_CURVE ( 'NONE', #170466, #175208, #140148, .T. ) ;
#234953=ORIENTED_EDGE ( 'NONE', *, *, #218461, .T. ) ;
#234954=AXIS2_PLACEMENT_3D ( 'NONE', #185452, #6808, #247981 ) ;
#234968=DIRECTION ( 'NONE',  ( 1.000000000000000000, 7.136802563874199107E-16, 1.554319503706929991E-16 ) ) ;
#234994=EDGE_CURVE ( 'NONE', #71034, #175321, #9649, .T. ) ;
#234999=ORIENTED_EDGE ( 'NONE', *, *, #186001, .T. ) ;
#235002=ORIENTED_EDGE ( 'NONE', *, *, #14134, .T. ) ;
#235037=VECTOR ( 'NONE', #161121, 1000.000000000000000 ) ;
#235038=LINE ( 'NONE', #14726, #67910 ) ;
#235041=EDGE_LOOP ( 'NONE', ( #143199, #245339, #240715, #59766 ) ) ;
#235045=CARTESIAN_POINT ( 'NONE',  ( 20.95159278453404283, 10.50942287431401390, -207.3947732279067395 ) ) ;
#235065=CARTESIAN_POINT ( 'NONE',  ( 20.94999999999999929, 18.51199663233068193, -231.2535697180530292 ) ) ;
#235067=PLANE ( 'NONE',  #134959 ) ;
#235075=CARTESIAN_POINT ( 'NONE',  ( 18.42595409746876101, -7.792936377315665908, -209.8606553024481798 ) ) ;
#235091=CARTESIAN_POINT ( 'NONE',  ( -21.95218792049438861, -1.435727727154726185, -193.9423655747830537 ) ) ;
#235118=AXIS2_PLACEMENT_3D ( 'NONE', #72938, #228136, #49490 ) ;
#235122=DIRECTION ( 'NONE',  ( 1.000000000000000000, 0.000000000000000000, 0.000000000000000000 ) ) ;
#235132=EDGE_LOOP ( 'NONE', ( #221719, #169383, #90629, #136115 ) ) ;
#235148=TOROIDAL_SURFACE ( 'NONE', #81000, 0.2000000000000000111, 0.1000000000000000056 ) ;
#235166=ORIENTED_EDGE ( 'NONE', *, *, #16340, .T. ) ;
#235172=DIRECTION ( 'NONE',  ( 1.000000000000000000, -0.000000000000000000, 0.000000000000000000 ) ) ;
#235195=CARTESIAN_POINT ( 'NONE',  ( -23.15000000000000213, 6.268811756569107274, -220.3853799378769622 ) ) ;
#235199=ORIENTED_EDGE ( 'NONE', *, *, #18965, .F. ) ;
#235275=EDGE_LOOP ( 'NONE', ( #2942, #217450, #32029, #17408 ) ) ;
#235282=CARTESIAN_POINT ( 'NONE',  ( -23.15000000000000213, -3.770473190032741062, -225.9805569534692324 ) ) ;
#235300=LINE ( 'NONE', #73699, #90186 ) ;
#235324=CARTESIAN_POINT ( 'NONE',  ( -18.52309608778515226, -0.8639146907862034208, -242.3454321524539523 ) ) ;
#235326=ORIENTED_EDGE ( 'NONE', *, *, #145678, .T. ) ;
#235339=DIRECTION ( 'NONE',  ( -1.000000000000000000, -0.000000000000000000, -0.000000000000000000 ) ) ;
#235344=DIRECTION ( 'NONE',  ( 1.000000000000000000, 0.000000000000000000, 0.000000000000000000 ) ) ;
#235355=AXIS2_PLACEMENT_3D ( 'NONE', #369, #202436, #218121 ) ;
#235362=CARTESIAN_POINT ( 'NONE',  ( 21.46681500598198156, -1.459285199489900542, -194.2995562827431684 ) ) ;
#235371=CARTESIAN_POINT ( 'NONE',  ( 20.22894356738504129, 10.82552933503960446, -207.1046633763657496 ) ) ;
#235392=DIRECTION ( 'NONE',  ( 0.000000000000000000, 0.7397890806274223241, 0.6728388485993012091 ) ) ;
#235410=CIRCLE ( 'NONE', #143667, 12.87499999999999467 ) ;
#235411=VERTEX_POINT ( 'NONE', #27661 ) ;
#235415=ORIENTED_EDGE ( 'NONE', *, *, #168538, .T. ) ;
#235422=DIRECTION ( 'NONE',  ( 0.000000000000000000, 0.9770955615653259541, 0.2128009952263860971 ) ) ;
#235425=CARTESIAN_POINT ( 'NONE',  ( 18.49999999999999289, 3.801854678198143933, -188.1465607323988252 ) ) ;
#235457=CARTESIAN_POINT ( 'NONE',  ( -22.00411653889210584, -1.446770167451707723, -193.8916177604859854 ) ) ;
#235471=EDGE_CURVE ( 'NONE', #139087, #87352, #17120, .T. ) ;
#235474=ORIENTED_EDGE ( 'NONE', *, *, #24391, .F. ) ;
#235484=EDGE_CURVE ( 'NONE', #142228, #214061, #126064, .T. ) ;
#235515=ORIENTED_EDGE ( 'NONE', *, *, #17880, .F. ) ;
#235545=VERTEX_POINT ( 'NONE', #152736 ) ;
#235580=CIRCLE ( 'NONE', #210648, 0.09999999999999832634 ) ;
#235587=VERTEX_POINT ( 'NONE', #210126 ) ;
#235590=EDGE_CURVE ( 'NONE', #175208, #169080, #154040, .T. ) ;
#235593=EDGE_CURVE ( 'NONE', #236966, #28807, #46955, .T. ) ;
#235605=DIRECTION ( 'NONE',  ( 0.000000000000000000, 0.6728388485993012091, -0.7397890806274222131 ) ) ;
#235622=DIRECTION ( 'NONE',  ( 1.000000000000000000, 0.000000000000000000, 0.000000000000000000 ) ) ;
#235627=ORIENTED_EDGE ( 'NONE', *, *, #103234, .T. ) ;
#235648=DIRECTION ( 'NONE',  ( 0.000000000000000000, -0.9770955615653301729, -0.2128009952263661964 ) ) ;
#235666=ORIENTED_EDGE ( 'NONE', *, *, #30353, .T. ) ;
#235714=VERTEX_POINT ( 'NONE', #45597 ) ;
#235720=CARTESIAN_POINT ( 'NONE',  ( 21.05000000000000071, 7.872214528623314500, -209.6555322433423498 ) ) ;
#235729=AXIS2_PLACEMENT_3D ( 'NONE', #52770, #95743, #132318 ) ;
#235733=DIRECTION ( 'NONE',  ( 0.000000000000000000, -0.2128009952263603954, 0.9770955615653315052 ) ) ;
#235764=ORIENTED_EDGE ( 'NONE', *, *, #121476, .F. ) ;
#235798=FACE_OUTER_BOUND ( 'NONE', #77072, .T. ) ;
#235812=ORIENTED_EDGE ( 'NONE', *, *, #234211, .F. ) ;
#235813=DIRECTION ( 'NONE',  ( -1.000000000000000000, -8.673617379884087537E-15, 0.000000000000000000 ) ) ;
#235846=CIRCLE ( 'NONE', #11000, 0.09999999999999939493 ) ;
#235859=AXIS2_PLACEMENT_3D ( 'NONE', #172758, #230111, #232705 ) ;
#235871=ORIENTED_EDGE ( 'NONE', *, *, #136931, .T. ) ;
#235910=VECTOR ( 'NONE', #75828, 1000.000000000000114 ) ;
#235911=ORIENTED_EDGE ( 'NONE', *, *, #235484, .F. ) ;
#235913=EDGE_LOOP ( 'NONE', ( #178322, #108199, #65050, #55008 ) ) ;
#235918=CARTESIAN_POINT ( 'NONE',  ( 23.14999999999999147, 4.054946580507614584, -200.1168758698121053 ) ) ;
#235933=CARTESIAN_POINT ( 'NONE',  ( 23.24999999999999289, 13.96869538424789070, -210.3925794786331949 ) ) ;
#235977=DIRECTION ( 'NONE',  ( 0.000000000000000000, 0.2128009952264665328, -0.9770955615653084125 ) ) ;
#235979=ORIENTED_EDGE ( 'NONE', *, *, #132698, .F. ) ;
#236012=CARTESIAN_POINT ( 'NONE',  ( -20.94999999999999929, -10.38870553492056104, -206.3818953267866902 ) ) ;
#236046=ORIENTED_EDGE ( 'NONE', *, *, #208907, .T. ) ;
#236047=AXIS2_PLACEMENT_3D ( 'NONE', #41798, #20954, #121349 ) ;
#236065=CARTESIAN_POINT ( 'NONE',  ( 20.94999999999999574, 2.859758780633683273, -208.6670499591424459 ) ) ;
#236068=DIRECTION ( 'NONE',  ( -1.000000000000000000, 0.000000000000000000, 0.000000000000000000 ) ) ;
#236121=EDGE_LOOP ( 'NONE', ( #209915, #114572, #74094, #160392 ) ) ;
#236127=CARTESIAN_POINT ( 'NONE',  ( 20.95520789717937404, 11.94775306454331698, -206.1558306364165389 ) ) ;
#236132=DIRECTION ( 'NONE',  ( 0.000000000000000000, 0.2128009952263604232, -0.9770955615653316162 ) ) ;
#236133=DIRECTION ( 'NONE',  ( 0.000000000000000000, 0.2128009952263601456, -0.9770955615653316162 ) ) ;
#236146=ORIENTED_EDGE ( 'NONE', *, *, #171366, .F. ) ;
#236182=VERTEX_POINT ( 'NONE', #68699 ) ;
#236224=AXIS2_PLACEMENT_3D ( 'NONE', #110801, #250316, #251601 ) ;
#236256=EDGE_LOOP ( 'NONE', ( #208457, #207697, #140554, #67001 ) ) ;
#236273=ORIENTED_EDGE ( 'NONE', *, *, #221581, .T. ) ;
#236343=EDGE_LOOP ( 'NONE', ( #107549, #21134, #156786, #69488 ) ) ;
#236461=ADVANCED_FACE ( 'NONE', ( #90177 ), #47198, .T. ) ;
#236466=VECTOR ( 'NONE', #129735, 1000.000000000000000 ) ;
#236475=CARTESIAN_POINT ( 'NONE',  ( -21.14999999999999858, 11.50215294792677057, -198.5972978622482970 ) ) ;
#236476=DIRECTION ( 'NONE',  ( -0.000000000000000000, 0.2128009952263604232, -0.9770955615653316162 ) ) ;
#236498=AXIS2_PLACEMENT_3D ( 'NONE', #228923, #89394, #153270 ) ;
#236502=DIRECTION ( 'NONE',  ( -1.000000000000000000, 0.000000000000000000, 0.000000000000000000 ) ) ;
#236506=CARTESIAN_POINT ( 'NONE',  ( -21.05000000000000071, 2.923777413779037548, -208.5507632484912222 ) ) ;
#236541=ADVANCED_FACE ( 'NONE', ( #31550 ), #152777, .T. ) ;
#236545=CARTESIAN_POINT ( 'NONE',  ( -20.94999999999999929, 12.87592094156238964, -205.3750039893633073 ) ) ;
#236556=DIRECTION ( 'NONE',  ( -1.000000000000000000, 0.000000000000000000, 0.000000000000000000 ) ) ;
#236559=CIRCLE ( 'NONE', #70004, 0.5000000000000005551 ) ;
#236589=CARTESIAN_POINT ( 'NONE',  ( -21.05000000000000071, 0.5450571430110628945, -208.9664790259058691 ) ) ;
#236603=CARTESIAN_POINT ( 'NONE',  ( -18.50000000000000000, -0.5913595841389520658, -242.4574432119242999 ) ) ;
#236625=DIRECTION ( 'NONE',  ( 1.000000000000000000, 0.000000000000000000, 0.000000000000000000 ) ) ;
#236640=AXIS2_PLACEMENT_3D ( 'NONE', #220282, #140723, #41649 ) ;
#236655=CARTESIAN_POINT ( 'NONE',  ( -21.05000000000000071, 6.093673009692400555, -199.5727803633481301 ) ) ;
#236679=VERTEX_POINT ( 'NONE', #242543 ) ;
#236697=DIRECTION ( 'NONE',  ( -1.000000000000000000, 0.000000000000000000, -0.000000000000000000 ) ) ;
#236707=ORIENTED_EDGE ( 'NONE', *, *, #107045, .T. ) ;
#236723=LINE ( 'NONE', #196319, #230386 ) ;
#236727=ORIENTED_EDGE ( 'NONE', *, *, #230162, .T. ) ;
#236737=CARTESIAN_POINT ( 'NONE',  ( -22.39999999999999503, -1.657885652111595665, -193.3876638332971254 ) ) ;
#236757=MECHANICAL_DESIGN_GEOMETRIC_PRESENTATION_REPRESENTATION('',(#120305),#16056);
#236764=EDGE_CURVE ( 'NONE', #28455, #234500, #198282, .T. ) ;
#236768=DIRECTION ( 'NONE',  ( 0.000000000000000000, 0.2128009952263630322, -0.9770955615653309501 ) ) ;
#236777=ORIENTED_EDGE ( 'NONE', *, *, #128649, .F. ) ;
#236868=CARTESIAN_POINT ( 'NONE',  ( 21.14999999999999858, 6.412126976762841046, -199.7058512474018244 ) ) ;
#236882=LINE ( 'NONE', #38694, #127443 ) ;
#236905=VERTEX_POINT ( 'NONE', #50739 ) ;
#236909=DIRECTION ( 'NONE',  ( -0.000000000000000000, -0.04908394489119836945, -0.9987946567507848261 ) ) ;
#236928=DIRECTION ( 'NONE',  ( 0.000000000000000000, 0.2128009952263552051, -0.9770955615653327264 ) ) ;
#236966=VERTEX_POINT ( 'NONE', #231995 ) ;
#236983=B_SPLINE_CURVE_WITH_KNOTS ( 'NONE', 3,
 ( #96274, #136689, #256593, #75478, #255311, #234513 ),
 .UNSPECIFIED., .F., .F.,
 ( 4, 2, 4 ),
 ( 0.000000000000000000, 0.0001568709654583418610, 0.0003137419309166837220 ),
 .UNSPECIFIED. ) ;
#237009=CYLINDRICAL_SURFACE ( 'NONE', #237054, 0.09999999999999939493 ) ;
#237046=DIRECTION ( 'NONE',  ( -1.000000000000000000, -0.000000000000000000, -0.000000000000000000 ) ) ;
#237054=AXIS2_PLACEMENT_3D ( 'NONE', #244685, #124763, #165166 ) ;
#237055=ORIENTED_EDGE ( 'NONE', *, *, #71482, .F. ) ;
#237068=EDGE_CURVE ( 'NONE', #46074, #101102, #110210, .T. ) ;
#237083=EDGE_CURVE ( 'NONE', #130647, #86168, #106283, .T. ) ;
#237114=EDGE_LOOP ( 'NONE', ( #171513, #110343, #94327 ) ) ;
#237266=ORIENTED_EDGE ( 'NONE', *, *, #219897, .T. ) ;
#237270=VERTEX_POINT ( 'NONE', #67444 ) ;
#237275=EDGE_CURVE ( 'NONE', #86168, #22692, #27245, .T. ) ;
#237281=CARTESIAN_POINT ( 'NONE',  ( -20.54999999999999716, -3.770473190032741062, -225.9805569534692324 ) ) ;
#237288=ORIENTED_EDGE ( 'NONE', *, *, #60149, .F. ) ;
#237304=DIRECTION ( 'NONE',  ( 0.000000000000000000, -0.2128009952263604232, 0.9770955615653316162 ) ) ;
#237311=DIRECTION ( 'NONE',  ( 0.000000000000000000, 0.8879235499942239596, 0.4599910535713220838 ) ) ;
#237317=ORIENTED_EDGE ( 'NONE', *, *, #79767, .T. ) ;
#237333=CARTESIAN_POINT ( 'NONE',  ( -20.64999999999999858, 6.268811756569107274, -220.3853799378769622 ) ) ;
#237334=AXIS2_PLACEMENT_3D ( 'NONE', #230172, #228899, #132358 ) ;
#237343=ORIENTED_EDGE ( 'NONE', *, *, #34603, .T. ) ;
#237344=DIRECTION ( 'NONE',  ( 1.000000000000000000, 0.000000000000000000, 0.000000000000000000 ) ) ;
#237357=ORIENTED_EDGE ( 'NONE', *, *, #86508, .F. ) ;
#237379=ORIENTED_EDGE ( 'NONE', *, *, #132107, .F. ) ;
#237387=AXIS2_PLACEMENT_3D ( 'NONE', #157654, #100169, #80611 ) ;
#237398=ORIENTED_EDGE ( 'NONE', *, *, #177727, .F. ) ;
#237405=CARTESIAN_POINT ( 'NONE',  ( 19.96984138294274302, 16.74228639170174304, -222.6578579384645025 ) ) ;
#237406=EDGE_CURVE ( 'NONE', #75595, #158102, #204381, .T. ) ;
#237416=ORIENTED_EDGE ( 'NONE', *, *, #197951, .T. ) ;
#237425=ORIENTED_EDGE ( 'NONE', *, *, #157508, .F. ) ;
#237440=APPLICATION_CONTEXT ( 'automotive_design' ) ;
#237443=DIRECTION ( 'NONE',  ( 1.000000000000000000, 3.190570557967288949E-16, 6.948722487160392945E-17 ) ) ;
#237444=ORIENTED_EDGE ( 'NONE', *, *, #140901, .F. ) ;
#237445=EDGE_LOOP ( 'NONE', ( #76830, #183485, #55851, #69580 ) ) ;
#237457=VERTEX_POINT ( 'NONE', #13904 ) ;
#237480=EDGE_CURVE ( 'NONE', #232474, #22587, #114873, .T. ) ;
#237490=ORIENTED_EDGE ( 'NONE', *, *, #135527, .F. ) ;
#237497=CIRCLE ( 'NONE', #129335, 0.1000000000000076938 ) ;
#237524=AXIS2_PLACEMENT_3D ( 'NONE', #205111, #149036, #168636 ) ;
#237573=DIRECTION ( 'NONE',  ( 0.000000000000000000, 0.2965989261549489275, 0.9550021345545417484 ) ) ;
#237575=VECTOR ( 'NONE', #106990, 1000.000000000000114 ) ;
#237640=B_SPLINE_CURVE_WITH_KNOTS ( 'NONE', 3,
 ( #213735, #113358, #173380, #209905, #212471, #130337, #191648, #33868, #72981, #54653 ),
 .UNSPECIFIED., .F., .F.,
 ( 4, 2, 2, 2, 4 ),
 ( 0.000000000000000000, 4.221631689690473076E-05, 8.443263379380946151E-05, 0.0001688652675875489649, 0.0003377305351750279445 ),
 .UNSPECIFIED. ) ;
#237663=ORIENTED_EDGE ( 'NONE', *, *, #257096, .T. ) ;
#237664=ORIENTED_EDGE ( 'NONE', *, *, #97754, .F. ) ;
#237689=CARTESIAN_POINT ( 'NONE',  ( -23.25000000000000000, 10.74948822439029250, -222.3968794097801549 ) ) ;
#237705=EDGE_CURVE ( 'NONE', #183554, #5736, #218908, .T. ) ;
#237740=DIRECTION ( 'NONE',  ( 1.000000000000000000, 0.000000000000000000, 0.000000000000000000 ) ) ;
#237748=EDGE_LOOP ( 'NONE', ( #163834, #202735, #78088, #47515 ) ) ;
#237762=EDGE_CURVE ( 'NONE', #15753, #162643, #226176, .T. ) ;
#237779=ADVANCED_FACE ( 'NONE', ( #128404 ), #200891, .T. ) ;
#237792=EDGE_CURVE ( 'NONE', #286, #256585, #52493, .T. ) ;
#237822=CYLINDRICAL_SURFACE ( 'NONE', #15320, 0.09999999999999939493 ) ;
#237831=CARTESIAN_POINT ( 'NONE',  ( -21.05000000000000071, 0.9150442794848296924, -205.2015109147324097 ) ) ;
#237840=VERTEX_POINT ( 'NONE', #206217 ) ;
#237886=DIRECTION ( 'NONE',  ( 0.000000000000000000, -0.9770955615653320603, -0.2128009952263585081 ) ) ;
#237929=ADVANCED_FACE ( 'NONE', ( #246616 ), #227053, .T. ) ;
#237942=CARTESIAN_POINT ( 'NONE',  ( 20.50589344624626165, 11.85461726721770326, -206.1687069564524393 ) ) ;
#237955=DIRECTION ( 'NONE',  ( 0.000000000000000000, -0.2128009952263603677, 0.9770955615653313941 ) ) ;
#237966=ORIENTED_EDGE ( 'NONE', *, *, #189403, .F. ) ;
#237997=VERTEX_POINT ( 'NONE', #52252 ) ;
#238003=AXIS2_PLACEMENT_3D ( 'NONE', #213329, #193787, #94671 ) ;
#238019=LINE ( 'NONE', #24139, #52475 ) ;
#238020=B_SPLINE_CURVE_WITH_KNOTS ( 'NONE', 3,
 ( #2637, #27393, #101719, #222970, #220428, #183856 ),
 .UNSPECIFIED., .F., .F.,
 ( 4, 2, 4 ),
 ( 1.301042606982605513E-18, 0.0001569047307838624067, 0.0003138094615677235123 ),
 .UNSPECIFIED. ) ;
#238050=ORIENTED_EDGE ( 'NONE', *, *, #185984, .T. ) ;
#238082=DIRECTION ( 'NONE',  ( 1.000000000000000000, 0.000000000000000000, 0.000000000000000000 ) ) ;
#238106=DIRECTION ( 'NONE',  ( 0.000000000000000000, 0.2128009952263604232, -0.9770955615653316162 ) ) ;
#238114=EDGE_LOOP ( 'NONE', ( #88606, #193612, #88242, #102406 ) ) ;
#238118=ORIENTED_EDGE ( 'NONE', *, *, #24405, .T. ) ;
#238126=CARTESIAN_POINT ( 'NONE',  ( -21.14999999999999858, 1.148907358139439339E-11, -201.0000000000015064 ) ) ;
#238164=ORIENTED_EDGE ( 'NONE', *, *, #51420, .T. ) ;
#238169=DIRECTION ( 'NONE',  ( 0.000000000000000000, 0.7397890806274222131, 0.6728388485993012091 ) ) ;
#238210=CIRCLE ( 'NONE', #9086, 0.1000000000000060979 ) ;
#238217=ORIENTED_EDGE ( 'NONE', *, *, #192520, .T. ) ;
#238247=ORIENTED_EDGE ( 'NONE', *, *, #102913, .T. ) ;
#238255=( BOUNDED_SURFACE ( )  B_SPLINE_SURFACE ( 3, 2, ( 
 ( #106097, #226036, #185665 ),
 ( #47418, #7020, #107402 ),
 ( #27907, #245639, #126975 ),
 ( #246909, #68293, #150411 ),
 ( #113826, #116411, #10890 ),
 ( #75992, #194689, #229930 ),
 ( #73454, #235075, #90406 ),
 ( #232522, #33063, #35615 ) ),
 .UNSPECIFIED., .F., .F., .F. ) 
 B_SPLINE_SURFACE_WITH_KNOTS ( ( 4, 2, 2, 4 ),
 ( 3, 3 ),
 ( 0.0001704874539069819431, 0.0003809798300636536481, 0.0004862260181419895142, 0.0005914722062203253260 ),
 ( 0.000000000000000000, 1.000000000000000000 ),
 .UNSPECIFIED. ) 
 GEOMETRIC_REPRESENTATION_ITEM ( )  RATIONAL_B_SPLINE_SURFACE ( (
 ( 1.000000000000000000, 0.7071067811865795472, 1.000000000000000000),
 ( 1.000000000000000000, 0.7670648383563467565, 1.000000000000000000),
 ( 1.000000000000000000, 0.8204820770268871355, 1.000000000000000000),
 ( 1.000000000000000000, 0.8877218296105150452, 1.000000000000000000),
 ( 1.000000000000000000, 0.9080815932665030621, 1.000000000000000000),
 ( 1.000000000000000000, 0.9395541505862222698, 1.000000000000000000),
 ( 1.000000000000000000, 0.9506520335379197162, 1.000000000000000000),
 ( 1.000000000000000000, 0.9504532311154330060, 1.000000000000000000) ) ) 
 REPRESENTATION_ITEM ( '' )  SURFACE ( )  );
#238260=LINE ( 'NONE', #42633, #107222 ) ;
#238299=CARTESIAN_POINT ( 'NONE',  ( 18.49999999999999289, 14.80545736607782814, -235.9842437978701639 ) ) ;
#238331=AXIS2_PLACEMENT_3D ( 'NONE', #73447, #194682, #14758 ) ;
#238370=AXIS2_PLACEMENT_3D ( 'NONE', #64861, #223926, #42738 ) ;
#238372=AXIS2_PLACEMENT_3D ( 'NONE', #10559, #153961, #169666 ) ;
#238392=CARTESIAN_POINT ( 'NONE',  ( 20.94999999999999574, 4.273531877263399892, -211.9976340888692050 ) ) ;
#238453=EDGE_CURVE ( 'NONE', #83539, #187924, #96772, .T. ) ;
#238461=CARTESIAN_POINT ( 'NONE',  ( 20.95512820512820440, 13.19486920349904224, -219.8744268493789491 ) ) ;
#238466=CIRCLE ( 'NONE', #72079, 0.5000000000000007772 ) ;
#238517=CYLINDRICAL_SURFACE ( 'NONE', #110465, 0.09999999999999939493 ) ;
#238547=CARTESIAN_POINT ( 'NONE',  ( 22.39999999999999503, 11.36188319272497438, -198.4231588494578773 ) ) ;
#238567=CIRCLE ( 'NONE', #126113, 0.2000000000000041744 ) ;
#238586=CARTESIAN_POINT ( 'NONE',  ( -23.15000000000000213, 4.617781596423511381, -222.2029736859691980 ) ) ;
#238602=DIRECTION ( 'NONE',  ( 0.000000000000000000, -0.2128009952263485993, 0.9770955615653341697 ) ) ;
#238615=AXIS2_PLACEMENT_3D ( 'NONE', #199296, #179736, #41521 ) ;
#238668=CARTESIAN_POINT ( 'NONE',  ( -23.25000000000000000, 1.148907358139439339E-11, -201.0000000000015064 ) ) ;
#238677=ORIENTED_EDGE ( 'NONE', *, *, #148817, .T. ) ;
#238684=CARTESIAN_POINT ( 'NONE',  ( 19.97071067695815572, 16.70338566981720518, -222.6168788084382868 ) ) ;
#238724=DIRECTION ( 'NONE',  ( 1.000000000000000000, 0.000000000000000000, 0.000000000000000000 ) ) ;
#238770=AXIS2_PLACEMENT_3D ( 'NONE', #8711, #127375, #167810 ) ;
#238772=EDGE_LOOP ( 'NONE', ( #186803, #78327, #149013, #221613 ) ) ;
#238781=VECTOR ( 'NONE', #127739, 1000.000000000000000 ) ;
#238796=DIRECTION ( 'NONE',  ( -1.000000000000000000, 0.000000000000000000, 0.000000000000000000 ) ) ;
#238803=AXIS2_PLACEMENT_3D ( 'NONE', #124495, #104876, #204013 ) ;
#238822=CARTESIAN_POINT ( 'NONE',  ( -20.54999999999999716, 6.878457983866232972, -212.1414458560986986 ) ) ;
#238853=CYLINDRICAL_SURFACE ( 'NONE', #204605, 0.09999999999999156786 ) ;
#238869=EDGE_CURVE ( 'NONE', #165014, #106096, #36334, .T. ) ;
#238911=CARTESIAN_POINT ( 'NONE',  ( 18.59999999999998366, 7.128833340094563376, -233.7327013124401276 ) ) ;
#238927=AXIS2_PLACEMENT_3D ( 'NONE', #168123, #188923, #29876 ) ;
#239016=FACE_OUTER_BOUND ( 'NONE', #117348, .T. ) ;
#239017=CIRCLE ( 'NONE', #134928, 0.09999999999999724387 ) ;
#239051=CARTESIAN_POINT ( 'NONE',  ( 21.14999999999999503, 1.148907358139439339E-11, -201.0000000000015064 ) ) ;
#239079=DIRECTION ( 'NONE',  ( 0.000000000000000000, 0.9770955615653317272, 0.2128009952263598126 ) ) ;
#239080=EDGE_CURVE ( 'NONE', #249430, #21586, #106757, .T. ) ;
#239110=DIRECTION ( 'NONE',  ( 0.000000000000000000, -0.2128009952263650861, 0.9770955615653305060 ) ) ;
#239119=VECTOR ( 'NONE', #201511, 1000.000000000000227 ) ;
#239122=DIRECTION ( 'NONE',  ( 0.000000000000000000, -0.9968797965484669232, -0.07893460099023190402 ) ) ;
#239143=AXIS2_PLACEMENT_3D ( 'NONE', #232330, #77075, #193197 ) ;
#239162=DIRECTION ( 'NONE',  ( 0.000000000000000000, 0.2128009952263603399, -0.9770955615653315052 ) ) ;
#239184=EDGE_CURVE ( 'NONE', #116019, #139309, #244994, .T. ) ;
#239195=DIRECTION ( 'NONE',  ( 0.000000000000000000, 0.2128009952263604232, -0.9770955615653316162 ) ) ;
#239223=VECTOR ( 'NONE', #136386, 1000.000000000000000 ) ;
#239224=ADVANCED_FACE ( 'NONE', ( #148474 ), #228035, .F. ) ;
#239229=DIRECTION ( 'NONE',  ( 0.000000000000000000, 0.2128009952263601456, -0.9770955615653316162 ) ) ;
#239236=CARTESIAN_POINT ( 'NONE',  ( 20.77526135991748291, 10.52954618004883613, -207.3738603278011681 ) ) ;
#239248=VERTEX_POINT ( 'NONE', #212309 ) ;
#239272=EDGE_CURVE ( 'NONE', #246315, #163980, #178165, .T. ) ;
#239304=VECTOR ( 'NONE', #63055, 1000.000000000000000 ) ;
#239307=DIRECTION ( 'NONE',  ( 1.000000000000000000, 0.000000000000000000, 0.000000000000000000 ) ) ;
#239312=DIRECTION ( 'NONE',  ( -0.000000000000000000, -0.2128009952263607285, 0.9770955615653316162 ) ) ;
#239321=DIRECTION ( 'NONE',  ( -3.440080580676165237E-14, 0.08413937888703756918, -0.9964539953858901900 ) ) ;
#239331=EDGE_CURVE ( 'NONE', #224326, #25296, #238260, .T. ) ;
#239365=AXIS2_PLACEMENT_3D ( 'NONE', #146977, #105261, #226506 ) ;
#239373=ORIENTED_EDGE ( 'NONE', *, *, #167040, .T. ) ;
#239396=ORIENTED_EDGE ( 'NONE', *, *, #75077, .F. ) ;
#239417=DIRECTION ( 'NONE',  ( -1.000000000000000000, -0.000000000000000000, -0.000000000000000000 ) ) ;
#239424=ORIENTED_EDGE ( 'NONE', *, *, #82500, .F. ) ;
#239439=EDGE_LOOP ( 'NONE', ( #225409, #74287, #135412, #92771 ) ) ;
#239449=CARTESIAN_POINT ( 'NONE',  ( 23.24999999999999289, 15.92646454033040371, -219.3818586450342423 ) ) ;
#239455=ORIENTED_EDGE ( 'NONE', *, *, #18355, .T. ) ;
#239465=ADVANCED_FACE ( 'NONE', ( #252072 ), #70902, .F. ) ;
#239474=VECTOR ( 'NONE', #8117, 1000.000000000000000 ) ;
#239502=EDGE_CURVE ( 'NONE', #137759, #191212, #51272, .T. ) ;
#239520=ORIENTED_EDGE ( 'NONE', *, *, #19899, .F. ) ;
#239522=LINE ( 'NONE', #219949, #190400 ) ;
#239542=CARTESIAN_POINT ( 'NONE',  ( 21.05000000000000071, 17.11694853917244075, -224.3781540347815735 ) ) ;
#239571=AXIS2_PLACEMENT_3D ( 'NONE', #177430, #19619, #99117 ) ;
#239586=EDGE_CURVE ( 'NONE', #154626, #60331, #170006, .T. ) ;
#239587=CARTESIAN_POINT ( 'NONE',  ( 22.59999999999999432, -2.381330705637465961, -189.5959759702857923 ) ) ;
#239600=DIRECTION ( 'NONE',  ( 0.000000000000000000, 0.2128009952263485993, -0.9770955615653341697 ) ) ;
#239602=VECTOR ( 'NONE', #91743, 1000.000000000000000 ) ;
#239650=EDGE_CURVE ( 'NONE', #185482, #44981, #154313, .T. ) ;
#239677=EDGE_LOOP ( 'NONE', ( #172393, #62441, #65982, #25565 ) ) ;
#239716=CARTESIAN_POINT ( 'NONE',  ( -20.85000000000000142, 17.16609282392353819, -224.6038045889790453 ) ) ;
#239718=ORIENTED_EDGE ( 'NONE', *, *, #196779, .F. ) ;
#239739=FACE_OUTER_BOUND ( 'NONE', #118556, .T. ) ;
#239766=DIRECTION ( 'NONE',  ( 0.000000000000000000, 0.2128009952263603677, -0.9770955615653313941 ) ) ;
#239807=CYLINDRICAL_SURFACE ( 'NONE', #135125, 0.1000000000000055844 ) ;
#239809=CARTESIAN_POINT ( 'NONE',  ( 20.94999999999999929, 15.00011753506359469, -219.4812630108571057 ) ) ;
#239818=ORIENTED_EDGE ( 'NONE', *, *, #116493, .T. ) ;
#239827=CARTESIAN_POINT ( 'NONE',  ( 23.14999999999999503, 10.92199707682457088, -220.3694341645321515 ) ) ;
#239834=ORIENTED_EDGE ( 'NONE', *, *, #150371, .T. ) ;
#239898=ADVANCED_FACE ( 'NONE', ( #71865 ), #74317, .F. ) ;
#239905=AXIS2_PLACEMENT_3D ( 'NONE', #182090, #157768, #35234 ) ;
#239918=ADVANCED_FACE ( 'NONE', ( #96516 ), #120102, .T. ) ;
#239920=DIRECTION ( 'NONE',  ( 6.938893903907220489E-15, -0.9770955615653313941, -0.2128009952263603677 ) ) ;
#239923=DIRECTION ( 'NONE',  ( 1.000000000000000000, 7.136802563874199107E-16, 1.554319503706929991E-16 ) ) ;
#239927=ORIENTED_EDGE ( 'NONE', *, *, #43147, .F. ) ;
#239980=CARTESIAN_POINT ( 'NONE',  ( 19.90621891164687440, 16.76439071345979315, -222.7593519876740231 ) ) ;
#240004=AXIS2_PLACEMENT_3D ( 'NONE', #117, #226530, #27110 ) ;
#240014=EDGE_CURVE ( 'NONE', #5146, #192537, #117389, .T. ) ;
#240015=ORIENTED_EDGE ( 'NONE', *, *, #27641, .T. ) ;
#240028=ORIENTED_EDGE ( 'NONE', *, *, #42884, .F. ) ;
#240039=DIRECTION ( 'NONE',  ( 1.000000000000000000, 3.190570557967288949E-16, 6.948722487160392945E-17 ) ) ;
#240048=ORIENTED_EDGE ( 'NONE', *, *, #144461, .T. ) ;
#240052=CARTESIAN_POINT ( 'NONE',  ( 23.14999999999999858, 10.74948822439028540, -222.3968794097801549 ) ) ;
#240053=AXIS2_PLACEMENT_3D ( 'NONE', #205379, #5896, #188402 ) ;
#240065=CIRCLE ( 'NONE', #111056, 12.87499999999999822 ) ;
#240066=AXIS2_PLACEMENT_3D ( 'NONE', #9022, #105515, #110687 ) ;
#240072=CARTESIAN_POINT ( 'NONE',  ( -20.64999999999999858, 7.128833340094563376, -233.7327013124401276 ) ) ;
#240135=CARTESIAN_POINT ( 'NONE',  ( 18.59999999999999787, 4.288595810029049993, -211.9930862808554934 ) ) ;
#240139=EDGE_CURVE ( 'NONE', #203538, #60331, #232527, .T. ) ;
#240145=DIRECTION ( 'NONE',  ( 0.000000000000000000, 0.2128009952263403282, -0.9770955615653358350 ) ) ;
#240201=CARTESIAN_POINT ( 'NONE',  ( 22.50000000000000000, 11.36146383068193444, -198.4232501820394816 ) ) ;
#240217=CIRCLE ( 'NONE', #77867, 0.3999999999999952482 ) ;
#240236=DIRECTION ( 'NONE',  ( -1.000000000000000000, -0.000000000000000000, -0.000000000000000000 ) ) ;
#240249=ORIENTED_EDGE ( 'NONE', *, *, #169830, .T. ) ;
#240253=DIRECTION ( 'NONE',  ( 1.000000000000000000, 0.000000000000000000, 0.000000000000000000 ) ) ;
#240275=EDGE_CURVE ( 'NONE', #219487, #157474, #87229, .T. ) ;
#240290=DIRECTION ( 'NONE',  ( 0.000000000000000000, 0.9770955615653316162, 0.2128009952263604232 ) ) ;
#240391=EDGE_CURVE ( 'NONE', #71034, #200289, #120299, .T. ) ;
#240405=ADVANCED_FACE ( 'NONE', ( #136625 ), #233203, .T. ) ;
#240417=FACE_OUTER_BOUND ( 'NONE', #9202, .T. ) ;
#240436=EDGE_LOOP ( 'NONE', ( #248218, #149247, #59850, #130657, #190633, #203032, #108952 ) ) ;
#240448=CARTESIAN_POINT ( 'NONE',  ( -21.05000000000000071, 6.176982137395727435, -199.7570632862319542 ) ) ;
#240475=CARTESIAN_POINT ( 'NONE',  ( -18.50000000000000000, 8.882751598337863541, -187.0399955572217721 ) ) ;
#240485=CARTESIAN_POINT ( 'NONE',  ( 23.25000000000000000, -4.914013037343258894, -233.1828366659746905 ) ) ;
#240495=CARTESIAN_POINT ( 'NONE',  ( -23.15000000000000213, -4.914013037343267776, -233.1828366659746905 ) ) ;
#240510=CARTESIAN_POINT ( 'NONE',  ( 23.24999999999999289, 8.882751598337874199, -187.0399955572217721 ) ) ;
#240517=ORIENTED_EDGE ( 'NONE', *, *, #118609, .T. ) ;
#240521=EDGE_CURVE ( 'NONE', #10221, #32161, #107768, .T. ) ;
#240561=CIRCLE ( 'NONE', #132414, 12.97499999999999964 ) ;
#240599=CIRCLE ( 'NONE', #211578, 0.1000000000000054040 ) ;
#240618=CARTESIAN_POINT ( 'NONE',  ( 18.59999999999999076, 10.80300742114540391, -220.2930047078982625 ) ) ;
#240635=EDGE_CURVE ( 'NONE', #155898, #54081, #132329, .T. ) ;
#240641=CARTESIAN_POINT ( 'NONE',  ( 20.94999999999999929, 7.128833340094563376, -233.7327013124401276 ) ) ;
#240645=DIRECTION ( 'NONE',  ( 0.000000000000000000, -0.9770955615653316162, -0.2128009952263604232 ) ) ;
#240652=CIRCLE ( 'NONE', #15839, 0.1000000000000055844 ) ;
#240660=CARTESIAN_POINT ( 'NONE',  ( 20.94999999999999574, 0.7653315920341953182, -212.6731560895497353 ) ) ;
#240662=CIRCLE ( 'NONE', #186514, 0.1000000000000068751 ) ;
#240711=EDGE_CURVE ( 'NONE', #106308, #213820, #178148, .T. ) ;
#240715=ORIENTED_EDGE ( 'NONE', *, *, #34870, .T. ) ;
#240719=DIRECTION ( 'NONE',  ( 0.000000000000000000, 0.2128009952263485993, -0.9770955615653341697 ) ) ;
#240746=LINE ( 'NONE', #222423, #98350 ) ;
#240757=TOROIDAL_SURFACE ( 'NONE', #153499, 0.6000000000000006439, 0.1000000000000000056 ) ;
#240794=AXIS2_PLACEMENT_3D ( 'NONE', #247888, #227036, #245332 ) ;
#240797=ADVANCED_FACE ( 'NONE', ( #192459 ), #94910, .F. ) ;
#240817=CARTESIAN_POINT ( 'NONE',  ( 22.57320508075688181, 11.48087284840413780, -198.4995883060917947 ) ) ;
#240831=FACE_OUTER_BOUND ( 'NONE', #37864, .T. ) ;
#240873=LINE ( 'NONE', #162624, #172622 ) ;
#240886=DIRECTION ( 'NONE',  ( 0.000000000000000000, 0.2128009952263598958, -0.9770955615653316162 ) ) ;
#240941=CARTESIAN_POINT ( 'NONE',  ( 23.25000000000000000, -5.011722593499792211, -233.2041167654973322 ) ) ;
#240944=ORIENTED_EDGE ( 'NONE', *, *, #57085, .F. ) ;
#240952=ORIENTED_EDGE ( 'NONE', *, *, #183341, .F. ) ;
#240956=ORIENTED_EDGE ( 'NONE', *, *, #132687, .T. ) ;
#240957=DIRECTION ( 'NONE',  ( 0.000000000000000000, 0.2128009952263403282, -0.9770955615653358350 ) ) ;
#240958=ORIENTED_EDGE ( 'NONE', *, *, #189412, .T. ) ;
#241000=CYLINDRICAL_SURFACE ( 'NONE', #251195, 0.09999999999999939493 ) ;
#241013=ADVANCED_FACE ( 'NONE', ( #46213 ), #20104, .F. ) ;
#241019=VECTOR ( 'NONE', #106597, 1000.000000000000227 ) ;
#241041=LINE ( 'NONE', #238461, #257997 ) ;
#241077=VERTEX_POINT ( 'NONE', #29280 ) ;
#241095=ORIENTED_EDGE ( 'NONE', *, *, #84302, .F. ) ;
#241103=ADVANCED_BREP_SHAPE_REPRESENTATION ( '', ( #22252, #2425 ), #52661 ) ;
#241116=DIRECTION ( 'NONE',  ( 0.000000000000000000, 0.2128009952263601456, -0.9770955615653316162 ) ) ;
#241162=EDGE_CURVE ( 'NONE', #237270, #112967, #70198, .T. ) ;
#241168=CARTESIAN_POINT ( 'NONE',  ( 21.05000000000000071, -1.362597741190629819, -194.8440013506711068 ) ) ;
#241182=CARTESIAN_POINT ( 'NONE',  ( 21.87500000000000355, 14.02742277431099893, -219.5907614236512870 ) ) ;
#241204=VERTEX_POINT ( 'NONE', #213000 ) ;
#241261=DIRECTION ( 'NONE',  ( 0.000000000000000000, 0.9770955615653316162, 0.2128009952263597848 ) ) ;
#241269=CARTESIAN_POINT ( 'NONE',  ( -21.29999999999995808, 0.8618440306782485516, -204.9572370243411115 ) ) ;
#241310=ORIENTED_EDGE ( 'NONE', *, *, #29746, .F. ) ;
#241346=DIRECTION ( 'NONE',  ( 1.000000000000000000, 0.000000000000000000, 0.000000000000000000 ) ) ;
#241349=ORIENTED_EDGE ( 'NONE', *, *, #194981, .F. ) ;
#241371=DIRECTION ( 'NONE',  ( -1.000000000000000000, -0.000000000000000000, -0.000000000000000000 ) ) ;
#241377=DIRECTION ( 'NONE',  ( -1.000000000000000000, 0.000000000000000000, 0.000000000000000000 ) ) ;
#241385=DIRECTION ( 'NONE',  ( 0.000000000000000000, 0.9968797965484755830, 0.07893460099012303277 ) ) ;
#241388=DIRECTION ( 'NONE',  ( 0.000000000000000000, 0.2128009952263605620, -0.9770955615653313941 ) ) ;
#241423=VECTOR ( 'NONE', #87542, 1000.000000000000000 ) ;
#241431=ORIENTED_EDGE ( 'NONE', *, *, #75022, .F. ) ;
#241432=CIRCLE ( 'NONE', #45785, 0.09999999999999691080 ) ;
#241457=ORIENTED_EDGE ( 'NONE', *, *, #92942, .F. ) ;
#241476=CARTESIAN_POINT ( 'NONE',  ( -18.59999999999999787, 0.7653315920341953182, -212.6731560895497353 ) ) ;
#241477=DIRECTION ( 'NONE',  ( -1.000000000000000000, -8.034189347746079853E-16, 2.566115377699053192E-16 ) ) ;
#241525=VECTOR ( 'NONE', #243263, 1000.000000000000227 ) ;
#241530=EDGE_CURVE ( 'NONE', #119503, #241591, #220197, .T. ) ;
#241532=CARTESIAN_POINT ( 'NONE',  ( -23.25000000000000000, 7.788796164756791818, -245.4641525896719543 ) ) ;
#241549=CARTESIAN_POINT ( 'NONE',  ( 23.24999999999999289, 10.94327717634720543, -220.4671437206886822 ) ) ;
#241550=CARTESIAN_POINT ( 'NONE',  ( -21.14999999999999858, -1.331831764083658554, -194.8847705854734045 ) ) ;
#241553=EDGE_CURVE ( 'NONE', #87352, #127248, #136981, .T. ) ;
#241557=CARTESIAN_POINT ( 'NONE',  ( 18.59999999999999076, 13.20456090973765662, -206.4140623547709765 ) ) ;
#241565=ADVANCED_FACE ( 'NONE', ( #26908 ), #182109, .T. ) ;
#241578=CARTESIAN_POINT ( 'NONE',  ( 21.09316766718127667, 6.215893237032393159, -199.6060609392288256 ) ) ;
#241591=VERTEX_POINT ( 'NONE', #201658 ) ;
#241612=DIRECTION ( 'NONE',  ( -0.000000000000000000, 0.2128009952263604232, -0.9770955615653316162 ) ) ;
#241644=ADVANCED_FACE ( 'NONE', ( #8600 ), #128543, .T. ) ;
#241645=ADVANCED_FACE ( 'NONE', ( #213197 ), #193656, .F. ) ;
#241649=CARTESIAN_POINT ( 'NONE',  ( 20.95512820512820795, 12.97672201526442137, -210.6599585865309052 ) ) ;
#241679=AXIS2_PLACEMENT_3D ( 'NONE', #20394, #81591, #103728 ) ;
#241761=CARTESIAN_POINT ( 'NONE',  ( 20.94999999999999929, -4.714262876194486473, -233.3440214805475819 ) ) ;
#241770=CARTESIAN_POINT ( 'NONE',  ( -20.64999999999999858, 6.268811756569107274, -220.3853799378769622 ) ) ;
#241790=ADVANCED_FACE ( 'NONE', ( #206504 ), #126970, .F. ) ;
#241801=DIRECTION ( 'NONE',  ( 0.000000000000000000, 0.2128009952263403282, -0.9770955615653358350 ) ) ;
#241855=DIRECTION ( 'NONE',  ( -2.940209281316620523E-16, 0.9770955615653310611, 0.2128009952263628657 ) ) ;
#241867=CARTESIAN_POINT ( 'NONE',  ( 21.05000000000000071, 0.4597584103430730762, -208.9850561804005906 ) ) ;
#241877=VECTOR ( 'NONE', #45797, 1000.000000000000000 ) ;
#241880=AXIS2_PLACEMENT_3D ( 'NONE', #99367, #155551, #139784 ) ;
#241882=ORIENTED_EDGE ( 'NONE', *, *, #108554, .T. ) ;
#241887=ORIENTED_EDGE ( 'NONE', *, *, #218461, .F. ) ;
#241890=VERTEX_POINT ( 'NONE', #171288 ) ;
#241893=DIRECTION ( 'NONE',  ( -1.000000000000000000, 0.000000000000000000, 0.000000000000000000 ) ) ;
#241923=CARTESIAN_POINT ( 'NONE',  ( 18.49999999999999645, 7.675662554762638479, -241.7139905447625381 ) ) ;
#241955=DIRECTION ( 'NONE',  ( 1.000000000000000000, 0.000000000000000000, 0.000000000000000000 ) ) ;
#241962=VECTOR ( 'NONE', #250526, 1000.000000000000227 ) ;
#241974=EDGE_LOOP ( 'NONE', ( #238118, #109208, #65595 ) ) ;
#242025=ORIENTED_EDGE ( 'NONE', *, *, #139640, .T. ) ;
#242034=DIRECTION ( 'NONE',  ( -0.000000000000000000, -0.07893460099012017395, 0.9968797965484759160 ) ) ;
#242048=DIRECTION ( 'NONE',  ( -1.000000000000000000, -0.000000000000000000, -0.000000000000000000 ) ) ;
#242068=CARTESIAN_POINT ( 'NONE',  ( 18.49999999999998934, 10.90071697730193456, -220.2717246083756208 ) ) ;
#242098=DIRECTION ( 'NONE',  ( -1.000000000000000000, -2.885090398161910739E-16, -6.283419270304611573E-17 ) ) ;
#242106=VECTOR ( 'NONE', #225385, 1000.000000000000000 ) ;
#242122=CIRCLE ( 'NONE', #92288, 0.09999999999999641120 ) ;
#242140=CIRCLE ( 'NONE', #154698, 0.09999999999999939493 ) ;
#242154=DIRECTION ( 'NONE',  ( 1.000000000000000000, 0.000000000000000000, 0.000000000000000000 ) ) ;
#242169=VERTEX_POINT ( 'NONE', #143653 ) ;
#242173=DIRECTION ( 'NONE',  ( 1.000000000000000000, 0.000000000000000000, 0.000000000000000000 ) ) ;
#242177=CARTESIAN_POINT ( 'NONE',  ( 20.94999999999999929, 0.6656436123793473270, -212.6810495496487476 ) ) ;
#242200=ORIENTED_EDGE ( 'NONE', *, *, #174786, .T. ) ;
#242201=AXIS2_PLACEMENT_3D ( 'NONE', #124677, #84193, #165078 ) ;
#242246=ORIENTED_EDGE ( 'NONE', *, *, #100150, .T. ) ;
#242273=LINE ( 'NONE', #105302, #129568 ) ;
#242310=CIRCLE ( 'NONE', #196522, 0.1000000000000055844 ) ;
#242311=DIRECTION ( 'NONE',  ( 1.000000000000000000, -0.000000000000000000, -0.000000000000000000 ) ) ;
#242355=DIRECTION ( 'NONE',  ( 1.000000000000000000, 0.000000000000000000, 0.000000000000000000 ) ) ;
#242366=DIRECTION ( 'NONE',  ( 0.000000000000000000, -0.9770955615653315052, -0.2128009952263603954 ) ) ;
#242428=CARTESIAN_POINT ( 'NONE',  ( -20.64999999999999858, 5.159242054424403534, -213.4109969955686665 ) ) ;
#242436=DIRECTION ( 'NONE',  ( 0.000000000000000000, 0.2128009952263596460, -0.9770955615653317272 ) ) ;
#242448=EDGE_CURVE ( 'NONE', #166449, #15753, #126238, .T. ) ;
#242451=FACE_OUTER_BOUND ( 'NONE', #131574, .T. ) ;
#242454=EDGE_CURVE ( 'NONE', #138601, #106738, #62340, .T. ) ;
#242469=PLANE ( 'NONE',  #66204 ) ;
#242470=CARTESIAN_POINT ( 'NONE',  ( 18.59999999999999076, 10.92199707682457088, -220.3694341645321515 ) ) ;
#242476=CARTESIAN_POINT ( 'NONE',  ( -20.94999999999999929, 7.783179459866052419, -245.3643104511423303 ) ) ;
#242504=AXIS2_PLACEMENT_3D ( 'NONE', #225063, #46439, #7322 ) ;
#242525=ORIENTED_EDGE ( 'NONE', *, *, #106905, .T. ) ;
#242535=DIRECTION ( 'NONE',  ( -1.000000000000000000, -2.885090398161910739E-16, -6.283419270304611573E-17 ) ) ;
#242540=DIRECTION ( 'NONE',  ( 0.000000000000000000, 0.9770955615653312831, 0.2128009952263620053 ) ) ;
#242543=CARTESIAN_POINT ( 'NONE',  ( 23.14999999999999858, 6.703231349641842307, -231.7785101893094577 ) ) ;
#242544=VERTEX_POINT ( 'NONE', #102917 ) ;
#242546=CIRCLE ( 'NONE', #188555, 11.70000000000000284 ) ;
#242587=FACE_OUTER_BOUND ( 'NONE', #136367, .T. ) ;
#242600=CARTESIAN_POINT ( 'NONE',  ( -20.54999999999999716, 6.353932154659650777, -220.7762181625030848 ) ) ;
#242604=ORIENTED_EDGE ( 'NONE', *, *, #65571, .F. ) ;
#242621=ADVANCED_FACE ( 'NONE', ( #200760 ), #233235, .F. ) ;
#242635=CARTESIAN_POINT ( 'NONE',  ( -20.94999999999999929, 0.3882413827466408840, -209.1776850584169551 ) ) ;
#242642=CARTESIAN_POINT ( 'NONE',  ( -21.05000000000000071, 4.252251777740764460, -211.8999245327126744 ) ) ;
#242670=VECTOR ( 'NONE', #6963, 1000.000000000000227 ) ;
#242682=EDGE_LOOP ( 'NONE', ( #158818, #9195, #198387 ) ) ;
#242692=CARTESIAN_POINT ( 'NONE',  ( -23.15000000000000213, 8.751106741858205140, -220.7398867978735950 ) ) ;
#242717=FACE_OUTER_BOUND ( 'NONE', #50064, .T. ) ;
#242742=DIRECTION ( 'NONE',  ( 0.000000000000000000, -0.7397890806274287634, -0.6728388485992942147 ) ) ;
#242749=ORIENTED_EDGE ( 'NONE', *, *, #128649, .T. ) ;
#242773=DIRECTION ( 'NONE',  ( 1.000000000000000000, 0.000000000000000000, 0.000000000000000000 ) ) ;
#242850=ORIENTED_EDGE ( 'NONE', *, *, #52577, .T. ) ;
#242860=ORIENTED_EDGE ( 'NONE', *, *, #224218, .T. ) ;
#242867=VERTEX_POINT ( 'NONE', #218704 ) ;
#242869=ORIENTED_EDGE ( 'NONE', *, *, #122890, .F. ) ;
#242878=DIRECTION ( 'NONE',  ( -1.000000000000000000, -0.000000000000000000, -0.000000000000000000 ) ) ;
#242887=AXIS2_PLACEMENT_3D ( 'NONE', #166215, #67081, #224854 ) ;
#242906=CIRCLE ( 'NONE', #151357, 2.100000000000004974 ) ;
#242920=AXIS2_PLACEMENT_3D ( 'NONE', #28443, #104059, #203180 ) ;
#242941=AXIS2_PLACEMENT_3D ( 'NONE', #61029, #197976, #117173 ) ;
#242954=DIRECTION ( 'NONE',  ( -1.000000000000000000, -0.000000000000000000, -0.000000000000000000 ) ) ;
#242977=CARTESIAN_POINT ( 'NONE',  ( -20.94999999999999929, 14.76289716703256083, -235.7888246855571026 ) ) ;
#243002=DIRECTION ( 'NONE',  ( -0.000000000000000000, -0.9770955615653316162, -0.2128009952263597848 ) ) ;
#243011=DIRECTION ( 'NONE',  ( 1.000000000000000000, 0.000000000000000000, 0.000000000000000000 ) ) ;
#243059=VERTEX_POINT ( 'NONE', #83026 ) ;
#243072=DIRECTION ( 'NONE',  ( 1.000000000000000000, 0.000000000000000000, 0.000000000000000000 ) ) ;
#243153=TOROIDAL_SURFACE ( 'NONE', #76560, 0.4000000000000012990, 0.1000000000000000056 ) ;
#243160=TOROIDAL_SURFACE ( 'NONE', #143396, 0.2000000000000000111, 0.1000000000000000056 ) ;
#243163=PLANE ( 'NONE',  #14461 ) ;
#243179=AXIS2_PLACEMENT_3D ( 'NONE', #162960, #63842, #139510 ) ;
#243229=CYLINDRICAL_SURFACE ( 'NONE', #240053, 0.1000000000000008937 ) ;
#243234=B_SPLINE_CURVE_WITH_KNOTS ( 'NONE', 3,
 ( #65383, #144902, #204880, #146195, #105768, #66677, #225716, #47083, #206183, #180214, #1546, #81078, #233158, #75367, #36237, #87497 ),
 .UNSPECIFIED., .F., .F.,
 ( 4, 3, 3, 3, 3, 4 ),
 ( 0.000000000000000000, 3.357088238234077717E-05, 6.714213034887153676E-05, 0.0001007408646120950283, 0.0001343627955914246212, 0.0001573956632896022318 ),
 .UNSPECIFIED. ) ;
#243250=CARTESIAN_POINT ( 'NONE',  ( -21.07946286933443503, 6.167755875232504792, -199.5782471168023449 ) ) ;
#243256=DIRECTION ( 'NONE',  ( -1.000000000000000000, -0.000000000000000000, -0.000000000000000000 ) ) ;
#243263=DIRECTION ( 'NONE',  ( -0.000000000000000000, -0.2128009952263603677, 0.9770955615653313941 ) ) ;
#243303=DIRECTION ( 'NONE',  ( 0.000000000000000000, 0.2128009952263618110, -0.9770955615653312831 ) ) ;
#243311=CARTESIAN_POINT ( 'NONE',  ( 20.94999999999999574, 0.3882413827466408840, -209.1776850584169551 ) ) ;
#243336=ORIENTED_EDGE ( 'NONE', *, *, #80845, .F. ) ;
#243341=ADVANCED_FACE ( 'NONE', ( #232867 ), #55451, .T. ) ;
#243352=DIRECTION ( 'NONE',  ( -1.000000000000000000, 0.000000000000000000, 0.000000000000000000 ) ) ;
#243402=CYLINDRICAL_SURFACE ( 'NONE', #168440, 0.09999999999999939493 ) ;
#243418=ORIENTED_EDGE ( 'NONE', *, *, #189132, .F. ) ;
#243481=EDGE_LOOP ( 'NONE', ( #105674, #253737, #41577, #10467 ) ) ;
#243568=FACE_OUTER_BOUND ( 'NONE', #141365, .T. ) ;
#243574=CARTESIAN_POINT ( 'NONE',  ( 21.14999999999999858, 9.104497675943859392, -211.5542940109215522 ) ) ;
#243598=ORIENTED_EDGE ( 'NONE', *, *, #87563, .F. ) ;
#243621=EDGE_LOOP ( 'NONE', ( #67405, #248132, #113396 ) ) ;
#243641=FACE_OUTER_BOUND ( 'NONE', #174887, .T. ) ;
#243674=EDGE_LOOP ( 'NONE', ( #221181, #129040, #197194 ) ) ;
#243680=ORIENTED_EDGE ( 'NONE', *, *, #26708, .T. ) ;
#243707=FACE_OUTER_BOUND ( 'NONE', #218271, .T. ) ;
#243710=ORIENTED_EDGE ( 'NONE', *, *, #216677, .F. ) ;
#243721=CARTESIAN_POINT ( 'NONE',  ( 21.04999999999999716, -1.244299762474901705, -194.8241018385075733 ) ) ;
#243742=ORIENTED_EDGE ( 'NONE', *, *, #161821, .F. ) ;
#243761=VECTOR ( 'NONE', #93590, 1000.000000000000227 ) ;
#243807=CYLINDRICAL_SURFACE ( 'NONE', #119931, 0.1000000000000122874 ) ;
#243812=DIRECTION ( 'NONE',  ( 0.000000000000000000, 0.9770955615653315052, 0.2128009952263603954 ) ) ;
#243826=ORIENTED_EDGE ( 'NONE', *, *, #95349, .T. ) ;
#243828=EDGE_LOOP ( 'NONE', ( #189793, #225602, #22116, #206988 ) ) ;
#243843=EDGE_LOOP ( 'NONE', ( #225882, #201261, #85867, #40100 ) ) ;
#243878=AXIS2_PLACEMENT_3D ( 'NONE', #148957, #88945, #10716 ) ;
#243884=ORIENTED_EDGE ( 'NONE', *, *, #104406, .F. ) ;
#243887=DIRECTION ( 'NONE',  ( 0.000000000000000000, -0.2128009952263485993, 0.9770955615653341697 ) ) ;
#243901=LINE ( 'NONE', #127828, #67673 ) ;
#243907=DIRECTION ( 'NONE',  ( 0.000000000000000000, 0.2128009952263603677, -0.9770955615653313941 ) ) ;
#243917=CIRCLE ( 'NONE', #214876, 0.09999999999999080458 ) ;
#243923=ORIENTED_EDGE ( 'NONE', *, *, #118530, .F. ) ;
#243967=FACE_OUTER_BOUND ( 'NONE', #128589, .T. ) ;
#243974=ADVANCED_FACE ( 'NONE', ( #135363 ), #17987, .T. ) ;
#243978=CARTESIAN_POINT ( 'NONE',  ( -2.995603634470829482E-16, -6.214048216528735402, -227.6835268426532082 ) ) ;
#243999=AXIS2_PLACEMENT_3D ( 'NONE', #138650, #239079, #214371 ) ;
#244029=ADVANCED_FACE ( 'NONE', ( #123518 ), #146905, .T. ) ;
#244057=EDGE_CURVE ( 'NONE', #185124, #220406, #238210, .T. ) ;
#244069=CARTESIAN_POINT ( 'NONE',  ( -23.25000000000000000, 8.793666940903476004, -220.9353059101866847 ) ) ;
#244083=AXIS2_PLACEMENT_3D ( 'NONE', #77101, #74579, #154122 ) ;
#244085=ORIENTED_EDGE ( 'NONE', *, *, #218245, .F. ) ;
#244098=VECTOR ( 'NONE', #132657, 1000.000000000000000 ) ;
#244112=ORIENTED_EDGE ( 'NONE', *, *, #125210, .T. ) ;
#244132=AXIS2_PLACEMENT_3D ( 'NONE', #184610, #120819, #103762 ) ;
#244134=AXIS2_PLACEMENT_3D ( 'NONE', #118721, #198228, #27346 ) ;
#244140=CARTESIAN_POINT ( 'NONE',  ( 18.52351027002947603, -0.8635125639127735342, -242.3458057457398809 ) ) ;
#244160=EDGE_CURVE ( 'NONE', #73041, #9423, #63527, .T. ) ;
#244209=CARTESIAN_POINT ( 'NONE',  ( -23.25000000000000000, 4.554494125284476169, -212.9355439031026265 ) ) ;
#244222=EDGE_CURVE ( 'NONE', #35875, #103565, #192433, .T. ) ;
#244238=CARTESIAN_POINT ( 'NONE',  ( 18.52928932188133970, 15.28939250479744949, -222.8979625946709007 ) ) ;
#244279=FACE_OUTER_BOUND ( 'NONE', #250728, .T. ) ;
#244296=CARTESIAN_POINT ( 'NONE',  ( -20.64999999999999858, 9.614325556249161409, -211.5456030694648746 ) ) ;
#244306=CARTESIAN_POINT ( 'NONE',  ( -18.39999999999999858, -0.7490476236415797295, -242.2033265267442061 ) ) ;
#244312=DIRECTION ( 'NONE',  ( 0.000000000000000000, -0.9770955615653259541, -0.2128009952263860971 ) ) ;
#244321=AXIS2_PLACEMENT_3D ( 'NONE', #29437, #231467, #69828 ) ;
#244327=CARTESIAN_POINT ( 'NONE',  ( 23.14999999999999503, 10.99842653345846699, -220.2504445088529792 ) ) ;
#244332=CYLINDRICAL_SURFACE ( 'NONE', #100471, 0.09999999999999939493 ) ;
#244340=FACE_OUTER_BOUND ( 'NONE', #174211, .T. ) ;
#244348=ORIENTED_EDGE ( 'NONE', *, *, #159099, .F. ) ;
#244382=ORIENTED_EDGE ( 'NONE', *, *, #202883, .T. ) ;
#244510=CARTESIAN_POINT ( 'NONE',  ( -20.64999999999999858, 6.300962096140152013, -220.8843452229073705 ) ) ;
#244514=DIRECTION ( 'NONE',  ( -0.8660254037843505559, 0.1064004976132069402, -0.4885477807828162988 ) ) ;
#244522=DIRECTION ( 'NONE',  ( 0.000000000000000000, -0.2128009952263485993, 0.9770955615653341697 ) ) ;
#244543=DIRECTION ( 'NONE',  ( 0.000000000000000000, 0.2128009952263606730, -0.9770955615653315052 ) ) ;
#244583=CARTESIAN_POINT ( 'NONE',  ( 20.94999999999999929, 10.71906255309368383, -222.4921384173655383 ) ) ;
#244625=AXIS2_PLACEMENT_3D ( 'NONE', #242642, #163137, #219228 ) ;
#244640=CIRCLE ( 'NONE', #132221, 0.1000000000000055844 ) ;
#244655=ORIENTED_EDGE ( 'NONE', *, *, #221372, .T. ) ;
#244660=DIRECTION ( 'NONE',  ( 0.000000000000000000, 0.2128009952263603677, -0.9770955615653313941 ) ) ;
#244664=CARTESIAN_POINT ( 'NONE',  ( -21.04386569057698964, 17.15049515251747891, -224.5321864300226480 ) ) ;
#244678=CARTESIAN_POINT ( 'NONE',  ( -23.15000000000000213, 6.277629359189123015, -229.8243190661787878 ) ) ;
#244684=FACE_OUTER_BOUND ( 'NONE', #99223, .T. ) ;
#244685=CARTESIAN_POINT ( 'NONE',  ( -20.64999999999999858, 6.857177884343597540, -212.0437362999421680 ) ) ;
#244692=EDGE_CURVE ( 'NONE', #139739, #5736, #59971, .T. ) ;
#244693=CARTESIAN_POINT ( 'NONE',  ( 21.11345278033298811, 11.28464776068242692, -211.0754094929459654 ) ) ;
#244715=CARTESIAN_POINT ( 'NONE',  ( 23.14999999999999858, 16.98881331171930498, -224.4946931418895417 ) ) ;
#244716=CARTESIAN_POINT ( 'NONE',  ( -22.47071067811865319, -1.546016791165058635, -193.4356622592196970 ) ) ;
#244720=DIRECTION ( 'NONE',  ( 0.000000000000000000, 0.2128009952263603954, -0.9770955615653315052 ) ) ;
#244770=ORIENTED_EDGE ( 'NONE', *, *, #148106, .T. ) ;
#244807=CIRCLE ( 'NONE', #257236, 0.1000000000000054040 ) ;
#244815=ADVANCED_FACE ( 'NONE', ( #78624 ), #53939, .T. ) ;
#244836=CARTESIAN_POINT ( 'NONE',  ( 20.04142135623730070, 8.980461154494401299, -187.0187154576991304 ) ) ;
#244839=CARTESIAN_POINT ( 'NONE',  ( -20.54999999999999716, 6.757359537351773859, -220.2789794402637824 ) ) ;
#244845=DIRECTION ( 'NONE',  ( 0.000000000000000000, -0.9770955615653316162, -0.2128009952263604232 ) ) ;
#244848=AXIS2_PLACEMENT_3D ( 'NONE', #209786, #10316, #91114 ) ;
#244883=EDGE_LOOP ( 'NONE', ( #54039, #203938, #48187, #241310, #88005 ) ) ;
#244910=DIRECTION ( 'NONE',  ( 1.000000000000000000, 2.885090398161910739E-16, 6.283419270304611573E-17 ) ) ;
#244927=VECTOR ( 'NONE', #32404, 1000.000000000000227 ) ;
#244931=ORIENTED_EDGE ( 'NONE', *, *, #103614, .T. ) ;
#244936=LINE ( 'NONE', #247511, #50322 ) ;
#244992=DIRECTION ( 'NONE',  ( 0.000000000000000000, -0.2128009952263603677, 0.9770955615653313941 ) ) ;
#244994=LINE ( 'NONE', #168077, #153066 ) ;
#244995=LINE ( 'NONE', #68955, #161111 ) ;
#245022=ADVANCED_FACE ( 'NONE', ( #160779 ), #139878, .T. ) ;
#245041=CARTESIAN_POINT ( 'NONE',  ( -18.59999999999999787, 7.128833340094563376, -233.7327013124401276 ) ) ;
#245048=CARTESIAN_POINT ( 'NONE',  ( 18.46932045258654398, -0.9001461170050899518, -242.3116320965393982 ) ) ;
#245086=CIRCLE ( 'NONE', #41102, 0.1000000000000054040 ) ;
#245093=VERTEX_POINT ( 'NONE', #91486 ) ;
#245100=CARTESIAN_POINT ( 'NONE',  ( 21.05000000000000071, 10.38152206507873387, -207.4259860971185958 ) ) ;
#245112=EDGE_CURVE ( 'NONE', #70808, #256115, #72667, .T. ) ;
#245138=VERTEX_POINT ( 'NONE', #190602 ) ;
#245146=EDGE_CURVE ( 'NONE', #93777, #212172, #111043, .T. ) ;
#245182=EDGE_LOOP ( 'NONE', ( #121703, #151170, #108792, #168037 ) ) ;
#245197=EDGE_CURVE ( 'NONE', #232353, #237270, #22610, .T. ) ;
#245199=ORIENTED_EDGE ( 'NONE', *, *, #159858, .F. ) ;
#245201=CARTESIAN_POINT ( 'NONE',  ( 21.05000000000000071, 7.525330762710603416, -212.0571253909869256 ) ) ;
#245228=CIRCLE ( 'NONE', #216153, 0.1000000000000055844 ) ;
#245234=ORIENTED_EDGE ( 'NONE', *, *, #75532, .T. ) ;
#245255=LINE ( 'NONE', #125304, #177856 ) ;
#245262=CARTESIAN_POINT ( 'NONE',  ( 21.05000000000096350, 11.98086986275577459, -206.1603386415442856 ) ) ;
#245279=CIRCLE ( 'NONE', #12247, 0.1000000000000054040 ) ;
#245316=DIRECTION ( 'NONE',  ( 0.000000000000000000, 0.2128009952263485993, -0.9770955615653341697 ) ) ;
#245322=FACE_OUTER_BOUND ( 'NONE', #31348, .T. ) ;
#245332=DIRECTION ( 'NONE',  ( -3.265361837132813093E-16, 0.9770955615653357240, 0.2128009952263411608 ) ) ;
#245339=ORIENTED_EDGE ( 'NONE', *, *, #221798, .T. ) ;
#245348=ORIENTED_EDGE ( 'NONE', *, *, #19330, .F. ) ;
#245355=CARTESIAN_POINT ( 'NONE',  ( 18.59999999999999076, 8.006782298343173565, -209.8034900594678618 ) ) ;
#245359=EDGE_CURVE ( 'NONE', #65554, #144682, #67620, .T. ) ;
#245365=FACE_OUTER_BOUND ( 'NONE', #249387, .T. ) ;
#245380=DIRECTION ( 'NONE',  ( 0.000000000000000000, 0.9803012954743849372, 0.1975078988072195840 ) ) ;
#245395=DIRECTION ( 'NONE',  ( 0.000000000000000000, 0.2128009952263582305, -0.9770955615653319493 ) ) ;
#245408=ORIENTED_EDGE ( 'NONE', *, *, #214227, .T. ) ;
#245451=ADVANCED_FACE ( 'NONE', ( #137845 ), #185265, .T. ) ;
#245459=CARTESIAN_POINT ( 'NONE',  ( -21.05000000000000071, -10.56629024491939894, -206.4738935375009703 ) ) ;
#245474=ORIENTED_EDGE ( 'NONE', *, *, #197607, .T. ) ;
#245556=CARTESIAN_POINT ( 'NONE',  ( -21.14999999999999858, 11.40444339177023814, -198.6185779617709670 ) ) ;
#245597=CARTESIAN_POINT ( 'NONE',  ( 23.25000000000000000, -13.98128454229088291, -192.0195388455185821 ) ) ;
#245608=VERTEX_POINT ( 'NONE', #74671 ) ;
#245616=PLANE ( 'NONE',  #6615 ) ;
#245633=ORIENTED_EDGE ( 'NONE', *, *, #247269, .F. ) ;
#245639=CARTESIAN_POINT ( 'NONE',  ( 18.51997666896887651, -7.657082092440962384, -209.9784881053329855 ) ) ;
#245683=DIRECTION ( 'NONE',  ( 1.000000000000000000, 1.794895427898103559E-16, 3.909090864890002444E-17 ) ) ;
#245685=EDGE_CURVE ( 'NONE', #103023, #183689, #230485, .T. ) ;
#245771=DIRECTION ( 'NONE',  ( -1.000000000000000000, 0.000000000000000000, 0.000000000000000000 ) ) ;
#245781=DIRECTION ( 'NONE',  ( 0.000000000000000000, -0.2128009952263601456, 0.9770955615653316162 ) ) ;
#245782=TOROIDAL_SURFACE ( 'NONE', #175102, 11.90000000000000213, 0.1000000000000000056 ) ;
#245799=ADVANCED_FACE ( 'NONE', ( #243967 ), #167042, .T. ) ;
#245820=DIRECTION ( 'NONE',  ( 0.000000000000000000, 0.2128009952263618110, -0.9770955615653311721 ) ) ;
#245831=ORIENTED_EDGE ( 'NONE', *, *, #30707, .T. ) ;
#245845=ORIENTED_EDGE ( 'NONE', *, *, #229017, .T. ) ;
#245866=ORIENTED_EDGE ( 'NONE', *, *, #184746, .T. ) ;
#245871=ORIENTED_EDGE ( 'NONE', *, *, #239272, .T. ) ;
#245886=AXIS2_PLACEMENT_3D ( 'NONE', #177008, #200393, #81682 ) ;
#245898=CARTESIAN_POINT ( 'NONE',  ( -23.25000000000000000, -3.281532336344785694, -226.3283167004137226 ) ) ;
#245908=ORIENTED_EDGE ( 'NONE', *, *, #202908, .T. ) ;
#245937=CIRCLE ( 'NONE', #183574, 4.099999999999989875 ) ;
#245938=FACE_BOUND ( 'NONE', #76139, .T. ) ;
#245941=CARTESIAN_POINT ( 'NONE',  ( 18.59999999999999787, 7.576017155224048061, -241.7224044826512284 ) ) ;
#245948=ORIENTED_EDGE ( 'NONE', *, *, #252118, .T. ) ;
#245958=AXIS2_PLACEMENT_3D ( 'NONE', #157389, #140340, #217301 ) ;
#245970=CARTESIAN_POINT ( 'NONE',  ( -20.94999999999999218, 17.16609282392352398, -224.6038045889790453 ) ) ;
#245990=ADVANCED_FACE ( 'NONE', ( #155184 ), #134279, .F. ) ;
#245998=VERTEX_POINT ( 'NONE', #215116 ) ;
#246003=CARTESIAN_POINT ( 'NONE',  ( -21.44999999999999929, 11.68239342655420110, -220.1014838121945161 ) ) ;
#246014=DIRECTION ( 'NONE',  ( 0.000000000000000000, 0.2128009952263485993, -0.9770955615653341697 ) ) ;
#246033=VERTEX_POINT ( 'NONE', #232132 ) ;
#246045=EDGE_LOOP ( 'NONE', ( #248888, #248711, #225, #78676 ) ) ;
#246064=ORIENTED_EDGE ( 'NONE', *, *, #84295, .T. ) ;
#246104=FACE_OUTER_BOUND ( 'NONE', #97599, .T. ) ;
#246109=VERTEX_POINT ( 'NONE', #256755 ) ;
#246131=TOROIDAL_SURFACE ( 'NONE', #167053, 11.65000000000000036, 0.1000000000000000056 ) ;
#246147=CARTESIAN_POINT ( 'NONE',  ( -20.54999999999999716, -8.852780557335606204, -215.5675418792430946 ) ) ;
#246167=AXIS2_PLACEMENT_3D ( 'NONE', #135018, #35961, #214571 ) ;
#246223=ORIENTED_EDGE ( 'NONE', *, *, #81952, .F. ) ;
#246227=EDGE_LOOP ( 'NONE', ( #249306, #13613, #48970, #198733 ) ) ;
#246230=ORIENTED_EDGE ( 'NONE', *, *, #153902, .T. ) ;
#246251=CARTESIAN_POINT ( 'NONE',  ( 21.14999999999999858, -8.874060656858240748, -215.4698323230865640 ) ) ;
#246292=CARTESIAN_POINT ( 'NONE',  ( -20.64999999999999858, -6.688413578037177842, -212.5825622730469036 ) ) ;
#246293=DIRECTION ( 'NONE',  ( -0.000000000000000000, 0.9770955615653313941, 0.2128009952263603954 ) ) ;
#246300=ORIENTED_EDGE ( 'NONE', *, *, #250588, .T. ) ;
#246305=AXIS2_PLACEMENT_3D ( 'NONE', #181757, #142603, #78775 ) ;
#246315=VERTEX_POINT ( 'NONE', #153603 ) ;
#246316=DIRECTION ( 'NONE',  ( 1.000000000000000000, -8.034189347746079853E-16, 2.566115377699053192E-16 ) ) ;
#246328=CARTESIAN_POINT ( 'NONE',  ( -21.05000000000000071, 0.6869237119019852011, -212.7787591058053067 ) ) ;
#246334=DIRECTION ( 'NONE',  ( -0.000000000000000000, -0.9770955615653317272, -0.2128009952263598126 ) ) ;
#246347=CARTESIAN_POINT ( 'NONE',  ( 21.97500000000000497, 14.02742277431099538, -219.5907614236512870 ) ) ;
#246353=AXIS2_PLACEMENT_3D ( 'NONE', #25083, #44624, #64184 ) ;
#246354=AXIS2_PLACEMENT_3D ( 'NONE', #192394, #193684, #213220 ) ;
#246367=CARTESIAN_POINT ( 'NONE',  ( -22.44366136229477249, -2.469944097043066389, -189.6151238087248601 ) ) ;
#246373=DIRECTION ( 'NONE',  ( -2.342056488767301376E-15, -0.3427706569149662763, 0.9394191166662954062 ) ) ;
#246382=DIRECTION ( 'NONE',  ( 0.000000000000000000, 0.3042567129659849434, 0.9525900758537926283 ) ) ;
#246437=B_SPLINE_CURVE_WITH_KNOTS ( 'NONE', 3,
 ( #214922, #178396, #252755, #35047, #37590, #174576, #194102 ),
 .UNSPECIFIED., .F., .F.,
 ( 4, 3, 4 ),
 ( 0.000000000000000000, 0.0007844235214594265501, 0.001767853679404345936 ),
 .UNSPECIFIED. ) ;
#246438=AXIS2_PLACEMENT_3D ( 'NONE', #146131, #224380, #167024 ) ;
#246531=AXIS2_PLACEMENT_3D ( 'NONE', #250773, #31769, #248217 ) ;
#246554=AXIS2_PLACEMENT_3D ( 'NONE', #118505, #79338, #136750 ) ;
#246586=CARTESIAN_POINT ( 'NONE',  ( 20.85000000000000142, 17.06838326776701109, -224.6250846885016870 ) ) ;
#246590=CARTESIAN_POINT ( 'NONE',  ( -20.94999999999999929, -4.656943609564680564, -233.1535107627236414 ) ) ;
#246611=EDGE_LOOP ( 'NONE', ( #77466, #139677, #95184, #10331 ) ) ;
#246616=FACE_OUTER_BOUND ( 'NONE', #41543, .T. ) ;
#246637=CARTESIAN_POINT ( 'NONE',  ( -18.50000000000000000, 13.63658454968486389, -219.6758818217417968 ) ) ;
#246660=DIRECTION ( 'NONE',  ( 2.952720810173289112E-16, -0.9770955615653302839, -0.2128009952263658355 ) ) ;
#246690=AXIS2_PLACEMENT_3D ( 'NONE', #29947, #50736, #152462 ) ;
#246703=CIRCLE ( 'NONE', #188439, 0.5000000000000048850 ) ;
#246731=CIRCLE ( 'NONE', #134303, 0.1000000000000008937 ) ;
#246751=ORIENTED_EDGE ( 'NONE', *, *, #117857, .T. ) ;
#246773=CIRCLE ( 'NONE', #117617, 0.09999999999999939493 ) ;
#246790=AXIS2_PLACEMENT_3D ( 'NONE', #165087, #242048, #125945 ) ;
#246904=CARTESIAN_POINT ( 'NONE',  ( -2.995603634470829482E-16, 10.99842653345846699, -220.2504445088529792 ) ) ;
#246909=CARTESIAN_POINT ( 'NONE',  ( 18.47073956224749480, -7.742049366311430703, -209.9614587431316579 ) ) ;
#246981=CARTESIAN_POINT ( 'NONE',  ( -23.25000000000000000, 6.681951250119205987, -231.6808006331528986 ) ) ;
#246985=CARTESIAN_POINT ( 'NONE',  ( -20.00857864376270001, 11.54723657985719321, -211.0222915228556246 ) ) ;
#246987=LINE ( 'NONE', #68368, #122777 ) ;
#246992=ORIENTED_EDGE ( 'NONE', *, *, #191280, .F. ) ;
#247015=CARTESIAN_POINT ( 'NONE',  ( -20.00857864376270001, 13.65786464920749843, -219.7735913778983559 ) ) ;
#247024=DIRECTION ( 'NONE',  ( 0.000000000000000000, -0.2128009952263604232, 0.9770955615653316162 ) ) ;
#247053=ORIENTED_EDGE ( 'NONE', *, *, #102025, .F. ) ;
#247062=CARTESIAN_POINT ( 'NONE',  ( 23.14999999999999858, 10.93950603019935564, -232.9027774310573022 ) ) ;
#247082=DIRECTION ( 'NONE',  ( 0.000000000000000000, -0.8149014228131981064, 0.5795995782408966956 ) ) ;
#247087=VERTEX_POINT ( 'NONE', #110918 ) ;
#247103=FACE_OUTER_BOUND ( 'NONE', #39394, .T. ) ;
#247108=DIRECTION ( 'NONE',  ( 1.000000000000000000, 0.000000000000000000, 0.000000000000000000 ) ) ;
#247128=DIRECTION ( 'NONE',  ( 0.000000000000000000, -0.2128009952263678062, 0.9770955615653298398 ) ) ;
#247129=FACE_OUTER_BOUND ( 'NONE', #51012, .T. ) ;
#247172=ORIENTED_EDGE ( 'NONE', *, *, #114224, .F. ) ;
#247177=CARTESIAN_POINT ( 'NONE',  ( -1.739115166359751170E-14, 16.67126802362264826, -222.8016931105129004 ) ) ;
#247188=ORIENTED_EDGE ( 'NONE', *, *, #70897, .F. ) ;
#247199=DIRECTION ( 'NONE',  ( -0.000000000000000000, -0.2128009952263603677, 0.9770955615653313941 ) ) ;
#247205=LINE ( 'NONE', #242068, #122530 ) ;
#247224=FACE_OUTER_BOUND ( 'NONE', #233878, .T. ) ;
#247245=ORIENTED_EDGE ( 'NONE', *, *, #184073, .F. ) ;
#247267=AXIS2_PLACEMENT_3D ( 'NONE', #3865, #40466, #143368 ) ;
#247269=EDGE_CURVE ( 'NONE', #81634, #159242, #204475, .T. ) ;
#247287=VECTOR ( 'NONE', #60908, 1000.000000000000227 ) ;
#247296=ORIENTED_EDGE ( 'NONE', *, *, #192520, .F. ) ;
#247310=AXIS2_PLACEMENT_3D ( 'NONE', #51747, #88300, #152191 ) ;
#247319=CIRCLE ( 'NONE', #201352, 11.65000000000000036 ) ;
#247322=CARTESIAN_POINT ( 'NONE',  ( -23.25000000000000000, 18.60970618848720903, -231.2322896185303875 ) ) ;
#247333=ADVANCED_FACE ( 'NONE', ( #198155 ), #108628, .T. ) ;
#247377=CIRCLE ( 'NONE', #10062, 0.1000000000000055844 ) ;
#247382=ORIENTED_EDGE ( 'NONE', *, *, #166687, .F. ) ;
#247389=AXIS2_PLACEMENT_3D ( 'NONE', #25088, #61618, #104559 ) ;
#247395=CIRCLE ( 'NONE', #218348, 0.1000000000000027534 ) ;
#247408=ORIENTED_EDGE ( 'NONE', *, *, #208587, .F. ) ;
#247472=ORIENTED_EDGE ( 'NONE', *, *, #242448, .F. ) ;
#247504=EDGE_LOOP ( 'NONE', ( #86327, #185676, #140740, #144451 ) ) ;
#247511=CARTESIAN_POINT ( 'NONE',  ( -23.15000000000000213, 6.757359537351773859, -220.2789794402638108 ) ) ;
#247519=FACE_OUTER_BOUND ( 'NONE', #212135, .T. ) ;
#247552=EDGE_CURVE ( 'NONE', #116714, #3257, #144585, .T. ) ;
#247554=CARTESIAN_POINT ( 'NONE',  ( -23.15000000000000213, 8.882751598337867094, -187.0399955572217721 ) ) ;
#247556=DIRECTION ( 'NONE',  ( 0.000000000000000000, -0.2128009952263604232, 0.9770955615653316162 ) ) ;
#247568=DIRECTION ( 'NONE',  ( 1.000000000000000000, 0.000000000000000000, 0.000000000000000000 ) ) ;
#247577=ORIENTED_EDGE ( 'NONE', *, *, #185110, .T. ) ;
#247596=AXIS2_PLACEMENT_3D ( 'NONE', #175627, #139007, #216001 ) ;
#247614=CARTESIAN_POINT ( 'NONE',  ( 18.43630871534865179, -0.9118679986080973077, -242.3006466030380750 ) ) ;
#247633=FACE_OUTER_BOUND ( 'NONE', #100453, .T. ) ;
#247634=EDGE_CURVE ( 'NONE', #224326, #175634, #121328, .T. ) ;
#247645=CARTESIAN_POINT ( 'NONE',  ( -22.42253884134832020, -2.477159594661237474, -189.6168107728914549 ) ) ;
#247648=ORIENTED_EDGE ( 'NONE', *, *, #165751, .T. ) ;
#247704=CARTESIAN_POINT ( 'NONE',  ( -23.15000000000000213, 11.48087284840413425, -198.4995883060917663 ) ) ;
#247705=ORIENTED_EDGE ( 'NONE', *, *, #6719, .T. ) ;
#247713=VERTEX_POINT ( 'NONE', #115745 ) ;
#247721=DIRECTION ( 'NONE',  ( 1.000000000000000000, 3.816239940179503281E-14, -1.218904804407150903E-14 ) ) ;
#247780=VERTEX_POINT ( 'NONE', #119615 ) ;
#247791=FACE_OUTER_BOUND ( 'NONE', #14532, .T. ) ;
#247793=ADVANCED_FACE ( 'NONE', ( #240831 ), #117186, .T. ) ;
#247844=FACE_OUTER_BOUND ( 'NONE', #234009, .T. ) ;
#247866=FACE_OUTER_BOUND ( 'NONE', #55737, .T. ) ;
#247888=CARTESIAN_POINT ( 'NONE',  ( 18.59999999999999787, 0.6656436123793491033, -212.6810495496487476 ) ) ;
#247917=FACE_OUTER_BOUND ( 'NONE', #134249, .T. ) ;
#247955=ORIENTED_EDGE ( 'NONE', *, *, #183324, .T. ) ;
#247962=DIRECTION ( 'NONE',  ( 0.000000000000000000, 0.6728388485993177515, -0.7397890806274072251 ) ) ;
#247981=DIRECTION ( 'NONE',  ( 0.000000000000000000, 0.2128009952263605065, -0.9770955615653315052 ) ) ;
#247989=CARTESIAN_POINT ( 'NONE',  ( -23.15000000000000213, 6.703231349641842307, -231.7785101893094577 ) ) ;
#247992=CARTESIAN_POINT ( 'NONE',  ( 21.08078803292165659, 6.171108002023541594, -199.5749562617978370 ) ) ;
#248008=VERTEX_POINT ( 'NONE', #124737 ) ;
#248011=VERTEX_POINT ( 'NONE', #9911 ) ;
#248016=DIRECTION ( 'NONE',  ( 0.000000000000000000, -0.9976611540403004241, -0.06835365183350541884 ) ) ;
#248025=DIRECTION ( 'NONE',  ( 0.000000000000000000, 0.2128009952263605897, -0.9770955615653315052 ) ) ;
#248035=CARTESIAN_POINT ( 'NONE',  ( 18.55121869061587958, 18.40663661316796151, -236.9846611508999388 ) ) ;
#248042=EDGE_CURVE ( 'NONE', #10221, #87043, #7347, .T. ) ;
#248046=DIRECTION ( 'NONE',  ( 1.000000000000000000, 0.000000000000000000, 0.000000000000000000 ) ) ;
#248054=EDGE_CURVE ( 'NONE', #206865, #150544, #93298, .T. ) ;
#248058=DIRECTION ( 'NONE',  ( 1.000000000000000000, 0.000000000000000000, 0.000000000000000000 ) ) ;
#248061=VECTOR ( 'NONE', #212520, 1000.000000000000000 ) ;
#248108=CARTESIAN_POINT ( 'NONE',  ( -20.54999999999999716, 6.659649981195239654, -220.3002595397864241 ) ) ;
#248127=AXIS2_PLACEMENT_3D ( 'NONE', #66516, #202173, #22268 ) ;
#248132=ORIENTED_EDGE ( 'NONE', *, *, #105248, .F. ) ;
#248138=( LENGTH_UNIT ( ) NAMED_UNIT ( * ) SI_UNIT ( .MILLI., .METRE. ) );
#248139=EDGE_LOOP ( 'NONE', ( #220590, #17457, #209682, #152254 ) ) ;
#248140=EDGE_CURVE ( 'NONE', #155898, #97694, #17409, .T. ) ;
#248197=ORIENTED_EDGE ( 'NONE', *, *, #195356, .F. ) ;
#248202=ADVANCED_FACE ( 'NONE', ( #78853 ), #37939, .T. ) ;
#248217=DIRECTION ( 'NONE',  ( 0.000000000000000000, 0.2128009952263601179, -0.9770955615653315052 ) ) ;
#248218=ORIENTED_EDGE ( 'NONE', *, *, #160759, .F. ) ;
#248219=EDGE_CURVE ( 'NONE', #156064, #77477, #113277, .T. ) ;
#248222=CIRCLE ( 'NONE', #23392, 0.1999999999999995670 ) ;
#248232=DIRECTION ( 'NONE',  ( 0.000000000000000000, 0.2128009952263362758, -0.9770955615653368342 ) ) ;
#248233=CARTESIAN_POINT ( 'NONE',  ( -20.00857864376270001, 11.76393579169289083, -211.0774408799668720 ) ) ;
#248281=DIRECTION ( 'NONE',  ( -1.000000000000000000, -0.000000000000000000, -0.000000000000000000 ) ) ;
#248295=DIRECTION ( 'NONE',  ( 1.000000000000000000, 0.000000000000000000, 0.000000000000000000 ) ) ;
#248303=CIRCLE ( 'NONE', #210888, 0.09999999999999939493 ) ;
#248323=CARTESIAN_POINT ( 'NONE',  ( -23.15000000000000213, 6.268811756569107274, -220.3853799378769622 ) ) ;
#248329=CIRCLE ( 'NONE', #123246, 0.1000000000000055844 ) ;
#248345=FACE_OUTER_BOUND ( 'NONE', #205437, .T. ) ;
#248349=CARTESIAN_POINT ( 'NONE',  ( 23.14999999999999858, 9.273719881888197847, -221.1390486761779925 ) ) ;
#248370=ORIENTED_EDGE ( 'NONE', *, *, #49856, .F. ) ;
#248425=DIRECTION ( 'NONE',  ( 1.000000000000000000, 0.000000000000000000, 0.000000000000000000 ) ) ;
#248432=VECTOR ( 'NONE', #189749, 1000.000000000000000 ) ;
#248433=CARTESIAN_POINT ( 'NONE',  ( -23.25000000000000000, 18.41524492703432614, -237.0006385043383546 ) ) ;
#248464=CARTESIAN_POINT ( 'NONE',  ( 21.05000000000000071, 1.148907358139439339E-11, -201.0000000000015064 ) ) ;
#248494=CIRCLE ( 'NONE', #61037, 0.5000000000000009992 ) ;
#248556=EDGE_CURVE ( 'NONE', #200910, #37909, #117170, .T. ) ;
#248558=ORIENTED_EDGE ( 'NONE', *, *, #79163, .T. ) ;
#248562=CIRCLE ( 'NONE', #123683, 1.899999999999997469 ) ;
#248587=ORIENTED_EDGE ( 'NONE', *, *, #2905, .F. ) ;
#248593=VERTEX_POINT ( 'NONE', #146233 ) ;
#248648=EDGE_CURVE ( 'NONE', #211413, #212703, #70549, .T. ) ;
#248650=VERTEX_POINT ( 'NONE', #235720 ) ;
#248656=LINE ( 'NONE', #184823, #251406 ) ;
#248659=DIRECTION ( 'NONE',  ( -0.000000000000000000, 0.9770955615653313941, 0.2128009952263603954 ) ) ;
#248701=AXIS2_PLACEMENT_3D ( 'NONE', #92514, #49552, #74283 ) ;
#248711=ORIENTED_EDGE ( 'NONE', *, *, #74303, .T. ) ;
#248715=VERTEX_POINT ( 'NONE', #32435 ) ;
#248735=EDGE_LOOP ( 'NONE', ( #87256, #119161, #222669, #119134, #196501 ) ) ;
#248753=CARTESIAN_POINT ( 'NONE',  ( 23.24999999999999645, 7.128833340094563376, -233.7327013124401276 ) ) ;
#248765=EDGE_LOOP ( 'NONE', ( #173028, #67983, #243418 ) ) ;
#248782=VERTEX_POINT ( 'NONE', #42657 ) ;
#248805=CARTESIAN_POINT ( 'NONE',  ( 22.47071067811865319, -1.546016791165055304, -193.4356622592196970 ) ) ;
#248825=DIRECTION ( 'NONE',  ( -2.812466655313718795E-14, -0.07893460099012014619, 0.9968797965484758050 ) ) ;
#248876=AXIS2_PLACEMENT_3D ( 'NONE', #117859, #253516, #215665 ) ;
#248884=ORIENTED_EDGE ( 'NONE', *, *, #169239, .T. ) ;
#248888=ORIENTED_EDGE ( 'NONE', *, *, #237480, .F. ) ;
#248912=LINE ( 'NONE', #171975, #249382 ) ;
#248930=CARTESIAN_POINT ( 'NONE',  ( -20.85000000000000142, 6.803341081522319200, -233.7601854879220298 ) ) ;
#248934=DIRECTION ( 'NONE',  ( 0.000000000000000000, 0.9752329468386375932, 0.2211802418852714114 ) ) ;
#248937=FACE_OUTER_BOUND ( 'NONE', #257666, .T. ) ;
#248948=CARTESIAN_POINT ( 'NONE',  ( -18.59999999999999787, 4.064367954407507533, -211.9684786640956418 ) ) ;
#248959=DIRECTION ( 'NONE',  ( 0.000000000000000000, 0.9525900758537791946, -0.3042567129660269654 ) ) ;
#249022=DIRECTION ( 'NONE',  ( 0.000000000000000000, 0.2128009952263630322, -0.9770955615653309501 ) ) ;
#249055=CARTESIAN_POINT ( 'NONE',  ( 20.95512820512820440, 11.25838014693916378, -210.9828572391344039 ) ) ;
#249099=FACE_OUTER_BOUND ( 'NONE', #243843, .T. ) ;
#249166=CYLINDRICAL_SURFACE ( 'NONE', #11969, 0.1000000000000054040 ) ;
#249178=DIRECTION ( 'NONE',  ( -0.000000000000000000, 0.2253241261139106999, -0.9742838591452712693 ) ) ;
#249184=ORIENTED_EDGE ( 'NONE', *, *, #221880, .T. ) ;
#249187=DIRECTION ( 'NONE',  ( 0.000000000000000000, -0.2128009952263603677, 0.9770955615653315052 ) ) ;
#249221=DIRECTION ( 'NONE',  ( 1.000000000000000000, 0.000000000000000000, 0.000000000000000000 ) ) ;
#249239=LINE ( 'NONE', #69323, #255589 ) ;
#249254=CARTESIAN_POINT ( 'NONE',  ( -20.94999999999999929, 14.61354176542825201, -235.9279552357344016 ) ) ;
#249294=LINE ( 'NONE', #31555, #230857 ) ;
#249299=EDGE_CURVE ( 'NONE', #133719, #200289, #67303, .T. ) ;
#249306=ORIENTED_EDGE ( 'NONE', *, *, #19429, .T. ) ;
#249328=CARTESIAN_POINT ( 'NONE',  ( 23.25000000000000000, 16.02417409648693436, -219.3605785455116006 ) ) ;
#249333=CARTESIAN_POINT ( 'NONE',  ( 20.94999999999999929, 18.34711819382569686, -236.8747682978092541 ) ) ;
#249335=EDGE_CURVE ( 'NONE', #7989, #48943, #3471, .T. ) ;
#249349=ORIENTED_EDGE ( 'NONE', *, *, #237705, .T. ) ;
#249350=DIRECTION ( 'NONE',  ( 1.000000000000000000, 0.000000000000000000, 0.000000000000000000 ) ) ;
#249352=ORIENTED_EDGE ( 'NONE', *, *, #35809, .T. ) ;
#249354=ORIENTED_EDGE ( 'NONE', *, *, #31189, .F. ) ;
#249382=VECTOR ( 'NONE', #113236, 1000.000000000000227 ) ;
#249386=TOROIDAL_SURFACE ( 'NONE', #170312, 0.2000000000000000111, 0.1000000000000000056 ) ;
#249387=EDGE_LOOP ( 'NONE', ( #91958, #7177, #140672, #93925 ) ) ;
#249427=CARTESIAN_POINT ( 'NONE',  ( -23.25000000000000000, 11.48087284840413425, -198.4995883060917663 ) ) ;
#249428=ORIENTED_EDGE ( 'NONE', *, *, #59279, .T. ) ;
#249430=VERTEX_POINT ( 'NONE', #153304 ) ;
#249431=ORIENTED_EDGE ( 'NONE', *, *, #161726, .F. ) ;
#249432=ADVANCED_FACE ( 'NONE', ( #89428 ), #211971, .F. ) ;
#249439=EDGE_LOOP ( 'NONE', ( #87456, #180675, #122840, #193917 ) ) ;
#249451=AXIS2_PLACEMENT_3D ( 'NONE', #225596, #126530, #206064 ) ;
#249472=DIRECTION ( 'NONE',  ( -3.265361837132812600E-16, 0.9770955615653313941, 0.2128009952263603677 ) ) ;
#249478=DIRECTION ( 'NONE',  ( -1.000000000000000000, -2.885090398161910739E-16, -6.283419270304611573E-17 ) ) ;
#249486=DIRECTION ( 'NONE',  ( -1.000000000000000000, -1.832422279913646096E-16, -3.990820347355631841E-17 ) ) ;
#249493=DIRECTION ( 'NONE',  ( 0.000000000000000000, -0.2128009952263403282, 0.9770955615653358350 ) ) ;
#249509=ADVANCED_FACE ( 'NONE', ( #188536 ), #29503, .T. ) ;
#249526=DIRECTION ( 'NONE',  ( 0.000000000000000000, 0.2128009952263603399, -0.9770955615653315052 ) ) ;
#249577=DIRECTION ( 'NONE',  ( 0.000000000000000000, 0.2128009952263650861, -0.9770955615653305060 ) ) ;
#249604=EDGE_CURVE ( 'NONE', #17954, #113101, #125892, .T. ) ;
#249637=EDGE_CURVE ( 'NONE', #146487, #223782, #188272, .T. ) ;
#249668=CARTESIAN_POINT ( 'NONE',  ( 20.94999999999999574, 0.4810385098657082859, -209.0827657365571213 ) ) ;
#249710=AXIS2_PLACEMENT_3D ( 'NONE', #59280, #158457, #138822 ) ;
#249717=DIRECTION ( 'NONE',  ( -1.000000000000000000, 0.000000000000000000, 0.000000000000000000 ) ) ;
#249737=ADVANCED_FACE ( 'NONE', ( #164831 ), #96652, .F. ) ;
#249743=CARTESIAN_POINT ( 'NONE',  ( -23.15000000000000213, 16.98881331171929787, -224.4946931418895417 ) ) ;
#249763=ORIENTED_EDGE ( 'NONE', *, *, #12914, .T. ) ;
#249776=EDGE_LOOP ( 'NONE', ( #29700, #94219, #20556 ) ) ;
#249802=VECTOR ( 'NONE', #65754, 1000.000000000000114 ) ;
#249849=AXIS2_PLACEMENT_3D ( 'NONE', #208135, #205528, #26936 ) ;
#249870=ORIENTED_EDGE ( 'NONE', *, *, #79395, .T. ) ;
#249895=VECTOR ( 'NONE', #2134, 1000.000000000000000 ) ;
#249957=CARTESIAN_POINT ( 'NONE',  ( -21.65000000000000213, 10.13883017033223943, -211.3290274220034632 ) ) ;
#249981=CIRCLE ( 'NONE', #137535, 3.999999999999998224 ) ;
#250002=CARTESIAN_POINT ( 'NONE',  ( 23.15000000000000213, -4.356730526971939632, -226.1082375506050539 ) ) ;
#250028=DIRECTION ( 'NONE',  ( 2.915501640297155269E-16, -0.9770955615653317272, -0.2128009952263597293 ) ) ;
#250062=ORIENTED_EDGE ( 'NONE', *, *, #27414, .T. ) ;
#250070=CARTESIAN_POINT ( 'NONE',  ( 20.94999027547553894, 18.34807417603272128, -236.8765254748879556 ) ) ;
#250073=ORIENTED_EDGE ( 'NONE', *, *, #44984, .T. ) ;
#250076=CARTESIAN_POINT ( 'NONE',  ( 20.94999999999999574, 11.77895973109482952, -206.1023438919106070 ) ) ;
#250187=CARTESIAN_POINT ( 'NONE',  ( 18.46163235739466302, -0.7174337875998068048, -242.2552085481934512 ) ) ;
#250191=ORIENTED_EDGE ( 'NONE', *, *, #44065, .T. ) ;
#250200=FACE_BOUND ( 'NONE', #190269, .T. ) ;
#250206=DIRECTION ( 'NONE',  ( 0.7071067811865302533, -0.6909108974501196876, -0.1504730267679053324 ) ) ;
#250220=TOROIDAL_SURFACE ( 'NONE', #150278, 1.900000000000002576, 0.1000000000000000056 ) ;
#250228=CARTESIAN_POINT ( 'NONE',  ( 20.94999999999999929, 9.480858690661944976, -221.0361137499737936 ) ) ;
#250229=DIRECTION ( 'NONE',  ( 1.000000000000000000, 0.000000000000000000, 0.000000000000000000 ) ) ;
#250273=ORIENTED_EDGE ( 'NONE', *, *, #222191, .T. ) ;
#250288=ORIENTED_EDGE ( 'NONE', *, *, #253196, .F. ) ;
#250289=ORIENTED_EDGE ( 'NONE', *, *, #122669, .T. ) ;
#250316=DIRECTION ( 'NONE',  ( 1.000000000000000000, 3.190570557967288949E-16, 6.948722487160392945E-17 ) ) ;
#250318=DIRECTION ( 'NONE',  ( 0.000000000000000000, 0.2128009952263603954, -0.9770955615653315052 ) ) ;
#250321=VERTEX_POINT ( 'NONE', #194375 ) ;
#250363=CARTESIAN_POINT ( 'NONE',  ( 20.94999999999999574, 11.84624361595475506, -206.1763227999733203 ) ) ;
#250388=DIRECTION ( 'NONE',  ( 0.000000000000000000, 0.2128009952263601456, -0.9770955615653316162 ) ) ;
#250409=CARTESIAN_POINT ( 'NONE',  ( 23.14999999999999503, 13.96869538424789070, -210.3925794786331949 ) ) ;
#250429=EDGE_CURVE ( 'NONE', #254024, #220753, #24729, .T. ) ;
#250493=ORIENTED_EDGE ( 'NONE', *, *, #211893, .T. ) ;
#250505=ORIENTED_EDGE ( 'NONE', *, *, #76968, .T. ) ;
#250507=ORIENTED_EDGE ( 'NONE', *, *, #195975, .F. ) ;
#250525=PLANE ( 'NONE',  #28155 ) ;
#250526=DIRECTION ( 'NONE',  ( -0.000000000000000000, 0.2128009952263603677, -0.9770955615653313941 ) ) ;
#250533=FACE_OUTER_BOUND ( 'NONE', #59436, .T. ) ;
#250561=ADVANCED_FACE ( 'NONE', ( #106786 ), #191505, .T. ) ;
#250564=ORIENTED_EDGE ( 'NONE', *, *, #71695, .T. ) ;
#250579=CARTESIAN_POINT ( 'NONE',  ( -21.65000000000000213, 12.03275902784684703, -220.0251779199349187 ) ) ;
#250582=AXIS2_PLACEMENT_3D ( 'NONE', #105997, #183011, #188134 ) ;
#250588=EDGE_CURVE ( 'NONE', #14516, #106738, #188624, .T. ) ;
#250597=CARTESIAN_POINT ( 'NONE',  ( 18.54148534481893762, 18.40294846151842734, -236.9778203247716419 ) ) ;
#250602=DIRECTION ( 'NONE',  ( 0.000000000000000000, 0.2128009952263568427, -0.9770955615653322823 ) ) ;
#250606=CARTESIAN_POINT ( 'NONE',  ( -21.14999999999999858, 6.093673009692400555, -199.5727803633481301 ) ) ;
#250614=AXIS2_PLACEMENT_3D ( 'NONE', #126721, #62891, #65454 ) ;
#250619=ORIENTED_EDGE ( 'NONE', *, *, #26630, .T. ) ;
#250630=AXIS2_PLACEMENT_3D ( 'NONE', #16356, #33373, #13768 ) ;
#250637=DIRECTION ( 'NONE',  ( 0.000000000000000000, 0.9770955615652945347, 0.2128009952265300653 ) ) ;
#250653=AXIS2_PLACEMENT_3D ( 'NONE', #12583, #56783, #73848 ) ;
#250692=ORIENTED_EDGE ( 'NONE', *, *, #126828, .T. ) ;
#250703=AXIS2_PLACEMENT_3D ( 'NONE', #137852, #177031, #212294 ) ;
#250714=ORIENTED_EDGE ( 'NONE', *, *, #219462, .T. ) ;
#250725=DIRECTION ( 'NONE',  ( 0.000000000000000000, -0.2128009952263403282, 0.9770955615653358350 ) ) ;
#250728=EDGE_LOOP ( 'NONE', ( #178138, #233332, #44878, #172058 ) ) ;
#250732=CARTESIAN_POINT ( 'NONE',  ( 21.14999999999999858, -0.09770955614504285569, -201.0212800995241764 ) ) ;
#250752=ORIENTED_EDGE ( 'NONE', *, *, #87740, .T. ) ;
#250758=EDGE_CURVE ( 'NONE', #19000, #154288, #172307, .T. ) ;
#250768=LINE ( 'NONE', #190838, #209628 ) ;
#250773=CARTESIAN_POINT ( 'NONE',  ( 21.05000000000000071, -3.770473190032740174, -225.9805569534692324 ) ) ;
#250795=ORIENTED_EDGE ( 'NONE', *, *, #16392, .T. ) ;
#250802=FACE_OUTER_BOUND ( 'NONE', #116844, .T. ) ;
#250805=CARTESIAN_POINT ( 'NONE',  ( -21.05000000000000071, 17.11694853917243364, -224.3781540347815451 ) ) ;
#250816=CARTESIAN_POINT ( 'NONE',  ( -20.94999999999999929, 18.34711819382569686, -236.8747682978092541 ) ) ;
#250817=ORIENTED_EDGE ( 'NONE', *, *, #184204, .F. ) ;
#250840=CIRCLE ( 'NONE', #234087, 0.2000000000000100864 ) ;
#250841=CIRCLE ( 'NONE', #121698, 0.09999999999999939493 ) ;
#250869=VERTEX_POINT ( 'NONE', #186022 ) ;
#250876=ORIENTED_EDGE ( 'NONE', *, *, #122668, .F. ) ;
#250898=DIRECTION ( 'NONE',  ( -1.000000000000000000, 0.000000000000000000, 0.000000000000000000 ) ) ;
#250911=ORIENTED_EDGE ( 'NONE', *, *, #221043, .F. ) ;
#250939=CIRCLE ( 'NONE', #55119, 4.049999999999997158 ) ;
#250987=EDGE_CURVE ( 'NONE', #147215, #135942, #55497, .T. ) ;
#251031=AXIS2_PLACEMENT_3D ( 'NONE', #252285, #73697, #47662 ) ;
#251040=CARTESIAN_POINT ( 'NONE',  ( 21.05000000000000071, -6.688413578037176066, -212.5825622730469036 ) ) ;
#251105=CARTESIAN_POINT ( 'NONE',  ( -20.85000000000000142, 7.128833340094563376, -233.7327013124401276 ) ) ;
#251119=DIRECTION ( 'NONE',  ( 0.000000000000000000, 0.2128009952263603677, -0.9770955615653313941 ) ) ;
#251156=EDGE_LOOP ( 'NONE', ( #256927, #103115, #199676, #159128 ) ) ;
#251166=ADVANCED_FACE ( 'NONE', ( #202401 ), #164068, .F. ) ;
#251175=DIRECTION ( 'NONE',  ( 1.000000000000000000, 2.885090398161910739E-16, 6.283419270304611573E-17 ) ) ;
#251195=AXIS2_PLACEMENT_3D ( 'NONE', #130994, #210535, #62362 ) ;
#251202=ORIENTED_EDGE ( 'NONE', *, *, #63189, .T. ) ;
#251203=DIRECTION ( 'NONE',  ( 1.000000000000000000, 0.000000000000000000, 0.000000000000000000 ) ) ;
#251208=DIRECTION ( 'NONE',  ( -1.000000000000000000, -0.000000000000000000, -0.000000000000000000 ) ) ;
#251222=CIRCLE ( 'NONE', #172199, 0.09999999999999939493 ) ;
#251250=CARTESIAN_POINT ( 'NONE',  ( 20.94999999999999929, 9.459578591139306880, -220.9384041938172345 ) ) ;
#251271=DIRECTION ( 'NONE',  ( -0.000000000000000000, -0.9770955615653316162, -0.2128009952263604232 ) ) ;
#251281=DIRECTION ( 'NONE',  ( 1.000000000000000000, 0.000000000000000000, 0.000000000000000000 ) ) ;
#251299=ORIENTED_EDGE ( 'NONE', *, *, #106560, .T. ) ;
#251307=ADVANCED_FACE ( 'NONE', ( #208821 ), #51588, .T. ) ;
#251364=EDGE_CURVE ( 'NONE', #19033, #127248, #249239, .T. ) ;
#251387=ORIENTED_EDGE ( 'NONE', *, *, #148297, .T. ) ;
#251388=EDGE_LOOP ( 'NONE', ( #39826, #243336, #221404, #197764 ) ) ;
#251406=VECTOR ( 'NONE', #109132, 1000.000000000000227 ) ;
#251426=DIRECTION ( 'NONE',  ( 0.000000000000000000, 0.2128009952263605065, -0.9770955615653315052 ) ) ;
#251449=EDGE_LOOP ( 'NONE', ( #120880, #235002, #22921, #119805 ) ) ;
#251458=CARTESIAN_POINT ( 'NONE',  ( 18.59999996954842771, -0.7115290284072351978, -242.4846381375031115 ) ) ;
#251463=EDGE_LOOP ( 'NONE', ( #144535, #109439, #170834, #91198 ) ) ;
#251477=CARTESIAN_POINT ( 'NONE',  ( 18.57071067811864040, 14.48943966439392206, -219.6948273410279455 ) ) ;
#251507=EDGE_CURVE ( 'NONE', #167762, #101102, #74481, .T. ) ;
#251521=ORIENTED_EDGE ( 'NONE', *, *, #18814, .T. ) ;
#251556=CARTESIAN_POINT ( 'NONE',  ( 21.00000000000000000, 14.02742277431099538, -219.5907614236512870 ) ) ;
#251601=DIRECTION ( 'NONE',  ( -3.265361837132813586E-16, 0.9770955615653357240, 0.2128009952263412996 ) ) ;
#251637=ORIENTED_EDGE ( 'NONE', *, *, #101358, .T. ) ;
#251645=CARTESIAN_POINT ( 'NONE',  ( -20.94999999999999929, 18.34711819382569686, -236.8747682978092541 ) ) ;
#251662=SPHERICAL_SURFACE ( 'NONE', #193780, 0.1000000000000000056 ) ;
#251676=AXIS2_PLACEMENT_3D ( 'NONE', #88593, #69072, #129034 ) ;
#251690=AXIS2_PLACEMENT_3D ( 'NONE', #110807, #230783, #32605 ) ;
#251715=CARTESIAN_POINT ( 'NONE',  ( -18.39999999999999858, -7.883686024897174072, -209.9138933503092233 ) ) ;
#251716=EDGE_CURVE ( 'NONE', #59486, #166165, #47702, .T. ) ;
#251732=FACE_OUTER_BOUND ( 'NONE', #19734, .T. ) ;
#251740=CARTESIAN_POINT ( 'NONE',  ( -21.11927991906891222, -1.363370130417240977, -194.6972729791065149 ) ) ;
#251794=CARTESIAN_POINT ( 'NONE',  ( -23.15000000000000213, 6.375212254182287097, -220.8739277186596155 ) ) ;
#251795=CIRCLE ( 'NONE', #114429, 2.000000000000003109 ) ;
#251823=ORIENTED_EDGE ( 'NONE', *, *, #193351, .T. ) ;
#251828=CARTESIAN_POINT ( 'NONE',  ( 18.49999999999998934, 10.92199707682457088, -220.3694341645321515 ) ) ;
#251829=DIRECTION ( 'NONE',  ( 0.000000000000000000, 0.9770955615653551529, 0.2128009952262517601 ) ) ;
#251863=CIRCLE ( 'NONE', #247596, 0.1000000000000055844 ) ;
#251866=CARTESIAN_POINT ( 'NONE',  ( -22.39999999999999503, 7.591056067193246548, -199.2444047917219052 ) ) ;
#251882=ADVANCED_FACE ( 'NONE', ( #14184 ), #174571, .T. ) ;
#251884=DIRECTION ( 'NONE',  ( 2.694716079187273439E-16, -0.9770955615653316162, -0.2128009952263598958 ) ) ;
#251888=EDGE_CURVE ( 'NONE', #242544, #179165, #197732, .T. ) ;
#251900=DIRECTION ( 'NONE',  ( 1.000000000000000000, 0.000000000000000000, 0.000000000000000000 ) ) ;
#251933=CARTESIAN_POINT ( 'NONE',  ( 18.49999999999999645, 7.661991824395936845, -241.5144583139544636 ) ) ;
#251936=AXIS2_PLACEMENT_3D ( 'NONE', #138591, #120388, #255954 ) ;
#251955=EDGE_LOOP ( 'NONE', ( #160064, #67502, #47929 ) ) ;
#251977=AXIS2_PLACEMENT_3D ( 'NONE', #194554, #205392, #15917 ) ;
#251988=( NAMED_UNIT ( * ) PLANE_ANGLE_UNIT ( ) SI_UNIT ( $, .RADIAN. ) );
#252035=CIRCLE ( 'NONE', #198051, 0.1000000000000055844 ) ;
#252072=FACE_OUTER_BOUND ( 'NONE', #116670, .T. ) ;
#252074=CARTESIAN_POINT ( 'NONE',  ( 22.42357213249528769, 7.476102374361162539, -199.2703749191446434 ) ) ;
#252103=EDGE_LOOP ( 'NONE', ( #147633, #75606, #222291, #103120 ) ) ;
#252105=EDGE_CURVE ( 'NONE', #101102, #198700, #27082, .T. ) ;
#252106=CARTESIAN_POINT ( 'NONE',  ( -22.50000000000088818, -2.434917201483803861, -189.6066865224547087 ) ) ;
#252110=EDGE_CURVE ( 'NONE', #135942, #248011, #30873, .T. ) ;
#252116=VERTEX_POINT ( 'NONE', #71274 ) ;
#252118=EDGE_CURVE ( 'NONE', #126149, #70740, #97753, .T. ) ;
#252125=CARTESIAN_POINT ( 'NONE',  ( -20.85000000000000142, 14.83511725869332132, -235.8887435844146978 ) ) ;
#252157=ORIENTED_EDGE ( 'NONE', *, *, #158296, .T. ) ;
#252234=AXIS2_PLACEMENT_3D ( 'NONE', #219064, #41751, #102965 ) ;
#252276=VERTEX_POINT ( 'NONE', #198895 ) ;
#252285=CARTESIAN_POINT ( 'NONE',  ( -22.50000000000000000, 1.148907358139439339E-11, -201.0000000000015064 ) ) ;
#252323=AXIS2_PLACEMENT_3D ( 'NONE', #229198, #113094, #192636 ) ;
#252362=ORIENTED_EDGE ( 'NONE', *, *, #8157, .F. ) ;
#252363=CYLINDRICAL_SURFACE ( 'NONE', #11214, 0.1000000000000055844 ) ;
#252366=DIRECTION ( 'NONE',  ( -0.7071067811865302533, 0.6909108974501196876, 0.1504730267679053324 ) ) ;
#252383=ADVANCED_FACE ( 'NONE', ( #158515 ), #39929, .F. ) ;
#252418=EDGE_LOOP ( 'NONE', ( #110675, #23914, #147028, #257150 ) ) ;
#252442=CIRCLE ( 'NONE', #240004, 0.2000000000000111688 ) ;
#252445=CARTESIAN_POINT ( 'NONE',  ( -18.59999999999999787, 7.939498413483247141, -209.7295111514051200 ) ) ;
#252451=FACE_OUTER_BOUND ( 'NONE', #114943, .T. ) ;
#252468=TOROIDAL_SURFACE ( 'NONE', #256718, 0.6000000000000009770, 0.1000000000000000056 ) ;
#252481=VECTOR ( 'NONE', #118955, 1000.000000000000227 ) ;
#252509=AXIS2_PLACEMENT_3D ( 'NONE', #224206, #166851, #209797 ) ;
#252515=EDGE_CURVE ( 'NONE', #37909, #26422, #148216, .T. ) ;
#252561=ORIENTED_EDGE ( 'NONE', *, *, #54292, .T. ) ;
#252614=ORIENTED_EDGE ( 'NONE', *, *, #101785, .T. ) ;
#252626=ORIENTED_EDGE ( 'NONE', *, *, #138889, .T. ) ;
#252636=AXIS2_PLACEMENT_3D ( 'NONE', #145421, #223666, #244522 ) ;
#252648=AXIS2_PLACEMENT_3D ( 'NONE', #22900, #102372, #121978 ) ;
#252651=DIRECTION ( 'NONE',  ( -1.000000000000000000, 0.000000000000000000, 0.000000000000000000 ) ) ;
#252678=CARTESIAN_POINT ( 'NONE',  ( -21.00219873199057830, 12.81059202956635623, -205.2846788580854422 ) ) ;
#252679=ORIENTED_EDGE ( 'NONE', *, *, #38007, .T. ) ;
#252751=CARTESIAN_POINT ( 'NONE',  ( 20.94999999999999929, 10.45765418377745526, -207.3040725013013912 ) ) ;
#252753=ORIENTED_EDGE ( 'NONE', *, *, #245197, .F. ) ;
#252755=CARTESIAN_POINT ( 'NONE',  ( 21.51976009735019346, 6.752178271738373816, -199.5294475661460467 ) ) ;
#252785=DIRECTION ( 'NONE',  ( -1.000000000000000000, 0.000000000000000000, 0.000000000000000000 ) ) ;
#252786=ORIENTED_EDGE ( 'NONE', *, *, #128428, .T. ) ;
#252789=CYLINDRICAL_SURFACE ( 'NONE', #136427, 0.09999999999999939493 ) ;
#252806=B_SPLINE_CURVE_WITH_KNOTS ( 'NONE', 3,
 ( #240201, #159381, #155550, #214213, #35601, #115105, #257129 ),
 .UNSPECIFIED., .F., .F.,
 ( 4, 3, 4 ),
 ( 0.000000000000000000, 3.357501770815708719E-05, 5.199112466349179362E-05 ),
 .UNSPECIFIED. ) ;
#252823=AXIS2_PLACEMENT_3D ( 'NONE', #4912, #208295, #187449 ) ;
#252825=EDGE_LOOP ( 'NONE', ( #43488, #190673, #153403, #8548 ) ) ;
#252828=ADVANCED_FACE ( 'NONE', ( #75666 ), #191500, .T. ) ;
#252844=ORIENTED_EDGE ( 'NONE', *, *, #189030, .T. ) ;
#252902=LINE ( 'NONE', #149984, #248061 ) ;
#252905=CARTESIAN_POINT ( 'NONE',  ( -21.07954763557489741, -1.282512354049770265, -194.8016594047362844 ) ) ;
#252924=ORIENTED_EDGE ( 'NONE', *, *, #115142, .F. ) ;
#252935=DIRECTION ( 'NONE',  ( 0.000000000000000000, 0.9964539953858966292, 0.08413937888696132461 ) ) ;
#252987=CARTESIAN_POINT ( 'NONE',  ( 22.40000000000020819, -2.598867842140045958, -189.5410128746470946 ) ) ;
#252999=EDGE_CURVE ( 'NONE', #44597, #83361, #115086, .T. ) ;
#253005=CARTESIAN_POINT ( 'NONE',  ( 21.14999999999999503, -1.391858308744749806, -194.6091531227728240 ) ) ;
#253020=ORIENTED_EDGE ( 'NONE', *, *, #225082, .F. ) ;
#253029=ORIENTED_EDGE ( 'NONE', *, *, #137755, .F. ) ;
#253031=DIRECTION ( 'NONE',  ( 0.000000000000000000, 0.2128009952263485993, -0.9770955615653341697 ) ) ;
#253037=CARTESIAN_POINT ( 'NONE',  ( -20.54999999999999716, 7.554435330547284444, -235.6868924355707691 ) ) ;
#253058=DIRECTION ( 'NONE',  ( -2.561896900575096011E-15, -0.7489048840758921743, 0.6626775042260560911 ) ) ;
#253061=EDGE_LOOP ( 'NONE', ( #204277, #83753, #233483, #195413 ) ) ;
#253083=FACE_OUTER_BOUND ( 'NONE', #73525, .T. ) ;
#253120=AXIS2_PLACEMENT_3D ( 'NONE', #106196, #207910, #127067 ) ;
#253168=LINE ( 'NONE', #74585, #235910 ) ;
#253196=EDGE_CURVE ( 'NONE', #10002, #61748, #223226, .T. ) ;
#253197=FACE_OUTER_BOUND ( 'NONE', #15194, .T. ) ;
#253226=CARTESIAN_POINT ( 'NONE',  ( -18.50000000000000000, 13.44116543737180081, -219.7184420207870801 ) ) ;
#253256=ORIENTED_EDGE ( 'NONE', *, *, #240521, .T. ) ;
#253278=CARTESIAN_POINT ( 'NONE',  ( 21.05000000000000071, 6.285328434420313748, -199.7189328463573190 ) ) ;
#253363=AXIS2_PLACEMENT_3D ( 'NONE', #117651, #180207, #139757 ) ;
#253375=DIRECTION ( 'NONE',  ( 1.000000000000000000, -1.387778780781444413E-14, 0.000000000000000000 ) ) ;
#253390=CARTESIAN_POINT ( 'NONE',  ( -20.89192007715127986, 18.40923646582965034, -236.9894833875398206 ) ) ;
#253408=DIRECTION ( 'NONE',  ( -0.000000000000000000, -0.2128009952263604232, 0.9770955615653316162 ) ) ;
#253416=LINE ( 'NONE', #156922, #123732 ) ;
#253449=VERTEX_POINT ( 'NONE', #209228 ) ;
#253463=ORIENTED_EDGE ( 'NONE', *, *, #134438, .F. ) ;
#253468=CIRCLE ( 'NONE', #61954, 11.65000000000001457 ) ;
#253470=ADVANCED_FACE ( 'NONE', ( #188384 ), #202012, .T. ) ;
#253516=DIRECTION ( 'NONE',  ( -0.000000000000000000, 0.9770955615653313941, 0.2128009952263603954 ) ) ;
#253526=VECTOR ( 'NONE', #80109, 1000.000000000000114 ) ;
#253544=CARTESIAN_POINT ( 'NONE',  ( 20.04142135623730070, 15.92646454033040015, -219.3818586450342423 ) ) ;
#253554=DIRECTION ( 'NONE',  ( -7.304098846218419643E-16, 0.9770955615653543758, 0.2128009952262553683 ) ) ;
#253580=LINE ( 'NONE', #153249, #84035 ) ;
#253593=EDGE_LOOP ( 'NONE', ( #250493, #148487, #6140, #140671 ) ) ;
#253613=CARTESIAN_POINT ( 'NONE',  ( -23.25000000000000000, 7.128833340094563376, -233.7327013124401276 ) ) ;
#253642=EDGE_CURVE ( 'NONE', #137759, #57651, #73055, .T. ) ;
#253651=VERTEX_POINT ( 'NONE', #38312 ) ;
#253662=ORIENTED_EDGE ( 'NONE', *, *, #56555, .T. ) ;
#253664=EDGE_CURVE ( 'NONE', #175321, #156593, #114708, .T. ) ;
#253685=DIRECTION ( 'NONE',  ( 0.000000000000000000, -0.9964539953858966292, -0.08413937888696132461 ) ) ;
#253724=EDGE_LOOP ( 'NONE', ( #44404, #190010, #125159, #241887, #83377, #141559 ) ) ;
#253735=LINE ( 'NONE', #137633, #52496 ) ;
#253737=ORIENTED_EDGE ( 'NONE', *, *, #218969, .F. ) ;
#253758=CARTESIAN_POINT ( 'NONE',  ( 23.14999999999999503, 10.90071697730193456, -220.2717246083756208 ) ) ;
#253768=CARTESIAN_POINT ( 'NONE',  ( 21.00023020733438273, 6.244489974106956609, -199.6400166642470140 ) ) ;
#253789=DIRECTION ( 'NONE',  ( -1.000000000000000000, 0.000000000000000000, 0.000000000000000000 ) ) ;
#253826=CARTESIAN_POINT ( 'NONE',  ( -22.50000000000000000, -2.479040261793999722, -189.6172560698084624 ) ) ;
#253888=ADVANCED_FACE ( 'NONE', ( #211501 ), #228506, .T. ) ;
#253917=VECTOR ( 'NONE', #76074, 1000.000000000000227 ) ;
#253923=VERTEX_POINT ( 'NONE', #95400 ) ;
#253949=DIRECTION ( 'NONE',  ( 0.000000000000000000, -0.2128009952263403282, 0.9770955615653358350 ) ) ;
#253964=CARTESIAN_POINT ( 'NONE',  ( -20.64999999999999858, 8.751106741858205140, -220.7398867978735950 ) ) ;
#253970=CYLINDRICAL_SURFACE ( 'NONE', #170558, 0.1000000000000008937 ) ;
#254001=EDGE_CURVE ( 'NONE', #139309, #256176, #10663, .T. ) ;
#254024=VERTEX_POINT ( 'NONE', #105641 ) ;
#254055=AXIS2_PLACEMENT_3D ( 'NONE', #115801, #235733, #57078 ) ;
#254056=FACE_OUTER_BOUND ( 'NONE', #4970, .T. ) ;
#254073=DIRECTION ( 'NONE',  ( 0.000000000000000000, -0.2128009952263604232, 0.9770955615653315052 ) ) ;
#254112=CIRCLE ( 'NONE', #83409, 0.09999999999999722999 ) ;
#254124=VERTEX_POINT ( 'NONE', #242600 ) ;
#254133=DIRECTION ( 'NONE',  ( -1.000000000000000000, -2.885090398161910739E-16, -6.283419270304611573E-17 ) ) ;
#254136=AXIS2_PLACEMENT_3D ( 'NONE', #72916, #131572, #113289 ) ;
#254145=DIRECTION ( 'NONE',  ( 1.000000000000000000, 0.000000000000000000, 0.000000000000000000 ) ) ;
#254150=DIRECTION ( 'NONE',  ( 1.000000000000000000, 0.000000000000000000, 0.000000000000000000 ) ) ;
#254151=DIRECTION ( 'NONE',  ( -1.000000000000000000, 0.000000000000000000, 0.000000000000000000 ) ) ;
#254165=AXIS2_PLACEMENT_3D ( 'NONE', #59232, #198784, #138776 ) ;
#254199=ORIENTED_EDGE ( 'NONE', *, *, #40051, .T. ) ;
#254203=DIRECTION ( 'NONE',  ( 0.000000000000000000, 0.9770955615653316162, 0.2128009952263604232 ) ) ;
#254213=FACE_OUTER_BOUND ( 'NONE', #40722, .T. ) ;
#254280=CARTESIAN_POINT ( 'NONE',  ( -18.59999999999999787, 14.76289716703255728, -235.7888246855571026 ) ) ;
#254307=EDGE_CURVE ( 'NONE', #248782, #126073, #110784, .T. ) ;
#254309=ORIENTED_EDGE ( 'NONE', *, *, #186001, .F. ) ;
#254347=DIRECTION ( 'NONE',  ( -0.000000000000000000, 0.2128009952263603677, -0.9770955615653313941 ) ) ;
#254399=EDGE_LOOP ( 'NONE', ( #184013, #98670, #121128, #121145 ) ) ;
#254400=DIRECTION ( 'NONE',  ( 0.000000000000000000, 0.2128009952263604232, -0.9770955615653316162 ) ) ;
#254422=DIRECTION ( 'NONE',  ( 0.000000000000000000, 0.2128009952263601179, -0.9770955615653315052 ) ) ;
#254448=ORIENTED_EDGE ( 'NONE', *, *, #179362, .F. ) ;
#254449=ORIENTED_EDGE ( 'NONE', *, *, #227428, .T. ) ;
#254455=VERTEX_POINT ( 'NONE', #148014 ) ;
#254466=DIRECTION ( 'NONE',  ( 0.000000000000000000, 0.7397890806274222131, 0.6728388485993012091 ) ) ;
#254480=ORIENTED_EDGE ( 'NONE', *, *, #93083, .F. ) ;
#254517=AXIS2_PLACEMENT_3D ( 'NONE', #63434, #142955, #84233 ) ;
#254521=ORIENTED_EDGE ( 'NONE', *, *, #228883, .F. ) ;
#254530=SURFACE_SIDE_STYLE ('',( #75930 ) ) ;
#254540=CARTESIAN_POINT ( 'NONE',  ( 21.04999999999953886, 6.144958646240215927, -199.6091629096070790 ) ) ;
#254566=CARTESIAN_POINT ( 'NONE',  ( 20.95512820512820440, 10.49413282287806481, -207.4737445703522383 ) ) ;
#254605=EDGE_CURVE ( 'NONE', #202021, #13934, #115247, .T. ) ;
#254607=ADVANCED_FACE ( 'NONE', ( #233963 ), #54041, .F. ) ;
#254634=DIRECTION ( 'NONE',  ( -1.000000000000000000, 0.000000000000000000, 0.000000000000000000 ) ) ;
#254643=LINE ( 'NONE', #61612, #217280 ) ;
#254669=CARTESIAN_POINT ( 'NONE',  ( 21.05000000000000071, -4.756823075239758225, -233.1486023682345490 ) ) ;
#254672=ADVANCED_FACE ( 'NONE', ( #159575 ), #27801, .T. ) ;
#254688=ADVANCED_FACE ( 'NONE', ( #38349 ), #237822, .T. ) ;
#254725=ORIENTED_EDGE ( 'NONE', *, *, #26630, .F. ) ;
#254728=DIRECTION ( 'NONE',  ( 0.000000000000000000, 0.2128009952263485993, -0.9770955615653341697 ) ) ;
#254749=DIRECTION ( 'NONE',  ( 1.000000000000000000, 0.000000000000000000, 0.000000000000000000 ) ) ;
#254782=EDGE_LOOP ( 'NONE', ( #118234, #87212, #11532, #233870 ) ) ;
#254795=DIRECTION ( 'NONE',  ( 1.000000000000000000, 0.000000000000000000, 0.000000000000000000 ) ) ;
#254798=EDGE_LOOP ( 'NONE', ( #79763, #256311, #151822, #91643, #105760 ) ) ;
#254871=CARTESIAN_POINT ( 'NONE',  ( 22.47007471830800895, -1.642974910573245850, -193.4561278898739829 ) ) ;
#254874=CARTESIAN_POINT ( 'NONE',  ( 18.49505816908824940, -0.6505778444486189915, -242.3635087541469773 ) ) ;
#254878=CARTESIAN_POINT ( 'NONE',  ( 20.30466543256790501, 10.84751624358901623, -207.0846662628387946 ) ) ;
#254887=FACE_OUTER_BOUND ( 'NONE', #70552, .T. ) ;
#254896=LINE ( 'NONE', #78868, #155474 ) ;
#255023=ORIENTED_EDGE ( 'NONE', *, *, #192145, .T. ) ;
#255025=ORIENTED_EDGE ( 'NONE', *, *, #235471, .T. ) ;
#255033=CARTESIAN_POINT ( 'NONE',  ( -20.00857864376270001, 13.63658454968486389, -219.6758818217417968 ) ) ;
#255071=CIRCLE ( 'NONE', #30298, 0.1000000000000035305 ) ;
#255095=LINE ( 'NONE', #156089, #53982 ) ;
#255104=AXIS2_PLACEMENT_3D ( 'NONE', #152994, #173856, #158139 ) ;
#255116=AXIS2_PLACEMENT_3D ( 'NONE', #596, #21491, #180553 ) ;
#255134=VERTEX_POINT ( 'NONE', #126564 ) ;
#255142=CARTESIAN_POINT ( 'NONE',  ( 20.94999999999999929, 18.34743685832669158, -236.8753540304231535 ) ) ;
#255153=ORIENTED_EDGE ( 'NONE', *, *, #226283, .F. ) ;
#255162=EDGE_CURVE ( 'NONE', #55595, #201052, #103590, .T. ) ;
#255184=CARTESIAN_POINT ( 'NONE',  ( -18.59999999999999787, 12.87592094156238609, -205.3750039893633073 ) ) ;
#255204=CARTESIAN_POINT ( 'NONE',  ( 20.94999999999999574, 2.859758780633683273, -208.6670499591424459 ) ) ;
#255231=EDGE_CURVE ( 'NONE', #116714, #253651, #195228, .T. ) ;
#255247=DIRECTION ( 'NONE',  ( 1.000000000000000000, 0.000000000000000000, 0.000000000000000000 ) ) ;
#255273=TOROIDAL_SURFACE ( 'NONE', #250653, 0.2000000000000000111, 0.1000000000000000056 ) ;
#255274=DIRECTION ( 'NONE',  ( 0.000000000000000000, -0.6728388485993083146, 0.7397890806274158848 ) ) ;
#255311=CARTESIAN_POINT ( 'NONE',  ( -22.60000000000080789, -2.453694707889708226, -189.5089297331973626 ) ) ;
#255312=ORIENTED_EDGE ( 'NONE', *, *, #229902, .F. ) ;
#255334=ORIENTED_EDGE ( 'NONE', *, *, #186698, .F. ) ;
#255348=CARTESIAN_POINT ( 'NONE',  ( -21.55000000000000426, 12.03275902784684703, -220.0251779199349187 ) ) ;
#255357=CARTESIAN_POINT ( 'NONE',  ( 18.59999999999999432, 4.158309866074138661, -211.9342015984041439 ) ) ;
#255368=ORIENTED_EDGE ( 'NONE', *, *, #192204, .T. ) ;
#255394=DIRECTION ( 'NONE',  ( 0.000000000000000000, 0.2128009952263601179, -0.9770955615653315052 ) ) ;
#255399=VECTOR ( 'NONE', #186642, 1000.000000000000227 ) ;
#255413=ORIENTED_EDGE ( 'NONE', *, *, #240014, .T. ) ;
#255476=FACE_OUTER_BOUND ( 'NONE', #48409, .T. ) ;
#255509=CARTESIAN_POINT ( 'NONE',  ( 22.49999999999999645, -2.401771312552908100, -189.4980873520050011 ) ) ;
#255519=EDGE_CURVE ( 'NONE', #143815, #11889, #250939, .T. ) ;
#255558=ADVANCED_FACE ( 'NONE', ( #143236 ), #164105, .T. ) ;
#255567=CARTESIAN_POINT ( 'NONE',  ( 23.24999999999999289, 8.980461154494404852, -187.0187154576991304 ) ) ;
#255589=VECTOR ( 'NONE', #151433, 1000.000000000000000 ) ;
#255612=CIRCLE ( 'NONE', #238927, 4.100000000000011191 ) ;
#255642=CARTESIAN_POINT ( 'NONE',  ( 20.95545211741311320, 11.95827706127094103, -206.1595911373138676 ) ) ;
#255670=CARTESIAN_POINT ( 'NONE',  ( -23.25000000000000000, 7.128833340094563376, -233.7327013124401276 ) ) ;
#255684=( BOUNDED_CURVE ( )  B_SPLINE_CURVE ( 3, ( #244238, #46046, #121763, #201268 ),
 .UNSPECIFIED., .F., .F. ) 
 B_SPLINE_CURVE_WITH_KNOTS ( ( 4, 4 ),
 ( 3.141592653589816653, 4.712388980384673687 ),
 .UNSPECIFIED. ) 
 CURVE ( )  GEOMETRIC_REPRESENTATION_ITEM ( )  RATIONAL_B_SPLINE_CURVE ( ( 1.000000000000000000, 0.8047378541243743744, 0.8047378541243743744, 1.000000000000000000 ) ) 
 REPRESENTATION_ITEM ( '' )  );
#255689=ORIENTED_EDGE ( 'NONE', *, *, #166432, .T. ) ;
#255715=CARTESIAN_POINT ( 'NONE',  ( -21.05000000000000071, -4.914013037343267776, -233.1828366659746905 ) ) ;
#255729=ORIENTED_EDGE ( 'NONE', *, *, #151876, .T. ) ;
#255837=DIRECTION ( 'NONE',  ( 0.000000000000000000, -0.2128009952263603677, 0.9770955615653313941 ) ) ;
#255853=DIRECTION ( 'NONE',  ( 0.000000000000000000, 0.9770955615653315052, 0.2128009952263603954 ) ) ;
#255928=DIRECTION ( 'NONE',  ( -1.000000000000000000, -7.136802563874199107E-16, -1.554319503706929991E-16 ) ) ;
#255947=ADVANCED_FACE ( 'NONE', ( #183360 ), #204181, .F. ) ;
#255954=DIRECTION ( 'NONE',  ( 0.000000000000000000, 0.2128009952263604510, -0.9770955615653315052 ) ) ;
#255977=AXIS2_PLACEMENT_3D ( 'NONE', #155661, #93072, #10980 ) ;
#256001=ORIENTED_EDGE ( 'NONE', *, *, #23461, .T. ) ;
#256051=DIRECTION ( 'NONE',  ( -0.7071067811865389130, 0.1504730267678074940, -0.6909108974501321221 ) ) ;
#256068=DIRECTION ( 'NONE',  ( 0.000000000000000000, 0.2128009952263604232, -0.9770955615653316162 ) ) ;
#256115=VERTEX_POINT ( 'NONE', #245898 ) ;
#256135=ADVANCED_FACE ( 'NONE', ( #77196 ), #219275, .T. ) ;
#256136=ORIENTED_EDGE ( 'NONE', *, *, #201811, .T. ) ;
#256142=CIRCLE ( 'NONE', #185479, 0.5000000000000014433 ) ;
#256147=VERTEX_POINT ( 'NONE', #17250 ) ;
#256160=DIRECTION ( 'NONE',  ( 0.000000000000000000, -0.9976611540403004241, -0.06835365183350541884 ) ) ;
#256168=ORIENTED_EDGE ( 'NONE', *, *, #119328, .F. ) ;
#256176=VERTEX_POINT ( 'NONE', #1506 ) ;
#256201=CARTESIAN_POINT ( 'NONE',  ( -20.94999999999999929, 10.71906255309368383, -222.4921384173655383 ) ) ;
#256213=ORIENTED_EDGE ( 'NONE', *, *, #102321, .F. ) ;
#256230=ORIENTED_EDGE ( 'NONE', *, *, #75532, .F. ) ;
#256235=VERTEX_POINT ( 'NONE', #18520 ) ;
#256301=EDGE_LOOP ( 'NONE', ( #231625, #220740, #143399, #40900 ) ) ;
#256311=ORIENTED_EDGE ( 'NONE', *, *, #69256, .T. ) ;
#256328=DIRECTION ( 'NONE',  ( 1.000000000000000000, 2.885090398161910739E-16, 6.283419270304611573E-17 ) ) ;
#256335=CIRCLE ( 'NONE', #143971, 2.000000000000003109 ) ;
#256390=ORIENTED_EDGE ( 'NONE', *, *, #163858, .F. ) ;
#256402=EDGE_LOOP ( 'NONE', ( #185469, #198643, #121131 ) ) ;
#256419=DIRECTION ( 'NONE',  ( 0.000000000000000000, -0.2128009952263650861, 0.9770955615653305060 ) ) ;
#256420=VERTEX_POINT ( 'NONE', #238392 ) ;
#256442=EDGE_CURVE ( 'NONE', #201117, #252116, #81846, .T. ) ;
#256444=ORIENTED_EDGE ( 'NONE', *, *, #257077, .T. ) ;
#256479=( BOUNDED_SURFACE ( )  B_SPLINE_SURFACE ( 3, 2, ( 
 ( #103007, #142145, #196976 ),
 ( #219103, #43060, #163019 ),
 ( #157917, #202130, #239980 ),
 ( #161743, #237405, #200848 ),
 ( #238684, #178754, #62624 ),
 ( #23527, #140875, #118756 ) ),
 .UNSPECIFIED., .F., .F., .T. ) 
 B_SPLINE_SURFACE_WITH_KNOTS ( ( 4, 2, 4 ),
 ( 3, 3 ),
 ( 4.712388980384689674, 5.497787143782137953, 6.283185307179586232 ),
 ( 0.000000000000000000, 1.000000000000000000 ),
 .UNSPECIFIED. ) 
 GEOMETRIC_REPRESENTATION_ITEM ( )  RATIONAL_B_SPLINE_SURFACE ( (
 ( 1.000000000000000000, 0.7071067811865408004, 1.000000000000000000),
 ( 1.000000000000000000, 0.7727932973489139989, 1.000000000000000000),
 ( 1.000000000000000000, 0.8282379607651187969, 1.000000000000000000),
 ( 1.000000000000000000, 0.9038128468037410768, 1.000000000000000000),
 ( 1.000000000000000000, 0.9240297172245056645, 1.000000000000000000),
 ( 1.000000000000000000, 0.9238795325112937329, 1.000000000000000000) ) ) 
 REPRESENTATION_ITEM ( '' )  SURFACE ( )  );
#256490=EDGE_CURVE ( 'NONE', #173016, #185405, #13812, .T. ) ;
#256527=DIRECTION ( 'NONE',  ( 1.000000000000000000, 0.000000000000000000, 0.000000000000000000 ) ) ;
#256537=EDGE_LOOP ( 'NONE', ( #87837, #108757, #228505, #9027 ) ) ;
#256545=DIRECTION ( 'NONE',  ( 0.000000000000000000, 0.2128009952263601456, -0.9770955615653316162 ) ) ;
#256564=TOROIDAL_SURFACE ( 'NONE', #2712, 0.6000000000000004219, 0.1000000000000000056 ) ;
#256585=VERTEX_POINT ( 'NONE', #50750 ) ;
#256593=CARTESIAN_POINT ( 'NONE',  ( -22.50485643085240284, -2.577349838974356100, -189.5360933269992358 ) ) ;
#256611=CARTESIAN_POINT ( 'NONE',  ( 22.59999999999999076, 11.46682355977092804, -198.4356847424421062 ) ) ;
#256633=ORIENTED_EDGE ( 'NONE', *, *, #215235, .F. ) ;
#256717=CARTESIAN_POINT ( 'NONE',  ( -18.59999999999999787, 8.980461154494397746, -187.0187154576991304 ) ) ;
#256718=AXIS2_PLACEMENT_3D ( 'NONE', #12026, #131945, #250602 ) ;
#256735=CIRCLE ( 'NONE', #127797, 4.300000000000024691 ) ;
#256755=CARTESIAN_POINT ( 'NONE',  ( 18.49999999999999289, 10.80300742114540391, -220.2930047078982625 ) ) ;
#256757=DIRECTION ( 'NONE',  ( 0.000000000000000000, 0.2128009952263605342, -0.9770955615653316162 ) ) ;
#256799=FACE_OUTER_BOUND ( 'NONE', #57522, .T. ) ;
#256804=VECTOR ( 'NONE', #137550, 1000.000000000000114 ) ;
#256829=AXIS2_PLACEMENT_3D ( 'NONE', #90193, #188043, #129338 ) ;
#256869=DIRECTION ( 'NONE',  ( -1.000000000000000000, -0.000000000000000000, -0.000000000000000000 ) ) ;
#256874=AXIS2_PLACEMENT_3D ( 'NONE', #146389, #142545, #202533 ) ;
#256877=ORIENTED_EDGE ( 'NONE', *, *, #212490, .F. ) ;
#256903=FACE_OUTER_BOUND ( 'NONE', #117309, .T. ) ;
#256911=ORIENTED_EDGE ( 'NONE', *, *, #65647, .T. ) ;
#256922=B_SPLINE_CURVE_WITH_KNOTS ( 'NONE', 3,
 ( #34839, #50494, #190038, #10116, #114350, #191349 ),
 .UNSPECIFIED., .F., .F.,
 ( 4, 2, 4 ),
 ( 0.000000000000000000, 0.0002113392456165961845, 0.0004226784912331923690 ),
 .UNSPECIFIED. ) ;
#256926=DIRECTION ( 'NONE',  ( 1.000000000000000000, 0.000000000000000000, 0.000000000000000000 ) ) ;
#256927=ORIENTED_EDGE ( 'NONE', *, *, #83032, .T. ) ;
#256953=CIRCLE ( 'NONE', #136344, 12.77499999999998970 ) ;
#256964=CARTESIAN_POINT ( 'NONE',  ( -21.64999999999999858, 11.60596396992029433, -220.2204734678737168 ) ) ;
#257026=AXIS2_PLACEMENT_3D ( 'NONE', #121422, #200920, #241346 ) ;
#257040=DIRECTION ( 'NONE',  ( 0.000000000000000000, -0.9770955615653313941, -0.2128009952263603677 ) ) ;
#257077=EDGE_CURVE ( 'NONE', #83539, #120381, #93460, .T. ) ;
#257078=DIRECTION ( 'NONE',  ( 0.000000000000000000, 0.9550021345545507412, -0.2965989261549202838 ) ) ;
#257096=EDGE_CURVE ( 'NONE', #51404, #159889, #16496, .T. ) ;
#257097=VERTEX_POINT ( 'NONE', #156011 ) ;
#257129=CARTESIAN_POINT ( 'NONE',  ( 22.48660254037844197, 11.37252324248628987, -198.4720136275361426 ) ) ;
#257135=DIRECTION ( 'NONE',  ( -0.000000000000000000, 0.9770955615653313941, 0.2128009952263603954 ) ) ;
#257149=DIRECTION ( 'NONE',  ( 0.000000000000000000, -0.9770955615653551529, -0.2128009952262517601 ) ) ;
#257150=ORIENTED_EDGE ( 'NONE', *, *, #157575, .F. ) ;
#257192=EDGE_CURVE ( 'NONE', #256420, #13934, #151766, .T. ) ;
#257232=DIRECTION ( 'NONE',  ( 0.000000000000000000, 0.2128009952263485993, -0.9770955615653341697 ) ) ;
#257236=AXIS2_PLACEMENT_3D ( 'NONE', #92965, #74737, #249493 ) ;
#257248=CIRCLE ( 'NONE', #32494, 0.1000000000000055844 ) ;
#257255=EDGE_LOOP ( 'NONE', ( #100904, #80632, #56024 ) ) ;
#257263=CIRCLE ( 'NONE', #157398, 12.87499999999999467 ) ;
#257267=DIRECTION ( 'NONE',  ( -1.000000000000000000, 0.000000000000000000, 0.000000000000000000 ) ) ;
#257274=VECTOR ( 'NONE', #239920, 1000.000000000000227 ) ;
#257309=CIRCLE ( 'NONE', #3466, 0.1000000000000055844 ) ;
#257318=CIRCLE ( 'NONE', #203211, 0.09999999999999767408 ) ;
#257329=CIRCLE ( 'NONE', #86674, 0.09999999999999939493 ) ;
#257332=CARTESIAN_POINT ( 'NONE',  ( -20.94999999999999929, 4.252251777740764460, -211.8999245327126744 ) ) ;
#257364=EDGE_CURVE ( 'NONE', #195237, #203031, #151945, .T. ) ;
#257367=ORIENTED_EDGE ( 'NONE', *, *, #165695, .F. ) ;
#257411=CARTESIAN_POINT ( 'NONE',  ( -22.39999999999999858, 7.612336166715881092, -199.3421143478784359 ) ) ;
#257451=CARTESIAN_POINT ( 'NONE',  ( 20.12518398540832365, 11.44831387781778353, -206.6908002495722769 ) ) ;
#257455=VERTEX_POINT ( 'NONE', #159235 ) ;
#257469=ORIENTED_EDGE ( 'NONE', *, *, #165116, .T. ) ;
#257475=AXIS2_PLACEMENT_3D ( 'NONE', #23742, #241477, #4136 ) ;
#257476=AXIS2_PLACEMENT_3D ( 'NONE', #48887, #9759, #167582 ) ;
#257525=CARTESIAN_POINT ( 'NONE',  ( 21.05000000000001847, 10.52493806863740389, -207.3780514093641614 ) ) ;
#257537=CARTESIAN_POINT ( 'NONE',  ( -21.53752568622134689, -1.347531963291977330, -194.3475782847241931 ) ) ;
#257541=ORIENTED_EDGE ( 'NONE', *, *, #207044, .F. ) ;
#257557=AXIS2_PLACEMENT_3D ( 'NONE', #129221, #108377, #191789 ) ;
#257560=ORIENTED_EDGE ( 'NONE', *, *, #22427, .F. ) ;
#257564=CARTESIAN_POINT ( 'NONE',  ( -20.64999999999999858, 8.772386841380839684, -220.8375963540301257 ) ) ;
#257578=CARTESIAN_POINT ( 'NONE',  ( 20.85000000000000142, 14.70949956575304185, -235.9560995168023112 ) ) ;
#257593=ORIENTED_EDGE ( 'NONE', *, *, #200637, .T. ) ;
#257610=DIRECTION ( 'NONE',  ( 6.938893903906840889E-14, -0.2128009952263485993, 0.9770955615653341697 ) ) ;
#257648=VECTOR ( 'NONE', #169376, 1000.000000000000114 ) ;
#257666=EDGE_LOOP ( 'NONE', ( #192133, #171949, #122798, #51103 ) ) ;
#257676=ADVANCED_FACE ( 'NONE', ( #242587 ), #65242, .F. ) ;
#257678=EDGE_LOOP ( 'NONE', ( #216834, #42239, #230432, #55308, #34568 ) ) ;
#257684=DIRECTION ( 'NONE',  ( 0.000000000000000000, 0.2128009952263403282, -0.9770955615653358350 ) ) ;
#257728=CARTESIAN_POINT ( 'NONE',  ( -21.05000000000000071, 0.5663372425336981042, -209.0641885820623997 ) ) ;
#257732=DIRECTION ( 'NONE',  ( 0.000000000000000000, -0.3427706569149635563, 0.9394191166662964054 ) ) ;
#257736=CARTESIAN_POINT ( 'NONE',  ( 21.14999999999999858, 8.882751598337874199, -187.0399955572217721 ) ) ;
#257757=CARTESIAN_POINT ( 'NONE',  ( 21.14999999999999503, -2.576749817950531707, -189.6385361693310756 ) ) ;
#257771=CARTESIAN_POINT ( 'NONE',  ( -21.05000000000000071, 12.82677665681127976, -205.1493534351658354 ) ) ;
#257790=VECTOR ( 'NONE', #210584, 1000.000000000000227 ) ;
#257800=VECTOR ( 'NONE', #230563, 1000.000000000000000 ) ;
#257807=EDGE_CURVE ( 'NONE', #183877, #165216, #143724, .T. ) ;
#257871=EDGE_LOOP ( 'NONE', ( #139086, #71382, #128413, #233631 ) ) ;
#257899=AXIS2_PLACEMENT_3D ( 'NONE', #163434, #242954, #64333 ) ;
#257911=CIRCLE ( 'NONE', #37414, 0.1000000000000055844 ) ;
#257997=VECTOR ( 'NONE', #81913, 1000.000000000000227 ) ;
#258000=VERTEX_POINT ( 'NONE', #243574 ) ;
#258003=CARTESIAN_POINT ( 'NONE',  ( -18.50000000000000000, -7.631834139421013852, -210.1304494778855769 ) ) ;
#258029=ORIENTED_EDGE ( 'NONE', *, *, #74926, .F. ) ;
#258080=CARTESIAN_POINT ( 'NONE',  ( 22.40000000000010516, -2.479040261794990485, -189.6172560698083487 ) ) ;
ENDSEC;
END-ISO-10303-21;
